ISO-10303-21;
HEADER;
FILE_DESCRIPTION (('STEP AP214'),
    '1' );
FILE_NAME ('4. Handle.step',
    '2026-10-09T14:04:53',
    ( '' ),
    ( '' ),
    'SwSTEP 2.0',
    'SolidWorks 2021',
    '' );
FILE_SCHEMA (( 'AUTOMOTIVE_DESIGN' ));
ENDSEC;

DATA;
#11=CARTESIAN_POINT ( 'NONE',  ( 43.35354003336124151, 484.2707123563831715, -0.03226067987456286701 ) ) ;
#13=CARTESIAN_POINT ( 'NONE',  ( -32.89862776688973867, 464.9311084009897854, 10.99515925127040283 ) ) ;
#26=CARTESIAN_POINT ( 'NONE',  ( -18.93093043102413375, 304.6959352974943158, 9.903868760122875869 ) ) ;
#31=DIRECTION ( 'NONE',  ( 1.000000000000000000, 0.000000000000000000, 0.000000000000000000 ) ) ;
#50=CARTESIAN_POINT ( 'NONE',  ( 44.26460937848495547, 463.8319445086722794, 7.881633536479285773 ) ) ;
#51=CARTESIAN_POINT ( 'NONE',  ( 33.77559172535807619, 464.7834715296606305, 7.192701217093271815 ) ) ;
#52=( BOUNDED_SURFACE ( )  B_SPLINE_SURFACE ( 3, 2, ( 
 ( #98850, #99925, #16904 ),
 ( #82687, #25559, #17442 ),
 ( #26100, #18510, #24494 ),
 ( #49783, #92359, #8792 ) ),
 .UNSPECIFIED., .F., .F., .F. ) 
 B_SPLINE_SURFACE_WITH_KNOTS ( ( 4, 4 ),
 ( 3, 3 ),
 ( -1.734723475976807094E-18, 0.001998086366838127629 ),
 ( 0.000000000000000000, 1.000000000000000000 ),
 .UNSPECIFIED. ) 
 GEOMETRIC_REPRESENTATION_ITEM ( )  RATIONAL_B_SPLINE_SURFACE ( (
 ( 1.000000000000000000, 0.7996726260853292967, 1.000000000000000000),
 ( 1.000000000000000000, 0.8085378326699110829, 1.000000000000000000),
 ( 1.000000000000000000, 0.8176579674344260917, 1.000000000000000000),
 ( 1.000000000000000000, 0.8258027051676627428, 1.000000000000000000) ) ) 
 REPRESENTATION_ITEM ( '' )  SURFACE ( )  );
#61=AXIS2_PLACEMENT_3D ( 'NONE', #48576, #41034, #67447 ) ;
#71=DIRECTION ( 'NONE',  ( 0.000000000000000000, 1.000000000000000000, 0.000000000000000000 ) ) ;
#72=CARTESIAN_POINT ( 'NONE',  ( -42.64669454907780732, 435.7301117833579838, 8.366116403065163354 ) ) ;
#81=EDGE_CURVE ( 'NONE', #25883, #24620, #13982, .T. ) ;
#90=CARTESIAN_POINT ( 'NONE',  ( -43.00000000000000000, 450.0000000000002274, 13.20242257375370976 ) ) ;
#97=ORIENTED_EDGE ( 'NONE', *, *, #94758, .T. ) ;
#98=TOROIDAL_SURFACE ( 'NONE', #91385, 12.00000000000001066, 3.000000000000000000 ) ;
#123=CARTESIAN_POINT ( 'NONE',  ( -40.46354120900181073, 490.2757239658857884, 11.42275260667292791 ) ) ;
#125=CARTESIAN_POINT ( 'NONE',  ( 40.31016602574527496, 437.2133713289363754, 22.20736800721878978 ) ) ;
#147=CARTESIAN_POINT ( 'NONE',  ( -33.56345473223404241, 299.9083031499212666, -8.874823776838020706 ) ) ;
#152=CARTESIAN_POINT ( 'NONE',  ( 27.09085371571751466, 307.6936400730292576, -8.364846265266118408 ) ) ;
#159=DIRECTION ( 'NONE',  ( 0.2276554125578255927, 0.04124382533949764312, 0.9728679047046888684 ) ) ;
#161=AXIS2_PLACEMENT_3D ( 'NONE', #28600, #84677, #76566 ) ;
#162=CARTESIAN_POINT ( 'NONE',  ( -32.70293721669443698, 464.5899875799652818, 16.75272535705724053 ) ) ;
#165=CARTESIAN_POINT ( 'NONE',  ( -34.47678062873980309, 437.1474145881088589, 5.468662283310430361 ) ) ;
#176=CARTESIAN_POINT ( 'NONE',  ( -46.00000000000000000, 450.0000000000002274, 13.20242257375370976 ) ) ;
#179=SURFACE_STYLE_USAGE ( .BOTH. , #33144 ) ;
#182=CARTESIAN_POINT ( 'NONE',  ( 44.26720285007096578, 485.4142925135624296, 2.510465450173711144 ) ) ;
#194=CARTESIAN_POINT ( 'NONE',  ( 35.45036406932566564, 436.3203772529585649, 5.179456583034234285 ) ) ;
#199=CARTESIAN_POINT ( 'NONE',  ( 20.49977525862259142, 302.8459220885798686, -10.00124997875687427 ) ) ;
#203=CARTESIAN_POINT ( 'NONE',  ( -37.22405814379114730, 463.3230035706858416, 20.09439497145941900 ) ) ;
#207=CARTESIAN_POINT ( 'NONE',  ( -46.00000000000000000, 500.0000000000002274, 15.00000000000000711 ) ) ;
#213=DIRECTION ( 'NONE',  ( 0.000000000000000000, 0.000000000000000000, -1.000000000000000000 ) ) ;
#218=CARTESIAN_POINT ( 'NONE',  ( 20.70154941269364812, 302.9148302143801175, 9.950696617737659011 ) ) ;
#220=CARTESIAN_POINT ( 'NONE',  ( -37.59043012194430844, 369.8415162678004435, 4.161255642873434191 ) ) ;
#224=EDGE_LOOP ( 'NONE', ( #40162, #29975, #24462, #52322, #2837 ) ) ;
#229=DIRECTION ( 'NONE',  ( -1.000000000000000000, 0.000000000000000000, 0.000000000000000000 ) ) ;
#234=VERTEX_POINT ( 'NONE', #27047 ) ;
#242=AXIS2_PLACEMENT_3D ( 'NONE', #2910, #93547, #94618 ) ;
#247=CARTESIAN_POINT ( 'NONE',  ( -43.43869229197126458, 464.9661605157749591, 13.42065392471462637 ) ) ;
#249=CARTESIAN_POINT ( 'NONE',  ( -13.82057366821712030, 304.5462546222179299, 9.872053150317878334 ) ) ;
#255=EDGE_CURVE ( 'NONE', #38940, #72492, #94463, .T. ) ;
#275=ORIENTED_EDGE ( 'NONE', *, *, #52695, .F. ) ;
#276=CARTESIAN_POINT ( 'NONE',  ( -46.00000000000000000, 488.5496196030049418, 3.680746121982443775 ) ) ;
#280=CARTESIAN_POINT ( 'NONE',  ( 31.26362620848352947, 298.2545286346129387, -9.251380759131620835 ) ) ;
#287=CARTESIAN_POINT ( 'NONE',  ( -35.57955382936916067, 363.3973965622570859, 2.919629247011395368 ) ) ;
#298=ORIENTED_EDGE ( 'NONE', *, *, #77843, .T. ) ;
#299=CARTESIAN_POINT ( 'NONE',  ( 38.47428897412589066, 485.7788508071993760, -4.770630528148340765 ) ) ;
#300=CARTESIAN_POINT ( 'NONE',  ( 32.15310320217080431, 439.7024266304582056, 23.94087012106557211 ) ) ;
#309=ORIENTED_EDGE ( 'NONE', *, *, #20951, .F. ) ;
#322=CARTESIAN_POINT ( 'NONE',  ( 25.95507789760542039, 309.1386286255022924, 10.94030088463808070 ) ) ;
#325=CARTESIAN_POINT ( 'NONE',  ( -37.27001300466930900, 460.4716935085137948, 2.455202772530845401 ) ) ;
#337=VERTEX_POINT ( 'NONE', #16789 ) ;
#341=CARTESIAN_POINT ( 'NONE',  ( -41.16035149709456675, 464.6079056639530904, 16.67014335653854218 ) ) ;
#343=CARTESIAN_POINT ( 'NONE',  ( -30.47452941428689144, 336.9182531266175715, 16.65730915348260410 ) ) ;
#348=CARTESIAN_POINT ( 'NONE',  ( 33.16497501405928716, 438.9508968883829425, 23.91452439716892187 ) ) ;
#351=CARTESIAN_POINT ( 'NONE',  ( 30.36308363480350536, 298.1723161944738081, 2.669529410806691150 ) ) ;
#354=AXIS2_PLACEMENT_3D ( 'NONE', #30290, #103624, #54514 ) ;
#357=CIRCLE ( 'NONE', #7239, 15.00000000000000711 ) ;
#363=CARTESIAN_POINT ( 'NONE',  ( -23.85731009206051567, 303.8684408157198504, 10.15848730775081599 ) ) ;
#367=DIRECTION ( 'NONE',  ( 0.2281669654646126255, 0.2206132685146504901, 0.9482982767178022021 ) ) ;
#369=B_SPLINE_CURVE_WITH_KNOTS ( 'NONE', 3,
 ( #79357, #70214, #86946, #54006 ),
 .UNSPECIFIED., .F., .F.,
 ( 4, 4 ),
 ( 0.000000000000000000, 0.002179261451102595427 ),
 .UNSPECIFIED. ) ;
#382=B_SPLINE_CURVE_WITH_KNOTS ( 'NONE', 3,
 ( #64122, #81847, #38263, #71124 ),
 .UNSPECIFIED., .F., .F.,
 ( 4, 4 ),
 ( 0.0009348627901856346525, 0.02189385877134459105 ),
 .UNSPECIFIED. ) ;
#422=CARTESIAN_POINT ( 'NONE',  ( 30.61824294310940076, 339.8033301911921171, 17.27473575236878389 ) ) ;
#433=CARTESIAN_POINT ( 'NONE',  ( -21.23684446602550935, 304.9566545053270943, -9.977713076987674512 ) ) ;
#442=CARTESIAN_POINT ( 'NONE',  ( -2.295593195902894124, 298.7070635967813246, -10.00347380708980261 ) ) ;
#449=CARTESIAN_POINT ( 'NONE',  ( -20.15810180139540364, 294.7575509362039838, 1.916965569035420369 ) ) ;
#452=CARTESIAN_POINT ( 'NONE',  ( 37.50059943756071590, 490.7879993827834255, 12.38039871356642507 ) ) ;
#456=B_SPLINE_CURVE_WITH_KNOTS ( 'NONE', 3,
 ( #78501, #3568, #102254, #28404 ),
 .UNSPECIFIED., .F., .F.,
 ( 4, 4 ),
 ( 0.008938635547386365732, 0.01006686641814317357 ),
 .UNSPECIFIED. ) ;
#457=VERTEX_POINT ( 'NONE', #94953 ) ;
#461=CARTESIAN_POINT ( 'NONE',  ( -4.691018660002292506, 301.0267645919033157, -10.01286726553616191 ) ) ;
#463=ADVANCED_FACE ( 'NONE', ( #21088 ), #52709, .F. ) ;
#464=ORIENTED_EDGE ( 'NONE', *, *, #17873, .F. ) ;
#473=CARTESIAN_POINT ( 'NONE',  ( -29.63900401201415136, 311.2735914789724916, -7.504590757657062738 ) ) ;
#480=CARTESIAN_POINT ( 'NONE',  ( -28.47508235818447986, 296.9186349479344926, -1.549936504308094598 ) ) ;
#482=DIRECTION ( 'NONE',  ( -1.000000000000000000, -0.000000000000000000, -0.000000000000000000 ) ) ;
#484=CARTESIAN_POINT ( 'NONE',  ( -33.00000000000004263, 485.0303364503728289, 0.9535057477319844876 ) ) ;
#485=CARTESIAN_POINT ( 'NONE',  ( -39.41908235148878958, 328.0183126189934342, 18.00525811984569913 ) ) ;
#494=CARTESIAN_POINT ( 'NONE',  ( 43.50722185568069023, 484.7945611035598290, 4.126806436305178849 ) ) ;
#495=CARTESIAN_POINT ( 'NONE',  ( -41.99101837128264236, 437.4456563656356138, 21.44456026107220126 ) ) ;
#496=ORIENTED_EDGE ( 'NONE', *, *, #13109, .T. ) ;
#500=CARTESIAN_POINT ( 'NONE',  ( -32.89532852795978357, 465.6911463857132389, 10.83018753746699581 ) ) ;
#515=CARTESIAN_POINT ( 'NONE',  ( 30.50814924115433158, 298.0999724620219240, -1.284670219152425297 ) ) ;
#539=CARTESIAN_POINT ( 'NONE',  ( -44.17836536378457168, 435.2619773020560956, 14.65562696767996087 ) ) ;
#540=CARTESIAN_POINT ( 'NONE',  ( 31.03867016165222026, 468.3124986733989772, 18.90871194958903345 ) ) ;
#543=CARTESIAN_POINT ( 'NONE',  ( 30.00000000000000355, 488.8442721620239695, 4.433647275927809162 ) ) ;
#552=CARTESIAN_POINT ( 'NONE',  ( -21.29975379448946171, 294.8969325209483259, -1.990407376643346327 ) ) ;
#554=CARTESIAN_POINT ( 'NONE',  ( -30.00000000000000000, 488.6481008951269587, 3.890293910847615333 ) ) ;
#574=CARTESIAN_POINT ( 'NONE',  ( -46.00000000000000000, 488.3725375423296668, 3.127739281037489771 ) ) ;
#583=CARTESIAN_POINT ( 'NONE',  ( -30.00000000000000355, 461.8887775513398992, 11.55279652844095573 ) ) ;
#585=CARTESIAN_POINT ( 'NONE',  ( -26.67480708604283990, 296.1445473584531669, -1.720936451573135129 ) ) ;
#586=EDGE_CURVE ( 'NONE', #87574, #89053, #59103, .T. ) ;
#593=CARTESIAN_POINT ( 'NONE',  ( 43.42366826522432177, 435.2488004288791217, 10.12833319149042310 ) ) ;
#597=CARTESIAN_POINT ( 'NONE',  ( 29.50756122520733271, 297.9063904818165724, 10.61050061783298126 ) ) ;
#600=CARTESIAN_POINT ( 'NONE',  ( 30.00000000000000000, 500.0000000000002274, -12.00000000000000711 ) ) ;
#603=CARTESIAN_POINT ( 'NONE',  ( -31.38880089262778483, 374.5722431920488589, 22.86451044521289333 ) ) ;
#617=CARTESIAN_POINT ( 'NONE',  ( 30.00647014684152580, 322.4127042974290021, 14.51058770105004392 ) ) ;
#634=B_SPLINE_SURFACE_WITH_KNOTS ( 'NONE', 1, 3, ( 
 ( #106536, #66085, #83328, #9421, #249, #49896, #49357, #42341 ),
 ( #82264, #8376, #15943, #41806, #25126, #98964, #74694, #75227 ) ),
 .UNSPECIFIED., .F., .F., .F.,
 ( 2, 2 ),
 ( 4, 2, 2, 4 ),
 ( 0.000000000000000000, 1.000000000000000000 ),
 ( 0.000000000000000000, 0.04450745600790868145, 0.06676118401186306728, 0.08901491201581737678 ),
 .UNSPECIFIED. ) ;
#639=CARTESIAN_POINT ( 'NONE',  ( -1.176549540017828299, 302.5210282605368661, 9.930800019558532199 ) ) ;
#658=FACE_OUTER_BOUND ( 'NONE', #92742, .T. ) ;
#662=CARTESIAN_POINT ( 'NONE',  ( 35.05476482818301776, 463.5208552852830053, 19.69826870374934558 ) ) ;
#665=CARTESIAN_POINT ( 'NONE',  ( 16.04675029026778788, 302.5605073873273341, 9.875078446694708134 ) ) ;
#670=CARTESIAN_POINT ( 'NONE',  ( -40.77380256327629837, 468.8478597483947965, 21.13608272249925690 ) ) ;
#674=CARTESIAN_POINT ( 'NONE',  ( 25.11756370350098422, 305.1043195247783615, -9.727872587232992529 ) ) ;
#686=CARTESIAN_POINT ( 'NONE',  ( -33.85195725564126690, 465.2464970902066739, 17.18122764674263081 ) ) ;
#688=CARTESIAN_POINT ( 'NONE',  ( -43.02621584241282449, 434.6128289108255558, 16.97888786059002086 ) ) ;
#689=CARTESIAN_POINT ( 'NONE',  ( -36.64823341582351901, 437.5392299810053487, 4.281405873620243163 ) ) ;
#696=VERTEX_POINT ( 'NONE', #75960 ) ;
#704=DIRECTION ( 'NONE',  ( -0.02876443885984900778, -0.9995862179207344322, 0.000000000000000000 ) ) ;
#720=EDGE_CURVE ( 'NONE', #58013, #63799, #70749, .T. ) ;
#730=CARTESIAN_POINT ( 'NONE',  ( -35.63058582597223278, 464.1921406587270553, 19.33089630041828855 ) ) ;
#735=CARTESIAN_POINT ( 'NONE',  ( 30.00000000000000355, 462.0097303356241127, 12.67201001740816579 ) ) ;
#737=CARTESIAN_POINT ( 'NONE',  ( 13.76424046522695122, 304.5457540960956067, -10.06505265514019243 ) ) ;
#743=CARTESIAN_POINT ( 'NONE',  ( 33.72905809600513294, 464.0430918388264558, 18.49991514059003705 ) ) ;
#747=CARTESIAN_POINT ( 'NONE',  ( -39.13914184472998414, 311.4509987364423864, 1.958682826505325325 ) ) ;
#748=CARTESIAN_POINT ( 'NONE',  ( -20.21880305278364887, 304.8280059657581091, -9.005058168222342729 ) ) ;
#758=ORIENTED_EDGE ( 'NONE', *, *, #923, .T. ) ;
#761=AXIS2_PLACEMENT_3D ( 'NONE', #98178, #38386, #104146 ) ;
#773=CARTESIAN_POINT ( 'NONE',  ( 33.67444716837086105, 489.3309112354449439, 10.55021651976763586 ) ) ;
#783=EDGE_CURVE ( 'NONE', #2324, #36626, #35973, .T. ) ;
#791=CARTESIAN_POINT ( 'NONE',  ( -43.74985542820358830, 435.5770091380367717, 16.96136490515571182 ) ) ;
#796=CARTESIAN_POINT ( 'NONE',  ( 42.09158233638500235, 465.7816406625409513, 14.79318349170030089 ) ) ;
#798=CARTESIAN_POINT ( 'NONE',  ( 36.53813723230013011, 463.3027015936760336, 20.13340496300989813 ) ) ;
#801=ORIENTED_EDGE ( 'NONE', *, *, #81569, .F. ) ;
#806=CARTESIAN_POINT ( 'NONE',  ( 42.20041562234358423, 435.2369744135583574, 7.788607701745475786 ) ) ;
#810=ORIENTED_EDGE ( 'NONE', *, *, #86547, .F. ) ;
#814=CARTESIAN_POINT ( 'NONE',  ( 34.70677891788760405, 301.1180127857406887, -8.590837488028862268 ) ) ;
#824=CARTESIAN_POINT ( 'NONE',  ( 37.71418762737119579, 397.5201552014418667, 6.419224431681028520 ) ) ;
#836=CARTESIAN_POINT ( 'NONE',  ( 44.33486631614394469, 435.2047139628968466, 12.56860447607852294 ) ) ;
#841=CARTESIAN_POINT ( 'NONE',  ( 35.03266379445575751, 463.2767948149638073, 4.632316356192585971 ) ) ;
#842=CARTESIAN_POINT ( 'NONE',  ( 37.71426591916371507, 395.7719197107890068, 6.364421788594514240 ) ) ;
#850=FACE_OUTER_BOUND ( 'NONE', #64159, .T. ) ;
#853=CARTESIAN_POINT ( 'NONE',  ( 0.000000000000000000, 303.8518027762758038, -10.00000000000000355 ) ) ;
#865=ORIENTED_EDGE ( 'NONE', *, *, #22367, .T. ) ;
#868=CARTESIAN_POINT ( 'NONE',  ( -33.80022934467059059, 484.1533297400397373, 1.810399503707904589 ) ) ;
#872=CARTESIAN_POINT ( 'NONE',  ( -40.04067698533295783, 464.2438039439664976, 17.93195299062574932 ) ) ;
#873=CARTESIAN_POINT ( 'NONE',  ( -30.72334302712536669, 348.3322246599395271, 19.95789250412614990 ) ) ;
#877=LINE ( 'NONE', #32789, #58739 ) ;
#882=CARTESIAN_POINT ( 'NONE',  ( 25.54696085151078933, 305.0816729924750916, 10.43539182524720843 ) ) ;
#886=AXIS2_PLACEMENT_3D ( 'NONE', #53992, #45408, #3879 ) ;
#887=CARTESIAN_POINT ( 'NONE',  ( -40.87544524660236078, 460.0150911311831692, 2.035358705197947149 ) ) ;
#895=CARTESIAN_POINT ( 'NONE',  ( -46.00000000000000000, 438.3878896346936358, 16.22878885428542262 ) ) ;
#897=CARTESIAN_POINT ( 'NONE',  ( 34.13897275414642962, 489.1603865319385704, 11.37941925723742997 ) ) ;
#917=CARTESIAN_POINT ( 'NONE',  ( -31.43600694729765976, 438.9210571544146546, 23.14859716537183942 ) ) ;
#923=EDGE_CURVE ( 'NONE', #74471, #5652, #82172, .T. ) ;
#938=CARTESIAN_POINT ( 'NONE',  ( 40.69624510163547626, 490.1121057833303212, 11.28177269626871571 ) ) ;
#942=VERTEX_POINT ( 'NONE', #37673 ) ;
#950=CARTESIAN_POINT ( 'NONE',  ( 0.000000000000000000, 81.00000000000000000, -7.000000000000006217 ) ) ;
#955=CARTESIAN_POINT ( 'NONE',  ( 31.44965036685163540, 392.5242412485162617, 24.22331400455512807 ) ) ;
#965=CARTESIAN_POINT ( 'NONE',  ( -35.69739812508499455, 430.4862580793411553, 4.964222856391316441 ) ) ;
#972=CARTESIAN_POINT ( 'NONE',  ( 35.81629280842074792, 437.2226580096241264, 4.496548509032537666 ) ) ;
#973=CARTESIAN_POINT ( 'NONE',  ( -4.544092625063217206, 294.7929985550143215, -8.922686206316964075 ) ) ;
#982=CARTESIAN_POINT ( 'NONE',  ( -42.75230560891496623, 485.3312079086282438, -3.156031357562171902 ) ) ;
#985=CARTESIAN_POINT ( 'NONE',  ( 35.00874989808714588, 491.4345812359342176, 12.31435046936197786 ) ) ;
#987=EDGE_CURVE ( 'NONE', #93305, #36055, #64077, .T. ) ;
#988=DIRECTION ( 'NONE',  ( 0.000000000000000000, 0.9180702648391438903, -0.3964176948853118110 ) ) ;
#993=ADVANCED_FACE ( 'NONE', ( #78604 ), #85825, .T. ) ;
#1001=CARTESIAN_POINT ( 'NONE',  ( -30.98504375482477968, 439.0255438726403554, 22.25332216733684021 ) ) ;
#1003=CARTESIAN_POINT ( 'NONE',  ( -32.13173123836700995, 314.4153265821008176, -7.484038042796930412 ) ) ;
#1006=CARTESIAN_POINT ( 'NONE',  ( -32.99999999999982947, 489.5971041675261972, 10.80646835458724908 ) ) ;
#1012=CARTESIAN_POINT ( 'NONE',  ( -29.25279567920904000, 297.1008376191005027, -9.510532046834983433 ) ) ;
#1020=CARTESIAN_POINT ( 'NONE',  ( -38.23306958165720459, 485.0121922191594308, -3.940089245333577850 ) ) ;
#1021=CARTESIAN_POINT ( 'NONE',  ( -40.92982833529047326, 415.5608250047296792, 27.55013716896922915 ) ) ;
#1022=CARTESIAN_POINT ( 'NONE',  ( -32.15166163075726047, 486.0589784586663882, 5.199393881401819684 ) ) ;
#1026=CARTESIAN_POINT ( 'NONE',  ( 0.000000000000000000, 0.000000000000000000, 0.000000000000000000 ) ) ;
#1035=CARTESIAN_POINT ( 'NONE',  ( 44.12472801210862627, 485.7238370326472818, 3.975897585121170863 ) ) ;
#1049=CARTESIAN_POINT ( 'NONE',  ( 46.00000000000000000, 488.5496196030049418, 3.680746121983992314 ) ) ;
#1055=DIRECTION ( 'NONE',  ( 0.000000000000000000, 0.000000000000000000, 1.000000000000000000 ) ) ;
#1062=CARTESIAN_POINT ( 'NONE',  ( 37.62251730745836653, 437.3427388312645121, 4.535622330043116435 ) ) ;
#1067=CARTESIAN_POINT ( 'NONE',  ( 51.01037695545453232, 450.0000000000002274, 8.202422573753707979 ) ) ;
#1075=CARTESIAN_POINT ( 'NONE',  ( -18.54415329739355300, 304.6135272573319526, -9.050647025036806070 ) ) ;
#1079=CIRCLE ( 'NONE', #61436, 1.000000000000000000 ) ;
#1080=FACE_OUTER_BOUND ( 'NONE', #43817, .T. ) ;
#1093=CARTESIAN_POINT ( 'NONE',  ( 31.99924010301233324, 487.3002804477013683, 7.702477312236240437 ) ) ;
#1097=AXIS2_PLACEMENT_3D ( 'NONE', #81472, #40508, #41042 ) ;
#1126=CARTESIAN_POINT ( 'NONE',  ( 32.84088564781247044, 464.9638558180851078, 11.24476942535891588 ) ) ;
#1129=ADVANCED_FACE ( 'NONE', ( #74756 ), #71942, .T. ) ;
#1143=CARTESIAN_POINT ( 'NONE',  ( -43.19180182214383024, 464.9217280168089133, 10.90460934093050582 ) ) ;
#1152=CARTESIAN_POINT ( 'NONE',  ( -33.73990888107731223, 486.9635486473591186, 1.197400340714733780 ) ) ;
#1158=CARTESIAN_POINT ( 'NONE',  ( 21.65154485178137378, 304.1284227431553404, 9.996232502259760011 ) ) ;
#1163=CARTESIAN_POINT ( 'NONE',  ( -41.47568486386963116, 477.4114866153279308, -1.106491860746871669 ) ) ;
#1169=ORIENTED_EDGE ( 'NONE', *, *, #74805, .F. ) ;
#1172=FACE_OUTER_BOUND ( 'NONE', #64148, .T. ) ;
#1174=CARTESIAN_POINT ( 'NONE',  ( -26.78010304687303034, 306.6307806999158743, 10.80426651792510739 ) ) ;
#1176=CARTESIAN_POINT ( 'NONE',  ( -32.15702871317409972, 435.6533017138530681, 19.42106620642798376 ) ) ;
#1186=CIRCLE ( 'NONE', #92529, 0.9999999999999971134 ) ;
#1194=CARTESIAN_POINT ( 'NONE',  ( -36.73887825314407252, 438.2333816059634160, 3.899276075025503996 ) ) ;
#1205=CARTESIAN_POINT ( 'NONE',  ( 31.35596682365932608, 438.0939828603627575, 22.55458131663555221 ) ) ;
#1213=CARTESIAN_POINT ( 'NONE',  ( -43.63899620156477965, 434.3182181978404515, 14.37213632273176422 ) ) ;
#1226=CARTESIAN_POINT ( 'NONE',  ( 34.98833365448072641, 302.4475715112917555, -0.2687722403786184100 ) ) ;
#1232=CARTESIAN_POINT ( 'NONE',  ( -36.29541806397919856, 438.2518625957745826, 3.876047449288457347 ) ) ;
#1256=AXIS2_PLACEMENT_3D ( 'NONE', #83241, #12397, #59515 ) ;
#1260=CARTESIAN_POINT ( 'NONE',  ( -32.68253575351214124, 486.6530702916673476, 8.413834116590887646 ) ) ;
#1280=CARTESIAN_POINT ( 'NONE',  ( 11.82165952410163356, 294.5900423753296309, -10.05563889079273387 ) ) ;
#1289=CARTESIAN_POINT ( 'NONE',  ( 38.51502786939295930, 460.6916007118329617, 1.299075388252284080 ) ) ;
#1291=CARTESIAN_POINT ( 'NONE',  ( -33.08716774766348578, 314.1783826430524300, -7.302587774995415337 ) ) ;
#1312=CARTESIAN_POINT ( 'NONE',  ( 34.16642289233210050, 463.8422268500519863, 18.98106911353328385 ) ) ;
#1318=B_SPLINE_CURVE_WITH_KNOTS ( 'NONE', 3,
 ( #56388, #73642, #55336, #81200, #104427, #15952, #32700, #65033, #23017, #82273, #56922, #23547, #47771, #89323, #49365, #47250 ),
 .UNSPECIFIED., .F., .F.,
 ( 4, 2, 2, 2, 2, 2, 2, 4 ),
 ( 7.439477314509340780E-15, 0.0007609940918443174962, 0.001141491137762725176, 0.001521988183681132530, 0.001902485229599540102, 0.002282982275517947673, 0.002663479321436355244, 0.003043976367354762382 ),
 .UNSPECIFIED. ) ;
#1322=DIRECTION ( 'NONE',  ( 1.000000000000000000, -0.000000000000000000, -0.000000000000000000 ) ) ;
#1324=LINE ( 'NONE', #34288, #96412 ) ;
#1338=VECTOR ( 'NONE', #17309, 1000.000000000000000 ) ;
#1357=CARTESIAN_POINT ( 'NONE',  ( -42.59877899174541938, 471.6663479800946561, 11.88906521140567918 ) ) ;
#1361=CARTESIAN_POINT ( 'NONE',  ( -46.00000000000000000, 488.9831568219305495, 4.757012338623842318 ) ) ;
#1363=CARTESIAN_POINT ( 'NONE',  ( 32.99999999999999289, 434.0826380246135727, 11.57835738278531323 ) ) ;
#1364=CARTESIAN_POINT ( 'NONE',  ( 29.09372310509538551, 297.2342953755526196, -1.479845727618128715 ) ) ;
#1365=CARTESIAN_POINT ( 'NONE',  ( 32.11411341898570981, 317.7919323371296514, -6.873671351699469412 ) ) ;
#1378=VERTEX_POINT ( 'NONE', #60219 ) ;
#1379=CARTESIAN_POINT ( 'NONE',  ( -22.67189858315301265, 304.4443818766867480, 10.06497620991740760 ) ) ;
#1381=CARTESIAN_POINT ( 'NONE',  ( 36.69747761309537992, 484.6510752690958839, -2.871877106304832061 ) ) ;
#1383=CARTESIAN_POINT ( 'NONE',  ( 32.65915130203010364, 487.2382554987875665, 8.056573295094644038 ) ) ;
#1396=EDGE_CURVE ( 'NONE', #75387, #97120, #56369, .T. ) ;
#1402=CARTESIAN_POINT ( 'NONE',  ( -43.22624402988198256, 434.6924416827911841, 9.644670084742074323 ) ) ;
#1403=CARTESIAN_POINT ( 'NONE',  ( 31.19792890532719198, 414.2215770364159084, 25.44228638033458623 ) ) ;
#1406=CARTESIAN_POINT ( 'NONE',  ( 16.97163447634728328, 303.5650180578880963, -10.06095676631376534 ) ) ;
#1412=B_SPLINE_CURVE_WITH_KNOTS ( 'NONE', 3,
 ( #39421, #57162, #56631, #89552 ),
 .UNSPECIFIED., .F., .F.,
 ( 4, 4 ),
 ( 0.000000000000000000, 0.001851782051266449803 ),
 .UNSPECIFIED. ) ;
#1415=CARTESIAN_POINT ( 'NONE',  ( -33.00000000000000000, 485.0303364503728289, 0.9535057477320436625 ) ) ;
#1428=CARTESIAN_POINT ( 'NONE',  ( 40.54867362617589777, 438.3503844673198842, 22.65705215920161919 ) ) ;
#1429=CARTESIAN_POINT ( 'NONE',  ( -32.01725138626208178, 362.9172354553742821, 22.63265723493709203 ) ) ;
#1438=CARTESIAN_POINT ( 'NONE',  ( 33.82934323895533169, 302.9354609585176945, 11.80188247845831917 ) ) ;
#1442=DIRECTION ( 'NONE',  ( 0.000000000000000000, 0.000000000000000000, 1.000000000000000000 ) ) ;
#1449=CARTESIAN_POINT ( 'NONE',  ( -24.23834595003092574, 304.0759229526369154, 10.20476466122759085 ) ) ;
#1455=CARTESIAN_POINT ( 'NONE',  ( 1.697392215626793099, 301.6957921518827561, 9.856842546290842222 ) ) ;
#1463=EDGE_LOOP ( 'NONE', ( #93051, #42549 ) ) ;
#1465=CARTESIAN_POINT ( 'NONE',  ( 41.47644909359268439, 477.1147368610181161, -1.041749719072760261 ) ) ;
#1473=CARTESIAN_POINT ( 'NONE',  ( 35.88361968365485666, 490.8299076634168046, 12.39904854651338972 ) ) ;
#1474=DIRECTION ( 'NONE',  ( -0.000000000000000000, -0.1492727218618779272, -0.9887960631535436251 ) ) ;
#1478=CARTESIAN_POINT ( 'NONE',  ( -35.02595189227570671, 491.4435019764551953, 12.32055256812894228 ) ) ;
#1480=CARTESIAN_POINT ( 'NONE',  ( -43.95063711303794207, 484.1591904870579697, -1.189330446659679241 ) ) ;
#1493=VERTEX_POINT ( 'NONE', #51 ) ;
#1502=CARTESIAN_POINT ( 'NONE',  ( -5.144603409922094528, 294.7784803138362690, -8.579809241137068554 ) ) ;
#1504=CARTESIAN_POINT ( 'NONE',  ( 6.752393983348615514, 294.7360562376221651, -7.398233510975328109 ) ) ;
#1509=CARTESIAN_POINT ( 'NONE',  ( 31.20657268416513475, 410.2456177201033825, 25.45174340587148265 ) ) ;
#1514=CARTESIAN_POINT ( 'NONE',  ( -32.22503847990287795, 485.9064490506194716, 4.829857536089223302 ) ) ;
#1520=CARTESIAN_POINT ( 'NONE',  ( -31.00389226642222340, 485.8187364282109115, 14.27494812388583512 ) ) ;
#1529=CARTESIAN_POINT ( 'NONE',  ( -8.890893604471449052, 294.6744728344740452, -4.583208782182904173 ) ) ;
#1541=CARTESIAN_POINT ( 'NONE',  ( 43.63899620156487202, 434.3182181978403946, 14.37213632273145336 ) ) ;
#1542=EDGE_CURVE ( 'NONE', #84380, #59429, #35822, .T. ) ;
#1544=FACE_OUTER_BOUND ( 'NONE', #57409, .T. ) ;
#1547=VERTEX_POINT ( 'NONE', #62331 ) ;
#1551=ORIENTED_EDGE ( 'NONE', *, *, #14177, .F. ) ;
#1560=CARTESIAN_POINT ( 'NONE',  ( -27.22372400652621849, 306.4093034055409817, -9.433020069181509371 ) ) ;
#1571=CARTESIAN_POINT ( 'NONE',  ( -34.28792013165121233, 484.9850795199450886, 0.1048768172220471973 ) ) ;
#1572=CARTESIAN_POINT ( 'NONE',  ( -32.46302019025186780, 342.3532878214976449, 19.26406215151588341 ) ) ;
#1588=CARTESIAN_POINT ( 'NONE',  ( 43.04469050570425992, 434.7734435962918269, 9.248231035222774565 ) ) ;
#1602=FACE_OUTER_BOUND ( 'NONE', #92437, .T. ) ;
#1603=DIRECTION ( 'NONE',  ( 0.000000000000000000, -0.000000000000000000, 1.000000000000000000 ) ) ;
#1604=DIRECTION ( 'NONE',  ( 0.000000000000000000, -0.000000000000000000, 1.000000000000000000 ) ) ;
#1610=CARTESIAN_POINT ( 'NONE',  ( -39.43526690229246867, 464.6969442309963938, 18.30945923499460903 ) ) ;
#1612=CARTESIAN_POINT ( 'NONE',  ( 30.00000000000000000, 488.8442721620239126, 4.433647275927487641 ) ) ;
#1628=CARTESIAN_POINT ( 'NONE',  ( 40.76154164607566344, 460.9888869747084073, 2.282783108351458701 ) ) ;
#1642=ORIENTED_EDGE ( 'NONE', *, *, #96728, .F. ) ;
#1653=EDGE_CURVE ( 'NONE', #101821, #58545, #98801, .T. ) ;
#1655=ORIENTED_EDGE ( 'NONE', *, *, #106374, .F. ) ;
#1673=CARTESIAN_POINT ( 'NONE',  ( -27.57151080649627417, 314.0751515626058676, 12.18133379269485239 ) ) ;
#1674=CARTESIAN_POINT ( 'NONE',  ( 27.97565635352651015, 315.9216507687758053, 12.64980990155120999 ) ) ;
#1675=( BOUNDED_SURFACE ( )  B_SPLINE_SURFACE ( 3, 2, ( 
 ( #57212, #90131, #543 ),
 ( #82570, #32983, #58291 ),
 ( #98215, #42104, #16233 ),
 ( #41050, #9723, #66380 ),
 ( #56686, #89609, #8675 ),
 ( #17854, #49118, #40515 ),
 ( #98732, #91735, #82018 ),
 ( #16774, #7597, #41577 ) ),
 .UNSPECIFIED., .F., .F., .F. ) 
 B_SPLINE_SURFACE_WITH_KNOTS ( ( 4, 2, 2, 4 ),
 ( 3, 3 ),
 ( 0.006812271038101246068, 0.007673844606678349028, 0.008535418175255451989, 0.01025856531240965618 ),
 ( 0.1554254205220907958, 1.000000000000000000 ),
 .UNSPECIFIED. ) 
 GEOMETRIC_REPRESENTATION_ITEM ( )  RATIONAL_B_SPLINE_SURFACE ( (
 ( 0.9279458904032336086, 0.7682035880786783899, 1.000000000000000000),
 ( 0.9304043519111940830, 0.7761124021571679243, 1.000000000000000000),
 ( 0.9321886790048431459, 0.7818525413430721382, 1.000000000000000000),
 ( 0.9342334009477870627, 0.7884303647649926194, 1.000000000000000000),
 ( 0.9344904078379445700, 0.7892571500144520691, 1.000000000000000000),
 ( 0.9330319136750675479, 0.7845652078663214457, 1.000000000000000000),
 ( 0.9290861136362296158, 0.7718716599718282723, 1.000000000000000000),
 ( 0.9231047755039956115, 0.7526298328880023369, 1.000000000000000000) ) ) 
 REPRESENTATION_ITEM ( '' )  SURFACE ( )  );
#1683=CARTESIAN_POINT ( 'NONE',  ( 32.82691535583474973, 485.1045372766795367, 1.724905475515037701 ) ) ;
#1687=CARTESIAN_POINT ( 'NONE',  ( 43.79395675348460060, 434.3550296691302037, 12.19643612484853001 ) ) ;
#1698=CARTESIAN_POINT ( 'NONE',  ( -27.21876204780540220, 312.2794116683786569, 10.72559560151416669 ) ) ;
#1710=CARTESIAN_POINT ( 'NONE',  ( 43.03265099500004709, 484.2747968070555089, -0.8099405866658345721 ) ) ;
#1711=CARTESIAN_POINT ( 'NONE',  ( 29.60994972707265305, 319.5812630551522489, 13.80934071871660151 ) ) ;
#1719=CARTESIAN_POINT ( 'NONE',  ( -43.51084452654468748, 465.2903130129606666, 9.421687747985890482 ) ) ;
#1720=CARTESIAN_POINT ( 'NONE',  ( -40.34377797254171583, 485.2472197438310104, -4.812374094186917084 ) ) ;
#1724=CARTESIAN_POINT ( 'NONE',  ( -46.00000000000000000, 460.6862940191606981, 7.630022560101465068 ) ) ;
#1725=VERTEX_POINT ( 'NONE', #11351 ) ;
#1728=CARTESIAN_POINT ( 'NONE',  ( 30.00000000000184031, 486.6562833505878416, 5.030808486058892193 ) ) ;
#1730=CARTESIAN_POINT ( 'NONE',  ( -32.53853074909311971, 344.3203851192521370, 19.65648080016363508 ) ) ;
#1737=B_SPLINE_CURVE_WITH_KNOTS ( 'NONE', 3,
 ( #77779, #21176, #103636, #78821 ),
 .UNSPECIFIED., .F., .F.,
 ( 4, 4 ),
 ( 0.000000000000000000, 0.0005776816123952190898 ),
 .UNSPECIFIED. ) ;
#1740=CARTESIAN_POINT ( 'NONE',  ( 13.63088759365579428, 294.5432864296589628, -2.065629630185572552 ) ) ;
#1747=EDGE_CURVE ( 'NONE', #103314, #69385, #75329, .T. ) ;
#1753=CARTESIAN_POINT ( 'NONE',  ( 31.88318484955206955, 435.8726686874541656, 17.58993604645352349 ) ) ;
#1756=CARTESIAN_POINT ( 'NONE',  ( 4.269533675236951709, 302.8261475636076625, 9.931633460720737716 ) ) ;
#1778=CARTESIAN_POINT ( 'NONE',  ( -36.59119455513882713, 438.2489652597741383, 3.879698295689448351 ) ) ;
#1782=ORIENTED_EDGE ( 'NONE', *, *, #40887, .T. ) ;
#1791=ORIENTED_EDGE ( 'NONE', *, *, #20378, .T. ) ;
#1795=CARTESIAN_POINT ( 'NONE',  ( 26.33485479066055746, 305.7717630634953707, -9.578373927320027903 ) ) ;
#1806=CARTESIAN_POINT ( 'NONE',  ( 35.19894401196863498, 355.5759600829595684, 2.569406999161085281 ) ) ;
#1811=DIRECTION ( 'NONE',  ( -0.000000000000000000, -1.000000000000000000, -0.000000000000000000 ) ) ;
#1813=CARTESIAN_POINT ( 'NONE',  ( 43.00000000000000000, 485.2629658518202405, -2.796394914059364911 ) ) ;
#1814=CARTESIAN_POINT ( 'NONE',  ( -33.13462985527915805, 435.1334760212066044, 11.13098077912248307 ) ) ;
#1816=CARTESIAN_POINT ( 'NONE',  ( 32.68851106861551159, 465.0799323318228176, 13.83425062237051151 ) ) ;
#1836=CARTESIAN_POINT ( 'NONE',  ( -30.99573784467934345, 309.3902544572148372, -8.491104135219801563 ) ) ;
#1837=CARTESIAN_POINT ( 'NONE',  ( -20.24579557674103825, 304.8297271373346575, -10.00469232190999413 ) ) ;
#1840=CARTESIAN_POINT ( 'NONE',  ( -43.50377727019364471, 435.9167426301696082, 18.24083946424745761 ) ) ;
#1841=EDGE_CURVE ( 'NONE', #99399, #47564, #36229, .T. ) ;
#1887=CARTESIAN_POINT ( 'NONE',  ( -43.40846727561957152, 434.3587631104416005, 15.36753962288952380 ) ) ;
#1889=DIRECTION ( 'NONE',  ( -1.619075244245005545E-14, -0.9887960631535431810, 0.1492727218618803420 ) ) ;
#1896=CARTESIAN_POINT ( 'NONE',  ( -41.59976559118467065, 472.6865677842792479, 16.01929606595135880 ) ) ;
#1897=CARTESIAN_POINT ( 'NONE',  ( -42.22982424653864797, 347.2022962952978560, 14.15837535828084448 ) ) ;
#1905=CARTESIAN_POINT ( 'NONE',  ( 24.96106100295528663, 303.9424320914693567, -9.763924114932871490 ) ) ;
#1906=CARTESIAN_POINT ( 'NONE',  ( 21.51569398614858031, 294.9107018935607130, -9.987480606144492512 ) ) ;
#1917=ADVANCED_FACE ( 'NONE', ( #46915 ), #31338, .T. ) ;
#1924=ORIENTED_EDGE ( 'NONE', *, *, #70173, .F. ) ;
#1938=CARTESIAN_POINT ( 'NONE',  ( 37.64086247411519537, 431.4033951771388615, 5.263547432144151550 ) ) ;
#1942=UNCERTAINTY_MEASURE_WITH_UNIT (LENGTH_MEASURE( 1.000000000000000082E-05 ), #98006, 'distance_accuracy_value', 'NONE');
#1943=ORIENTED_EDGE ( 'NONE', *, *, #85149, .T. ) ;
#1948=CARTESIAN_POINT ( 'NONE',  ( -30.00000000000000000, 488.0703656971138571, 7.691389546088009510 ) ) ;
#1951=EDGE_LOOP ( 'NONE', ( #7356, #25088, #51858, #40070, #60430, #55409 ) ) ;
#1958=CARTESIAN_POINT ( 'NONE',  ( -31.36074749248147953, 339.5349300696510682, 18.44790366892796030 ) ) ;
#1963=ORIENTED_EDGE ( 'NONE', *, *, #53294, .T. ) ;
#1964=CARTESIAN_POINT ( 'NONE',  ( -32.66787492830678730, 465.0722615638545108, 12.52936269481466525 ) ) ;
#1968=CARTESIAN_POINT ( 'NONE',  ( -31.69622719680273448, 348.2611537118722254, 20.17808803883451318 ) ) ;
#1971=EDGE_LOOP ( 'NONE', ( #12366, #18193, #59824, #30066, #41908 ) ) ;
#1979=CARTESIAN_POINT ( 'NONE',  ( 25.69789908786751909, 305.2354844591588972, 10.47141389340269058 ) ) ;
#1986=( BOUNDED_SURFACE ( )  B_SPLINE_SURFACE ( 3, 2, ( 
 ( #49944, #100090, #26260 ),
 ( #83378, #58589, #57491 ),
 ( #9473, #34342, #99554 ),
 ( #59122, #51542, #10023 ),
 ( #17067, #91490, #32738 ),
 ( #41325, #65605, #824 ),
 ( #66671, #33793, #66133 ),
 ( #99011, #84457, #50995 ),
 ( #25176, #41856, #10548 ),
 ( #82850, #43467, #17604 ),
 ( #16519, #98490, #92005 ),
 ( #90416, #42930, #94692 ),
 ( #28376, #61799, #78477 ),
 ( #4603, #53155, #20841 ),
 ( #13198, #102761, #53671 ),
 ( #95212, #35946, #20308 ),
 ( #86605, #43992, #37000 ),
 ( #86072, #70401, #103299 ),
 ( #36479, #76880, #2996 ),
 ( #12144, #37536, #45073 ),
 ( #44536, #68816, #2455 ),
 ( #60727, #29446, #52071 ),
 ( #45602, #62318, #77955 ),
 ( #101167, #19241, #21343 ),
 ( #28926, #27327, #69868 ),
 ( #4070, #61252, #12670 ),
 ( #84986, #54184, #85526 ),
 ( #101699, #87122, #11069 ),
 ( #94137, #46126, #35403 ),
 ( #93615, #27859, #68271 ),
 ( #19770, #60206, #93074 ),
 ( #52599, #11607, #77424 ),
 ( #3540, #102226, #69348 ),
 ( #71981, #6169, #14258 ),
 ( #96797, #64435, #6708 ),
 ( #15332, #48219, #97307 ),
 ( #105411, #104890, #56297 ),
 ( #81122, #79537, #71437 ),
 ( #89237, #7231, #47161 ),
 ( #5131, #96281, #88701 ),
 ( #22406, #62846, #80061 ),
 ( #54715, #39101, #38573 ),
 ( #104336, #87650, #31552 ),
 ( #31030, #39635, #23461 ),
 ( #47689, #55250, #79013 ),
 ( #70921, #38065, #55765 ),
 ( #22929, #103815, #29958 ),
 ( #95733, #13732, #21874 ),
 ( #88174, #5650, #72506 ),
 ( #63911, #46640, #14794 ),
 ( #30485, #80588, #63386 ),
 ( #1226, #17055, #82302 ),
 ( #89872, #83365, #58019 ),
 ( #90945, #99542, #90405 ),
 ( #48332, #49933, #73127 ),
 ( #66121, #32725, #98999 ),
 ( #15979, #50455, #97958 ),
 ( #26247, #25165, #82839 ),
 ( #9464, #814, #56952 ),
 ( #33783, #24108, #48857 ),
 ( #24633, #81225, #81749 ),
 ( #16507, #91992, #7872 ),
 ( #8941, #7344, #8412 ),
 ( #106032, #42375, #74731 ),
 ( #57479, #40252, #40779 ),
 ( #41314, #32178, #41843 ),
 ( #33249, #98480, #65061 ),
 ( #66659, #73671, #25719 ),
 ( #58579, #280, #91478 ),
 ( #106574, #17593, #49393 ),
 ( #65594, #75266, #74202 ),
 ( #1364, #34328, #67205 ),
 ( #100080, #59112, #100612 ),
 ( #2979, #94124, #1905 ),
 ( #35392, #85515, #11594 ),
 ( #35934, #11058, #42918 ),
 ( #101687, #68807, #84974 ),
 ( #19754, #86059, #69335 ),
 ( #36987, #69855, #12133 ),
 ( #44523, #43454, #83898 ),
 ( #93602, #27846, #19229 ),
 ( #76868, #26773, #61240 ),
 ( #75810, #59644, #101152 ),
 ( #60717, #76332, #77945 ),
 ( #68260, #34859, #28912 ),
 ( #52059, #52589, #60196 ) ),
 .UNSPECIFIED., .F., .F., .F. ) 
 B_SPLINE_SURFACE_WITH_KNOTS ( ( 4, 2, 2, 2, 2, 2, 2, 2, 2, 2, 2, 2, 2, 2, 2, 2, 2, 2, 2, 2, 2, 2, 2, 2, 2, 2, 2, 2, 2, 2, 2, 2, 2, 2, 2, 2, 2, 2, 2, 2, 2, 2, 4 ),
 ( 3, 3 ),
 ( 0.06920511848905148977, 0.08726663333270481826, 0.1053281481763581329, 0.1233896630200114614, 0.1324204204418381325, 0.1369357991527514473, 0.1414511778636647898, 0.1595126927073181045, 0.1685434501291447618, 0.1730588288400580765, 0.1753165181955147478, 0.1775742075509714191, 0.1866049649727980764, 0.1888626543282547199, 0.1911203436837113911, 0.1956357223946247337, 0.1962001447334889015, 0.1964823559029209854, 0.1967645670723530693, 0.1978934117500814049, 0.2001511011055380762, 0.2024087904609947475, 0.2025498960457107755, 0.2026910016304268314, 0.2029732127998589153, 0.2035376351387230831, 0.2046664798164514187, 0.2052309021553155866, 0.2053720077400316146, 0.2054425605323896287, 0.2055131133247476705, 0.2057953244941797544, 0.2069241691719080900, 0.2074885915107722578, 0.2077708026802043417, 0.2080530138496364256, 0.2091818585273647613, 0.2103107032050930969, 0.2105929143745251808, 0.2107340199592412366, 0.2108751255439572647, 0.2114395478828214325, 0.2136972372382780760 ),
 ( 0.000000000000000000, 1.000000000000000000 ),
 .UNSPECIFIED. ) 
 GEOMETRIC_REPRESENTATION_ITEM ( )  RATIONAL_B_SPLINE_SURFACE ( (
 ( 1.000000000000000000, 0.7071068666372158917, 1.000000000000000000),
 ( 1.000000000000000000, 0.7071069334655512018, 1.000000000000000000),
 ( 1.000000000000000000, 0.7071067806429638392, 1.000000000000000000),
 ( 1.000000000000000000, 0.7071067806429638392, 1.000000000000000000),
 ( 1.000000000000000000, 0.7071067801986182788, 1.000000000000000000),
 ( 1.000000000000000000, 0.7071067801986182788, 1.000000000000000000),
 ( 1.000000000000000000, 0.7071052001454407598, 1.000000000000000000),
 ( 1.000000000000000000, 0.7071044926390116503, 1.000000000000000000),
 ( 1.000000000000000000, 0.7071050701755247081, 1.000000000000000000),
 ( 1.000000000000000000, 0.7071061918383323430, 1.000000000000000000),
 ( 1.000000000000000000, 0.7071065781433840680, 1.000000000000000000),
 ( 1.000000000000000000, 0.7071068693410902384, 1.000000000000000000),
 ( 1.000000000000000000, 0.7071066685034318455, 1.000000000000000000),
 ( 1.000000000000000000, 0.7071047597315383015, 1.000000000000000000),
 ( 1.000000000000000000, 0.7071038952480431794, 1.000000000000000000),
 ( 1.000000000000000000, 0.7071067879969044068, 1.000000000000000000),
 ( 1.000000000000000000, 0.7071060229798925567, 1.000000000000000000),
 ( 1.000000000000000000, 0.7071045510378535237, 1.000000000000000000),
 ( 1.000000000000000000, 0.7071047759561507329, 1.000000000000000000),
 ( 1.000000000000000000, 0.7071057096469625103, 1.000000000000000000),
 ( 1.000000000000000000, 0.7071060902437995566, 1.000000000000000000),
 ( 1.000000000000000000, 0.7071066634560565500, 1.000000000000000000),
 ( 1.000000000000000000, 0.7071075604197455400, 1.000000000000000000),
 ( 1.000000000000000000, 0.7071021497887993723, 1.000000000000000000),
 ( 1.000000000000000000, 0.7070768753575527032, 1.000000000000000000),
 ( 1.000000000000000000, 0.7070957430991587911, 1.000000000000000000),
 ( 1.000000000000000000, 0.7071005200448091665, 1.000000000000000000),
 ( 1.000000000000000000, 0.7071069032146458655, 1.000000000000000000),
 ( 1.000000000000000000, 0.7071070792554502438, 1.000000000000000000),
 ( 1.000000000000000000, 0.7071020376249698147, 1.000000000000000000),
 ( 1.000000000000000000, 0.7071032367434819665, 1.000000000000000000),
 ( 1.000000000000000000, 0.7071062266188036238, 1.000000000000000000),
 ( 1.000000000000000000, 0.7071064999784369975, 1.000000000000000000),
 ( 1.000000000000000000, 0.7071067279415800266, 1.000000000000000000),
 ( 1.000000000000000000, 0.7071067734869487253, 1.000000000000000000),
 ( 1.000000000000000000, 0.7071067871051068821, 1.000000000000000000),
 ( 1.000000000000000000, 0.7071062041018818523, 1.000000000000000000),
 ( 1.000000000000000000, 0.7070992872384374017, 1.000000000000000000),
 ( 1.000000000000000000, 0.7070832079407209925, 1.000000000000000000),
 ( 1.000000000000000000, 0.7070350815532235877, 1.000000000000000000),
 ( 1.000000000000000000, 0.7070089198012663445, 1.000000000000000000),
 ( 1.000000000000000000, 0.7070369844464885478, 1.000000000000000000),
 ( 1.000000000000000000, 0.7070957717068352411, 1.000000000000000000),
 ( 1.000000000000000000, 0.7071063006734819023, 1.000000000000000000),
 ( 1.000000000000000000, 0.7071066758728855595, 1.000000000000000000),
 ( 1.000000000000000000, 0.7071068482684416123, 1.000000000000000000),
 ( 1.000000000000000000, 0.7071067509067768819, 1.000000000000000000),
 ( 1.000000000000000000, 0.7071064712481558434, 1.000000000000000000),
 ( 1.000000000000000000, 0.7071060929135511985, 1.000000000000000000),
 ( 1.000000000000000000, 0.7071047181370017087, 1.000000000000000000),
 ( 1.000000000000000000, 0.7071035035220220033, 1.000000000000000000),
 ( 1.000000000000000000, 0.7071009480114961443, 1.000000000000000000),
 ( 1.000000000000000000, 0.7071013247174512406, 1.000000000000000000),
 ( 1.000000000000000000, 0.7071045817508229137, 1.000000000000000000),
 ( 1.000000000000000000, 0.7071059709058636900, 1.000000000000000000),
 ( 1.000000000000000000, 0.7071066865108602828, 1.000000000000000000),
 ( 1.000000000000000000, 0.7071067743865847577, 1.000000000000000000),
 ( 1.000000000000000000, 0.7071067840454771103, 1.000000000000000000),
 ( 1.000000000000000000, 0.7071068029700603441, 1.000000000000000000),
 ( 1.000000000000000000, 0.7071068959044196633, 1.000000000000000000),
 ( 1.000000000000000000, 0.7071069647084402554, 1.000000000000000000),
 ( 1.000000000000000000, 0.7071074002998787300, 1.000000000000000000),
 ( 1.000000000000000000, 0.7071080365385555844, 1.000000000000000000),
 ( 1.000000000000000000, 0.7071115864958791297, 1.000000000000000000),
 ( 1.000000000000000000, 0.7071144955833897905, 1.000000000000000000),
 ( 1.000000000000000000, 0.7071126567777766825, 1.000000000000000000),
 ( 1.000000000000000000, 0.7071112265437271560, 1.000000000000000000),
 ( 1.000000000000000000, 0.7071089973616805358, 1.000000000000000000),
 ( 1.000000000000000000, 0.7071082539167721226, 1.000000000000000000),
 ( 1.000000000000000000, 0.7071071327761628833, 1.000000000000000000),
 ( 1.000000000000000000, 0.7071068561964874988, 1.000000000000000000),
 ( 1.000000000000000000, 0.7071064601745752354, 1.000000000000000000),
 ( 1.000000000000000000, 0.7070930974566089766, 1.000000000000000000),
 ( 1.000000000000000000, 0.7070887504644172150, 1.000000000000000000),
 ( 1.000000000000000000, 0.7070959029254426653, 1.000000000000000000),
 ( 1.000000000000000000, 0.7071036569772559677, 1.000000000000000000),
 ( 1.000000000000000000, 0.7071050404321805871, 1.000000000000000000),
 ( 1.000000000000000000, 0.7071063254753164884, 1.000000000000000000),
 ( 1.000000000000000000, 0.7071066210311753863, 1.000000000000000000),
 ( 1.000000000000000000, 0.7071068435589438206, 1.000000000000000000),
 ( 1.000000000000000000, 0.7071067323499335977, 1.000000000000000000),
 ( 1.000000000000000000, 0.7071044733372250368, 1.000000000000000000),
 ( 1.000000000000000000, 0.7070984845377915606, 1.000000000000000000),
 ( 1.000000000000000000, 0.7070731566999163276, 1.000000000000000000),
 ( 1.000000000000000000, 0.7070931432108062964, 1.000000000000000000),
 ( 1.000000000000000000, 0.7071067811865465735, 1.000000000000000000) ) ) 
 REPRESENTATION_ITEM ( '' )  SURFACE ( )  );
#1990=CARTESIAN_POINT ( 'NONE',  ( 30.00000000000000000, 461.8423635046865456, 11.25802415799502221 ) ) ;
#1994=CARTESIAN_POINT ( 'NONE',  ( 6.379164974645483710, 294.7476919991335080, 1.915027880699541107 ) ) ;
#1996=CARTESIAN_POINT ( 'NONE',  ( 46.00000000000000000, 463.8885932308145357, 10.44912889354677432 ) ) ;
#2012=FACE_OUTER_BOUND ( 'NONE', #85586, .T. ) ;
#2015=EDGE_CURVE ( 'NONE', #64595, #50361, #25487, .T. ) ;
#2019=DIRECTION ( 'NONE',  ( 0.000000000000000000, 0.000000000000000000, -1.000000000000000000 ) ) ;
#2032=ORIENTED_EDGE ( 'NONE', *, *, #10442, .T. ) ;
#2033=CIRCLE ( 'NONE', #82965, 0.9999999999999849010 ) ;
#2051=CARTESIAN_POINT ( 'NONE',  ( 26.75035470498962908, 311.3380438201987772, 11.49138685496244605 ) ) ;
#2056=CARTESIAN_POINT ( 'NONE',  ( -32.75411547143850299, 465.7435926370450829, 11.50418982276456958 ) ) ;
#2059=CARTESIAN_POINT ( 'NONE',  ( -29.45362385905110969, 325.9253963054578662, 15.14270878922920716 ) ) ;
#2060=CARTESIAN_POINT ( 'NONE',  ( 38.82095363404105370, 477.1416748918212534, -1.685506013212387133 ) ) ;
#2062=CARTESIAN_POINT ( 'NONE',  ( -43.53997681417765619, 465.2530638215212093, 9.299393732150377900 ) ) ;
#2078=CARTESIAN_POINT ( 'NONE',  ( 43.81028729233673147, 434.3199584132789255, 12.84475684849125265 ) ) ;
#2094=CARTESIAN_POINT ( 'NONE',  ( 32.81992448453895150, 465.7192846569213316, 11.17271167765130890 ) ) ;
#2107=CARTESIAN_POINT ( 'NONE',  ( -34.64092164578498512, 485.1226699209325943, -1.978063925740380924 ) ) ;
#2108=CARTESIAN_POINT ( 'NONE',  ( -42.67513304101517946, 370.1312389253066044, 17.76078588121451318 ) ) ;
#2109=CARTESIAN_POINT ( 'NONE',  ( -32.13509466278925686, 486.0944799719932803, 5.282526334130711376 ) ) ;
#2119=DIRECTION ( 'NONE',  ( 0.000000000000000000, 0.000000000000000000, -1.000000000000000000 ) ) ;
#2120=CARTESIAN_POINT ( 'NONE',  ( 42.64669454893656564, 435.7301117832689101, 8.366116403187898953 ) ) ;
#2132=EDGE_CURVE ( 'NONE', #51980, #104099, #97802, .T. ) ;
#2134=CARTESIAN_POINT ( 'NONE',  ( 29.50756122520733271, 297.9063904818165724, 10.61050061783298126 ) ) ;
#2151=CARTESIAN_POINT ( 'NONE',  ( -44.47476153554900691, 485.8001565544831237, -0.4986688628725900463 ) ) ;
#2161=CARTESIAN_POINT ( 'NONE',  ( -34.25876023350725319, 436.5729693652305059, 6.423321597049534759 ) ) ;
#2174=ORIENTED_EDGE ( 'NONE', *, *, #60499, .T. ) ;
#2175=CARTESIAN_POINT ( 'NONE',  ( -19.70764564238368877, 304.7954121406193053, 9.925013215726751881 ) ) ;
#2179=AXIS2_PLACEMENT_3D ( 'NONE', #4659, #13785, #4125 ) ;
#2187=B_SPLINE_CURVE_WITH_KNOTS ( 'NONE', 3,
 ( #50053, #33915, #99672, #91598 ),
 .UNSPECIFIED., .F., .F.,
 ( 4, 4 ),
 ( 0.0005359291086695390635, 0.02814212626749257318 ),
 .UNSPECIFIED. ) ;
#2216=CARTESIAN_POINT ( 'NONE',  ( -43.11534632275843393, 435.4435433140276928, 9.329549855370979472 ) ) ;
#2223=CARTESIAN_POINT ( 'NONE',  ( 43.43869229197125748, 464.9661605157749591, 13.42065392471466900 ) ) ;
#2231=ORIENTED_EDGE ( 'NONE', *, *, #30179, .F. ) ;
#2243=CARTESIAN_POINT ( 'NONE',  ( -38.82069281039413511, 477.2384714551109823, -1.705991107642487403 ) ) ;
#2260=CARTESIAN_POINT ( 'NONE',  ( -33.00000000000000000, 461.8802764867013479, 14.89328939273682195 ) ) ;
#2272=CARTESIAN_POINT ( 'NONE',  ( -35.76964818834205317, 490.7750452587320069, 12.37427806642345196 ) ) ;
#2280=VERTEX_POINT ( 'NONE', #49445 ) ;
#2283=CARTESIAN_POINT ( 'NONE',  ( 32.80436725737454395, 485.2967250516980471, 5.900038805303855938 ) ) ;
#2289=CARTESIAN_POINT ( 'NONE',  ( -43.00000000000000000, 487.9285348210879647, 8.903916466045071587 ) ) ;
#2301=CARTESIAN_POINT ( 'NONE',  ( -26.27902093981875709, 306.9027577142574614, -9.548073367145329726 ) ) ;
#2324=VERTEX_POINT ( 'NONE', #51036 ) ;
#2331=CARTESIAN_POINT ( 'NONE',  ( 20.37278541768183615, 303.8378246129572631, -10.00297115033342266 ) ) ;
#2350=CARTESIAN_POINT ( 'NONE',  ( 36.23446467943824700, 484.5294442010003877, -2.438443429321658140 ) ) ;
#2354=CARTESIAN_POINT ( 'NONE',  ( 19.62651309133643451, 302.7443318707399840, -10.02279753415084329 ) ) ;
#2355=CARTESIAN_POINT ( 'NONE',  ( -43.65809794933295507, 484.6141936383213533, 3.261896584726788451 ) ) ;
#2362=CARTESIAN_POINT ( 'NONE',  ( 40.04008949875137802, 489.2273486934136031, 11.31296313617416338 ) ) ;
#2368=ORIENTED_EDGE ( 'NONE', *, *, #91354, .F. ) ;
#2375=CARTESIAN_POINT ( 'NONE',  ( -42.44954169440552505, 319.4024488318097497, -4.056765102163490511 ) ) ;
#2376=CARTESIAN_POINT ( 'NONE',  ( -16.94033034664163395, 304.5648766887006218, -9.060986148973602994 ) ) ;
#2399=CARTESIAN_POINT ( 'NONE',  ( 33.07276483573664905, 438.9325140356084489, 23.89537236861388081 ) ) ;
#2412=ORIENTED_EDGE ( 'NONE', *, *, #29212, .F. ) ;
#2413=CARTESIAN_POINT ( 'NONE',  ( 44.17836536378433010, 435.2619773020561524, 14.65562696768152939 ) ) ;
#2424=CARTESIAN_POINT ( 'NONE',  ( 46.00000000000000000, 437.9690125970928989, 14.09127711025711527 ) ) ;
#2429=CARTESIAN_POINT ( 'NONE',  ( -31.01497228917065740, 439.2907934540658630, 22.60551266133744264 ) ) ;
#2430=SURFACE_STYLE_FILL_AREA ( #3512 ) ;
#2436=CARTESIAN_POINT ( 'NONE',  ( -31.56403572835066740, 299.1279782509382130, 2.888934931175894061 ) ) ;
#2439=VERTEX_POINT ( 'NONE', #1415 ) ;
#2443=DIRECTION ( 'NONE',  ( 0.000000000000000000, 0.000000000000000000, -1.000000000000000000 ) ) ;
#2445=CARTESIAN_POINT ( 'NONE',  ( 34.06332199976886699, 330.0526646846329299, -3.810096259360388427 ) ) ;
#2455=CARTESIAN_POINT ( 'NONE',  ( 36.52123894458239306, 336.4625677502544363, -1.853260623619672254 ) ) ;
#2456=CARTESIAN_POINT ( 'NONE',  ( 33.76223957822399768, 470.3517299622893120, 6.012945920426372659 ) ) ;
#2478=EDGE_LOOP ( 'NONE', ( #75258, #41029, #82508, #53204, #82867, #87980 ) ) ;
#2479=PRESENTATION_STYLE_ASSIGNMENT (( #51025 ) ) ;
#2483=CARTESIAN_POINT ( 'NONE',  ( -30.00000000000000355, 489.8675765671131330, 6.488452894192523246 ) ) ;
#2493=CARTESIAN_POINT ( 'NONE',  ( -32.16538108541509189, 380.2607361627312343, 24.62015355867497490 ) ) ;
#2504=CARTESIAN_POINT ( 'NONE',  ( 37.75272971733728866, 439.5327643512869145, 23.94694555366715605 ) ) ;
#2505=CARTESIAN_POINT ( 'NONE',  ( -30.62731428441585280, 345.4184166943421133, 19.40310956832407996 ) ) ;
#2513=CARTESIAN_POINT ( 'NONE',  ( 33.88977485408606327, 303.0407094117610427, 11.82755560641012949 ) ) ;
#2518=CARTESIAN_POINT ( 'NONE',  ( 40.14457621257771081, 319.6395341497199070, 7.969219972960137177 ) ) ;
#2526=CARTESIAN_POINT ( 'NONE',  ( -46.00000000000000000, 438.2046082539383178, 15.52554165154989718 ) ) ;
#2527=CARTESIAN_POINT ( 'NONE',  ( 43.43869229197123616, 464.9661605157746180, 13.42065392471466900 ) ) ;
#2528=CARTESIAN_POINT ( 'NONE',  ( 7.447654142610081962, 302.7211820200652141, 9.909313547127384325 ) ) ;
#2549=CARTESIAN_POINT ( 'NONE',  ( 36.89180422215369504, 490.9813389901171377, 12.46623009904601886 ) ) ;
#2553=CARTESIAN_POINT ( 'NONE',  ( 41.45706716801920777, 469.3214718807730605, 0.9913651918923074291 ) ) ;
#2563=CARTESIAN_POINT ( 'NONE',  ( 41.31926252412274181, 484.8188849810109105, -3.609462884267104599 ) ) ;
#2576=SURFACE_STYLE_USAGE ( .BOTH. , #10140 ) ;
#2583=CARTESIAN_POINT ( 'NONE',  ( 24.78221252497267812, 307.0969609602097421, 9.444540541783652543 ) ) ;
#2605=CARTESIAN_POINT ( 'NONE',  ( -8.392508714418884352, 295.8888084830546745, -10.03187903922855462 ) ) ;
#2618=CARTESIAN_POINT ( 'NONE',  ( -32.91522635463739732, 465.6822307888476189, 10.74522530471147164 ) ) ;
#2634=CARTESIAN_POINT ( 'NONE',  ( 33.97359119245064818, 434.1099241184709285, 11.80501937577160732 ) ) ;
#2640=VERTEX_POINT ( 'NONE', #7263 ) ;
#2643=CARTESIAN_POINT ( 'NONE',  ( -33.00000000000000000, 500.0000000000002274, 12.00000000000000711 ) ) ;
#2646=CARTESIAN_POINT ( 'NONE',  ( -28.87041204057529953, 309.8980437891780753, -7.840642016239513623 ) ) ;
#2647=CARTESIAN_POINT ( 'NONE',  ( -27.64572936686021620, 308.2012678581347700, 11.18963121372878078 ) ) ;
#2673=CARTESIAN_POINT ( 'NONE',  ( 3.947200808969410168, 295.9771890841021786, -10.00641236124329225 ) ) ;
#2674=CIRCLE ( 'NONE', #81884, 5.000000000000001776 ) ;
#2675=CARTESIAN_POINT ( 'NONE',  ( 38.68218982724705057, 320.0845437455996603, 16.10279619727025135 ) ) ;
#2676=DIRECTION ( 'NONE',  ( -1.000000000000000000, 0.000000000000000000, 0.000000000000000000 ) ) ;
#2682=CARTESIAN_POINT ( 'NONE',  ( -17.35892867067943257, 294.5707697310705839, -10.05973541782409164 ) ) ;
#2695=VERTEX_POINT ( 'NONE', #38098 ) ;
#2703=CARTESIAN_POINT ( 'NONE',  ( 40.62630098558985026, 465.1700311123280471, 17.15319754903183380 ) ) ;
#2704=CARTESIAN_POINT ( 'NONE',  ( 39.69476719265632170, 459.8381870091881183, 1.879428691192534639 ) ) ;
#2708=VERTEX_POINT ( 'NONE', #105446 ) ;
#2709=CARTESIAN_POINT ( 'NONE',  ( -43.62838954006690528, 434.9736691849527119, 14.34345830637882813 ) ) ;
#2712=ADVANCED_FACE ( 'NONE', ( #59027 ), #23137, .T. ) ;
#2715=CARTESIAN_POINT ( 'NONE',  ( -18.68300284223528607, 303.6622989438827744, -10.04032382280791325 ) ) ;
#2718=B_SPLINE_CURVE_WITH_KNOTS ( 'NONE', 3,
 ( #25347, #50116, #66844, #57135 ),
 .UNSPECIFIED., .F., .F.,
 ( 4, 4 ),
 ( 9.813077866773594792E-18, 0.002032023592285936864 ),
 .UNSPECIFIED. ) ;
#2732=DIRECTION ( 'NONE',  ( 0.2237693372482006948, 0.01887181578571533666, 0.9744594082240938260 ) ) ;
#2743=CARTESIAN_POINT ( 'NONE',  ( 26.54817876223620488, 310.6276912632132507, 11.31208242866018132 ) ) ;
#2777=DIRECTION ( 'NONE',  ( 0.000000000000000000, 0.000000000000000000, -1.000000000000000000 ) ) ;
#2801=CARTESIAN_POINT ( 'NONE',  ( -43.52075891743682234, 484.7805561108189636, 4.063293749114582631 ) ) ;
#2804=DIRECTION ( 'NONE',  ( -2.289888280286174020E-15, 0.1409055682485933769, -0.9900230405584211635 ) ) ;
#2807=CARTESIAN_POINT ( 'NONE',  ( 43.50377727019363761, 435.9167426301696082, 18.24083946424738301 ) ) ;
#2809=CARTESIAN_POINT ( 'NONE',  ( -42.74810220189110765, 488.2594957234280173, 9.352615981973224635 ) ) ;
#2811=CARTESIAN_POINT ( 'NONE',  ( 41.09279801121592612, 437.4012895414161335, 21.36373234332642923 ) ) ;
#2825=CARTESIAN_POINT ( 'NONE',  ( -34.88900972249400212, 464.6206820655984870, 18.69027339340994232 ) ) ;
#2837=ORIENTED_EDGE ( 'NONE', *, *, #93820, .T. ) ;
#2839=ADVANCED_FACE ( 'NONE', ( #94600 ), #53586, .F. ) ;
#2850=ORIENTED_EDGE ( 'NONE', *, *, #40644, .F. ) ;
#2865=CARTESIAN_POINT ( 'NONE',  ( 21.11457545795382984, 303.9328293617413692, -9.982777457638777108 ) ) ;
#2878=ADVANCED_FACE ( 'NONE', ( #68727 ), #101549, .F. ) ;
#2882=CARTESIAN_POINT ( 'NONE',  ( -20.19958611121843362, 294.7560298975799924, -2.020357152961808289 ) ) ;
#2885=CARTESIAN_POINT ( 'NONE',  ( -34.16642289233707430, 463.8422268500496557, 18.98106911353877280 ) ) ;
#2890=CARTESIAN_POINT ( 'NONE',  ( -35.76606322701502449, 391.3003520932923038, 5.706814156549728345 ) ) ;
#2903=CARTESIAN_POINT ( 'NONE',  ( -41.62319636543390544, 315.3244859196361745, -5.086071370403092651 ) ) ;
#2906=CARTESIAN_POINT ( 'NONE',  ( -15.63133122982432788, 304.5550785334672241, 8.873930169606314422 ) ) ;
#2908=FACE_OUTER_BOUND ( 'NONE', #69505, .T. ) ;
#2910=CARTESIAN_POINT ( 'NONE',  ( 33.00000000000000000, 490.5636507777048791, 7.413185101890169548 ) ) ;
#2921=ORIENTED_EDGE ( 'NONE', *, *, #80243, .F. ) ;
#2932=DIRECTION ( 'NONE',  ( -0.9081249930085217859, -0.3474488548199749505, -0.2336413712456777148 ) ) ;
#2937=CARTESIAN_POINT ( 'NONE',  ( -46.00000000000000000, 500.0000000000002274, -12.00000000000000711 ) ) ;
#2943=CARTESIAN_POINT ( 'NONE',  ( 33.82585650164579505, 464.6969192971359917, 6.993179704490867010 ) ) ;
#2964=ORIENTED_EDGE ( 'NONE', *, *, #6813, .T. ) ;
#2965=CARTESIAN_POINT ( 'NONE',  ( -41.98130293123099932, 462.0609698853085661, 3.143960326148259377 ) ) ;
#2967=CARTESIAN_POINT ( 'NONE',  ( -46.00000000000000000, 450.0000000000002274, 18.20242257375371153 ) ) ;
#2968=CARTESIAN_POINT ( 'NONE',  ( -37.45552949318529556, 490.9506234891537702, 12.34579642396192156 ) ) ;
#2969=CARTESIAN_POINT ( 'NONE',  ( -39.34066475191858103, 315.0823817570354208, 6.824423801037188930 ) ) ;
#2972=ORIENTED_EDGE ( 'NONE', *, *, #70560, .F. ) ;
#2973=CARTESIAN_POINT ( 'NONE',  ( -35.71679196358923747, 338.0497572594834992, -1.698451522311290374 ) ) ;
#2979=CARTESIAN_POINT ( 'NONE',  ( 27.31492851351466200, 296.3978788581767390, -1.665144278812466183 ) ) ;
#2981=CARTESIAN_POINT ( 'NONE',  ( 35.76320840016588676, 388.4727839510825333, 5.610592865731860002 ) ) ;
#2991=CIRCLE ( 'NONE', #59839, 4.999999999999993783 ) ;
#2995=ADVANCED_FACE ( 'NONE', ( #22840 ), #30703, .F. ) ;
#2996=CARTESIAN_POINT ( 'NONE',  ( 36.70943602865214928, 339.3630517424467712, -1.204202434040655856 ) ) ;
#3000=CARTESIAN_POINT ( 'NONE',  ( 31.96364149859393677, 438.9703530481821758, 23.62892465267417208 ) ) ;
#3010=EDGE_LOOP ( 'NONE', ( #61446, #47558, #91406, #85811, #6860 ) ) ;
#3020=DIRECTION ( 'NONE',  ( 0.000000000000000000, 0.000000000000000000, 1.000000000000000000 ) ) ;
#3036=CARTESIAN_POINT ( 'NONE',  ( -25.35453098390112103, 306.3427856472554254, 10.49981900249395750 ) ) ;
#3044=CARTESIAN_POINT ( 'NONE',  ( 43.00000000000000000, 436.5989882784185738, 19.94133085611158407 ) ) ;
#3045=CARTESIAN_POINT ( 'NONE',  ( -31.35172730056181578, 439.1959017414955042, 22.91783259691881014 ) ) ;
#3049=ORIENTED_EDGE ( 'NONE', *, *, #70416, .F. ) ;
#3055=CARTESIAN_POINT ( 'NONE',  ( 24.17704328875259634, 304.0406177940266730, 10.19684960573361465 ) ) ;
#3062=CARTESIAN_POINT ( 'NONE',  ( 38.00810289691445831, 309.9188390917963716, 5.520346969804636572 ) ) ;
#3064=EDGE_CURVE ( 'NONE', #75855, #27394, #51372, .T. ) ;
#3097=CARTESIAN_POINT ( 'NONE',  ( -46.00000000000000000, 450.0000000000002274, 13.20242257375370976 ) ) ;
#3107=CARTESIAN_POINT ( 'NONE',  ( 43.41290683822506935, 487.0833545439620593, 7.569976829064905210 ) ) ;
#3110=EDGE_LOOP ( 'NONE', ( #13685, #43062, #36659, #66962 ) ) ;
#3120=( NAMED_UNIT ( * ) PLANE_ANGLE_UNIT ( ) SI_UNIT ( $, .RADIAN. ) );
#3127=EDGE_LOOP ( 'NONE', ( #69501, #44962, #48378, #27285 ) ) ;
#3130=CARTESIAN_POINT ( 'NONE',  ( 27.76828805976974834, 314.2092757663235147, 11.21267187466577298 ) ) ;
#3137=B_SPLINE_CURVE_WITH_KNOTS ( 'NONE', 3,
 ( #4700, #21434, #87746, #103389 ),
 .UNSPECIFIED., .F., .F.,
 ( 4, 4 ),
 ( 0.000000000000000000, 0.001872901900679948758 ),
 .UNSPECIFIED. ) ;
#3141=CARTESIAN_POINT ( 'NONE',  ( -31.21933008645656926, 405.2090764464551853, 25.56980379099173817 ) ) ;
#3153=CARTESIAN_POINT ( 'NONE',  ( -9.720388148956621066, 294.7585724938156773, -10.04291177946082314 ) ) ;
#3170=CARTESIAN_POINT ( 'NONE',  ( -43.51882896341776075, 485.1238987962696001, -1.698943142573396292 ) ) ;
#3173=CIRCLE ( 'NONE', #29101, 10.02537308446410869 ) ;
#3175=DIRECTION ( 'NONE',  ( 0.000000000000000000, 0.8047643452607258219, -0.5935944310697964799 ) ) ;
#3179=CARTESIAN_POINT ( 'NONE',  ( 32.57720510843783757, 345.4073167506460891, 19.87011376397160944 ) ) ;
#3187=VERTEX_POINT ( 'NONE', #56745 ) ;
#3191=DIRECTION ( 'NONE',  ( -1.000000000000000000, -0.000000000000000000, -0.000000000000000000 ) ) ;
#3194=CARTESIAN_POINT ( 'NONE',  ( -24.89134784884370433, 306.1294686800183058, -8.721742491190038749 ) ) ;
#3196=CARTESIAN_POINT ( 'NONE',  ( -34.06266673247649379, 303.3474602219233702, 11.90248453523486560 ) ) ;
#3223=CARTESIAN_POINT ( 'NONE',  ( 33.89780391220055833, 435.9360085663053042, 7.958081226251983331 ) ) ;
#3225=CARTESIAN_POINT ( 'NONE',  ( 5.800920608168121717, 296.2164713808183478, -10.01425861749307700 ) ) ;
#3226=CARTESIAN_POINT ( 'NONE',  ( 33.56345473223404241, 299.9083031499212666, -8.874823776838020706 ) ) ;
#3227=CARTESIAN_POINT ( 'NONE',  ( 43.28639662975297853, 353.0009670098160086, 11.32799993555481954 ) ) ;
#3253=CARTESIAN_POINT ( 'NONE',  ( -34.89791961505246576, 436.0442787761182899, 7.592671863475971783 ) ) ;
#3263=( BOUNDED_SURFACE ( )  B_SPLINE_SURFACE ( 3, 2, ( 
 ( #42064, #66341, #8634 ),
 ( #33468, #2120, #92200 ),
 ( #74950, #34014, #25941 ),
 ( #1588, #25391, #42594 ) ),
 .UNSPECIFIED., .F., .F., .T. ) 
 B_SPLINE_SURFACE_WITH_KNOTS ( ( 4, 4 ),
 ( 3, 3 ),
 ( 0.000000000000000000, 0.001940382064934518527 ),
 ( 0.000000000000000000, 1.000000000000000000 ),
 .UNSPECIFIED. ) 
 GEOMETRIC_REPRESENTATION_ITEM ( )  RATIONAL_B_SPLINE_SURFACE ( (
 ( 1.000000000000000000, 0.8014084173415135792, 1.000000000000000000),
 ( 1.000000000000000000, 0.8101072955757671057, 1.000000000000000000),
 ( 1.000000000000000000, 0.8191355677487397458, 1.000000000000000000),
 ( 1.000000000000000000, 0.8274249441182489617, 1.000000000000000000) ) ) 
 REPRESENTATION_ITEM ( '' )  SURFACE ( )  );
#3290=CARTESIAN_POINT ( 'NONE',  ( -31.21933008645656926, 405.2090764464551853, 25.56980379099173817 ) ) ;
#3298=CARTESIAN_POINT ( 'NONE',  ( -32.94539137533585205, 488.0149952105291504, 9.145905951731968742 ) ) ;
#3304=CARTESIAN_POINT ( 'NONE',  ( -42.37751841893185656, 435.9440627571721620, 7.948837343527475063 ) ) ;
#3306=CARTESIAN_POINT ( 'NONE',  ( 41.70256300459684695, 461.0340457114389778, 3.032228049028138361 ) ) ;
#3314=ORIENTED_EDGE ( 'NONE', *, *, #41239, .T. ) ;
#3315=CARTESIAN_POINT ( 'NONE',  ( 36.59842210978576560, 438.2481675559515111, 3.880703544898916224 ) ) ;
#3322=CARTESIAN_POINT ( 'NONE',  ( 46.00000000000000711, 438.0945115977546038, 11.27406305469638070 ) ) ;
#3324=CARTESIAN_POINT ( 'NONE',  ( -33.00000000000000000, 489.5971041675261404, 10.80646835458718868 ) ) ;
#3336=CARTESIAN_POINT ( 'NONE',  ( -43.65587342670181670, 462.3497007921330351, 4.817139433394860504 ) ) ;
#3339=ORIENTED_EDGE ( 'NONE', *, *, #64113, .T. ) ;
#3355=CARTESIAN_POINT ( 'NONE',  ( 42.80674476973947407, 434.8200572688797934, 17.89667068458266641 ) ) ;
#3359=CARTESIAN_POINT ( 'NONE',  ( 17.09834626446250638, 294.5833046993913626, -2.056795529506987297 ) ) ;
#3362=CARTESIAN_POINT ( 'NONE',  ( 42.10086803841214476, 435.6552064019005002, 19.95582312411065828 ) ) ;
#3365=CARTESIAN_POINT ( 'NONE',  ( 39.81879459130803411, 485.8579414158143095, -5.000253522669845019 ) ) ;
#3373=CARTESIAN_POINT ( 'NONE',  ( 32.30809144287577794, 435.2315602164904362, 15.37655368195066963 ) ) ;
#3380=CARTESIAN_POINT ( 'NONE',  ( -43.00000000000000000, 461.9428920847514632, 12.03309428281654725 ) ) ;
#3414=CARTESIAN_POINT ( 'NONE',  ( -30.00000000000000000, 488.8442721620238558, 4.433647275927475206 ) ) ;
#3425=CARTESIAN_POINT ( 'NONE',  ( 42.34430797737972796, 436.4403912042729985, 6.776599765011303234 ) ) ;
#3435=CARTESIAN_POINT ( 'NONE',  ( -35.56416567029047116, 496.2909070316903239, -10.19064917708978335 ) ) ;
#3437=FACE_OUTER_BOUND ( 'NONE', #74348, .T. ) ;
#3444=CARTESIAN_POINT ( 'NONE',  ( 33.13158811909483603, 464.8683774687789310, 15.82274808412723743 ) ) ;
#3445=CARTESIAN_POINT ( 'NONE',  ( -36.71129544689416946, 382.4568683582283484, 5.283419339595673669 ) ) ;
#3467=ORIENTED_EDGE ( 'NONE', *, *, #95223, .F. ) ;
#3476=B_SPLINE_CURVE_WITH_KNOTS ( 'NONE', 3,
 ( #66202, #91037, #2526, #895 ),
 .UNSPECIFIED., .F., .F.,
 ( 4, 4 ),
 ( 0.000000000000000000, 0.002179111408645760528 ),
 .UNSPECIFIED. ) ;
#3477=AXIS2_PLACEMENT_3D ( 'NONE', #71061, #87790, #24661 ) ;
#3483=DIRECTION ( 'NONE',  ( 0.3573389821851922776, -0.9339747597290041226, 0.000000000000000000 ) ) ;
#3489=CARTESIAN_POINT ( 'NONE',  ( -37.06599482041617932, 437.8929527014068412, 4.336831230530949099 ) ) ;
#3504=EDGE_CURVE ( 'NONE', #65472, #72783, #16395, .T. ) ;
#3510=CARTESIAN_POINT ( 'NONE',  ( -31.44385389780523354, 439.7015230996784680, 23.50466788255525330 ) ) ;
#3512=FILL_AREA_STYLE ('',( #61224 ) ) ;
#3519=DIRECTION ( 'NONE',  ( 1.000000000000000000, 0.000000000000000000, 0.000000000000000000 ) ) ;
#3520=ADVANCED_FACE ( 'NONE', ( #59637 ), #45797, .T. ) ;
#3523=FACE_OUTER_BOUND ( 'NONE', #13578, .T. ) ;
#3529=CARTESIAN_POINT ( 'NONE',  ( 45.48003679188781234, 379.8448106960472614, 7.220331889307936457 ) ) ;
#3540=CARTESIAN_POINT ( 'NONE',  ( 39.24201634569103447, 311.8066870805746476, 2.048417762942908560 ) ) ;
#3542=CARTESIAN_POINT ( 'NONE',  ( 43.72580207737490809, 464.6834397206198446, 7.653156261474082456 ) ) ;
#3545=CARTESIAN_POINT ( 'NONE',  ( 32.15310320217080431, 439.7024266304582625, 23.94087012106557566 ) ) ;
#3553=AXIS2_PLACEMENT_3D ( 'NONE', #18158, #51017, #10043 ) ;
#3563=FACE_OUTER_BOUND ( 'NONE', #45116, .T. ) ;
#3568=CARTESIAN_POINT ( 'NONE',  ( 0.7521598644401954470, 299.9999999999999432, 9.936704142781159987 ) ) ;
#3580=CARTESIAN_POINT ( 'NONE',  ( -30.83453506004888212, 330.9311655802554242, 16.54362330515257540 ) ) ;
#3581=VERTEX_POINT ( 'NONE', #806 ) ;
#3585=LINE ( 'NONE', #30533, #92139 ) ;
#3587=CARTESIAN_POINT ( 'NONE',  ( 35.01485412685309484, 439.9564946629565725, 24.34373102818600998 ) ) ;
#3597=CARTESIAN_POINT ( 'NONE',  ( 31.31887015984906952, 437.4276192545529511, 20.46811517093788524 ) ) ;
#3598=CARTESIAN_POINT ( 'NONE',  ( 27.29305843655094321, 296.4586347574746696, 2.285620244940167023 ) ) ;
#3614=CARTESIAN_POINT ( 'NONE',  ( 17.64519143783728694, 294.6036040355394903, 9.884243018850950691 ) ) ;
#3623=ORIENTED_EDGE ( 'NONE', *, *, #51361, .T. ) ;
#3625=CARTESIAN_POINT ( 'NONE',  ( -43.09948196127322007, 484.9577458347781658, -0.8563396247088991275 ) ) ;
#3627=CARTESIAN_POINT ( 'NONE',  ( 35.45036406932405981, 436.3203772529684557, 5.179456583039796946 ) ) ;
#3632=CARTESIAN_POINT ( 'NONE',  ( 36.25009977769053648, 490.9522084974081508, 12.45337240579055482 ) ) ;
#3638=CARTESIAN_POINT ( 'NONE',  ( -42.57704743493911081, 486.1612337113409126, 7.852296464539661791 ) ) ;
#3646=CARTESIAN_POINT ( 'NONE',  ( 41.72175139494278540, 485.6241823541927261, -4.286260377903978736 ) ) ;
#3659=DIRECTION ( 'NONE',  ( -1.000000000000000000, 0.000000000000000000, 0.000000000000000000 ) ) ;
#3666=EDGE_CURVE ( 'NONE', #98535, #91921, #35738, .T. ) ;
#3670=CARTESIAN_POINT ( 'NONE',  ( 23.87963945136024080, 306.2497715304713211, 10.24640825507572117 ) ) ;
#3672=CARTESIAN_POINT ( 'NONE',  ( -39.83997765698394034, 460.7086825730506234, 2.106271324414739077 ) ) ;
#3677=TOROIDAL_SURFACE ( 'NONE', #57078, 12.00000000000000711, 3.000000000000000000 ) ;
#3723=CARTESIAN_POINT ( 'NONE',  ( 40.84956872111840909, 369.3158774004744487, 25.50800020339859131 ) ) ;
#3729=ORIENTED_EDGE ( 'NONE', *, *, #63845, .F. ) ;
#3735=CARTESIAN_POINT ( 'NONE',  ( -27.78400705216732902, 308.4281219000443457, -8.192438691479090096 ) ) ;
#3736=CARTESIAN_POINT ( 'NONE',  ( -39.47463750696404361, 315.8169378728001675, 7.009586823238445952 ) ) ;
#3742=ADVANCED_FACE ( 'NONE', ( #49661 ), #1675, .T. ) ;
#3746=ORIENTED_EDGE ( 'NONE', *, *, #94758, .F. ) ;
#3763=CARTESIAN_POINT ( 'NONE',  ( 3.010187908141165103, 299.5653876365747692, -10.00571708631404810 ) ) ;
#3766=CARTESIAN_POINT ( 'NONE',  ( -9.819056950928635175, 294.6481068335448299, 1.893705519456528652 ) ) ;
#3778=DIRECTION ( 'NONE',  ( 0.000000000000000000, 0.000000000000000000, -1.000000000000000000 ) ) ;
#3820=CARTESIAN_POINT ( 'NONE',  ( 33.00000000000000000, 450.0000000000002274, 13.20242257375370976 ) ) ;
#3826=CARTESIAN_POINT ( 'NONE',  ( -22.20318009218133071, 295.0333587257888439, 9.975590323731541531 ) ) ;
#3834=CARTESIAN_POINT ( 'NONE',  ( 32.87517070013015541, 485.0717976019059847, 1.466424316699966202 ) ) ;
#3860=CARTESIAN_POINT ( 'NONE',  ( 32.13020926079881434, 464.8240734303054182, 14.61769217561763945 ) ) ;
#3866=EDGE_CURVE ( 'NONE', #91921, #17636, #30585, .T. ) ;
#3868=CARTESIAN_POINT ( 'NONE',  ( -32.64206520361308606, 464.2415374745227155, 8.403253426436839035 ) ) ;
#3873=ORIENTED_EDGE ( 'NONE', *, *, #76722, .F. ) ;
#3875=CARTESIAN_POINT ( 'NONE',  ( -21.24460900603666857, 302.9489078580693331, -9.979273875210839861 ) ) ;
#3879=DIRECTION ( 'NONE',  ( 0.000000000000000000, 0.000000000000000000, -1.000000000000000000 ) ) ;
#3895=CARTESIAN_POINT ( 'NONE',  ( -36.12201691787056035, 490.9181190026608306, 12.43842860963000696 ) ) ;
#3897=( BOUNDED_SURFACE ( )  B_SPLINE_SURFACE ( 3, 2, ( 
 ( #45994, #46513, #56161 ),
 ( #71313, #6568, #6039 ),
 ( #55117, #30896, #72375 ),
 ( #30353, #70794, #79409 ) ),
 .UNSPECIFIED., .F., .F., .F. ) 
 B_SPLINE_SURFACE_WITH_KNOTS ( ( 4, 4 ),
 ( 3, 3 ),
 ( -1.821459649775647449E-17, 0.0004290382097840233990 ),
 ( 0.000000000000000000, 1.000000000000000000 ),
 .UNSPECIFIED. ) 
 GEOMETRIC_REPRESENTATION_ITEM ( )  RATIONAL_B_SPLINE_SURFACE ( (
 ( 1.000000000000000000, 0.7888522786294254185, 1.000000000000000000),
 ( 1.000000000000000000, 0.7909287578650892048, 1.000000000000000000),
 ( 1.000000000000000000, 0.7929954621607017140, 1.000000000000000000),
 ( 1.000000000000000000, 0.7950530193019101910, 1.000000000000000000) ) ) 
 REPRESENTATION_ITEM ( '' )  SURFACE ( )  );
#3904=CIRCLE ( 'NONE', #77970, 2.999999999999999112 ) ;
#3912=CARTESIAN_POINT ( 'NONE',  ( 19.38370409691060203, 304.7210516941073024, -9.027791792081334421 ) ) ;
#3913=CARTESIAN_POINT ( 'NONE',  ( 44.17836536378482748, 435.2619773020558682, 14.65562696767865170 ) ) ;
#3955=CARTESIAN_POINT ( 'NONE',  ( 39.36202273480931524, 437.3280700035287509, 5.163426856674600884 ) ) ;
#3963=CARTESIAN_POINT ( 'NONE',  ( 36.69878522478096983, 484.6513904560040373, -2.872853880322673970 ) ) ;
#3967=CARTESIAN_POINT ( 'NONE',  ( -43.98494780545747318, 485.1299400072931007, -0.2561545286475674366 ) ) ;
#3981=ORIENTED_EDGE ( 'NONE', *, *, #106268, .F. ) ;
#3991=CIRCLE ( 'NONE', #86690, 0.9999999999999990008 ) ;
#3995=ORIENTED_EDGE ( 'NONE', *, *, #28861, .F. ) ;
#3997=ORIENTED_EDGE ( 'NONE', *, *, #42575, .F. ) ;
#4014=CIRCLE ( 'NONE', #86718, 7.000000000000006217 ) ;
#4039=SURFACE_STYLE_USAGE ( .BOTH. , #36453 ) ;
#4043=CARTESIAN_POINT ( 'NONE',  ( -41.94726657799440517, 461.2497493223742708, 3.266452559861955596 ) ) ;
#4050=CARTESIAN_POINT ( 'NONE',  ( -34.66390255139928200, 326.6599121232922016, -4.408687661176519335 ) ) ;
#4054=CARTESIAN_POINT ( 'NONE',  ( -43.47770857297121694, 484.8227827122652229, 4.253339224812703101 ) ) ;
#4070=CARTESIAN_POINT ( 'NONE',  ( 41.12303835364165394, 320.9630341345189777, 4.352592110578689777 ) ) ;
#4074=CARTESIAN_POINT ( 'NONE',  ( 31.33064812253037701, 438.2812499056968818, 22.63898674761892948 ) ) ;
#4097=CARTESIAN_POINT ( 'NONE',  ( -44.17588657941835351, 463.1658906400270439, 6.343983253503433950 ) ) ;
#4116=CARTESIAN_POINT ( 'NONE',  ( -45.40857618788439254, 438.4254554321796036, 6.241827246365757809 ) ) ;
#4121=CARTESIAN_POINT ( 'NONE',  ( 42.87890296919691480, 485.5827577773664530, 6.686241925529814445 ) ) ;
#4123=ORIENTED_EDGE ( 'NONE', *, *, #101926, .T. ) ;
#4125=DIRECTION ( 'NONE',  ( 0.6621791990579487530, 0.000000000000000000, -0.7493455199939301759 ) ) ;
#4127=CARTESIAN_POINT ( 'NONE',  ( 24.43287555171192693, 295.5625495699969747, 10.08955056188434796 ) ) ;
#4131=CIRCLE ( 'NONE', #45477, 15.00000000000001243 ) ;
#4141=ORIENTED_EDGE ( 'NONE', *, *, #87040, .T. ) ;
#4163=CARTESIAN_POINT ( 'NONE',  ( 12.08334041755991706, 304.5866437775407007, -10.05636128505472549 ) ) ;
#4164=DIRECTION ( 'NONE',  ( -1.000000000000000000, 0.000000000000000000, 0.000000000000000000 ) ) ;
#4166=CARTESIAN_POINT ( 'NONE',  ( -42.75202416090640156, 486.5826644064231914, 6.942705799449254478 ) ) ;
#4172=CARTESIAN_POINT ( 'NONE',  ( 39.80120353649597575, 485.6913716985618521, -4.529092486720104560 ) ) ;
#4176=CARTESIAN_POINT ( 'NONE',  ( 41.14934085771739092, 484.9010050731022829, -3.779718508949024169 ) ) ;
#4192=VERTEX_POINT ( 'NONE', #950 ) ;
#4193=CARTESIAN_POINT ( 'NONE',  ( 23.39524124133658844, 305.8619436084897529, 9.157947684428933144 ) ) ;
#4232=CARTESIAN_POINT ( 'NONE',  ( -46.00000000000000000, 436.1162229055561852, 10.84634507115767477 ) ) ;
#4233=CARTESIAN_POINT ( 'NONE',  ( -46.00000000000000711, 460.8553455089887052, 7.925197340742291985 ) ) ;
#4245=CARTESIAN_POINT ( 'NONE',  ( 33.16832779733599068, 391.0018465421582619, 25.58625501838764649 ) ) ;
#4246=FACE_OUTER_BOUND ( 'NONE', #52682, .T. ) ;
#4259=CARTESIAN_POINT ( 'NONE',  ( -28.47185190024522683, 309.2877488384496019, -7.987972226861596248 ) ) ;
#4260=CARTESIAN_POINT ( 'NONE',  ( -38.95921387178869821, 313.4153382223458948, 6.403111246584953342 ) ) ;
#4278=CARTESIAN_POINT ( 'NONE',  ( -43.50377727019363761, 435.9167426301696651, 18.24083946424746117 ) ) ;
#4285=CARTESIAN_POINT ( 'NONE',  ( 2.922700453347648608, 295.7443989525935422, -10.00347189219364097 ) ) ;
#4288=CARTESIAN_POINT ( 'NONE',  ( -19.30606845287076823, 294.6887117073658260, 1.902827613119838501 ) ) ;
#4291=FACE_OUTER_BOUND ( 'NONE', #73788, .T. ) ;
#4300=CARTESIAN_POINT ( 'NONE',  ( -44.51476414391957803, 462.1216152431910018, 5.766699157894676908 ) ) ;
#4327=CARTESIAN_POINT ( 'NONE',  ( 44.13780905824104650, 464.3951235510549509, 9.689956794375980564 ) ) ;
#4350=CARTESIAN_POINT ( 'NONE',  ( -29.50756122520733271, 297.9063904818165724, 10.61050061783298126 ) ) ;
#4369=CARTESIAN_POINT ( 'NONE',  ( 33.05096523792742147, 434.2951806504310639, 15.74562047622584871 ) ) ;
#4372=ORIENTED_EDGE ( 'NONE', *, *, #99851, .F. ) ;
#4377=ORIENTED_EDGE ( 'NONE', *, *, #40482, .T. ) ;
#4382=CARTESIAN_POINT ( 'NONE',  ( 42.20041562234358423, 435.2369744135583574, 7.788607701745475786 ) ) ;
#4390=CARTESIAN_POINT ( 'NONE',  ( -32.43176025746394231, 464.5282231482061661, 9.485014939603443551 ) ) ;
#4397=CARTESIAN_POINT ( 'NONE',  ( -33.19020058218139013, 314.4820628366123856, -7.226409737576505066 ) ) ;
#4402=CARTESIAN_POINT ( 'NONE',  ( -20.70020626257101526, 302.9146223833919294, 9.950651519756169350 ) ) ;
#4418=CARTESIAN_POINT ( 'NONE',  ( -35.44924304867188880, 490.5768697630985571, 12.28200392830173726 ) ) ;
#4433=CYLINDRICAL_SURFACE ( 'NONE', #28858, 15.00000000000001243 ) ;
#4459=AXIS2_PLACEMENT_3D ( 'NONE', #79437, #5549, #96694 ) ;
#4462=CARTESIAN_POINT ( 'NONE',  ( -33.83651168700076539, 463.7543666047556599, 7.167145050625423508 ) ) ;
#4473=CARTESIAN_POINT ( 'NONE',  ( 36.71696399481749751, 413.9589844344937433, 6.177452124062001282 ) ) ;
#4480=DIRECTION ( 'NONE',  ( 0.000000000000000000, 0.000000000000000000, 1.000000000000000000 ) ) ;
#4483=DIRECTION ( 'NONE',  ( 0.000000000000000000, 0.000000000000000000, 1.000000000000000000 ) ) ;
#4484=EDGE_LOOP ( 'NONE', ( #53982, #14772, #1782, #13671, #12838 ) ) ;
#4515=CARTESIAN_POINT ( 'NONE',  ( 32.22120753352783140, 464.6691781026584636, 10.60621122532586291 ) ) ;
#4535=EDGE_CURVE ( 'NONE', #62559, #60854, #25281, .T. ) ;
#4555=CARTESIAN_POINT ( 'NONE',  ( -40.96169049688617747, 435.9986040634732376, 6.367590718067607014 ) ) ;
#4576=CARTESIAN_POINT ( 'NONE',  ( 35.31481630306472397, 361.5983975385465214, 3.569375408695424579 ) ) ;
#4580=CARTESIAN_POINT ( 'NONE',  ( 36.49104508226335497, 491.8392457932880575, 12.58580469730120299 ) ) ;
#4581=PLANE ( 'NONE',  #93940 ) ;
#4583=CARTESIAN_POINT ( 'NONE',  ( -31.63278175528669323, 313.0349085595907468, -7.829891971190884981 ) ) ;
#4602=CIRCLE ( 'NONE', #13197, 0.9999999999999998890 ) ;
#4603=CARTESIAN_POINT ( 'NONE',  ( 43.46308961903932300, 361.0392705997022631, 12.69300088796138226 ) ) ;
#4604=CARTESIAN_POINT ( 'NONE',  ( -43.41290683822509067, 487.0833545439620593, 7.569976829064872348 ) ) ;
#4616=EDGE_CURVE ( 'NONE', #2439, #23591, #30352, .T. ) ;
#4633=CARTESIAN_POINT ( 'NONE',  ( 34.47678062874018678, 436.2905755606503817, 4.953078263945744908 ) ) ;
#4645=ORIENTED_EDGE ( 'NONE', *, *, #49109, .T. ) ;
#4651=CARTESIAN_POINT ( 'NONE',  ( -43.60048788927255004, 433.3707788411693400, 14.72783989749648370 ) ) ;
#4655=VERTEX_POINT ( 'NONE', #48341 ) ;
#4659=CARTESIAN_POINT ( 'NONE',  ( 42.23079339798723453, 461.4509360991310132, 2.027626716395714901 ) ) ;
#4661=CARTESIAN_POINT ( 'NONE',  ( 22.33420830224751086, 303.2829233726812959, 10.02965477944128736 ) ) ;
#4662=AXIS2_PLACEMENT_3D ( 'NONE', #42257, #49278, #75147 ) ;
#4663=CARTESIAN_POINT ( 'NONE',  ( 9.404048505571516614, 302.6623157415702394, -10.04027336087706246 ) ) ;
#4675=CARTESIAN_POINT ( 'NONE',  ( 43.03894652950350519, 464.9992092536281802, 11.55502599541015840 ) ) ;
#4679=CARTESIAN_POINT ( 'NONE',  ( -2.576959554038571877E-15, 37.86482112153537116, -10.52123582012687919 ) ) ;
#4680=CARTESIAN_POINT ( 'NONE',  ( 31.96161004470365086, 465.6201165449652990, 10.43791023679830587 ) ) ;
#4689=CARTESIAN_POINT ( 'NONE',  ( 32.99999999999999289, 435.0774731480752280, 11.67986145722082014 ) ) ;
#4692=AXIS2_PLACEMENT_3D ( 'NONE', #69455, #3659, #35516 ) ;
#4698=CARTESIAN_POINT ( 'NONE',  ( -41.16726895037174216, 460.1166845890182344, 2.127318685287579836 ) ) ;
#4699=CARTESIAN_POINT ( 'NONE',  ( -32.17646412119387378, 464.6980787822280377, 10.84896803612861227 ) ) ;
#4700=CARTESIAN_POINT ( 'NONE',  ( -46.00000000000000000, 461.9428920847514632, 12.03309428281624172 ) ) ;
#4706=CARTESIAN_POINT ( 'NONE',  ( 39.83118896912491635, 485.8577528566769388, -4.999724294277989145 ) ) ;
#4707=CARTESIAN_POINT ( 'NONE',  ( 38.16398975109107994, 438.4461414108280337, 23.47828886419992145 ) ) ;
#4717=CARTESIAN_POINT ( 'NONE',  ( -27.47093694407817210, 296.2799286419132727, -9.692114557244172701 ) ) ;
#4718=ORIENTED_EDGE ( 'NONE', *, *, #100847, .T. ) ;
#4725=VERTEX_POINT ( 'NONE', #84456 ) ;
#4735=CARTESIAN_POINT ( 'NONE',  ( 43.59756234217316972, 434.3244621007173123, 14.55946156040339368 ) ) ;
#4742=VECTOR ( 'NONE', #69101, 1000.000000000000000 ) ;
#4766=AXIS2_PLACEMENT_3D ( 'NONE', #4861, #62061, #61521 ) ;
#4779=CARTESIAN_POINT ( 'NONE',  ( 33.12808147879884757, 378.7724976115550817, 24.67513802460110028 ) ) ;
#4787=CARTESIAN_POINT ( 'NONE',  ( -35.04731574020232898, 463.2729383095255571, 4.642530231459612189 ) ) ;
#4791=CARTESIAN_POINT ( 'NONE',  ( -35.76309173223387461, 307.1545808062370497, 12.84636953888385769 ) ) ;
#4805=CARTESIAN_POINT ( 'NONE',  ( -43.02661387979790675, 465.7449615347597387, 11.43319743843399827 ) ) ;
#4812=FACE_OUTER_BOUND ( 'NONE', #19807, .T. ) ;
#4816=CARTESIAN_POINT ( 'NONE',  ( 41.57853103384506710, 486.0999730836878143, 12.35226384734806793 ) ) ;
#4818=CARTESIAN_POINT ( 'NONE',  ( 40.32076386538651747, 316.2483603545517781, 3.170981411441938569 ) ) ;
#4819=CARTESIAN_POINT ( 'NONE',  ( -13.61497193734505018, 294.5438151431720257, 1.871498990400385809 ) ) ;
#4822=DIRECTION ( 'NONE',  ( -1.000000000000000000, 0.000000000000000000, 0.000000000000000000 ) ) ;
#4828=( BOUNDED_SURFACE ( )  B_SPLINE_SURFACE ( 3, 2, ( 
 ( #100168, #43006, #58661 ),
 ( #18764, #100691, #85606 ),
 ( #44071, #76956, #101765 ),
 ( #1994, #34941, #84532 ),
 ( #59731, #51613, #2528 ),
 ( #35478, #6108, #103756 ),
 ( #64884, #69418, #56230 ),
 ( #89168, #15273, #55185 ),
 ( #21808, #71376, #7169 ),
 ( #48155, #96210, #77501 ),
 ( #47623, #39033, #29894 ),
 ( #71915, #88112, #14192 ),
 ( #104278, #79999, #13670 ),
 ( #81056, #64373, #97247 ),
 ( #104817, #23392, #88635 ),
 ( #30419, #63314, #22338 ),
 ( #5585, #3614, #6644 ),
 ( #22866, #11679, #23937 ),
 ( #30965, #46578, #79475 ),
 ( #38512, #56779, #44612 ) ),
 .UNSPECIFIED., .F., .F., .T. ) 
 B_SPLINE_SURFACE_WITH_KNOTS ( ( 4, 2, 2, 2, 2, 2, 2, 2, 2, 4 ),
 ( 3, 3 ),
 ( 0.02241040388483112045, 0.02720928303954221750, 0.02960872261689776602, 0.03080844240557554028, 0.03200816219425331455, 0.03680704134896441160, 0.03740690124330330046, 0.03800676113764218933, 0.03920648092631996706, 0.04160592050367551559 ),
 ( 0.000000000000000000, 1.000000000000000000 ),
 .UNSPECIFIED. ) 
 GEOMETRIC_REPRESENTATION_ITEM ( )  RATIONAL_B_SPLINE_SURFACE ( (
 ( 1.000000000000000000, 0.7071075261733695827, 1.000000000000000000),
 ( 1.000000000000000000, 0.7071101665621289944, 1.000000000000000000),
 ( 1.000000000000000000, 0.7071141823279891714, 1.000000000000000000),
 ( 1.000000000000000000, 0.7071130896529220777, 1.000000000000000000),
 ( 1.000000000000000000, 0.7071116450707854995, 1.000000000000000000),
 ( 1.000000000000000000, 0.7071091581537886084, 1.000000000000000000),
 ( 1.000000000000000000, 0.7071082983977113878, 1.000000000000000000),
 ( 1.000000000000000000, 0.7071070359255379190, 1.000000000000000000),
 ( 1.000000000000000000, 0.7071066027460465309, 1.000000000000000000),
 ( 1.000000000000000000, 0.7071078295206322251, 1.000000000000000000),
 ( 1.000000000000000000, 0.7071068908989407431, 1.000000000000000000),
 ( 1.000000000000000000, 0.7071067684955979482, 1.000000000000000000),
 ( 1.000000000000000000, 0.7071080599920462895, 1.000000000000000000),
 ( 1.000000000000000000, 0.7071121107070883482, 1.000000000000000000),
 ( 1.000000000000000000, 0.7071147513002663532, 1.000000000000000000),
 ( 1.000000000000000000, 0.7071223048250396825, 1.000000000000000000),
 ( 1.000000000000000000, 0.7071265701120853508, 1.000000000000000000),
 ( 1.000000000000000000, 0.7071280438862577178, 1.000000000000000000),
 ( 1.000000000000000000, 0.7071102363992133322, 1.000000000000000000),
 ( 1.000000000000000000, 0.7071067811865472397, 1.000000000000000000) ) ) 
 REPRESENTATION_ITEM ( '' )  SURFACE ( )  );
#4835=ORIENTED_EDGE ( 'NONE', *, *, #6512, .F. ) ;
#4838=CARTESIAN_POINT ( 'NONE',  ( -43.71297783477830734, 485.1278128289774259, -1.116606130290624721 ) ) ;
#4839=CARTESIAN_POINT ( 'NONE',  ( -44.13784562318695492, 464.3950638386332344, 9.689741638643303290 ) ) ;
#4842=VERTEX_POINT ( 'NONE', #18138 ) ;
#4861=CARTESIAN_POINT ( 'NONE',  ( -46.00000000000000000, 500.0000000000002274, 0.000000000000000000 ) ) ;
#4871=CARTESIAN_POINT ( 'NONE',  ( 43.00000000000000000, 500.0000000000002274, -12.00000000000000711 ) ) ;
#4872=VERTEX_POINT ( 'NONE', #60726 ) ;
#4874=DIRECTION ( 'NONE',  ( 0.000000000000000000, 0.8273160954982761162, -0.5617366626182478395 ) ) ;
#4909=CARTESIAN_POINT ( 'NONE',  ( -30.00000000000000000, 486.5488479675415192, 4.838494452963876036 ) ) ;
#4915=CARTESIAN_POINT ( 'NONE',  ( -36.45417852791157998, 303.1973759554606431, -8.097999875148085280 ) ) ;
#4920=CARTESIAN_POINT ( 'NONE',  ( 31.97895150603505954, 464.8429202049701416, 12.52771109945640582 ) ) ;
#4922=CARTESIAN_POINT ( 'NONE',  ( 43.47770857297122404, 484.8227827122696567, 4.253339224811428565 ) ) ;
#4934=CARTESIAN_POINT ( 'NONE',  ( -38.07677585881090465, 439.4430026352447385, 23.85998911115680698 ) ) ;
#4945=DIRECTION ( 'NONE',  ( -1.000000000000000000, 0.000000000000000000, 0.000000000000000000 ) ) ;
#4964=CARTESIAN_POINT ( 'NONE',  ( -34.29149597887493428, 464.1889238631191006, 18.11295844668995159 ) ) ;
#4974=CARTESIAN_POINT ( 'NONE',  ( 3.373304793538787205, 304.8518027749948942, -9.000000000275658607 ) ) ;
#4986=CARTESIAN_POINT ( 'NONE',  ( 33.95156263172584943, 464.5083255208626838, 6.608064661821377861 ) ) ;
#4998=AXIS2_PLACEMENT_3D ( 'NONE', #76021, #66886, #2119 ) ;
#4999=ORIENTED_EDGE ( 'NONE', *, *, #68476, .F. ) ;
#5006=CYLINDRICAL_SURFACE ( 'NONE', #42450, 15.00000000000001243 ) ;
#5007=CARTESIAN_POINT ( 'NONE',  ( -39.81879459130762200, 485.8579414158143663, -5.000253522669930284 ) ) ;
#5017=CARTESIAN_POINT ( 'NONE',  ( -42.00953037517896149, 328.3444845812533117, 6.160407614653865771 ) ) ;
#5018=CARTESIAN_POINT ( 'NONE',  ( 21.42997177938648790, 302.9814582950376689, -9.972298323676696441 ) ) ;
#5026=EDGE_CURVE ( 'NONE', #22245, #35905, #19994, .T. ) ;
#5027=CARTESIAN_POINT ( 'NONE',  ( -43.51084452654468748, 465.2903130129606666, 9.421687747985890482 ) ) ;
#5030=CARTESIAN_POINT ( 'NONE',  ( -35.57955382936916067, 363.3973965622570859, 2.919629247011395368 ) ) ;
#5031=CARTESIAN_POINT ( 'NONE',  ( 0.000000000000000000, 0.000000000000000000, 0.000000000000000000 ) ) ;
#5035=DIRECTION ( 'NONE',  ( 0.000000000000000000, 0.000000000000000000, 1.000000000000000000 ) ) ;
#5054=CARTESIAN_POINT ( 'NONE',  ( 33.00000000000000000, 464.3970849722209095, 17.41240408234224191 ) ) ;
#5062=EDGE_LOOP ( 'NONE', ( #45012, #53920, #28548, #73690 ) ) ;
#5101=CARTESIAN_POINT ( 'NONE',  ( -43.00000000000000000, 500.0000000000002274, 0.000000000000000000 ) ) ;
#5109=CARTESIAN_POINT ( 'NONE',  ( 35.65243850163849970, 370.5602105955105117, 3.802963908744633859 ) ) ;
#5110=CARTESIAN_POINT ( 'NONE',  ( 43.60658154848616874, 484.6917668751715382, 3.660634294265139754 ) ) ;
#5119=ORIENTED_EDGE ( 'NONE', *, *, #41219, .F. ) ;
#5123=CARTESIAN_POINT ( 'NONE',  ( -33.46689243938315883, 485.1693579410822394, 2.982310567416428082 ) ) ;
#5129=DIRECTION ( 'NONE',  ( 0.000000000000000000, -0.9612814585411639801, -0.2755684261031591809 ) ) ;
#5131=CARTESIAN_POINT ( 'NONE',  ( 38.31452810505570028, 308.8792753538928082, 1.313130104885508409 ) ) ;
#5142=CARTESIAN_POINT ( 'NONE',  ( -44.21332904831282917, 435.2494715644501184, 14.45449769377396976 ) ) ;
#5147=CARTESIAN_POINT ( 'NONE',  ( -37.22806219796889593, 463.3233819687147275, 20.09366234602755696 ) ) ;
#5154=ORIENTED_EDGE ( 'NONE', *, *, #73734, .F. ) ;
#5185=CARTESIAN_POINT ( 'NONE',  ( 42.57704743493908950, 486.1612337113410263, 7.852296464539637810 ) ) ;
#5187=B_SPLINE_CURVE_WITH_KNOTS ( 'NONE', 3,
 ( #54266, #30044, #93704, #86163 ),
 .UNSPECIFIED., .F., .F.,
 ( 4, 4 ),
 ( 0.000000000000000000, 0.0002807886668503978950 ),
 .UNSPECIFIED. ) ;
#5190=CARTESIAN_POINT ( 'NONE',  ( -39.04140135027484604, 485.1684443570406984, -4.294922607834923411 ) ) ;
#5191=CARTESIAN_POINT ( 'NONE',  ( 4.240583847320349875, 300.6920699671493935, -10.01075340237639466 ) ) ;
#5193=VERTEX_POINT ( 'NONE', #63910 ) ;
#5201=B_SPLINE_CURVE_WITH_KNOTS ( 'NONE', 3,
 ( #55499, #81375, #46380, #13990, #62573, #39883, #5898, #89496 ),
 .UNSPECIFIED., .F., .F.,
 ( 4, 2, 2, 4 ),
 ( 0.01261646774359793076, 0.01360218180360692891, 0.01458789586361592880, 0.01655932398363392857 ),
 .UNSPECIFIED. ) ;
#5215=CARTESIAN_POINT ( 'NONE',  ( 11.62073187254187800, 304.6006958623242440, 8.883628455833934012 ) ) ;
#5231=APPLICATION_CONTEXT ( 'automotive_design' ) ;
#5240=CARTESIAN_POINT ( 'NONE',  ( -35.01745854983780504, 439.9565213148654266, 24.34375494391401418 ) ) ;
#5249=CARTESIAN_POINT ( 'NONE',  ( -24.37088254901632567, 295.3567874699774620, -9.892597027135842325 ) ) ;
#5250=EDGE_LOOP ( 'NONE', ( #40177, #54221, #49647, #46580 ) ) ;
#5254=CARTESIAN_POINT ( 'NONE',  ( 44.49963734947851890, 484.8409368627545746, 4.258617019819923577 ) ) ;
#5259=CARTESIAN_POINT ( 'NONE',  ( -26.91057709476854143, 308.9819425013278078, 11.14264308179486918 ) ) ;
#5270=CARTESIAN_POINT ( 'NONE',  ( 43.78670674861668743, 485.1174847320907020, -0.7624762964478807303 ) ) ;
#5282=CARTESIAN_POINT ( 'NONE',  ( 40.69645897022265757, 459.9644416451189954, 1.990281397237154692 ) ) ;
#5302=CARTESIAN_POINT ( 'NONE',  ( -45.99999999999995737, 436.0465585466099014, 12.15788407233835677 ) ) ;
#5307=CIRCLE ( 'NONE', #50021, 0.9999999999999955591 ) ;
#5315=CARTESIAN_POINT ( 'NONE',  ( -42.64966854229462001, 465.0854819100622422, 13.23715615004961599 ) ) ;
#5321=CARTESIAN_POINT ( 'NONE',  ( -33.50309374949996766, 462.9597815144458650, 5.626781216141202080 ) ) ;
#5322=CIRCLE ( 'NONE', #19143, 1.000000000000000000 ) ;
#5324=VERTEX_POINT ( 'NONE', #78342 ) ;
#5326=CARTESIAN_POINT ( 'NONE',  ( -33.88476750031885842, 303.0319408999416737, 11.82541583672366414 ) ) ;
#5331=ADVANCED_FACE ( 'NONE', ( #79407 ), #20348, .F. ) ;
#5348=CARTESIAN_POINT ( 'NONE',  ( -33.00000000000000000, 500.0000000000002274, 0.000000000000000000 ) ) ;
#5352=CARTESIAN_POINT ( 'NONE',  ( 41.57463006680435313, 490.5138385441047149, 10.95471580061642669 ) ) ;
#5353=CARTESIAN_POINT ( 'NONE',  ( -44.11331465659100104, 485.7406967462471243, 4.043683577890781145 ) ) ;
#5356=CARTESIAN_POINT ( 'NONE',  ( 40.95420997525301487, 387.0967036739339164, 27.26945002580065136 ) ) ;
#5357=CARTESIAN_POINT ( 'NONE',  ( 38.80611043514134906, 310.3396361600358659, 1.678686578570257604 ) ) ;
#5388=ORIENTED_EDGE ( 'NONE', *, *, #13975, .T. ) ;
#5395=CARTESIAN_POINT ( 'NONE',  ( -13.63040502537293364, 294.5432906843956289, -2.065628440375496755 ) ) ;
#5407=ORIENTED_EDGE ( 'NONE', *, *, #9730, .T. ) ;
#5414=CARTESIAN_POINT ( 'NONE',  ( -40.88293604215247967, 432.5779639752643675, 26.56799667982232549 ) ) ;
#5431=CARTESIAN_POINT ( 'NONE',  ( 30.00000000000000000, 464.1059074601051861, 11.21808947555551761 ) ) ;
#5433=CARTESIAN_POINT ( 'NONE',  ( -31.95432916196071105, 439.7272652150242038, 23.87563020249913848 ) ) ;
#5434=CARTESIAN_POINT ( 'NONE',  ( -32.21355997171083629, 436.2367427661213242, 19.10635534054698326 ) ) ;
#5435=CARTESIAN_POINT ( 'NONE',  ( -31.79789196896621561, 436.0544141482667442, 18.02941909552264477 ) ) ;
#5441=CARTESIAN_POINT ( 'NONE',  ( -31.64006577679478482, 298.9319948211945075, -1.094726330376324164 ) ) ;
#5448=CARTESIAN_POINT ( 'NONE',  ( 31.37378682588860102, 432.3277640841818084, 23.18600726979659399 ) ) ;
#5451=TOROIDAL_SURFACE ( 'NONE', #63981, 12.00000000000001066, 3.000000000000000000 ) ;
#5455=CARTESIAN_POINT ( 'NONE',  ( -32.85155332502864667, 463.8111683108724037, 7.359358840565868753 ) ) ;
#5456=EDGE_LOOP ( 'NONE', ( #13635, #53666, #96911, #62829 ) ) ;
#5461=CARTESIAN_POINT ( 'NONE',  ( -31.93762527360473413, 311.0806311593118494, -8.077542931250780711 ) ) ;
#5466=( BOUNDED_SURFACE ( )  B_SPLINE_SURFACE ( 3, 2, ( 
 ( #28371, #45069, #87646 ),
 ( #54709, #44532, #29954 ),
 ( #101695, #94689, #94132 ),
 ( #95207, #85523, #77420 ) ),
 .UNSPECIFIED., .F., .F., .F. ) 
 B_SPLINE_SURFACE_WITH_KNOTS ( ( 4, 4 ),
 ( 3, 3 ),
 ( 2.125036258071588691E-17, 0.002033478645169251378 ),
 ( 0.000000000000000000, 1.000000000000000000 ),
 .UNSPECIFIED. ) 
 GEOMETRIC_REPRESENTATION_ITEM ( )  RATIONAL_B_SPLINE_SURFACE ( (
 ( 1.000000000000000000, 0.7976994903569333273, 1.000000000000000000),
 ( 1.000000000000000000, 0.8066624588212726321, 1.000000000000000000),
 ( 1.000000000000000000, 0.8158483196103470947, 1.000000000000000000),
 ( 1.000000000000000000, 0.8239349643288683689, 1.000000000000000000) ) ) 
 REPRESENTATION_ITEM ( '' )  SURFACE ( )  );
#5474=CARTESIAN_POINT ( 'NONE',  ( 11.68506151312264585, 302.5966585334010119, -10.05423947740817958 ) ) ;
#5483=AXIS2_PLACEMENT_3D ( 'NONE', #1026, #48544, #73344 ) ;
#5500=CARTESIAN_POINT ( 'NONE',  ( 43.89279753500678538, 435.4168038201353284, 16.20034641759606586 ) ) ;
#5505=ORIENTED_EDGE ( 'NONE', *, *, #36927, .F. ) ;
#5525=ORIENTED_EDGE ( 'NONE', *, *, #49602, .F. ) ;
#5532=EDGE_CURVE ( 'NONE', #88846, #33881, #61381, .T. ) ;
#5536=CARTESIAN_POINT ( 'NONE',  ( -45.99999999999998579, 438.2690552493292557, 10.57781013089698519 ) ) ;
#5537=CARTESIAN_POINT ( 'NONE',  ( -41.09810318407317453, 320.7440978425470917, 4.299128587728701767 ) ) ;
#5538=CARTESIAN_POINT ( 'NONE',  ( 29.11493748322932618, 306.8126351454100700, -9.108972071340021515 ) ) ;
#5540=DIRECTION ( 'NONE',  ( 0.000000000000000000, 0.000000000000000000, 1.000000000000000000 ) ) ;
#5548=CARTESIAN_POINT ( 'NONE',  ( -31.19792890532719198, 414.2215770364159084, 25.44228638033458623 ) ) ;
#5549=DIRECTION ( 'NONE',  ( -1.000000000000000000, 0.000000000000000000, 0.000000000000000000 ) ) ;
#5557=CARTESIAN_POINT ( 'NONE',  ( -43.49681020211324523, 485.4584596168100461, 3.971815216374599888 ) ) ;
#5585=CARTESIAN_POINT ( 'NONE',  ( 17.71442011948034079, 294.6047081709573945, 1.884973053585294211 ) ) ;
#5599=CARTESIAN_POINT ( 'NONE',  ( -46.00000000000000000, 488.5500823950412155, 3.682191395223604946 ) ) ;
#5630=CARTESIAN_POINT ( 'NONE',  ( 31.67567424330222536, 316.9529563565766921, -6.082121426484099480 ) ) ;
#5642=DIRECTION ( 'NONE',  ( 0.000000000000000000, 0.000000000000000000, 1.000000000000000000 ) ) ;
#5650=CARTESIAN_POINT ( 'NONE',  ( 37.43609172732153922, 304.6718852671700120, -7.742307645728699228 ) ) ;
#5651=CARTESIAN_POINT ( 'NONE',  ( -30.00000000000000355, 461.9728594894708635, 12.10976292102400897 ) ) ;
#5652=VERTEX_POINT ( 'NONE', #69681 ) ;
#5653=B_SPLINE_CURVE_WITH_KNOTS ( 'NONE', 3,
 ( #97035, #71168, #63091, #104062 ),
 .UNSPECIFIED., .F., .F.,
 ( 4, 4 ),
 ( 4.336808689942017736E-18, 0.001257843226828393984 ),
 .UNSPECIFIED. ) ;
#5655=CARTESIAN_POINT ( 'NONE',  ( 41.50820411079202898, 461.5963371455317770, 2.703439750996501800 ) ) ;
#5667=CARTESIAN_POINT ( 'NONE',  ( -35.22245897681465721, 463.4774333389162848, 19.78759537333588625 ) ) ;
#5695=CARTESIAN_POINT ( 'NONE',  ( -45.49129229133219354, 409.1704227378016299, 8.337099328860718472 ) ) ;
#5705=CARTESIAN_POINT ( 'NONE',  ( -39.65933660911444036, 485.2174287600329308, -4.382854859800878522 ) ) ;
#5711=CARTESIAN_POINT ( 'NONE',  ( 38.46722833635603678, 463.5298926290464578, 19.68359823307360301 ) ) ;
#5714=CARTESIAN_POINT ( 'NONE',  ( 0.000000000000000000, 304.8518027762758038, -10.00000000000000355 ) ) ;
#5746=CARTESIAN_POINT ( 'NONE',  ( -41.49004542385903704, 469.3954094756242625, 1.006055279744931807 ) ) ;
#5747=CARTESIAN_POINT ( 'NONE',  ( 46.00000000000000000, 488.7535717826328892, 4.225312566654727320 ) ) ;
#5752=ORIENTED_EDGE ( 'NONE', *, *, #86543, .F. ) ;
#5759=CARTESIAN_POINT ( 'NONE',  ( -43.58313552198230667, 464.0053785828559967, 6.081445975066273490 ) ) ;
#5764=CARTESIAN_POINT ( 'NONE',  ( -29.07128654445882887, 296.9339959557834163, -9.548856946219741459 ) ) ;
#5766=CARTESIAN_POINT ( 'NONE',  ( 32.15310320217081141, 439.7024266304580919, 23.94087012106558987 ) ) ;
#5768=AXIS2_PLACEMENT_3D ( 'NONE', #37422, #79426, #5540 ) ;
#5771=ORIENTED_EDGE ( 'NONE', *, *, #17948, .T. ) ;
#5774=CARTESIAN_POINT ( 'NONE',  ( -28.48625763317001613, 313.7440504870126574, 12.33904525942641861 ) ) ;
#5775=AXIS2_PLACEMENT_3D ( 'NONE', #92787, #27576, #9196 ) ;
#5777=CARTESIAN_POINT ( 'NONE',  ( 21.92116886295261935, 305.2355041402309439, 9.019527013375345348 ) ) ;
#5785=CARTESIAN_POINT ( 'NONE',  ( 44.23653098086412427, 485.2868257420024634, 1.778614644177207049 ) ) ;
#5827=CARTESIAN_POINT ( 'NONE',  ( 41.13969092038016839, 328.1746007070119617, 10.04740730255401360 ) ) ;
#5829=B_SPLINE_CURVE_WITH_KNOTS ( 'NONE', 3,
 ( #247, #56376, #15940, #89311 ),
 .UNSPECIFIED., .F., .F.,
 ( 4, 4 ),
 ( 0.000000000000000000, 0.001704530934785217656 ),
 .UNSPECIFIED. ) ;
#5831=ORIENTED_EDGE ( 'NONE', *, *, #88394, .F. ) ;
#5837=CARTESIAN_POINT ( 'NONE',  ( -34.86182526428664374, 302.9466520364554754, 3.792971351233738631 ) ) ;
#5851=CARTESIAN_POINT ( 'NONE',  ( 35.05271644150917609, 437.8393516193232244, 4.418594605297464284 ) ) ;
#5861=CARTESIAN_POINT ( 'NONE',  ( 9.681569006902808638, 294.6516795043963839, -2.504656372061118130 ) ) ;
#5866=EDGE_CURVE ( 'NONE', #47564, #103578, #106546, .T. ) ;
#5883=DIRECTION ( 'NONE',  ( 0.000000000000000000, -0.8047643452609457571, 0.5935944310694981629 ) ) ;
#5887=CARTESIAN_POINT ( 'NONE',  ( -41.32194754023652195, 489.6440166213180873, 10.86036015010107114 ) ) ;
#5895=CARTESIAN_POINT ( 'NONE',  ( -34.87911814922733100, 490.1438948620115070, 11.96539694033642398 ) ) ;
#5898=CARTESIAN_POINT ( 'NONE',  ( -9.924744359744972044, 294.6447758367797860, -1.393037881691840951 ) ) ;
#5922=CARTESIAN_POINT ( 'NONE',  ( 43.51084452654469459, 465.2903130129626561, 9.421687747985401984 ) ) ;
#5926=CARTESIAN_POINT ( 'NONE',  ( -38.23020704518376789, 485.0116943706008783, -3.938850139310159371 ) ) ;
#5941=CARTESIAN_POINT ( 'NONE',  ( -31.78065384406837524, 439.0075755211457249, 23.52222141353437834 ) ) ;
#5943=CARTESIAN_POINT ( 'NONE',  ( -36.71473571993598739, 414.8596714204733189, 6.147209701973896934 ) ) ;
#5953=CARTESIAN_POINT ( 'NONE',  ( -28.82563007256410970, 306.5180035891726789, -9.177916022869450074 ) ) ;
#5962=CARTESIAN_POINT ( 'NONE',  ( 25.64256898552931929, 308.3509028655254838, 9.746403327101473835 ) ) ;
#5968=CARTESIAN_POINT ( 'NONE',  ( -44.22850192779651479, 464.1424782767533088, 8.760746036170912632 ) ) ;
#5971=CARTESIAN_POINT ( 'NONE',  ( -24.51380645006441128, 303.7709942971744113, -9.801562582197524520 ) ) ;
#5995=EDGE_CURVE ( 'NONE', #17876, #38472, #81855, .T. ) ;
#6024=CARTESIAN_POINT ( 'NONE',  ( -11.59898333071130772, 303.6009974801674502, 9.883690217586748261 ) ) ;
#6039=CARTESIAN_POINT ( 'NONE',  ( 32.90753060622966331, 485.1134061474841701, 5.490696813887106842 ) ) ;
#6047=CARTESIAN_POINT ( 'NONE',  ( 36.64739769383395185, 372.7567539989593115, 4.301078365670656822 ) ) ;
#6054=CARTESIAN_POINT ( 'NONE',  ( -39.23477672781254455, 311.7615262522152761, 2.036766034490009147 ) ) ;
#6059=CARTESIAN_POINT ( 'NONE',  ( -36.24373624681329176, 462.2822415611975657, 3.475315787151807001 ) ) ;
#6067=AXIS2_PLACEMENT_3D ( 'NONE', #70108, #87365, #5883 ) ;
#6070=CARTESIAN_POINT ( 'NONE',  ( -29.45362385905110969, 325.9253963054578662, 15.14270878922920716 ) ) ;
#6076=CARTESIAN_POINT ( 'NONE',  ( -42.11386565846122210, 436.0925768526294632, 7.550517934405435838 ) ) ;
#6081=ADVANCED_FACE ( 'NONE', ( #2012 ), #8512, .T. ) ;
#6086=( BOUNDED_SURFACE ( )  B_SPLINE_SURFACE ( 3, 2, ( 
 ( #79839, #54483, #87429 ),
 ( #78774, #53459, #28686 ),
 ( #104112, #37839, #30800 ),
 ( #78255, #12972, #95503 ) ),
 .UNSPECIFIED., .F., .F., .F. ) 
 B_SPLINE_SURFACE_WITH_KNOTS ( ( 4, 4 ),
 ( 3, 3 ),
 ( 7.329206686002009974E-17, 0.002404295360991625784 ),
 ( 0.000000000000000000, 1.000000000000000000 ),
 .UNSPECIFIED. ) 
 GEOMETRIC_REPRESENTATION_ITEM ( )  RATIONAL_B_SPLINE_SURFACE ( (
 ( 1.000000000000000000, 0.8162384603570761454, 1.000000000000000000),
 ( 1.000000000000000000, 0.8104306387031265935, 1.000000000000000000),
 ( 1.000000000000000000, 0.8018372346786888372, 1.000000000000000000),
 ( 1.000000000000000000, 0.7927020107002136218, 1.000000000000000000) ) ) 
 REPRESENTATION_ITEM ( '' )  SURFACE ( )  );
#6106=CIRCLE ( 'NONE', #52606, 6.000000000000001776 ) ;
#6108=CARTESIAN_POINT ( 'NONE',  ( 8.413831435758774902, 294.6898084274850476, 9.902566404003444234 ) ) ;
#6109=ORIENTED_EDGE ( 'NONE', *, *, #70359, .T. ) ;
#6115=EDGE_LOOP ( 'NONE', ( #75169, #104271, #43693, #51600 ) ) ;
#6129=CARTESIAN_POINT ( 'NONE',  ( -46.00000000000000000, 461.7884530655983326, 10.79543072756972677 ) ) ;
#6141=DIRECTION ( 'NONE',  ( -0.000000000000000000, -1.000000000000000000, -0.000000000000000000 ) ) ;
#6148=CARTESIAN_POINT ( 'NONE',  ( 36.73963609038971612, 391.1744242912104141, 5.928860386883613387 ) ) ;
#6149=CIRCLE ( 'NONE', #71596, 15.00000000000001421 ) ;
#6150=ORIENTED_EDGE ( 'NONE', *, *, #13817, .F. ) ;
#6152=CARTESIAN_POINT ( 'NONE',  ( -25.14694300620596579, 305.1179679012358292, -9.724845900475482807 ) ) ;
#6155=CARTESIAN_POINT ( 'NONE',  ( -43.48483803624229438, 478.3762783859466481, 6.210097532620542538 ) ) ;
#6169=CARTESIAN_POINT ( 'NONE',  ( 40.95117681093327633, 312.9070568743562717, -5.696314580190224852 ) ) ;
#6194=CARTESIAN_POINT ( 'NONE',  ( -43.72734063489070877, 464.0947689350268774, 7.873621169220604621 ) ) ;
#6207=ORIENTED_EDGE ( 'NONE', *, *, #48723, .F. ) ;
#6210=CARTESIAN_POINT ( 'NONE',  ( 31.84110979627772409, 331.2976162219903244, 16.86535362664712068 ) ) ;
#6212=CARTESIAN_POINT ( 'NONE',  ( 33.00000000000000000, 489.5971041675262541, 10.80646835458729349 ) ) ;
#6215=CARTESIAN_POINT ( 'NONE',  ( -46.00000000000000000, 488.2691388621310011, 2.804837155779786428 ) ) ;
#6221=CARTESIAN_POINT ( 'NONE',  ( -39.65885301127526930, 485.6927826267795467, -4.533530942908484462 ) ) ;
#6244=CARTESIAN_POINT ( 'NONE',  ( 19.73463816634106038, 304.7971333121957969, 8.925379062039111133 ) ) ;
#6260=CARTESIAN_POINT ( 'NONE',  ( -45.99999999998767919, 436.0044609851116206, 15.17967024737457749 ) ) ;
#6270=CARTESIAN_POINT ( 'NONE',  ( 38.85446894546473828, 460.8903912184138676, 2.218456751109172398 ) ) ;
#6275=CARTESIAN_POINT ( 'NONE',  ( 42.57704743493908950, 486.1612337113410831, 7.852296464539689325 ) ) ;
#6281=CARTESIAN_POINT ( 'NONE',  ( -40.17205142263708240, 310.2804317922712016, -6.358608209531249500 ) ) ;
#6286=CIRCLE ( 'NONE', #30435, 1.000000000000000666 ) ;
#6291=CARTESIAN_POINT ( 'NONE',  ( -25.07191001826344490, 307.6538819443658213, 10.57909120790611723 ) ) ;
#6292=ORIENTED_EDGE ( 'NONE', *, *, #48303, .F. ) ;
#6293=CARTESIAN_POINT ( 'NONE',  ( 19.83463548332445825, 303.8035096162420245, 9.926734387303334017 ) ) ;
#6310=ORIENTED_EDGE ( 'NONE', *, *, #30046, .F. ) ;
#6325=DIRECTION ( 'NONE',  ( -0.9133097175878012175, -0.1295276157553482965, 0.3861190962856225206 ) ) ;
#6330=CARTESIAN_POINT ( 'NONE',  ( -46.00000000000000000, 438.2642212955981336, 10.59429296198687886 ) ) ;
#6331=DIRECTION ( 'NONE',  ( -0.9915366780650367584, -0.1269898409407732853, -0.02699252395736589927 ) ) ;
#6341=CARTESIAN_POINT ( 'NONE',  ( 27.91797385465295989, 308.8116655838868496, 11.34157976637432341 ) ) ;
#6342=CARTESIAN_POINT ( 'NONE',  ( 43.00000000000024158, 485.2629658518202973, -2.796394914059508352 ) ) ;
#6343=AXIS2_PLACEMENT_3D ( 'NONE', #7986, #40897, #73782 ) ;
#6350=CARTESIAN_POINT ( 'NONE',  ( -34.28628779893050194, 463.1569812994642348, 5.966395430562092095 ) ) ;
#6352=ORIENTED_EDGE ( 'NONE', *, *, #94444, .T. ) ;
#6353=CARTESIAN_POINT ( 'NONE',  ( 32.15963082908665172, 464.7082849654401002, 10.94047064225035903 ) ) ;
#6354=CARTESIAN_POINT ( 'NONE',  ( -31.35447620051816031, 299.6032654252466614, 11.00407147780933670 ) ) ;
#6384=EDGE_CURVE ( 'NONE', #103542, #18315, #58531, .T. ) ;
#6385=CARTESIAN_POINT ( 'NONE',  ( 37.45552916193109638, 490.9506484630742875, 12.34578863136703930 ) ) ;
#6386=CARTESIAN_POINT ( 'NONE',  ( -44.12472801210821416, 485.7238370326489871, 3.975897585127424527 ) ) ;
#6387=CARTESIAN_POINT ( 'NONE',  ( 43.41290683822503382, 487.0833545439620593, 7.569976829064901658 ) ) ;
#6399=CARTESIAN_POINT ( 'NONE',  ( 39.56197461363974099, -0.1944580884125578779, -19.78098730681987405 ) ) ;
#6402=ORIENTED_EDGE ( 'NONE', *, *, #44781, .T. ) ;
#6406=DIRECTION ( 'NONE',  ( -0.000000000000000000, -1.000000000000000000, -0.000000000000000000 ) ) ;
#6408=ORIENTED_EDGE ( 'NONE', *, *, #83198, .T. ) ;
#6419=CARTESIAN_POINT ( 'NONE',  ( 32.11440402022499541, 433.9890634525672795, 24.22968092281466923 ) ) ;
#6436=AXIS2_PLACEMENT_3D ( 'NONE', #46952, #63701, #80913 ) ;
#6448=CARTESIAN_POINT ( 'NONE',  ( -8.763358074753723415, 294.6787817714944140, 1.900260594084348220 ) ) ;
#6461=CARTESIAN_POINT ( 'NONE',  ( -1.023312400211863871, 296.8556866932425464, -10.00051715684043074 ) ) ;
#6463=ADVANCED_FACE ( 'NONE', ( #33213 ), #634, .F. ) ;
#6470=CARTESIAN_POINT ( 'NONE',  ( -42.73562161879612376, 422.3951324741119606, 19.42488791944230542 ) ) ;
#6474=CARTESIAN_POINT ( 'NONE',  ( 19.36103579130787367, 294.6347466944262692, -10.04613669444748680 ) ) ;
#6477=TOROIDAL_SURFACE ( 'NONE', #75384, 8.000000000000007105, 1.000000000000000888 ) ;
#6484=CARTESIAN_POINT ( 'NONE',  ( -36.05525903195442083, 302.6656030494100378, -8.225097448474809170 ) ) ;
#6491=CARTESIAN_POINT ( 'NONE',  ( 23.96530074296727975, 306.2618658405915539, 9.248980163680499800 ) ) ;
#6498=CARTESIAN_POINT ( 'NONE',  ( -35.83770293177492050, 439.9021865884288331, 24.29457972161610968 ) ) ;
#6500=CARTESIAN_POINT ( 'NONE',  ( -27.15064582331548237, 305.1140881896778296, -9.501787623090212520 ) ) ;
#6509=CIRCLE ( 'NONE', #61690, 1.000000000000000666 ) ;
#6512=EDGE_CURVE ( 'NONE', #88846, #93114, #1324, .T. ) ;
#6514=DIRECTION ( 'NONE',  ( 0.000000000000000000, 1.000000000000000000, -1.224646799147353207E-16 ) ) ;
#6540=CARTESIAN_POINT ( 'NONE',  ( -32.83699446692833135, 465.7129794908040594, 11.08673065710671857 ) ) ;
#6546=EDGE_LOOP ( 'NONE', ( #28352, #87371, #49044, #6727, #77961 ) ) ;
#6550=CARTESIAN_POINT ( 'NONE',  ( -15.72109914222335902, 304.5560401976859453, 9.874133138051915282 ) ) ;
#6554=FACE_OUTER_BOUND ( 'NONE', #96155, .T. ) ;
#6558=ADVANCED_FACE ( 'NONE', ( #76832, #53100 ), #20253, .T. ) ;
#6568=CARTESIAN_POINT ( 'NONE',  ( 32.92521947946379868, 485.8269030686106476, 5.191998502003437821 ) ) ;
#6578=CARTESIAN_POINT ( 'NONE',  ( 44.07878952698373354, 464.4042052658809894, 9.617740716628523145 ) ) ;
#6585=CARTESIAN_POINT ( 'NONE',  ( 34.73799231214650263, 320.8457050503890287, -5.619366639134932839 ) ) ;
#6596=CARTESIAN_POINT ( 'NONE',  ( -43.02661387979790675, 465.7449615347597387, 11.43319743843399827 ) ) ;
#6601=CARTESIAN_POINT ( 'NONE',  ( -30.35537264529554946, 338.7115663565144246, 18.05293407820170515 ) ) ;
#6608=DIRECTION ( 'NONE',  ( -0.000000000000000000, -1.000000000000000000, -0.000000000000000000 ) ) ;
#6617=AXIS2_PLACEMENT_3D ( 'NONE', #74458, #56129, #41572 ) ;
#6643=B_SPLINE_SURFACE_WITH_KNOTS ( 'NONE', 1, 3, ( 
 ( #56575, #433, #31288, #64174, #106724, #98108, #97045, #88963, #72758, #75426, #35543, #10159, #84598, #67874, #77023, #59799, #10680, #34487, #52209, #99704, #84057, #19378, #51677, #965, #100757, #43073, #25875, #11206 ),
 ( #42526, #25318, #66814, #26926, #59264, #17213, #92676, #58731, #51140, #9615, #82993, #27460, #75961, #68418, #2059, #85122, #18833, #44139, #91630, #50600, #92137, #3141, #66273, #18286, #9088, #99160, #1520, #43596 ) ),
 .UNSPECIFIED., .F., .F., .F.,
 ( 2, 2 ),
 ( 4, 2, 2, 2, 2, 2, 2, 2, 2, 2, 2, 2, 2, 4 ),
 ( 0.000000000000000000, 1.000000000000000000 ),
 ( 0.08901491201581737678, 0.1032490540155679704, 0.1174831960153185778, 0.1317173380150691853, 0.1459514800148197788, 0.1744197640143299588, 0.2028880480138401388, 0.2598246160128514504, 0.3167611840118632616, 0.4306343200098861623, 0.5445074560079088410, 0.6583805920059359051, 0.7722537280039543095, 1.000000000000000000 ),
 .UNSPECIFIED. ) ;
#6644=CARTESIAN_POINT ( 'NONE',  ( 17.32310258173999884, 302.5970833027072899, 9.883176158642797304 ) ) ;
#6645=ORIENTED_EDGE ( 'NONE', *, *, #54274, .T. ) ;
#6647=DIRECTION ( 'NONE',  ( -0.000000000000000000, -1.000000000000000000, -0.000000000000000000 ) ) ;
#6649=EDGE_CURVE ( 'NONE', #72783, #12603, #48060, .T. ) ;
#6674=CARTESIAN_POINT ( 'NONE',  ( 34.63438812787640586, 463.6460534741173660, 19.43326544948845935 ) ) ;
#6678=CARTESIAN_POINT ( 'NONE',  ( -40.07586470527510158, 337.7832441655235129, 20.21182470898328631 ) ) ;
#6684=CARTESIAN_POINT ( 'NONE',  ( 23.34833856664048923, 304.4235486217770017, -9.877270693249020184 ) ) ;
#6687=CARTESIAN_POINT ( 'NONE',  ( -27.38137115745341887, 306.5387002105908323, -9.403261508857470474 ) ) ;
#6691=DIRECTION ( 'NONE',  ( 0.000000000000000000, -0.9911985061125714314, 0.1323839925376427140 ) ) ;
#6696=B_SPLINE_CURVE_WITH_KNOTS ( 'NONE', 3,
 ( #99172, #65761, #15604, #97571 ),
 .UNSPECIFIED., .F., .F.,
 ( 4, 4 ),
 ( 0.000000000000000000, 0.001668351617186237222 ),
 .UNSPECIFIED. ) ;
#6708=CARTESIAN_POINT ( 'NONE',  ( 33.43853150106103556, 315.3224335203053670, -7.014529384187835781 ) ) ;
#6718=CARTESIAN_POINT ( 'NONE',  ( 44.15895461028591740, 485.1651389999606181, 0.5848183293818906003 ) ) ;
#6722=VERTEX_POINT ( 'NONE', #12093 ) ;
#6727=ORIENTED_EDGE ( 'NONE', *, *, #104724, .T. ) ;
#6736=CARTESIAN_POINT ( 'NONE',  ( 42.76230833568492073, 461.1825766694568642, 3.198895819599614221 ) ) ;
#6744=EDGE_CURVE ( 'NONE', #23775, #9645, #17151, .T. ) ;
#6755=CARTESIAN_POINT ( 'NONE',  ( 20.33092854325555621, 302.8589055981394154, 9.938509071751244761 ) ) ;
#6756=CARTESIAN_POINT ( 'NONE',  ( -43.60671974750798796, 374.5964741257981245, 14.40348595307846757 ) ) ;
#6763=EDGE_LOOP ( 'NONE', ( #104933, #74489, #83872, #85133 ) ) ;
#6765=CARTESIAN_POINT ( 'NONE',  ( 20.97754405179127346, 294.8763868968453608, 9.942224931492237516 ) ) ;
#6772=CARTESIAN_POINT ( 'NONE',  ( 41.35030302661661494, 464.3615232856287776, 17.53848297742646523 ) ) ;
#6780=CARTESIAN_POINT ( 'NONE',  ( -37.26845974722169785, 490.8898249940490359, 12.42613736167099425 ) ) ;
#6788=CARTESIAN_POINT ( 'NONE',  ( -43.00000000000000000, 459.9277931459707247, 6.461582622321705216 ) ) ;
#6789=CARTESIAN_POINT ( 'NONE',  ( 6.657112139591454536, 304.7445950413702462, 8.914202688817031373 ) ) ;
#6790=ORIENTED_EDGE ( 'NONE', *, *, #30179, .T. ) ;
#6798=CARTESIAN_POINT ( 'NONE',  ( 43.19180182229770537, 464.9217280166857336, 10.90460934079956523 ) ) ;
#6799=CIRCLE ( 'NONE', #73925, 2.999999999999992450 ) ;
#6801=CARTESIAN_POINT ( 'NONE',  ( -32.06000226508932371, 464.8616989741469183, 13.97143297948053764 ) ) ;
#6810=CARTESIAN_POINT ( 'NONE',  ( 35.52862250380135123, 439.1409266922558459, 24.07163373315673738 ) ) ;
#6813=EDGE_CURVE ( 'NONE', #36986, #103730, #1079, .T. ) ;
#6832=CARTESIAN_POINT ( 'NONE',  ( -30.46048364471454661, 326.5320051201829870, 15.51034741246410498 ) ) ;
#6837=ORIENTED_EDGE ( 'NONE', *, *, #1747, .T. ) ;
#6842=CARTESIAN_POINT ( 'NONE',  ( 46.00000000000000711, 486.3401354059829487, 3.362847677636602306 ) ) ;
#6858=CARTESIAN_POINT ( 'NONE',  ( 13.58757579978431629, 304.5480424167135993, -9.064568323117281778 ) ) ;
#6860=ORIENTED_EDGE ( 'NONE', *, *, #84496, .T. ) ;
#6866=CYLINDRICAL_SURFACE ( 'NONE', #23920, 5.000000000000001776 ) ;
#6869=EDGE_CURVE ( 'NONE', #100861, #98784, #4602, .T. ) ;
#6870=CARTESIAN_POINT ( 'NONE',  ( 46.00000000000000000, 450.0000000000002274, 13.20242257375370976 ) ) ;
#6873=ORIENTED_EDGE ( 'NONE', *, *, #82191, .F. ) ;
#6878=CARTESIAN_POINT ( 'NONE',  ( -40.00898563721548840, 463.9413272056387996, 18.74131282407823207 ) ) ;
#6888=CARTESIAN_POINT ( 'NONE',  ( 39.42236559726133294, 328.0579091555865148, 18.01452268087317776 ) ) ;
#6893=CARTESIAN_POINT ( 'NONE',  ( 0.000000000000000000, 69.00000000000000000, -4.999999999999993783 ) ) ;
#6896=EDGE_LOOP ( 'NONE', ( #2850, #96097, #36749, #14788 ) ) ;
#6897=CARTESIAN_POINT ( 'NONE',  ( -42.21835935851050436, 436.4384481632509392, 19.62208033733266177 ) ) ;
#6899=CARTESIAN_POINT ( 'NONE',  ( -25.28458893461199253, 304.8349036104926881, 10.37793651244948379 ) ) ;
#6900=CARTESIAN_POINT ( 'NONE',  ( 32.76922047444633534, 484.1128301720478930, 1.839745883407026161 ) ) ;
#6913=CARTESIAN_POINT ( 'NONE',  ( 36.64367452218242249, 437.9806829953244574, 4.218857897681470348 ) ) ;
#6931=ORIENTED_EDGE ( 'NONE', *, *, #28199, .T. ) ;
#6935=ADVANCED_FACE ( 'NONE', ( #33095 ), #42321, .F. ) ;
#6961=FACE_OUTER_BOUND ( 'NONE', #13996, .T. ) ;
#6977=CARTESIAN_POINT ( 'NONE',  ( -8.557829126458644353, 294.6841484303073457, -5.194105103834561810 ) ) ;
#6978=VERTEX_POINT ( 'NONE', #52970 ) ;
#6983=CARTESIAN_POINT ( 'NONE',  ( -0.9627149523877855941, 294.8487549629966225, 9.936351565768161365 ) ) ;
#6987=CARTESIAN_POINT ( 'NONE',  ( 35.96015918321334226, 491.7728760210418386, 12.54260821243886248 ) ) ;
#6989=EDGE_CURVE ( 'NONE', #2280, #84655, #23636, .T. ) ;
#6998=ORIENTED_EDGE ( 'NONE', *, *, #10917, .T. ) ;
#7006=CARTESIAN_POINT ( 'NONE',  ( -32.09911992168215988, 438.9232547152093957, 23.66653216045978070 ) ) ;
#7007=CARTESIAN_POINT ( 'NONE',  ( -28.36969756101606066, 307.4744456504976142, -9.185496674863943056 ) ) ;
#7016=CARTESIAN_POINT ( 'NONE',  ( -26.90859973661891402, 304.9597527792883511, -9.536681949199044439 ) ) ;
#7025=CARTESIAN_POINT ( 'NONE',  ( 30.63851678811156631, 340.2470915159922811, 17.36724565301306811 ) ) ;
#7030=AXIS2_PLACEMENT_3D ( 'NONE', #41526, #57169, #105210 ) ;
#7036=CARTESIAN_POINT ( 'NONE',  ( -37.72381677393462240, 438.6275846837065728, 23.63981362230112282 ) ) ;
#7040=FACE_OUTER_BOUND ( 'NONE', #93887, .T. ) ;
#7045=ORIENTED_EDGE ( 'NONE', *, *, #45975, .F. ) ;
#7052=CARTESIAN_POINT ( 'NONE',  ( 20.49977525862255590, 302.8459220885798686, -10.00124997875689203 ) ) ;
#7054=VERTEX_POINT ( 'NONE', #61075 ) ;
#7063=CARTESIAN_POINT ( 'NONE',  ( 44.26141237093871439, 435.3133447328257830, 11.28309783997975480 ) ) ;
#7075=DIRECTION ( 'NONE',  ( -0.000000000000000000, -1.000000000000000000, -0.000000000000000000 ) ) ;
#7076=DIRECTION ( 'NONE',  ( 0.9167413600884036784, 0.000000000000000000, -0.3994812620177121132 ) ) ;
#7078=CARTESIAN_POINT ( 'NONE',  ( 37.67992928262796681, 491.6871197847727899, 12.48602433195153161 ) ) ;
#7088=CARTESIAN_POINT ( 'NONE',  ( 32.85155332502864667, 463.8111683108725174, 7.359358840565818127 ) ) ;
#7090=CARTESIAN_POINT ( 'NONE',  ( 30.00000000000000000, 461.8887775513396150, 11.55279652844105698 ) ) ;
#7092=CARTESIAN_POINT ( 'NONE',  ( -32.87547266101557852, 465.6993878536674742, 10.91512469976539279 ) ) ;
#7105=B_SPLINE_CURVE_WITH_KNOTS ( 'NONE', 3,
 ( #47436, #45864, #63654, #39376 ),
 .UNSPECIFIED., .F., .F.,
 ( 4, 4 ),
 ( 0.0008676662333014916340, 0.02106922348384824423 ),
 .UNSPECIFIED. ) ;
#7112=CARTESIAN_POINT ( 'NONE',  ( 45.99999999997967848, 463.5320417905273302, 9.382446278464357192 ) ) ;
#7117=EDGE_CURVE ( 'NONE', #33657, #42175, #71877, .T. ) ;
#7118=CARTESIAN_POINT ( 'NONE',  ( 35.80004365250785980, 328.0257370263789767, -3.832668609434584095 ) ) ;
#7128=CARTESIAN_POINT ( 'NONE',  ( 33.33807306180359831, 464.2324349908041654, 17.97546588399033141 ) ) ;
#7133=CARTESIAN_POINT ( 'NONE',  ( 33.56345473223404241, 299.9083031499212666, -8.874823776838020706 ) ) ;
#7134=DIRECTION ( 'NONE',  ( 0.9135154255858337624, 0.3026456445970197029, 0.2718366807904842863 ) ) ;
#7135=CARTESIAN_POINT ( 'NONE',  ( -43.51084452654406221, 465.2903130129679994, 9.421687747986709383 ) ) ;
#7138=CARTESIAN_POINT ( 'NONE',  ( -30.86777479908530708, 345.9147241694792001, 18.50750428929681490 ) ) ;
#7143=ORIENTED_EDGE ( 'NONE', *, *, #91024, .T. ) ;
#7169=CARTESIAN_POINT ( 'NONE',  ( 10.24586172992462707, 302.6397306569780312, 9.891919218941357173 ) ) ;
#7180=CARTESIAN_POINT ( 'NONE',  ( -38.67559328634845173, 490.7810811343264845, 11.84720182290557844 ) ) ;
#7183=CARTESIAN_POINT ( 'NONE',  ( 33.50629336895840282, 439.8577465421020065, 24.25469227980369524 ) ) ;
#7196=CARTESIAN_POINT ( 'NONE',  ( -43.00000000000000000, 436.0987441542287115, 7.567257455462727656 ) ) ;
#7202=CARTESIAN_POINT ( 'NONE',  ( 35.63058582596927693, 464.1921406587381966, 19.33089630041451201 ) ) ;
#7209=CARTESIAN_POINT ( 'NONE',  ( -39.84233570596349949, 333.3323931548420660, 19.23895789620553032 ) ) ;
#7212=CARTESIAN_POINT ( 'NONE',  ( 29.86158665938207335, 311.4578868317084925, -8.460588905613484201 ) ) ;
#7220=ORIENTED_EDGE ( 'NONE', *, *, #64286, .F. ) ;
#7226=ORIENTED_EDGE ( 'NONE', *, *, #10243, .F. ) ;
#7231=CARTESIAN_POINT ( 'NONE',  ( 40.52582510012484107, 311.5116601731387505, -6.047907428142603514 ) ) ;
#7233=ORIENTED_EDGE ( 'NONE', *, *, #6384, .T. ) ;
#7239=AXIS2_PLACEMENT_3D ( 'NONE', #25810, #68892, #59199 ) ;
#7243=ADVANCED_FACE ( 'NONE', ( #74316 ), #78710, .T. ) ;
#7245=CARTESIAN_POINT ( 'NONE',  ( 43.97702309827923983, 485.9235625652956969, 4.765750180331959740 ) ) ;
#7246=CIRCLE ( 'NONE', #102031, 10.00000000000000178 ) ;
#7251=EDGE_CURVE ( 'NONE', #27394, #41040, #33766, .T. ) ;
#7256=CARTESIAN_POINT ( 'NONE',  ( -15.43387005369899256, 294.5569523601460560, -10.06267239232150068 ) ) ;
#7258=CARTESIAN_POINT ( 'NONE',  ( 32.03420920423157270, 464.8550977446587922, 13.91744750517720952 ) ) ;
#7263=CARTESIAN_POINT ( 'NONE',  ( -33.07276483573667747, 438.9325140356154975, 23.89537236861306013 ) ) ;
#7275=CARTESIAN_POINT ( 'NONE',  ( -45.29202373334744181, 362.1633252469901549, 4.985022154565413643 ) ) ;
#7285=CARTESIAN_POINT ( 'NONE',  ( 18.41162169223098033, 304.6294254666754568, 9.889731659030220001 ) ) ;
#7291=CARTESIAN_POINT ( 'NONE',  ( 39.01446284274602760, 463.6644110202811362, 19.39997085980421687 ) ) ;
#7292=CARTESIAN_POINT ( 'NONE',  ( -32.85155332502864667, 463.8111683108725174, 7.359358840565846549 ) ) ;
#7295=( LENGTH_UNIT ( ) NAMED_UNIT ( * ) SI_UNIT ( .MILLI., .METRE. ) );
#7297=CARTESIAN_POINT ( 'NONE',  ( -35.15824258293415028, 491.5080798214892752, 12.36499586378574733 ) ) ;
#7300=CARTESIAN_POINT ( 'NONE',  ( 33.84761347220318584, 488.7471039746334895, 11.01988148152525504 ) ) ;
#7317=CARTESIAN_POINT ( 'NONE',  ( 43.03894652950267385, 464.9992092536288624, 11.55502599541370046 ) ) ;
#7319=ADVANCED_FACE ( 'NONE', ( #36043 ), #12709, .F. ) ;
#7327=VERTEX_POINT ( 'NONE', #36574 ) ;
#7336=CARTESIAN_POINT ( 'NONE',  ( 41.18667489362654521, 461.2717826764273923, 2.470602812283018590 ) ) ;
#7344=CARTESIAN_POINT ( 'NONE',  ( 34.32150620555758280, 300.7240803741787545, -8.683067128579168070 ) ) ;
#7348=CARTESIAN_POINT ( 'NONE',  ( -35.74483125092430669, 413.6409941285803598, 6.029078300230034770 ) ) ;
#7356=ORIENTED_EDGE ( 'NONE', *, *, #11079, .T. ) ;
#7357=CARTESIAN_POINT ( 'NONE',  ( -29.01873216445066461, 322.4064345883938358, 14.26934359691588483 ) ) ;
#7373=EDGE_CURVE ( 'NONE', #94269, #2324, #81295, .T. ) ;
#7385=ORIENTED_EDGE ( 'NONE', *, *, #25370, .T. ) ;
#7387=CARTESIAN_POINT ( 'NONE',  ( 45.99999999999999289, 461.1540656895900270, 8.531485566175636137 ) ) ;
#7390=FILL_AREA_STYLE_COLOUR ( '', #86131 ) ;
#7409=CARTESIAN_POINT ( 'NONE',  ( 29.29894309263326591, 313.0438134959539411, 12.40351596629518482 ) ) ;
#7411=ADVANCED_FACE ( 'NONE', ( #105502 ), #101135, .T. ) ;
#7413=CARTESIAN_POINT ( 'NONE',  ( -42.00989057912099156, 460.5566595377404155, 2.543045191514750059 ) ) ;
#7417=FACE_OUTER_BOUND ( 'NONE', #29082, .T. ) ;
#7418=CARTESIAN_POINT ( 'NONE',  ( -31.99941821087105609, 300.2995772073126659, 11.16780820574502009 ) ) ;
#7424=CARTESIAN_POINT ( 'NONE',  ( 1.128077836147720614, 302.8478239976497548, 9.936168295454386623 ) ) ;
#7425=CARTESIAN_POINT ( 'NONE',  ( 3.308538776003295379, 303.8518027751323984, 9.936999415074360797 ) ) ;
#7435=B_SPLINE_CURVE_WITH_KNOTS ( 'NONE', 3,
 ( #54027, #38938, #70766, #45443 ),
 .UNSPECIFIED., .F., .F.,
 ( 4, 4 ),
 ( 1.734723475976807094E-18, 0.001714393297546049902 ),
 .UNSPECIFIED. ) ;
#7442=CARTESIAN_POINT ( 'NONE',  ( -31.32517564075410021, 438.3829390354193265, 22.69287758365890539 ) ) ;
#7448=CARTESIAN_POINT ( 'NONE',  ( 32.87537929229700495, 485.0716560791287861, 1.465306988351172235 ) ) ;
#7452=EDGE_CURVE ( 'NONE', #14964, #45269, #89135, .T. ) ;
#7486=CARTESIAN_POINT ( 'NONE',  ( -11.70968583459649182, 294.5933543508184016, -2.054959069366733448 ) ) ;
#7497=CARTESIAN_POINT ( 'NONE',  ( -1.262177448353618889E-26, 294.8518027762758038, -10.00000000000000178 ) ) ;
#7498=ORIENTED_EDGE ( 'NONE', *, *, #24544, .T. ) ;
#7503=CARTESIAN_POINT ( 'NONE',  ( -1.012484434415161560, 302.8485832914468006, 9.936327107976619999 ) ) ;
#7506=B_SPLINE_SURFACE_WITH_KNOTS ( 'NONE', 1, 3, ( 
 ( #36231, #35151, #91774, #59416, #27610, #84739, #75577, #101457, #92278, #68572, #68021, #1673, #61012, #19522, #69103, #52357, #85823, #44284, #44828, #100906, #27075, #3290, #11901, #36761, #93897, #34631, #59957, #20052 ),
 ( #77714, #3826, #99849, #104093, #70680, #4350, #21626, #21112, #96021, #86879, #37284, #38851, #55520, #54456, #46918, #71712, #53944, #87928, #103572, #104627, #63663, #30776, #54997, #5414, #95480, #69628, #38336, #94442 ) ),
 .UNSPECIFIED., .F., .F., .F.,
 ( 2, 2 ),
 ( 4, 2, 2, 2, 2, 2, 2, 2, 2, 2, 2, 2, 2, 4 ),
 ( 0.000000000000000000, 1.000000000000000000 ),
 ( 0.08901491201581737678, 0.1032490540155679704, 0.1174831960153185778, 0.1317173380150691853, 0.1459514800148197788, 0.1744197640143299588, 0.2028880480138401388, 0.2598246160128514504, 0.3167611840118632616, 0.4306343200098861623, 0.5445074560079088410, 0.6583805920059359051, 0.7722537280039543095, 1.000000000000000000 ),
 .UNSPECIFIED. ) ;
#7507=CARTESIAN_POINT ( 'NONE',  ( 36.47828316237635704, 491.8387149836095205, 12.58546224877309427 ) ) ;
#7510=CARTESIAN_POINT ( 'NONE',  ( -33.94783393359910662, 484.1261039197349305, 1.321740980884785532 ) ) ;
#7512=VERTEX_POINT ( 'NONE', #99520 ) ;
#7525=CARTESIAN_POINT ( 'NONE',  ( -31.88319856737524205, 439.4127412706010887, 23.53498064488175956 ) ) ;
#7527=CARTESIAN_POINT ( 'NONE',  ( -33.52518095673029563, 327.1007879220064751, -3.538621449569222310 ) ) ;
#7537=CARTESIAN_POINT ( 'NONE',  ( -24.97190087653902424, 295.6134355416385233, -1.836602347154774550 ) ) ;
#7541=B_SPLINE_CURVE_WITH_KNOTS ( 'NONE', 3,
 ( #40408, #25324, #31295, #72765 ),
 .UNSPECIFIED., .F., .F.,
 ( 4, 4 ),
 ( 6.938893903907228378E-18, 0.001632242847431727550 ),
 .UNSPECIFIED. ) ;
#7544=CARTESIAN_POINT ( 'NONE',  ( 46.00000000000000000, 500.0000000000002274, 0.000000000000000000 ) ) ;
#7545=CARTESIAN_POINT ( 'NONE',  ( 24.84269077136356074, 307.1603884938444367, 9.459414721148165839 ) ) ;
#7559=EDGE_CURVE ( 'NONE', #85705, #78207, #78796, .T. ) ;
#7582=VERTEX_POINT ( 'NONE', #84427 ) ;
#7586=EDGE_CURVE ( 'NONE', #66822, #19762, #13345, .T. ) ;
#7594=CARTESIAN_POINT ( 'NONE',  ( 0.000000000000000000, 81.00000000000000000, 0.000000000000000000 ) ) ;
#7597=CARTESIAN_POINT ( 'NONE',  ( 29.99999999999999289, 488.6917380704417724, 8.883757572940274017 ) ) ;
#7623=ORIENTED_EDGE ( 'NONE', *, *, #7944, .F. ) ;
#7631=CARTESIAN_POINT ( 'NONE',  ( 33.00000000000000000, 485.0303364503728289, 0.9535057477322557151 ) ) ;
#7637=CARTESIAN_POINT ( 'NONE',  ( -32.21797308369322366, 464.6987731533837405, 10.77720717743534173 ) ) ;
#7652=CARTESIAN_POINT ( 'NONE',  ( -31.21933008645656926, 405.2090764464551853, 25.56980379099173817 ) ) ;
#7654=CARTESIAN_POINT ( 'NONE',  ( -33.04853154822947658, 439.4047662902898423, 23.83380291423519282 ) ) ;
#7668=CYLINDRICAL_SURFACE ( 'NONE', #21195, 15.00000000000000711 ) ;
#7670=FACE_BOUND ( 'NONE', #84723, .T. ) ;
#7677=CIRCLE ( 'NONE', #23193, 0.9999999999999793499 ) ;
#7683=EDGE_LOOP ( 'NONE', ( #69214, #76926, #83246, #86329 ) ) ;
#7698=ORIENTED_EDGE ( 'NONE', *, *, #9619, .T. ) ;
#7709=CARTESIAN_POINT ( 'NONE',  ( 35.50943207940664337, 439.1423799595334572, 24.07278252408766761 ) ) ;
#7732=CARTESIAN_POINT ( 'NONE',  ( -43.29658055318886767, 324.1952503670673877, -2.852919881210743913 ) ) ;
#7734=CARTESIAN_POINT ( 'NONE',  ( -37.04388863813380794, 311.3287000699716032, 13.89786840526617517 ) ) ;
#7737=CARTESIAN_POINT ( 'NONE',  ( 29.41762786570794219, 308.7428865632042516, -8.884592557111700373 ) ) ;
#7745=DIRECTION ( 'NONE',  ( -1.000000000000000000, 0.000000000000000000, 0.000000000000000000 ) ) ;
#7750=CARTESIAN_POINT ( 'NONE',  ( -36.64367452218617416, 437.9806829953259921, 4.218857897671346002 ) ) ;
#7764=ORIENTED_EDGE ( 'NONE', *, *, #88020, .F. ) ;
#7767=( NAMED_UNIT ( * ) PLANE_ANGLE_UNIT ( ) SI_UNIT ( $, .RADIAN. ) );
#7770=CARTESIAN_POINT ( 'NONE',  ( 43.60560354499546065, 484.6927786831506637, 3.665222855544667979 ) ) ;
#7775=EDGE_LOOP ( 'NONE', ( #99410, #67049, #60869, #92434, #64147, #60514 ) ) ;
#7779=CARTESIAN_POINT ( 'NONE',  ( 29.45101819180745650, 310.9056806215746747, -7.594963747789880593 ) ) ;
#7781=ORIENTED_EDGE ( 'NONE', *, *, #47769, .T. ) ;
#7784=DIRECTION ( 'NONE',  ( 0.000000000000000000, 0.000000000000000000, -1.000000000000000000 ) ) ;
#7785=CARTESIAN_POINT ( 'NONE',  ( -17.09932871081075589, 294.5833313981810875, -2.056789631266450424 ) ) ;
#7787=CARTESIAN_POINT ( 'NONE',  ( -33.00000000000000711, 484.0323588803976804, 1.017072797580844679 ) ) ;
#7788=CARTESIAN_POINT ( 'NONE',  ( -36.52561726181225055, 463.3029834606193731, 20.13286708880156084 ) ) ;
#7795=ORIENTED_EDGE ( 'NONE', *, *, #105654, .F. ) ;
#7801=CARTESIAN_POINT ( 'NONE',  ( 44.13004363183722489, 485.1789828605022876, 0.5705925370718127887 ) ) ;
#7802=CARTESIAN_POINT ( 'NONE',  ( -35.52817563886351593, 439.1305428102971291, 24.06292914475137579 ) ) ;
#7803=CARTESIAN_POINT ( 'NONE',  ( 25.40899158128945601, 304.9361475457282040, 10.40122582195319545 ) ) ;
#7804=CARTESIAN_POINT ( 'NONE',  ( -37.50484670062839143, 362.5590287838574568, 3.193838888351949734 ) ) ;
#7825=ORIENTED_EDGE ( 'NONE', *, *, #37630, .T. ) ;
#7829=CARTESIAN_POINT ( 'NONE',  ( -35.47838770905752881, 490.5979824476968361, 12.29204623667650864 ) ) ;
#7848=DIRECTION ( 'NONE',  ( 0.000000000000000000, 0.000000000000000000, -1.000000000000000000 ) ) ;
#7872=CARTESIAN_POINT ( 'NONE',  ( 28.83990699788477841, 306.5324003088252880, -9.174548767398087890 ) ) ;
#7888=CARTESIAN_POINT ( 'NONE',  ( -22.02345313010431838, 305.2775641474292456, 10.02869406391017648 ) ) ;
#7890=CARTESIAN_POINT ( 'NONE',  ( 32.87494462546104756, 485.1684504739468480, 5.618872456256310599 ) ) ;
#7891=CARTESIAN_POINT ( 'NONE',  ( 31.06723445740051659, 439.4129214212010197, 22.80782786576363108 ) ) ;
#7918=CARTESIAN_POINT ( 'NONE',  ( 35.44563196690202744, 355.0508310518326311, 1.542887188955126110 ) ) ;
#7921=B_SPLINE_CURVE_WITH_KNOTS ( 'NONE', 3,
 ( #15127, #23789, #98168, #56639 ),
 .UNSPECIFIED., .F., .F.,
 ( 4, 4 ),
 ( 0.000000000000000000, 0.002232172794123124613 ),
 .UNSPECIFIED. ) ;
#7933=CARTESIAN_POINT ( 'NONE',  ( 33.11890921805852628, 438.9412750689605787, 23.90522689637583653 ) ) ;
#7942=CARTESIAN_POINT ( 'NONE',  ( 33.00540147335379260, 487.4196752801331627, 9.523982417622169905 ) ) ;
#7943=CARTESIAN_POINT ( 'NONE',  ( 36.51610996680960142, 309.5552553936822164, 13.45073210680923026 ) ) ;
#7944=EDGE_CURVE ( 'NONE', #75855, #59443, #19246, .T. ) ;
#7949=CARTESIAN_POINT ( 'NONE',  ( -41.75908120488647768, 460.3944608375931011, 2.386179269091041721 ) ) ;
#7956=CARTESIAN_POINT ( 'NONE',  ( -28.21399895733517127, 296.8976392795444212, 2.382931296657796683 ) ) ;
#7983=CARTESIAN_POINT ( 'NONE',  ( -31.74546804893367380, 439.0126127266693175, 23.49846720828339386 ) ) ;
#7986=CARTESIAN_POINT ( 'NONE',  ( -43.00000000000000000, 500.0000000000002274, 0.000000000000000000 ) ) ;
#8013=EDGE_LOOP ( 'NONE', ( #93128, #6645, #75969, #7795 ) ) ;
#8017=CARTESIAN_POINT ( 'NONE',  ( 29.49295069903413591, 326.6849569854988431, 15.30827334355864799 ) ) ;
#8022=CARTESIAN_POINT ( 'NONE',  ( -32.65817089032885434, 465.7881089174890690, 12.85132715801033854 ) ) ;
#8037=CARTESIAN_POINT ( 'NONE',  ( -1.249646147729365664, 294.8475419170777059, -9.939938411486226144 ) ) ;
#8038=B_SPLINE_CURVE_WITH_KNOTS ( 'NONE', 3,
 ( #104218, #96147, #94572, #29846 ),
 .UNSPECIFIED., .F., .F.,
 ( 4, 4 ),
 ( 5.721958498152796815E-17, 0.001000218973298496470 ),
 .UNSPECIFIED. ) ;
#8040=ORIENTED_EDGE ( 'NONE', *, *, #99417, .T. ) ;
#8050=CARTESIAN_POINT ( 'NONE',  ( -32.28552837373656814, 464.7648866755938570, 15.30384310834764428 ) ) ;
#8061=ORIENTED_EDGE ( 'NONE', *, *, #60748, .F. ) ;
#8067=CARTESIAN_POINT ( 'NONE',  ( 0.000000000000000000, 303.8518027762758038, 9.936999415352289589 ) ) ;
#8072=CARTESIAN_POINT ( 'NONE',  ( -34.81734560031965486, 344.2880855494414050, 0.4170339163263865334 ) ) ;
#8079=CARTESIAN_POINT ( 'NONE',  ( -30.00000000000000000, 490.5636507776930557, 7.413185101875094496 ) ) ;
#8083=CARTESIAN_POINT ( 'NONE',  ( -25.60610463954871463, 295.7997949935824522, -1.796194680006651945 ) ) ;
#8088=CARTESIAN_POINT ( 'NONE',  ( -32.57492934538399965, 345.3439590197779125, 19.85777474157123024 ) ) ;
#8097=CARTESIAN_POINT ( 'NONE',  ( -41.20375261497546404, 436.5366665730131785, 21.37241632499251764 ) ) ;
#8099=CARTESIAN_POINT ( 'NONE',  ( 19.70764564238371719, 304.7954121406193622, 9.925013215726785631 ) ) ;
#8100=CARTESIAN_POINT ( 'NONE',  ( -32.89862776688993762, 464.9311084009894444, 10.99515925127032467 ) ) ;
#8119=FACE_OUTER_BOUND ( 'NONE', #60005, .T. ) ;
#8134=AXIS2_PLACEMENT_3D ( 'NONE', #7544, #14048, #38369 ) ;
#8137=AXIS2_PLACEMENT_3D ( 'NONE', #52860, #28097, #85788 ) ;
#8146=ORIENTED_EDGE ( 'NONE', *, *, #71855, .F. ) ;
#8151=CARTESIAN_POINT ( 'NONE',  ( -44.14911905790387436, 464.3766534541992996, 9.623404994945699897 ) ) ;
#8180=CARTESIAN_POINT ( 'NONE',  ( 46.00000000000000000, 459.9277931459795354, 6.461582622334325343 ) ) ;
#8193=CARTESIAN_POINT ( 'NONE',  ( 44.21332904831284338, 435.2494715644501184, 14.45449769377390581 ) ) ;
#8207=CIRCLE ( 'NONE', #34123, 1.000000000000001998 ) ;
#8211=EDGE_CURVE ( 'NONE', #98501, #23399, #41662, .T. ) ;
#8236=CARTESIAN_POINT ( 'NONE',  ( -25.66200995656152273, 305.1858995196985802, 10.45951546437543733 ) ) ;
#8248=CARTESIAN_POINT ( 'NONE',  ( 40.98595185921475803, 438.0930894115431897, 22.33269956591867356 ) ) ;
#8256=CARTESIAN_POINT ( 'NONE',  ( 34.12349128637390550, 490.1895789250395978, 12.63944770676189933 ) ) ;
#8262=CARTESIAN_POINT ( 'NONE',  ( 37.43130592803709078, 464.0780360860962901, 19.48660943767455223 ) ) ;
#8267=CARTESIAN_POINT ( 'NONE',  ( -38.68218982724705057, 320.0845437455996603, 16.10279619727025135 ) ) ;
#8269=CARTESIAN_POINT ( 'NONE',  ( -33.56345473223404241, 299.9083031499212666, -8.874823776838020706 ) ) ;
#8273=CARTESIAN_POINT ( 'NONE',  ( 29.15784866723035051, 310.4008174516520171, -7.717995496960369906 ) ) ;
#8274=( BOUNDED_SURFACE ( )  B_SPLINE_SURFACE ( 3, 2, ( 
 ( #53320, #78117, #102929 ),
 ( #86769, #98016, #64083 ),
 ( #32783, #91006, #55929 ),
 ( #88871, #41902, #96958 ) ),
 .UNSPECIFIED., .F., .F., .F. ) 
 B_SPLINE_SURFACE_WITH_KNOTS ( ( 4, 4 ),
 ( 3, 3 ),
 ( 6.071532165918824830E-18, 0.002491432948284471368 ),
 ( 0.000000000000000000, 1.000000000000000000 ),
 .UNSPECIFIED. ) 
 GEOMETRIC_REPRESENTATION_ITEM ( )  RATIONAL_B_SPLINE_SURFACE ( (
 ( 1.000000000000000000, 0.7978714159192654698, 1.000000000000000000),
 ( 1.000000000000000000, 0.8097755972629270271, 1.000000000000000000),
 ( 1.000000000000000000, 0.8213938805858149728, 1.000000000000000000),
 ( 1.000000000000000000, 0.8328393170029660952, 1.000000000000000000) ) ) 
 REPRESENTATION_ITEM ( '' )  SURFACE ( )  );
#8285=DIRECTION ( 'NONE',  ( 0.000000000000000000, -1.000000000000000000, 0.000000000000000000 ) ) ;
#8292=VERTEX_POINT ( 'NONE', #4838 ) ;
#8323=CARTESIAN_POINT ( 'NONE',  ( -9.740083726531054253, 294.6493269980090872, -10.04303756037258566 ) ) ;
#8342=CARTESIAN_POINT ( 'NONE',  ( 31.73032761413494640, 329.8498846259531092, 16.53112576517208865 ) ) ;
#8343=CARTESIAN_POINT ( 'NONE',  ( -36.41465019936182301, 334.9862706725128305, -2.190136381357836282 ) ) ;
#8351=B_SPLINE_CURVE_WITH_KNOTS ( 'NONE', 3,
 ( #74134, #6755, #218, #105454, #31595, #40182, #64480, #57947, #81681, #15376, #73060, #7803, #56347, #80108, #15909, #90872, #97349, #39675, #23502, #24570, #89282, #104936, #48263, #40711, #64994, #33182, #66054, #16439, #105968, #8342, #6210, #98931, #97887, #73599, #39149, #31078, #72549, #63957, #96843, #22972, #24042, #32112, #88744, #56883, #14837, #89809, #47733, #90331 ),
 .UNSPECIFIED., .F., .F.,
 ( 4, 2, 2, 2, 2, 2, 2, 2, 2, 2, 2, 2, 2, 2, 2, 2, 2, 2, 2, 2, 2, 2, 2, 4 ),
 ( -6.000000001701573511E-08, 0.001117306459296872004, 0.002234672918593761000, 0.003352039377890650429, 0.004469405837187538991, 0.005586772296484427552, 0.006704138755781317849, 0.007821505215078206411, 0.008938871674375094972, 0.01117360459296873505, 0.01340833751156237687, 0.01787780334874965876, 0.02234726918593694239, 0.02681673502312422255, 0.03128620086031150965, 0.03575566669749879328, 0.04469459837187320095, 0.05363353004624760167, 0.07151139339499641701, 0.08045032506937090100, 0.08938925674374539887, 0.1072671200924942003, 0.1251449834412430295, 0.1430228467899918310 ),
 .UNSPECIFIED. ) ;
#8352=ORIENTED_EDGE ( 'NONE', *, *, #36655, .T. ) ;
#8355=CARTESIAN_POINT ( 'NONE',  ( 41.32430911664878437, 464.3530259918923662, 17.56657173514240711 ) ) ;
#8369=CARTESIAN_POINT ( 'NONE',  ( -36.28158941437202145, 490.9587137816652671, 12.45622313966492101 ) ) ;
#8373=CARTESIAN_POINT ( 'NONE',  ( 32.94539137534210482, 488.0149952105423381, 9.145905951749446317 ) ) ;
#8376=CARTESIAN_POINT ( 'NONE',  ( -3.364021409948656505, 294.8518027753228807, 9.936999415087239385 ) ) ;
#8380=CARTESIAN_POINT ( 'NONE',  ( 44.21332904831284338, 435.2494715644500616, 14.45449769377396976 ) ) ;
#8392=CARTESIAN_POINT ( 'NONE',  ( -40.36516081889102026, 459.8940149412733831, 1.928085546549958451 ) ) ;
#8398=CARTESIAN_POINT ( 'NONE',  ( 37.72536826885050232, 463.3861702155475086, 19.97111768659700815 ) ) ;
#8407=ORIENTED_EDGE ( 'NONE', *, *, #44864, .T. ) ;
#8412=CARTESIAN_POINT ( 'NONE',  ( 28.76128244818236013, 306.4537308956344077, -9.192937457247751354 ) ) ;
#8416=CARTESIAN_POINT ( 'NONE',  ( -43.71037717921252863, 462.3391554988666599, 4.824299547746595529 ) ) ;
#8418=CARTESIAN_POINT ( 'NONE',  ( -28.21644434148578640, 308.7733337496239301, -9.112255642778066544 ) ) ;
#8422=DIRECTION ( 'NONE',  ( -0.8400944247696989775, 0.000000000000000000, 0.5424401879201693477 ) ) ;
#8424=FACE_OUTER_BOUND ( 'NONE', #86846, .T. ) ;
#8452=CARTESIAN_POINT ( 'NONE',  ( 27.57151080649627417, 314.0751515626058676, 12.18133379269485239 ) ) ;
#8454=CARTESIAN_POINT ( 'NONE',  ( 20.21880305278364887, 304.8280059657581091, -9.005058168222342729 ) ) ;
#8472=CARTESIAN_POINT ( 'NONE',  ( -32.16580085343982631, 416.1844688050518357, 25.51939514139120746 ) ) ;
#8477=ORIENTED_EDGE ( 'NONE', *, *, #17687, .T. ) ;
#8480=CARTESIAN_POINT ( 'NONE',  ( 32.30597388339071330, 435.2336684711225985, 15.38768761833313903 ) ) ;
#8481=CARTESIAN_POINT ( 'NONE',  ( 31.41235438697622584, 299.6634614727072972, 11.01818356005949440 ) ) ;
#8489=CARTESIAN_POINT ( 'NONE',  ( -30.00000000000000000, 450.0000000000002274, 13.20242257375370976 ) ) ;
#8492=CARTESIAN_POINT ( 'NONE',  ( -24.48781666683216685, 295.5147073160107425, 2.079262953486592735 ) ) ;
#8498=CARTESIAN_POINT ( 'NONE',  ( 8.090408256587625857, 295.7505182605545997, 5.908160356365994126 ) ) ;
#8508=DIRECTION ( 'NONE',  ( 0.000000000000000000, 0.000000000000000000, -1.000000000000000000 ) ) ;
#8512=CYLINDRICAL_SURFACE ( 'NONE', #53225, 15.00000000000000711 ) ;
#8516=CARTESIAN_POINT ( 'NONE',  ( 33.00000000000000000, 450.0000000000002274, 1.202422573753698876 ) ) ;
#8530=EDGE_CURVE ( 'NONE', #75683, #21601, #20318, .T. ) ;
#8533=ORIENTED_EDGE ( 'NONE', *, *, #75469, .T. ) ;
#8548=ORIENTED_EDGE ( 'NONE', *, *, #45419, .T. ) ;
#8552=CARTESIAN_POINT ( 'NONE',  ( 31.42152527681154339, 380.7394937707176723, 23.45597763386094314 ) ) ;
#8562=TOROIDAL_SURFACE ( 'NONE', #82643, 12.00000000000001066, 3.000000000000000000 ) ;
#8573=CARTESIAN_POINT ( 'NONE',  ( -0.7515601776302233139, 295.1017350047013110, -10.00017833058035599 ) ) ;
#8583=UNCERTAINTY_MEASURE_WITH_UNIT (LENGTH_MEASURE( 1.000000000000000082E-05 ), #97329, 'distance_accuracy_value', 'NONE');
#8586=DIRECTION ( 'NONE',  ( 0.000000000000000000, 0.000000000000000000, -1.000000000000000000 ) ) ;
#8592=AXIS2_PLACEMENT_3D ( 'NONE', #61197, #62273, #77907 ) ;
#8602=CARTESIAN_POINT ( 'NONE',  ( -31.35596682365704524, 438.0939828603719661, 22.55458131664422439 ) ) ;
#8604=CARTESIAN_POINT ( 'NONE',  ( -32.89619668145245868, 321.6758930293437402, -5.892485756851701950 ) ) ;
#8612=CARTESIAN_POINT ( 'NONE',  ( -25.88003106869689418, 295.8060735027391956, -9.795024457689359920 ) ) ;
#8617=CARTESIAN_POINT ( 'NONE',  ( -37.69778599684636333, 484.8925473506873800, -3.622119997864802876 ) ) ;
#8618=CARTESIAN_POINT ( 'NONE',  ( -41.32756079954049255, 330.3955937106402985, 10.56840023132855499 ) ) ;
#8624=ADVANCED_FACE ( 'NONE', ( #3523 ), #27147, .T. ) ;
#8630=CARTESIAN_POINT ( 'NONE',  ( -40.61431708406630747, 438.3130824198840969, 22.61094925422919388 ) ) ;
#8631=ORIENTED_EDGE ( 'NONE', *, *, #87659, .F. ) ;
#8632=DIRECTION ( 'NONE',  ( 0.000000000000000000, 0.000000000000000000, -1.000000000000000000 ) ) ;
#8634=CARTESIAN_POINT ( 'NONE',  ( 43.00000000000000000, 436.0987441542287115, 7.567257455462732096 ) ) ;
#8635=CARTESIAN_POINT ( 'NONE',  ( -32.19135603494724762, 464.6890496749877002, 10.76801839735351329 ) ) ;
#8638=AXIS2_PLACEMENT_3D ( 'NONE', #95116, #6608, #87551 ) ;
#8648=CARTESIAN_POINT ( 'NONE',  ( 21.29975379448946171, 294.8969325209483259, -1.990407376643353210 ) ) ;
#8653=CARTESIAN_POINT ( 'NONE',  ( 37.52575628271135599, 438.0832219636473042, 4.091974619413631054 ) ) ;
#8654=CARTESIAN_POINT ( 'NONE',  ( -46.00000000000000000, 450.0000000000002274, 8.202422573753707979 ) ) ;
#8658=ADVANCED_FACE ( 'NONE', ( #86054 ), #93372, .F. ) ;
#8671=CARTESIAN_POINT ( 'NONE',  ( 42.09158233638500235, 465.7816406625409513, 14.79318349170030089 ) ) ;
#8673=CARTESIAN_POINT ( 'NONE',  ( -43.00000000000000000, 465.8747179598608454, 15.20075430169035968 ) ) ;
#8675=CARTESIAN_POINT ( 'NONE',  ( 30.00000000000000355, 489.4338083968374349, 5.745752720320034257 ) ) ;
#8689=CARTESIAN_POINT ( 'NONE',  ( 43.64071296021040069, 465.1114042828264701, 8.837889712622711613 ) ) ;
#8711=CARTESIAN_POINT ( 'NONE',  ( 35.62292360717185602, 485.2979424254040737, -2.983350328823797692 ) ) ;
#8715=CARTESIAN_POINT ( 'NONE',  ( 32.14406631781839252, 464.7180616791956709, 11.03187369810257046 ) ) ;
#8723=EDGE_LOOP ( 'NONE', ( #7498, #27513, #57294, #66828 ) ) ;
#8724=CARTESIAN_POINT ( 'NONE',  ( 43.11534632275464674, 435.4435433140300233, 9.329549855361735311 ) ) ;
#8727=ORIENTED_EDGE ( 'NONE', *, *, #86547, .T. ) ;
#8729=CARTESIAN_POINT ( 'NONE',  ( 40.75641113481592726, 360.0948485545300741, 24.37153223514695100 ) ) ;
#8735=CARTESIAN_POINT ( 'NONE',  ( -30.23256681546976665, 333.1711909956446220, 15.81959552928561052 ) ) ;
#8745=CARTESIAN_POINT ( 'NONE',  ( 42.89089171630051567, 462.3282028664104928, 4.511925770464189966 ) ) ;
#8748=CARTESIAN_POINT ( 'NONE',  ( -33.74271564777242816, 484.1802673187708592, 2.058285076122308155 ) ) ;
#8759=CYLINDRICAL_SURFACE ( 'NONE', #84185, 15.00000000000001421 ) ;
#8766=CARTESIAN_POINT ( 'NONE',  ( -33.15900708678776709, 406.2917883087327482, 25.90049563504663510 ) ) ;
#8773=( BOUNDED_SURFACE ( )  B_SPLINE_SURFACE ( 3, 2, ( 
 ( #43390, #27783, #1840 ),
 ( #35867, #68743, #85445 ),
 ( #44455, #76273, #101088 ),
 ( #75199, #51466, #91931 ) ),
 .UNSPECIFIED., .F., .F., .F. ) 
 B_SPLINE_SURFACE_WITH_KNOTS ( ( 4, 4 ),
 ( 3, 3 ),
 ( -1.647987302177966740E-17, 0.001448708294673844077 ),
 ( 0.000000000000000000, 1.000000000000000000 ),
 .UNSPECIFIED. ) 
 GEOMETRIC_REPRESENTATION_ITEM ( )  RATIONAL_B_SPLINE_SURFACE ( (
 ( 1.000000000000000000, 0.7788880963805115965, 1.000000000000000000),
 ( 1.000000000000000000, 0.7852432470597578984, 1.000000000000000000),
 ( 1.000000000000000000, 0.7915643316728345757, 1.000000000000000000),
 ( 1.000000000000000000, 0.7978714159192749067, 1.000000000000000000) ) ) 
 REPRESENTATION_ITEM ( '' )  SURFACE ( )  );
#8784=CARTESIAN_POINT ( 'NONE',  ( -34.47678062873981020, 437.1474145881089157, 5.468662283310369077 ) ) ;
#8792=CARTESIAN_POINT ( 'NONE',  ( -43.71037717921241494, 462.3391554988664325, 4.824299547746271344 ) ) ;
#8801=CARTESIAN_POINT ( 'NONE',  ( -39.84233570596349949, 333.3323931548420660, 19.23895789620553032 ) ) ;
#8803=CARTESIAN_POINT ( 'NONE',  ( -33.08751701378358945, 301.6823158026044780, 11.49690784967660662 ) ) ;
#8805=ORIENTED_EDGE ( 'NONE', *, *, #72338, .F. ) ;
#8806=CARTESIAN_POINT ( 'NONE',  ( 24.69596357296672906, 306.0113623816489508, -9.748045212393256165 ) ) ;
#8816=CARTESIAN_POINT ( 'NONE',  ( -33.00496812084341514, 465.6658704666166386, 15.15901827095481735 ) ) ;
#8817=EDGE_CURVE ( 'NONE', #80767, #26711, #38718, .T. ) ;
#8835=CARTESIAN_POINT ( 'NONE',  ( 43.51067860848580438, 485.4417974898075272, 3.909400899863179735 ) ) ;
#8837=SURFACE_STYLE_USAGE ( .BOTH. , #83264 ) ;
#8845=CARTESIAN_POINT ( 'NONE',  ( -32.62396605173334763, 486.1273723460411134, 7.520682129455360965 ) ) ;
#8853=CARTESIAN_POINT ( 'NONE',  ( -9.789044728064858703, 294.6486233851414909, -2.043184600578024757 ) ) ;
#8854=CARTESIAN_POINT ( 'NONE',  ( 33.00496812083873976, 465.6658704666190829, 15.15901827093887810 ) ) ;
#8858=LINE ( 'NONE', #207, #55018 ) ;
#8875=CARTESIAN_POINT ( 'NONE',  ( -41.96602095134714716, 327.8757771672179615, 6.048261806728006285 ) ) ;
#8883=CARTESIAN_POINT ( 'NONE',  ( 38.45306524269546600, 463.5271487759612796, 19.68908736396432246 ) ) ;
#8889=CARTESIAN_POINT ( 'NONE',  ( -33.95156263172582101, 464.5083255208627975, 6.608064661821575037 ) ) ;
#8896=EDGE_CURVE ( 'NONE', #79894, #48783, #55484, .T. ) ;
#8897=CARTESIAN_POINT ( 'NONE',  ( -35.58515402554202467, 490.6697164559567454, 12.32566724388538049 ) ) ;
#8908=CARTESIAN_POINT ( 'NONE',  ( 43.59756234217299209, 434.3244621007144133, 14.55946156040475614 ) ) ;
#8926=ORIENTED_EDGE ( 'NONE', *, *, #70173, .T. ) ;
#8940=( GEOMETRIC_REPRESENTATION_CONTEXT ( 3 ) GLOBAL_UNCERTAINTY_ASSIGNED_CONTEXT ( ( #17105 ) ) GLOBAL_UNIT_ASSIGNED_CONTEXT ( ( #57913, #106465, #98384 ) ) REPRESENTATION_CONTEXT ( 'NONE', 'WORKASPACE' ) );
#8941=CARTESIAN_POINT ( 'NONE',  ( 33.03761854510200635, 300.1793615339376515, -0.8055793472020765789 ) ) ;
#8956=CARTESIAN_POINT ( 'NONE',  ( 34.05209713062498622, 485.0008159996403378, 0.6776390644912295702 ) ) ;
#8957=CARTESIAN_POINT ( 'NONE',  ( 31.35484960135613619, 439.6865637981555324, 23.41922880401698137 ) ) ;
#8958=CARTESIAN_POINT ( 'NONE',  ( 32.68648381767908973, 486.2785269687594223, 6.276066868107815999 ) ) ;
#8963=VERTEX_POINT ( 'NONE', #15482 ) ;
#8973=DIRECTION ( 'NONE',  ( -0.000000000000000000, -1.000000000000000000, -0.000000000000000000 ) ) ;
#8975=FILL_AREA_STYLE ('',( #27887 ) ) ;
#8979=CARTESIAN_POINT ( 'NONE',  ( 18.59882702213898753, 304.6205295274080527, -9.049158645989061611 ) ) ;
#8983=CARTESIAN_POINT ( 'NONE',  ( 16.98789274048672127, 303.5779513886026280, -10.05824692440026169 ) ) ;
#8999=CARTESIAN_POINT ( 'NONE',  ( -40.70972807814067096, 464.1553110665033159, 18.16976512832724922 ) ) ;
#9000=CARTESIAN_POINT ( 'NONE',  ( -31.16305316186402408, 374.7586899056589118, 23.86554239046190418 ) ) ;
#9008=CARTESIAN_POINT ( 'NONE',  ( 25.99470359582689838, 305.5572448969162451, 10.54713035941321131 ) ) ;
#9012=CARTESIAN_POINT ( 'NONE',  ( 42.41247034190681831, 353.4773973720574531, 15.30157164444485574 ) ) ;
#9017=CARTESIAN_POINT ( 'NONE',  ( -20.64401833605449355, 302.8990037343777999, 9.947032289444299735 ) ) ;
#9019=DIRECTION ( 'NONE',  ( 0.9086146812045996501, 0.000000000000000000, 0.4176354404255748221 ) ) ;
#9023=CARTESIAN_POINT ( 'NONE',  ( 7.726405549742459300, 296.0527277817394634, 6.373329964583255958 ) ) ;
#9050=B_SPLINE_CURVE_WITH_KNOTS ( 'NONE', 3,
 ( #62125, #78795, #78273, #69663 ),
 .UNSPECIFIED., .F., .F.,
 ( 4, 4 ),
 ( 5.721958498152796815E-17, 0.001448684797825249872 ),
 .UNSPECIFIED. ) ;
#9059=ORIENTED_EDGE ( 'NONE', *, *, #14452, .F. ) ;
#9060=B_SPLINE_CURVE_WITH_KNOTS ( 'NONE', 3,
 ( #60797, #26335, #36019, #93149 ),
 .UNSPECIFIED., .F., .F.,
 ( 4, 4 ),
 ( 0.000000000000000000, 0.0002642584603507367683 ),
 .UNSPECIFIED. ) ;
#9064=CARTESIAN_POINT ( 'NONE',  ( 39.59239511134280320, 490.2207323505293175, 11.38527476693367646 ) ) ;
#9067=VERTEX_POINT ( 'NONE', #18163 ) ;
#9069=CARTESIAN_POINT ( 'NONE',  ( -4.404494731813556108, 294.7962499846886431, -8.995593899024026285 ) ) ;
#9074=ADVANCED_FACE ( 'NONE', ( #92029 ), #42412, .F. ) ;
#9079=CARTESIAN_POINT ( 'NONE',  ( 30.46151443478357024, 326.5429411037146679, 15.51295837324801141 ) ) ;
#9088=CARTESIAN_POINT ( 'NONE',  ( -31.11679462788039530, 441.4271381875185511, 23.27438508043199406 ) ) ;
#9093=B_SPLINE_CURVE_WITH_KNOTS ( 'NONE', 3,
 ( #15359, #24025, #6736, #80615 ),
 .UNSPECIFIED., .F., .F.,
 ( 4, 4 ),
 ( 8.420559318810145779E-18, 0.001259908249732933022 ),
 .UNSPECIFIED. ) ;
#9098=CARTESIAN_POINT ( 'NONE',  ( -3.947200809147736411, 295.9771890841169011, -10.00641236124439715 ) ) ;
#9109=CARTESIAN_POINT ( 'NONE',  ( 35.43142158411064457, 491.1302584545976515, 12.10548931029503983 ) ) ;
#9112=EDGE_LOOP ( 'NONE', ( #56861, #75835, #64307, #94961 ) ) ;
#9120=VERTEX_POINT ( 'NONE', #52098 ) ;
#9125=CARTESIAN_POINT ( 'NONE',  ( -31.13499213488098505, 439.5204445682307437, 23.00710445961532358 ) ) ;
#9127=CARTESIAN_POINT ( 'NONE',  ( -28.57185684847394569, 309.4411263248405817, -7.951019538551619803 ) ) ;
#9134=CARTESIAN_POINT ( 'NONE',  ( -26.35358385847169416, 295.9512351630701232, -9.763468370421369613 ) ) ;
#9139=CARTESIAN_POINT ( 'NONE',  ( -35.85122874546545546, 485.1582092647775539, -2.238595989622043092 ) ) ;
#9140=CARTESIAN_POINT ( 'NONE',  ( -41.13637439020717324, 328.1376453396359238, 10.03865748547844561 ) ) ;
#9147=CIRCLE ( 'NONE', #5768, 2.999999999999999112 ) ;
#9190=CARTESIAN_POINT ( 'NONE',  ( 32.54922218626916930, 319.8023524069591303, -6.363686095274232457 ) ) ;
#9191=CARTESIAN_POINT ( 'NONE',  ( 41.35053930177047476, 461.4196900451150327, 2.572867796617790415 ) ) ;
#9192=CARTESIAN_POINT ( 'NONE',  ( -33.13449099605734460, 435.1334182590073851, 11.13154690284580894 ) ) ;
#9195=EDGE_LOOP ( 'NONE', ( #95142, #99144, #68812, #62307 ) ) ;
#9196=DIRECTION ( 'NONE',  ( 0.000000000000000000, -0.9746667163790341259, 0.2236622274388584686 ) ) ;
#9199=ORIENTED_EDGE ( 'NONE', *, *, #66561, .T. ) ;
#9201=ADVANCED_FACE ( 'NONE', ( #3563 ), #86458, .F. ) ;
#9205=CARTESIAN_POINT ( 'NONE',  ( -19.73463816634106038, 304.7971333121957969, 8.925379062039111133 ) ) ;
#9211=CARTESIAN_POINT ( 'NONE',  ( -43.18779636046989623, 464.9503604947622648, 14.53715779820235099 ) ) ;
#9217=CARTESIAN_POINT ( 'NONE',  ( -43.60637357072565834, 484.6919820420359315, 3.661610076652439094 ) ) ;
#9228=CARTESIAN_POINT ( 'NONE',  ( -43.47770857297121694, 484.8227827122652229, 4.253339224812703101 ) ) ;
#9237=CARTESIAN_POINT ( 'NONE',  ( 32.85560242642285544, 465.7063348014125950, 11.00043030342014028 ) ) ;
#9240=CARTESIAN_POINT ( 'NONE',  ( -24.41759963816039303, 295.4108152942529841, -1.881177368969137786 ) ) ;
#9255=CARTESIAN_POINT ( 'NONE',  ( 33.00000000000000000, 463.5362553048592531, 6.739467187734345721 ) ) ;
#9264=ORIENTED_EDGE ( 'NONE', *, *, #36499, .T. ) ;
#9276=EDGE_CURVE ( 'NONE', #69972, #62753, #81880, .T. ) ;
#9290=B_SPLINE_CURVE_WITH_KNOTS ( 'NONE', 3,
 ( #77429, #93077, #102765, #21347 ),
 .UNSPECIFIED., .F., .F.,
 ( 4, 4 ),
 ( 3.469446951953614189E-18, 0.002190562081053277436 ),
 .UNSPECIFIED. ) ;
#9300=CARTESIAN_POINT ( 'NONE',  ( 38.28801327779752484, 438.9528884713969319, 23.36340610710418986 ) ) ;
#9312=CARTESIAN_POINT ( 'NONE',  ( 32.82923647385615595, 434.9827616338783400, 12.60812312004859237 ) ) ;
#9319=CARTESIAN_POINT ( 'NONE',  ( -43.74855578046756222, 328.6220886837048170, -1.765109843966993441 ) ) ;
#9336=CARTESIAN_POINT ( 'NONE',  ( -35.50215413661368302, 437.6258544849081886, 4.714593920598203702 ) ) ;
#9354=CARTESIAN_POINT ( 'NONE',  ( 43.97709758272655733, 485.9234630640622186, 4.765357663000028943 ) ) ;
#9362=CARTESIAN_POINT ( 'NONE',  ( 29.77392050318139383, 311.5487359906569509, -7.436788483390921023 ) ) ;
#9369=CARTESIAN_POINT ( 'NONE',  ( -17.66251776275359475, 294.6000992765483488, -10.05350143900042781 ) ) ;
#9370=AXIS2_PLACEMENT_3D ( 'NONE', #103702, #46009, #4480 ) ;
#9389=CARTESIAN_POINT ( 'NONE',  ( -36.12596508061012202, 304.2006385358498051, 0.1548427460391987032 ) ) ;
#9399=ORIENTED_EDGE ( 'NONE', *, *, #86875, .F. ) ;
#9410=B_SPLINE_CURVE_WITH_KNOTS ( 'NONE', 3,
 ( #58302, #59388, #42114, #1093, #75548, #100351, #67996, #43190 ),
 .UNSPECIFIED., .F., .F.,
 ( 4, 2, 2, 4 ),
 ( 2.862293735361731706E-17, 0.002162274530409172366, 0.003243411795613744888, 0.004324549060818317844 ),
 .UNSPECIFIED. ) ;
#9418=CARTESIAN_POINT ( 'NONE',  ( 33.00000000000000000, 450.0000000000002274, 13.20242257375370976 ) ) ;
#9421=CARTESIAN_POINT ( 'NONE',  ( -12.19423397773156736, 304.5852035401753710, 9.880331998383338643 ) ) ;
#9426=DIRECTION ( 'NONE',  ( 0.000000000000000000, 0.000000000000000000, -1.000000000000000000 ) ) ;
#9430=ORIENTED_EDGE ( 'NONE', *, *, #92820, .T. ) ;
#9438=CIRCLE ( 'NONE', #12906, 0.9999999999999967804 ) ;
#9439=CARTESIAN_POINT ( 'NONE',  ( -43.02621584241282449, 434.6128289108255558, 16.97888786059002086 ) ) ;
#9445=DIRECTION ( 'NONE',  ( 0.000000000000000000, -0.1492727218618817575, -0.9887960631535429590 ) ) ;
#9453=AXIS2_PLACEMENT_3D ( 'NONE', #83985, #58660, #9019 ) ;
#9456=CARTESIAN_POINT ( 'NONE',  ( -34.62641242406925812, 302.5981200378967060, 3.709061959311505063 ) ) ;
#9458=ADVANCED_FACE ( 'NONE', ( #69765 ), #24799, .F. ) ;
#9464=CARTESIAN_POINT ( 'NONE',  ( 33.38386847897551490, 300.5334109687220234, -0.7226634255821527963 ) ) ;
#9469=ORIENTED_EDGE ( 'NONE', *, *, #65165, .T. ) ;
#9473=CARTESIAN_POINT ( 'NONE',  ( 43.61934421053724975, 427.3517207320185776, 15.28054217563496842 ) ) ;
#9478=CARTESIAN_POINT ( 'NONE',  ( -22.84042588457585765, 304.5089447765301998, 10.07913915037610053 ) ) ;
#9483=ADVANCED_FACE ( 'NONE', ( #47587 ), #91127, .F. ) ;
#9484=CARTESIAN_POINT ( 'NONE',  ( 32.62589942841201207, 485.9514140855832238, 7.203752716018509972 ) ) ;
#9487=CARTESIAN_POINT ( 'NONE',  ( 46.00000000000002842, 436.0961602813633249, 11.28239370168154032 ) ) ;
#9493=CARTESIAN_POINT ( 'NONE',  ( 36.69945015609330596, 461.9657866046125037, 3.159955898139067187 ) ) ;
#9499=ORIENTED_EDGE ( 'NONE', *, *, #12477, .F. ) ;
#9502=CARTESIAN_POINT ( 'NONE',  ( 31.14694070047868735, 432.3293837220155069, 24.29762062537629319 ) ) ;
#9512=ADVANCED_FACE ( 'NONE', ( #92294 ), #12079, .F. ) ;
#9520=ORIENTED_EDGE ( 'NONE', *, *, #59820, .T. ) ;
#9524=CARTESIAN_POINT ( 'NONE',  ( 40.92167885334222888, 438.1321558251088959, 22.38353683390997517 ) ) ;
#9525=CARTESIAN_POINT ( 'NONE',  ( -31.19216271077053548, 416.1733914895696671, 25.29150983624480631 ) ) ;
#9529=ORIENTED_EDGE ( 'NONE', *, *, #57916, .F. ) ;
#9534=CARTESIAN_POINT ( 'NONE',  ( 34.86560210343121469, 302.9523858308785975, 3.794354053605914157 ) ) ;
#9547=CARTESIAN_POINT ( 'NONE',  ( -22.72024110750421144, 303.4016505345416590, 10.05551265021215102 ) ) ;
#9554=CARTESIAN_POINT ( 'NONE',  ( 1.128086991930825622, 302.6818553553993070, 9.936167255975588475 ) ) ;
#9558=CARTESIAN_POINT ( 'NONE',  ( 0.000000000000000000, -19.99999999999998934, 0.000000000000000000 ) ) ;
#9559=ORIENTED_EDGE ( 'NONE', *, *, #56319, .F. ) ;
#9585=EDGE_CURVE ( 'NONE', #59429, #58935, #104228, .T. ) ;
#9598=CARTESIAN_POINT ( 'NONE',  ( 1.140108047462715213, 294.8483045722556994, -9.950907916673100928 ) ) ;
#9604=CARTESIAN_POINT ( 'NONE',  ( 28.08241411638673313, 315.5964502779369241, 11.56403391043465767 ) ) ;
#9615=CARTESIAN_POINT ( 'NONE',  ( -25.95507789760542039, 309.1386286255022924, 10.94030088463808070 ) ) ;
#9619=EDGE_CURVE ( 'NONE', #90133, #100942, #18186, .T. ) ;
#9626=CARTESIAN_POINT ( 'NONE',  ( -9.297673743024688520, 295.3592874400207506, -10.03978397955126312 ) ) ;
#9633=CARTESIAN_POINT ( 'NONE',  ( -21.19348424345039206, 294.8901562694577478, 1.945151701991078896 ) ) ;
#9645=VERTEX_POINT ( 'NONE', #46287 ) ;
#9652=CARTESIAN_POINT ( 'NONE',  ( 35.22756082728740523, 435.7361056000421513, 6.213820150723853075 ) ) ;
#9665=CARTESIAN_POINT ( 'NONE',  ( -36.70909933119551027, 484.6513994032500818, -2.859602155942893020 ) ) ;
#9666=CARTESIAN_POINT ( 'NONE',  ( -40.63912328307429078, 353.8711978207421112, 23.30721375645484983 ) ) ;
#9684=FACE_OUTER_BOUND ( 'NONE', #102675, .T. ) ;
#9698=FACE_OUTER_BOUND ( 'NONE', #15311, .T. ) ;
#9708=CARTESIAN_POINT ( 'NONE',  ( -41.43869626312952903, 465.5146466453550715, 16.04577920756167231 ) ) ;
#9718=CARTESIAN_POINT ( 'NONE',  ( -33.00000000000000000, 450.0000000000002274, 13.20242257375370976 ) ) ;
#9720=CARTESIAN_POINT ( 'NONE',  ( 35.66932529116966322, 438.9565575286536045, 4.011496722538590909 ) ) ;
#9721=CARTESIAN_POINT ( 'NONE',  ( 41.33517203638527349, 460.1869644147471945, 2.191757750721595066 ) ) ;
#9722=CARTESIAN_POINT ( 'NONE',  ( -33.52854060314342632, 435.4521953938931347, 9.505701922647736168 ) ) ;
#9723=CARTESIAN_POINT ( 'NONE',  ( 29.99999999999916156, 487.3993633549791298, 6.447931125014418896 ) ) ;
#9729=CARTESIAN_POINT ( 'NONE',  ( -20.37278541768183615, 303.8378246129572631, -10.00297115033342266 ) ) ;
#9730=EDGE_CURVE ( 'NONE', #60518, #97465, #90081, .T. ) ;
#9745=CARTESIAN_POINT ( 'NONE',  ( -1.128238012697766912, 300.0000000000000000, 9.936150108905552614 ) ) ;
#9768=CARTESIAN_POINT ( 'NONE',  ( 24.93816302196866275, 307.4233949143036284, 10.52291764336465008 ) ) ;
#9780=CARTESIAN_POINT ( 'NONE',  ( 42.10086803841213765, 435.6552064019005570, 19.95582312411065828 ) ) ;
#9799=CARTESIAN_POINT ( 'NONE',  ( 31.69432218924449174, 348.2033222337485086, 20.16708524006936187 ) ) ;
#9807=CARTESIAN_POINT ( 'NONE',  ( -40.38558023182025636, 460.4657127107437873, 1.744790644328846119 ) ) ;
#9812=PLANE ( 'NONE',  #86768 ) ;
#9814=CARTESIAN_POINT ( 'NONE',  ( 42.79777464980544011, 484.2777864412636859, -1.379167304946101513 ) ) ;
#9817=CARTESIAN_POINT ( 'NONE',  ( 30.00000000002700773, 486.5488479674867790, 4.838494452995623085 ) ) ;
#9820=EDGE_CURVE ( 'NONE', #103023, #101842, #104205, .T. ) ;
#9831=CARTESIAN_POINT ( 'NONE',  ( -41.99669677994153005, 488.0206791017693604, 9.049833624058100767 ) ) ;
#9835=CARTESIAN_POINT ( 'NONE',  ( 42.21835935850999988, 436.4384481632506549, 19.62208033733222123 ) ) ;
#9837=CARTESIAN_POINT ( 'NONE',  ( -35.75416653242249510, 438.1735696696629248, 3.975240391341059887 ) ) ;
#9838=( BOUNDED_SURFACE ( )  B_SPLINE_SURFACE ( 3, 2, ( 
 ( #71997, #80077, #22945 ),
 ( #95749, #46658, #48233 ),
 ( #7245, #87668, #40155 ),
 ( #13747, #55781, #46144 ) ),
 .UNSPECIFIED., .F., .F., .F. ) 
 B_SPLINE_SURFACE_WITH_KNOTS ( ( 4, 4 ),
 ( 3, 3 ),
 ( -8.673617379884035472E-19, 0.001949576957920114064 ),
 ( 0.000000000000000000, 1.000000000000000000 ),
 .UNSPECIFIED. ) 
 GEOMETRIC_REPRESENTATION_ITEM ( )  RATIONAL_B_SPLINE_SURFACE ( (
 ( 1.000000000000000000, 0.7964405967476593240, 1.000000000000000000),
 ( 1.000000000000000000, 0.8057025330220216608, 1.000000000000000000),
 ( 1.000000000000000000, 0.8148370924185578401, 1.000000000000000000),
 ( 1.000000000000000000, 0.8238944711860017867, 1.000000000000000000) ) ) 
 REPRESENTATION_ITEM ( '' )  SURFACE ( )  );
#9856=AXIS2_PLACEMENT_3D ( 'NONE', #105801, #99838, #82050 ) ;
#9867=CARTESIAN_POINT ( 'NONE',  ( -30.00000000000000000, 461.8665070935974768, 11.40527499426167424 ) ) ;
#9876=ADVANCED_FACE ( 'NONE', ( #96957 ), #23774, .F. ) ;
#9892=DIRECTION ( 'NONE',  ( 0.000000000000000000, 0.000000000000000000, -1.000000000000000000 ) ) ;
#9902=ORIENTED_EDGE ( 'NONE', *, *, #78433, .T. ) ;
#9916=CARTESIAN_POINT ( 'NONE',  ( -33.00000000000000000, 435.0774731480752848, 11.67986145722080948 ) ) ;
#9938=CARTESIAN_POINT ( 'NONE',  ( -39.10808401951415902, 311.3452410718041961, 1.932008273133060783 ) ) ;
#9939=CARTESIAN_POINT ( 'NONE',  ( -16.97161852214282618, 303.5650176660444117, -10.06095684947478830 ) ) ;
#9959=B_SPLINE_CURVE_WITH_KNOTS ( 'NONE', 3,
 ( #49610, #57164, #66331, #99214, #32400, #90076, #98681, #24835, #65272, #106779, #14576, #32930, #88498, #98162 ),
 .UNSPECIFIED., .F., .F.,
 ( 4, 2, 2, 2, 2, 2, 4 ),
 ( 2.023315308605685309E-16, 0.001829618653527544016, 0.002744427980291228204, 0.003659237307054911958, 0.005488855960582240436, 0.006403665287345909445, 0.007318474614109578454 ),
 .UNSPECIFIED. ) ;
#9971=EDGE_CURVE ( 'NONE', #81556, #80103, #3585, .T. ) ;
#9973=CARTESIAN_POINT ( 'NONE',  ( -36.87655955837857391, 438.2068510013161813, 3.933030107424692279 ) ) ;
#9974=CARTESIAN_POINT ( 'NONE',  ( 32.15166163075728178, 486.0589784586659903, 5.199393881400817818 ) ) ;
#9992=CARTESIAN_POINT ( 'NONE',  ( -39.83572194810943756, 489.3931820501592824, 11.44122026684815907 ) ) ;
#9995=CARTESIAN_POINT ( 'NONE',  ( -31.36710069068199402, 439.6781111632997181, 23.41206205511423732 ) ) ;
#9999=ORIENTED_EDGE ( 'NONE', *, *, #30789, .F. ) ;
#10003=CARTESIAN_POINT ( 'NONE',  ( 32.22503847990217452, 485.9064490506207790, 4.829857536092636572 ) ) ;
#10004=CARTESIAN_POINT ( 'NONE',  ( -40.13939232030954685, 319.6057995888056666, 7.960803243963931131 ) ) ;
#10007=CARTESIAN_POINT ( 'NONE',  ( -33.77601377298719143, 321.0243391643527389, -5.815655461559389394 ) ) ;
#10023=CARTESIAN_POINT ( 'NONE',  ( 37.68814790064792675, 414.9506305060368163, 6.370022659008212074 ) ) ;
#10027=CARTESIAN_POINT ( 'NONE',  ( -23.17317412221422046, 304.6499743691934441, 10.11024954114910024 ) ) ;
#10030=CARTESIAN_POINT ( 'NONE',  ( 51.01037695545453232, 450.0000000000002274, 18.20242257375371153 ) ) ;
#10033=CARTESIAN_POINT ( 'NONE',  ( 32.73605680485899683, 486.1418706179427431, 5.972480793486623973 ) ) ;
#10035=DIRECTION ( 'NONE',  ( 0.000000000000000000, 0.000000000000000000, 1.000000000000000000 ) ) ;
#10037=ORIENTED_EDGE ( 'NONE', *, *, #60908, .T. ) ;
#10043=DIRECTION ( 'NONE',  ( 0.000000000000000000, -0.9459915920726907901, 0.3241911592375332218 ) ) ;
#10049=( NAMED_UNIT ( * ) SI_UNIT ( $, .STERADIAN. ) SOLID_ANGLE_UNIT ( ) );
#10050=CARTESIAN_POINT ( 'NONE',  ( 33.00496812083888898, 465.6658704666191966, 15.15901827093884258 ) ) ;
#10051=CARTESIAN_POINT ( 'NONE',  ( 30.35537264529554946, 338.7115663565144246, 18.05293407820170515 ) ) ;
#10063=CARTESIAN_POINT ( 'NONE',  ( -24.31638901882701020, 305.3158659931349916, 10.26002132804774192 ) ) ;
#10064=ORIENTED_EDGE ( 'NONE', *, *, #5026, .F. ) ;
#10065=EDGE_LOOP ( 'NONE', ( #82426, #9264, #53820, #37049 ) ) ;
#10071=CARTESIAN_POINT ( 'NONE',  ( 33.99969272045851199, 439.9157840834117223, 24.30689657658924574 ) ) ;
#10072=CARTESIAN_POINT ( 'NONE',  ( -32.18022093138533535, 410.2521187074748354, 25.67972843377013703 ) ) ;
#10082=CARTESIAN_POINT ( 'NONE',  ( 26.54313204476279253, 306.2751507266256681, 10.71856527558073857 ) ) ;
#10085=EDGE_LOOP ( 'NONE', ( #25788, #34366 ) ) ;
#10087=CARTESIAN_POINT ( 'NONE',  ( 40.36332270526656174, 321.1565039326854389, 8.346576249228172983 ) ) ;
#10119=CARTESIAN_POINT ( 'NONE',  ( -35.64643974835908580, 491.6938676210187396, 12.49042095397502372 ) ) ;
#10122=CARTESIAN_POINT ( 'NONE',  ( 43.48294143132324763, 479.1558696509461015, 6.034796630239570803 ) ) ;
#10134=CARTESIAN_POINT ( 'NONE',  ( -35.61562608342421044, 436.8850424094961227, 4.737375314588414987 ) ) ;
#10140=SURFACE_SIDE_STYLE ('',( #76463 ) ) ;
#10149=CARTESIAN_POINT ( 'NONE',  ( 31.69611817388674879, 348.2576632951648890, 20.17743617868276473 ) ) ;
#10159=CARTESIAN_POINT ( 'NONE',  ( -32.11411341898570981, 317.7919323371296514, -6.873671351699469412 ) ) ;
#10168=CARTESIAN_POINT ( 'NONE',  ( -7.742691193564556151, 302.4167829614867742, -10.02995440365129021 ) ) ;
#10174=CARTESIAN_POINT ( 'NONE',  ( -16.30160124920373477, 294.5672738068976741, 9.876520238985763811 ) ) ;
#10179=B_SPLINE_SURFACE_WITH_KNOTS ( 'NONE', 1, 3, ( 
 ( #27332, #60730, #37539, #69871, #35407, #68275, #70405, #61802 ),
 ( #103303, #19773, #94696, #101171, #69351, #52602, #85531, #11610 ) ),
 .UNSPECIFIED., .F., .F., .F.,
 ( 2, 2 ),
 ( 4, 2, 2, 4 ),
 ( 0.000000000000000000, 1.000000000000000000 ),
 ( 0.000000000000000000, 0.04450745600790868145, 0.06676118401186306728, 0.08901491201581737678 ),
 .UNSPECIFIED. ) ;
#10186=CARTESIAN_POINT ( 'NONE',  ( -44.14412608174431085, 435.2201606271638639, 14.45841244836588757 ) ) ;
#10196=CARTESIAN_POINT ( 'NONE',  ( 34.99229983299962754, 435.2421343821194455, 7.288263853914603629 ) ) ;
#10210=CARTESIAN_POINT ( 'NONE',  ( -42.78144316814210413, 391.1871488574614659, 19.62185425083864843 ) ) ;
#10211=CARTESIAN_POINT ( 'NONE',  ( -32.80551872593252227, 486.0171861992462254, 5.671217483526080017 ) ) ;
#10227=CARTESIAN_POINT ( 'NONE',  ( 32.19136361712703120, 464.6890450778107606, 10.76797718186793773 ) ) ;
#10236=EDGE_CURVE ( 'NONE', #85207, #72809, #19437, .T. ) ;
#10242=CARTESIAN_POINT ( 'NONE',  ( 20.97754405179121662, 294.8763868968453608, 9.942224931492262385 ) ) ;
#10243=EDGE_CURVE ( 'NONE', #91205, #12476, #89981, .T. ) ;
#10244=FACE_OUTER_BOUND ( 'NONE', #86560, .T. ) ;
#10264=CARTESIAN_POINT ( 'NONE',  ( 24.80105969489321893, 306.0237540681346218, -9.745911707960095427 ) ) ;
#10265=CARTESIAN_POINT ( 'NONE',  ( 39.69617136735197249, 460.2157148251832837, 2.207451131566625868 ) ) ;
#10270=EDGE_LOOP ( 'NONE', ( #35833, #22155, #59950, #93774, #67723, #32356 ) ) ;
#10273=ORIENTED_EDGE ( 'NONE', *, *, #57720, .F. ) ;
#10319=CARTESIAN_POINT ( 'NONE',  ( 32.35336999986095208, 300.6590557721156642, 11.25190399080426751 ) ) ;
#10338=CARTESIAN_POINT ( 'NONE',  ( 25.35866071869866190, 306.3477625189083255, 10.50099866488358202 ) ) ;
#10345=CARTESIAN_POINT ( 'NONE',  ( -38.85520731754901647, 460.5778612837317496, 2.285564115289548059 ) ) ;
#10349=CARTESIAN_POINT ( 'NONE',  ( -45.99999999999999289, 462.9157814553173012, 7.768519869190400939 ) ) ;
#10351=ORIENTED_EDGE ( 'NONE', *, *, #99851, .T. ) ;
#10352=CARTESIAN_POINT ( 'NONE',  ( -18.75715577600996298, 302.6227400944664510, -10.04868916684661073 ) ) ;
#10381=CARTESIAN_POINT ( 'NONE',  ( 32.13614325032531127, 435.4396166566540956, 16.27706860089754670 ) ) ;
#10402=CARTESIAN_POINT ( 'NONE',  ( -34.06332199976886699, 330.0526646846329299, -3.810096259360388427 ) ) ;
#10403=CARTESIAN_POINT ( 'NONE',  ( -30.00000000000000000, 461.8887775513397855, 11.55279652844097171 ) ) ;
#10407=EDGE_CURVE ( 'NONE', #17539, #101821, #28646, .T. ) ;
#10408=CARTESIAN_POINT ( 'NONE',  ( -43.40712426123182155, 434.3590067275359274, 15.37327885490237911 ) ) ;
#10417=EDGE_LOOP ( 'NONE', ( #101801, #83671, #59680, #103603 ) ) ;
#10424=VERTEX_POINT ( 'NONE', #51456 ) ;
#10433=FACE_OUTER_BOUND ( 'NONE', #104847, .T. ) ;
#10442=EDGE_CURVE ( 'NONE', #104224, #6978, #102063, .T. ) ;
#10448=CARTESIAN_POINT ( 'NONE',  ( -43.67509741642822974, 485.0313177283814525, 1.734658348000118755 ) ) ;
#10463=CARTESIAN_POINT ( 'NONE',  ( 43.84452598814514346, 485.1288417159794903, -0.7004174638389097929 ) ) ;
#10467=CARTESIAN_POINT ( 'NONE',  ( -40.93720775505873632, 312.8591800994336722, -5.708390564187923566 ) ) ;
#10470=EDGE_LOOP ( 'NONE', ( #10273, #103939, #41356, #50716, #496, #83495, #36220, #25383, #17679 ) ) ;
#10502=CARTESIAN_POINT ( 'NONE',  ( -37.62251730745835943, 437.3427388312646258, 4.535622330043169725 ) ) ;
#10519=CARTESIAN_POINT ( 'NONE',  ( -43.59756234217329052, 434.3244621007144133, 14.55946156040312545 ) ) ;
#10528=CARTESIAN_POINT ( 'NONE',  ( -42.57785836761692622, 484.8814997681452610, 8.276214290995149270 ) ) ;
#10529=CARTESIAN_POINT ( 'NONE',  ( -21.97639485782973878, 294.9974105476200066, 1.968212750500118124 ) ) ;
#10531=ORIENTED_EDGE ( 'NONE', *, *, #16337, .T. ) ;
#10538=CARTESIAN_POINT ( 'NONE',  ( 35.57955382936916067, 363.3973965622570859, 2.919629247011395368 ) ) ;
#10540=CARTESIAN_POINT ( 'NONE',  ( 34.84618260875170392, 489.9833681528626812, 11.97975507378813731 ) ) ;
#10548=CARTESIAN_POINT ( 'NONE',  ( 37.67371248340228362, 380.0629637908955374, 5.300177988891823233 ) ) ;
#10580=CARTESIAN_POINT ( 'NONE',  ( -32.18945282278795617, 486.1438615785898492, 5.458730664921381148 ) ) ;
#10587=CARTESIAN_POINT ( 'NONE',  ( -25.78371382301346415, 306.9235641000283863, 10.63880919120126478 ) ) ;
#10596=CARTESIAN_POINT ( 'NONE',  ( -30.95268495340540937, 348.5034653024914064, 18.99969819225128020 ) ) ;
#10597=CARTESIAN_POINT ( 'NONE',  ( -30.00000000000000000, 450.0000000000002274, 25.20242257375371864 ) ) ;
#10604=CARTESIAN_POINT ( 'NONE',  ( -33.00000000000000000, 485.0303364503728289, 0.9535057477320436625 ) ) ;
#10605=CARTESIAN_POINT ( 'NONE',  ( 25.59799303312738061, 305.1324663277200102, 10.44726884554200375 ) ) ;
#10610=CARTESIAN_POINT ( 'NONE',  ( 21.19348424345033521, 294.8901562694577478, 1.945151701991110205 ) ) ;
#10612=ADVANCED_FACE ( 'NONE', ( #72423 ), #7668, .T. ) ;
#10618=CARTESIAN_POINT ( 'NONE',  ( 34.64166250171380312, 490.4813561613898401, 11.60003975507685325 ) ) ;
#10634=CARTESIAN_POINT ( 'NONE',  ( 37.50059943756144776, 490.7879993827856993, 12.38039871356534505 ) ) ;
#10640=CARTESIAN_POINT ( 'NONE',  ( -43.03987588564135081, 486.0760633267553317, 5.817066388976053659 ) ) ;
#10652=CARTESIAN_POINT ( 'NONE',  ( -35.51073831230387157, 436.6043880790006710, 4.950196615276987622 ) ) ;
#10660=ORIENTED_EDGE ( 'NONE', *, *, #8530, .T. ) ;
#10664=CARTESIAN_POINT ( 'NONE',  ( 2.806318047554528849, 294.8278478787091785, -9.615287951362873287 ) ) ;
#10669=CARTESIAN_POINT ( 'NONE',  ( 24.88870436626125837, 307.3804518054343475, 10.51319220944573729 ) ) ;
#10674=B_SPLINE_CURVE_WITH_KNOTS ( 'NONE', 3,
 ( #74249, #100653, #325, #84486, #67766, #26813, #66701, #82882, #83407, #92034, #51029, #33289 ),
 .UNSPECIFIED., .F., .F.,
 ( 4, 2, 2, 2, 2, 4 ),
 ( 1.829968831002800917E-16, 0.002066773779721026074, 0.004133547559441869135, 0.005166934449302291316, 0.006200321339162713496, 0.008267095118883622043 ),
 .UNSPECIFIED. ) ;
#10675=CARTESIAN_POINT ( 'NONE',  ( -42.57704743493907529, 486.1612337113410831, 7.852296464539637810 ) ) ;
#10680=CARTESIAN_POINT ( 'NONE',  ( -34.94338628507543376, 342.5355909536760350, -0.9693026116843473927 ) ) ;
#10690=CARTESIAN_POINT ( 'NONE',  ( -9.549008551970846526, 295.0805096965098642, -10.04182235106918952 ) ) ;
#10710=AXIS2_PLACEMENT_3D ( 'NONE', #89848, #96366, #76307 ) ;
#10719=CARTESIAN_POINT ( 'NONE',  ( -25.13271562044587526, 306.2273044284306707, -9.700012334803982839 ) ) ;
#10723=CARTESIAN_POINT ( 'NONE',  ( -43.00000000000000000, 464.8825480873695710, 15.07585856869432206 ) ) ;
#10728=AXIS2_PLACEMENT_3D ( 'NONE', #14983, #57033, #47878 ) ;
#10729=CARTESIAN_POINT ( 'NONE',  ( -44.48436518344863799, 465.3427600001859332, 9.644189083065656476 ) ) ;
#10730=VERTEX_POINT ( 'NONE', #89146 ) ;
#10732=CARTESIAN_POINT ( 'NONE',  ( -27.91514439139539405, 308.8047814446088069, 11.33986536342479390 ) ) ;
#10748=CARTESIAN_POINT ( 'NONE',  ( 18.91736802153303998, 304.6924624432400606, 8.903130582026813400 ) ) ;
#10757=CARTESIAN_POINT ( 'NONE',  ( 0.6398555294277069594, 296.1023409384113734, -10.00028515034549592 ) ) ;
#10759=PLANE ( 'NONE',  #87132 ) ;
#10763=VERTEX_POINT ( 'NONE', #18466 ) ;
#10767=CARTESIAN_POINT ( 'NONE',  ( 37.20098947014512447, 438.1443347308020293, 4.012567541587164222 ) ) ;
#10771=CARTESIAN_POINT ( 'NONE',  ( -44.32938218976925526, 463.8543910928598848, 7.949978264524292904 ) ) ;
#10774=FACE_OUTER_BOUND ( 'NONE', #91153, .T. ) ;
#10779=CARTESIAN_POINT ( 'NONE',  ( -46.00000000000000000, 450.0000000000002274, 1.202422573753698876 ) ) ;
#10781=CARTESIAN_POINT ( 'NONE',  ( 35.76482652855951017, 405.2378813769876729, 6.148826621638260548 ) ) ;
#10782=CARTESIAN_POINT ( 'NONE',  ( 40.11988102503458009, 460.2461986766708719, 2.235918385956437326 ) ) ;
#10787=FACE_OUTER_BOUND ( 'NONE', #46882, .T. ) ;
#10792=( BOUNDED_SURFACE ( )  B_SPLINE_SURFACE ( 3, 2, ( 
 ( #39531, #71341, #89130 ),
 ( #104236, #105829, #81529 ),
 ( #104777, #7654, #40571 ),
 ( #73453, #63806, #32513 ) ),
 .UNSPECIFIED., .F., .F., .T. ) 
 B_SPLINE_SURFACE_WITH_KNOTS ( ( 4, 4 ),
 ( 3, 3 ),
 ( 6.559423143537301826E-18, 0.0001614739849780087732 ),
 ( 0.000000000000000000, 1.000000000000000000 ),
 .UNSPECIFIED. ) 
 GEOMETRIC_REPRESENTATION_ITEM ( )  RATIONAL_B_SPLINE_SURFACE ( (
 ( 1.000000000000000000, 0.9028401456532985092, 1.000000000000000000),
 ( 1.000000000000000000, 0.9031964952773765543, 1.000000000000000000),
 ( 1.000000000000000000, 0.9035643897146851122, 1.000000000000000000),
 ( 1.000000000000000000, 0.9039444415359824125, 1.000000000000000000) ) ) 
 REPRESENTATION_ITEM ( '' )  SURFACE ( )  );
#10810=EDGE_LOOP ( 'NONE', ( #82918, #81804, #5505, #33018 ) ) ;
#10824=EDGE_CURVE ( 'NONE', #78207, #89572, #35618, .T. ) ;
#10839=EDGE_CURVE ( 'NONE', #3581, #84046, #65845, .T. ) ;
#10844=CARTESIAN_POINT ( 'NONE',  ( -20.45609435626379380, 304.8998821832971657, 8.947188782534524876 ) ) ;
#10845=CARTESIAN_POINT ( 'NONE',  ( 31.35596682365711274, 438.0939828603570732, 22.55458131664589061 ) ) ;
#10853=CARTESIAN_POINT ( 'NONE',  ( 36.31162387720077334, 438.2523736922215676, 3.875403351156465614 ) ) ;
#10858=CARTESIAN_POINT ( 'NONE',  ( 42.51410301897681165, 462.6487061729961283, 3.764838390842401239 ) ) ;
#10879=ORIENTED_EDGE ( 'NONE', *, *, #52609, .T. ) ;
#10888=CARTESIAN_POINT ( 'NONE',  ( -42.99999999999852207, 487.9285348210879647, 8.903916466045032507 ) ) ;
#10892=CARTESIAN_POINT ( 'NONE',  ( 38.47428897412579119, 485.7788508071993760, -4.770630528148342542 ) ) ;
#10899=CARTESIAN_POINT ( 'NONE',  ( -33.95909125837312104, 464.3583096732938316, 17.59538848557463453 ) ) ;
#10909=CARTESIAN_POINT ( 'NONE',  ( -43.17545047952408765, 487.6211760455623221, 8.487215481670535411 ) ) ;
#10917=EDGE_CURVE ( 'NONE', #58545, #61408, #55506, .T. ) ;
#10966=CARTESIAN_POINT ( 'NONE',  ( 32.70432414512695374, 489.1110749878063757, 10.33859015772799950 ) ) ;
#10968=B_SPLINE_CURVE_WITH_KNOTS ( 'NONE', 3,
 ( #9729, #18952, #2715, #76067, #35661, #100877, #59385, #95325, #34597, #46244 ),
 .UNSPECIFIED., .F., .F.,
 ( 4, 2, 2, 2, 4 ),
 ( -5.999999999415129831E-08, 0.002545901231907733622, 0.005091862463815460815, 0.01018378492763092474, 0.02036762985526185607 ),
 .UNSPECIFIED. ) ;
#10975=ORIENTED_EDGE ( 'NONE', *, *, #35133, .F. ) ;
#10978=SURFACE_STYLE_FILL_AREA ( #84890 ) ;
#10980=CARTESIAN_POINT ( 'NONE',  ( -35.44355846852403857, 438.5242933846664641, 4.909140697160467859 ) ) ;
#10989=CARTESIAN_POINT ( 'NONE',  ( 33.00000000000000000, 485.0303364503728289, 0.9535057477322557151 ) ) ;
#10992=CARTESIAN_POINT ( 'NONE',  ( -37.96433707770334109, 307.9427360707604180, 1.079370785649505837 ) ) ;
#11000=CARTESIAN_POINT ( 'NONE',  ( -44.53215874387177564, 465.2814620064186215, 9.437388644039931052 ) ) ;
#11018=CARTESIAN_POINT ( 'NONE',  ( -43.00000000000000000, 500.0000000000002274, 0.000000000000000000 ) ) ;
#11026=CARTESIAN_POINT ( 'NONE',  ( 32.89395609997539083, 463.7240567052265305, 7.148062722715214257 ) ) ;
#11039=CARTESIAN_POINT ( 'NONE',  ( 43.87333262551332069, 435.3945242957474306, 16.14343998350848253 ) ) ;
#11051=CARTESIAN_POINT ( 'NONE',  ( -41.20682028735892999, 328.7367104015643804, 10.18925674989210250 ) ) ;
#11058=CARTESIAN_POINT ( 'NONE',  ( 26.54372762322449475, 296.0128866330822461, -9.750039548960653946 ) ) ;
#11059=CARTESIAN_POINT ( 'NONE',  ( 28.21644434148578640, 308.7733337496239301, -9.112255642778066544 ) ) ;
#11063=ORIENTED_EDGE ( 'NONE', *, *, #7117, .F. ) ;
#11069=CARTESIAN_POINT ( 'NONE',  ( 34.91905476978136136, 321.9141106910175836, -5.351601672289109324 ) ) ;
#11079=EDGE_CURVE ( 'NONE', #82451, #9067, #32061, .T. ) ;
#11098=ORIENTED_EDGE ( 'NONE', *, *, #20142, .T. ) ;
#11113=ORIENTED_EDGE ( 'NONE', *, *, #21094, .F. ) ;
#11116=CARTESIAN_POINT ( 'NONE',  ( 42.51481257291533922, 437.0237169648399345, 20.73861080916342203 ) ) ;
#11126=CARTESIAN_POINT ( 'NONE',  ( 29.60571183216354996, 297.6835046505696596, 2.558988572085852731 ) ) ;
#11131=CARTESIAN_POINT ( 'NONE',  ( 40.93668190287354491, 325.7203899766267341, 9.467451731427237505 ) ) ;
#11133=ADVANCED_FACE ( 'NONE', ( #67407 ), #34165, .F. ) ;
#11138=CARTESIAN_POINT ( 'NONE',  ( 42.61140200160141944, 465.9030374194820752, 13.21253569360416869 ) ) ;
#11164=CARTESIAN_POINT ( 'NONE',  ( 33.00000000000000000, 450.0000000000002274, 13.20242257375370976 ) ) ;
#11166=CARTESIAN_POINT ( 'NONE',  ( 39.95753117817223909, 490.6049172992408671, 11.69497456421692227 ) ) ;
#11167=CARTESIAN_POINT ( 'NONE',  ( -42.87890743753310119, 485.5827513095709946, 6.686224016762015943 ) ) ;
#11181=EDGE_LOOP ( 'NONE', ( #98615, #59425, #55927, #64364, #85027, #17665 ) ) ;
#11195=CARTESIAN_POINT ( 'NONE',  ( 25.07810932049445540, 307.4824937442463693, 9.536528439053487460 ) ) ;
#11206=CARTESIAN_POINT ( 'NONE',  ( -35.56416567029047116, 496.2909070316903239, -10.19064917708978335 ) ) ;
#11228=EDGE_CURVE ( 'NONE', #22409, #98784, #28447, .T. ) ;
#11236=EDGE_LOOP ( 'NONE', ( #68989, #14025, #34449, #60476 ) ) ;
#11241=EDGE_LOOP ( 'NONE', ( #101914, #102107, #95583, #77592 ) ) ;
#11243=ORIENTED_EDGE ( 'NONE', *, *, #79449, .T. ) ;
#11247=CARTESIAN_POINT ( 'NONE',  ( 42.67612106404315142, 370.2343072762694760, 17.77331514814132163 ) ) ;
#11248=CARTESIAN_POINT ( 'NONE',  ( -26.03786948766120091, 306.7736357239633662, -9.576938274587746491 ) ) ;
#11252=CARTESIAN_POINT ( 'NONE',  ( -43.81012751977135622, 434.3196218770653445, 12.85389645199988706 ) ) ;
#11260=CARTESIAN_POINT ( 'NONE',  ( -30.12911869256660324, 316.8191984638645522, 13.35676862894592176 ) ) ;
#11261=CARTESIAN_POINT ( 'NONE',  ( -32.84237740334653921, 485.2251842821277137, 5.746442123024029236 ) ) ;
#11265=ADVANCED_FACE ( 'NONE', ( #7417 ), #104375, .F. ) ;
#11267=ORIENTED_EDGE ( 'NONE', *, *, #55871, .F. ) ;
#11277=EDGE_CURVE ( 'NONE', #61408, #7512, #63318, .T. ) ;
#11286=CARTESIAN_POINT ( 'NONE',  ( 4.926264938193783749, 301.1864079208653493, -10.01402411462960806 ) ) ;
#11293=CARTESIAN_POINT ( 'NONE',  ( -3.269135563215229023, 294.8518027752268722, -10.00000000024436275 ) ) ;
#11298=CARTESIAN_POINT ( 'NONE',  ( -32.99999999999992184, 465.3568906370357467, 17.69306951624802338 ) ) ;
#11321=ORIENTED_EDGE ( 'NONE', *, *, #4535, .T. ) ;
#11329=CARTESIAN_POINT ( 'NONE',  ( -32.78741055188834963, 485.3331003366709524, 5.977022408746728743 ) ) ;
#11351=CARTESIAN_POINT ( 'NONE',  ( 43.03185303983483578, 485.3613526602390493, 6.073233449168488285 ) ) ;
#11365=CIRCLE ( 'NONE', #90371, 12.00000000000000711 ) ;
#11379=CARTESIAN_POINT ( 'NONE',  ( 42.48722704179519383, 465.9004001135055546, 13.75636562493388126 ) ) ;
#11380=CARTESIAN_POINT ( 'NONE',  ( 33.51588970236548448, 434.0196042276504045, 13.78171046059029869 ) ) ;
#11400=VERTEX_POINT ( 'NONE', #60143 ) ;
#11407=CARTESIAN_POINT ( 'NONE',  ( -13.48373700555449162, 302.5481773704228772, -10.06453227936397354 ) ) ;
#11424=CARTESIAN_POINT ( 'NONE',  ( 42.53724782439362428, 437.0052025638185569, 20.70619558814934180 ) ) ;
#11430=( BOUNDED_SURFACE ( )  B_SPLINE_SURFACE ( 3, 2, ( 
 ( #49994, #90461, #24169 ),
 ( #66182, #89411, #91010 ),
 ( #74267, #98540, #82902 ),
 ( #25227, #341, #33310 ),
 ( #81284, #55930, #17118 ),
 ( #56483, #98017, #8999 ),
 ( #40841, #872, #16573 ),
 ( #73733, #48916, #6878 ),
 ( #32784, #106635, #66722 ),
 ( #41905, #65121, #88872 ),
 ( #74792, #39799, #15505 ),
 ( #14961, #24691, #47856 ) ),
 .UNSPECIFIED., .F., .F., .F. ) 
 B_SPLINE_SURFACE_WITH_KNOTS ( ( 4, 2, 2, 2, 2, 4 ),
 ( 3, 3 ),
 ( 0.001868552850199507254, 0.003758858514504430717, 0.005649164178809354397, 0.006594317010961816238, 0.007539469843114278078, 0.009429775507419201758 ),
 ( 0.000000000000000000, 1.000000000000000000 ),
 .UNSPECIFIED. ) 
 GEOMETRIC_REPRESENTATION_ITEM ( )  RATIONAL_B_SPLINE_SURFACE ( (
 ( 1.000000000000000000, 0.7560596356352350389, 1.000000000000000000),
 ( 1.000000000000000000, 0.7673542365376597729, 1.000000000000000000),
 ( 1.000000000000000000, 0.7800062459456665875, 1.000000000000000000),
 ( 1.000000000000000000, 0.8052793511181970398, 1.000000000000000000),
 ( 1.000000000000000000, 0.8179389361350274390, 1.000000000000000000),
 ( 1.000000000000000000, 0.8361751068035501167, 1.000000000000000000),
 ( 1.000000000000000000, 0.8421576244855180082, 1.000000000000000000),
 ( 1.000000000000000000, 0.8536052415463137866, 1.000000000000000000),
 ( 1.000000000000000000, 0.8590641661814891750, 1.000000000000000000),
 ( 1.000000000000000000, 0.8745109084890774209, 1.000000000000000000),
 ( 1.000000000000000000, 0.8835763275885871737, 1.000000000000000000),
 ( 1.000000000000000000, 0.8909749942927646105, 1.000000000000000000) ) ) 
 REPRESENTATION_ITEM ( '' )  SURFACE ( )  );
#11433=EDGE_LOOP ( 'NONE', ( #46708, #5771, #41924, #60246 ) ) ;
#11489=CARTESIAN_POINT ( 'NONE',  ( 41.92198544132045868, 435.4206365487824542, 7.395723383306480159 ) ) ;
#11492=CARTESIAN_POINT ( 'NONE',  ( 43.21901510197806573, 436.3299561109158731, 19.40633274081966420 ) ) ;
#11495=EDGE_CURVE ( 'NONE', #64080, #95206, #76813, .T. ) ;
#11500=CARTESIAN_POINT ( 'NONE',  ( -35.56416567323501710, 480.2820146177156175, -4.363888856302766683 ) ) ;
#11502=CARTESIAN_POINT ( 'NONE',  ( -33.26763304901776763, 435.2198496106717585, 10.58492093550778179 ) ) ;
#11516=CARTESIAN_POINT ( 'NONE',  ( 0.000000000000000000, 67.00000000000002842, -7.025805963803935406 ) ) ;
#11522=CARTESIAN_POINT ( 'NONE',  ( -27.82417241905227101, 305.6171509223005387, -9.386799076929978725 ) ) ;
#11523=CARTESIAN_POINT ( 'NONE',  ( 8.431345355002174176E-24, 304.8518027762757470, -9.000000000000005329 ) ) ;
#11529=EDGE_CURVE ( 'NONE', #74683, #11535, #11365, .T. ) ;
#11535=VERTEX_POINT ( 'NONE', #27794 ) ;
#11540=CIRCLE ( 'NONE', #61545, 12.00000000000001066 ) ;
#11556=CARTESIAN_POINT ( 'NONE',  ( 32.17608548772838617, 486.0066403424745545, 5.076835838892871600 ) ) ;
#11566=B_SPLINE_CURVE_WITH_KNOTS ( 'NONE', 3,
 ( #22633, #14474, #64142, #97008 ),
 .UNSPECIFIED., .F., .F.,
 ( 4, 4 ),
 ( 3.469446951953614189E-18, 0.0001993833013644588040 ),
 .UNSPECIFIED. ) ;
#11568=CARTESIAN_POINT ( 'NONE',  ( 33.94783393359906398, 484.1261039197348737, 1.321740980885009353 ) ) ;
#11575=FACE_OUTER_BOUND ( 'NONE', #19486, .T. ) ;
#11579=( NAMED_UNIT ( * ) PLANE_ANGLE_UNIT ( ) SI_UNIT ( $, .RADIAN. ) );
#11583=CARTESIAN_POINT ( 'NONE',  ( -41.70256300459694643, 461.0340457114390347, 3.032228049028243611 ) ) ;
#11589=CARTESIAN_POINT ( 'NONE',  ( -35.99330346212021681, 343.8006504399280061, -0.4438237030743195644 ) ) ;
#11590=CARTESIAN_POINT ( 'NONE',  ( 46.00000000000000000, 450.0000000000002274, 13.20242257375370976 ) ) ;
#11594=CARTESIAN_POINT ( 'NONE',  ( 24.55741454880129027, 303.7856203223532816, -9.798360968772033885 ) ) ;
#11595=CARTESIAN_POINT ( 'NONE',  ( 44.43774958859658142, 337.2802145563449017, 0.2445019049555710311 ) ) ;
#11607=CARTESIAN_POINT ( 'NONE',  ( 41.10432692360283369, 313.4425910679791514, -5.561186666570553605 ) ) ;
#11608=CARTESIAN_POINT ( 'NONE',  ( 43.72316710615049118, 464.1667603278397110, 8.066774506831963620 ) ) ;
#11610=CARTESIAN_POINT ( 'NONE',  ( -19.70764564238367100, 304.7954121406193053, 9.925013215726757210 ) ) ;
#11611=CARTESIAN_POINT ( 'NONE',  ( 31.03678703375047476, 438.6650838204854495, 21.86890379897699788 ) ) ;
#11618=ADVANCED_FACE ( 'NONE', ( #24150 ), #80742, .T. ) ;
#11631=CARTESIAN_POINT ( 'NONE',  ( 34.28937322550587652, 463.1540285681008413, 5.961485652431926852 ) ) ;
#11632=DIRECTION ( 'NONE',  ( -1.000000000000000000, -0.000000000000000000, -0.000000000000000000 ) ) ;
#11640=CARTESIAN_POINT ( 'NONE',  ( 43.71217423904096222, 435.6632154632235938, 9.092528312217307729 ) ) ;
#11652=CARTESIAN_POINT ( 'NONE',  ( -32.84088564781242781, 464.9638558180852215, 11.24476942535882706 ) ) ;
#11656=CARTESIAN_POINT ( 'NONE',  ( -31.35426068356128582, 438.7453971934658625, 22.94710527597258931 ) ) ;
#11662=ORIENTED_EDGE ( 'NONE', *, *, #61984, .T. ) ;
#11663=FACE_OUTER_BOUND ( 'NONE', #106147, .T. ) ;
#11664=CARTESIAN_POINT ( 'NONE',  ( 22.02269777243552795, 303.1965344776037341, 10.01107272578568441 ) ) ;
#11670=CARTESIAN_POINT ( 'NONE',  ( 26.18186645338464302, 296.0319025976779699, 2.191702204871421422 ) ) ;
#11673=ORIENTED_EDGE ( 'NONE', *, *, #99441, .T. ) ;
#11679=CARTESIAN_POINT ( 'NONE',  ( 19.03532703341449306, 294.6737986316037450, 9.899163670852404451 ) ) ;
#11680=CARTESIAN_POINT ( 'NONE',  ( 42.88690168185203788, 465.8389250139256319, 12.02233836084533181 ) ) ;
#11688=FACE_OUTER_BOUND ( 'NONE', #83713, .T. ) ;
#11690=CARTESIAN_POINT ( 'NONE',  ( 34.24294763429116983, 434.2296471008492631, 10.63362831703380174 ) ) ;
#11696=CARTESIAN_POINT ( 'NONE',  ( 36.50553548277586913, 490.9914377858967782, 12.47054410074822783 ) ) ;
#11712=CARTESIAN_POINT ( 'NONE',  ( -37.03219520467648351, 439.7234317543791917, 24.13053059517222820 ) ) ;
#11719=CARTESIAN_POINT ( 'NONE',  ( -43.41290683822509067, 487.0833545439620593, 7.569976829064872348 ) ) ;
#11720=ORIENTED_EDGE ( 'NONE', *, *, #82812, .T. ) ;
#11721=DIRECTION ( 'NONE',  ( -1.224646799147353454E-16, 0.000000000000000000, -1.000000000000000000 ) ) ;
#11729=CARTESIAN_POINT ( 'NONE',  ( 27.89340747318720659, 311.6758220793392979, 11.81716561949889766 ) ) ;
#11730=( BOUNDED_SURFACE ( )  B_SPLINE_SURFACE ( 3, 2, ( 
 ( #28347, #11583, #44510 ),
 ( #77935, #4043, #18117 ),
 ( #2965, #19215, #67192 ),
 ( #77399, #102200, #68793 ) ),
 .UNSPECIFIED., .F., .F., .T. ) 
 B_SPLINE_SURFACE_WITH_KNOTS ( ( 4, 4 ),
 ( 3, 3 ),
 ( 2.688821387764050996E-17, 0.001313222278771114223 ),
 ( 0.000000000000000000, 1.000000000000000000 ),
 .UNSPECIFIED. ) 
 GEOMETRIC_REPRESENTATION_ITEM ( )  RATIONAL_B_SPLINE_SURFACE ( (
 ( 1.000000000000000000, 0.8270258197359517949, 1.000000000000000000),
 ( 1.000000000000000000, 0.8180084242886423995, 1.000000000000000000),
 ( 1.000000000000000000, 0.8088315090908753113, 1.000000000000000000),
 ( 1.000000000000000000, 0.7996726260853282975, 1.000000000000000000) ) ) 
 REPRESENTATION_ITEM ( '' )  SURFACE ( )  );
#11754=CARTESIAN_POINT ( 'NONE',  ( 35.61553451506884471, 436.8848301207117402, 4.737533046128437952 ) ) ;
#11756=CARTESIAN_POINT ( 'NONE',  ( 46.00000000000000000, 500.0000000000002274, 0.000000000000000000 ) ) ;
#11778=ORIENTED_EDGE ( 'NONE', *, *, #24588, .F. ) ;
#11786=CARTESIAN_POINT ( 'NONE',  ( 33.10746446218201555, 427.7639272436880447, 25.07524900334581019 ) ) ;
#11799=CARTESIAN_POINT ( 'NONE',  ( -37.31364329941698799, 312.6956583181383280, 14.24415654474395332 ) ) ;
#11810=CIRCLE ( 'NONE', #75568, 0.9999999999999860112 ) ;
#11814=CARTESIAN_POINT ( 'NONE',  ( -35.45036406932566564, 436.3203772529605544, 5.179456583033978490 ) ) ;
#11819=EDGE_CURVE ( 'NONE', #9067, #51980, #83940, .T. ) ;
#11829=CARTESIAN_POINT ( 'NONE',  ( 1.959911964311880306, 298.2559866372270676, -10.00257402834314213 ) ) ;
#11837=ORIENTED_EDGE ( 'NONE', *, *, #70664, .T. ) ;
#11839=CARTESIAN_POINT ( 'NONE',  ( 46.00000000000000000, 487.9613292052891325, 0.4638920459505368465 ) ) ;
#11843=VERTEX_POINT ( 'NONE', #18714 ) ;
#11859=DIRECTION ( 'NONE',  ( -1.000000000000000000, 0.000000000000000000, 0.000000000000000000 ) ) ;
#11867=EDGE_LOOP ( 'NONE', ( #86189, #1169, #38242, #92862 ) ) ;
#11870=ORIENTED_EDGE ( 'NONE', *, *, #100717, .T. ) ;
#11876=AXIS2_PLACEMENT_3D ( 'NONE', #50153, #32409, #39951 ) ;
#11892=EDGE_CURVE ( 'NONE', #11843, #49452, #83405, .T. ) ;
#11901=CARTESIAN_POINT ( 'NONE',  ( -31.19792890532719198, 414.2215770364159084, 25.44228638033458623 ) ) ;
#11907=CARTESIAN_POINT ( 'NONE',  ( 32.93292175078001094, 485.0466323666404378, 1.209345195306204657 ) ) ;
#11910=CARTESIAN_POINT ( 'NONE',  ( -32.01581173012083070, 487.4782005592821861, 8.020290309115868155 ) ) ;
#11920=CARTESIAN_POINT ( 'NONE',  ( -32.99999999999998579, 435.0774731480752280, 11.67986145722083613 ) ) ;
#11926=CARTESIAN_POINT ( 'NONE',  ( 35.75416653242308485, 438.1735696696630953, 3.975240391340852497 ) ) ;
#11931=CARTESIAN_POINT ( 'NONE',  ( 32.28552837373269568, 464.7648866755952213, 15.30384310833107975 ) ) ;
#11932=CARTESIAN_POINT ( 'NONE',  ( 46.00000000000000711, 438.3662639930333285, 10.23871118457565821 ) ) ;
#11937=AXIS2_PLACEMENT_3D ( 'NONE', #42780, #19086, #92385 ) ;
#11943=CARTESIAN_POINT ( 'NONE',  ( -43.78501619230171116, 462.5250674819244523, 5.126974144517244980 ) ) ;
#11945=ORIENTED_EDGE ( 'NONE', *, *, #104724, .F. ) ;
#11952=EDGE_CURVE ( 'NONE', #80767, #95757, #34606, .T. ) ;
#11969=CARTESIAN_POINT ( 'NONE',  ( 38.63430842791552777, 485.8001267274092925, -4.834053598481960812 ) ) ;
#11976=CARTESIAN_POINT ( 'NONE',  ( -33.68177706158874685, 464.5004658938952389, 17.05886715805492315 ) ) ;
#11991=ORIENTED_EDGE ( 'NONE', *, *, #67566, .F. ) ;
#12010=ORIENTED_EDGE ( 'NONE', *, *, #39557, .T. ) ;
#12027=EDGE_CURVE ( 'NONE', #26488, #33657, #77320, .T. ) ;
#12031=B_SPLINE_CURVE_WITH_KNOTS ( 'NONE', 3,
 ( #68573, #59958, #18434, #52904 ),
 .UNSPECIFIED., .F., .F.,
 ( 4, 4 ),
 ( 4.596659206114855704E-17, 0.001829834443479903209 ),
 .UNSPECIFIED. ) ;
#12040=CARTESIAN_POINT ( 'NONE',  ( -33.63427961064055438, 325.9154870834976236, -4.827994974213513757 ) ) ;
#12042=CARTESIAN_POINT ( 'NONE',  ( -43.58530483650574183, 484.9293427334362718, 0.7222135195706615995 ) ) ;
#12045=CARTESIAN_POINT ( 'NONE',  ( -35.35823899438766915, 463.7178658455626419, 19.28807933141518305 ) ) ;
#12052=CARTESIAN_POINT ( 'NONE',  ( 33.70841932975968547, 485.0774894644218875, 1.934193826885754364 ) ) ;
#12067=CARTESIAN_POINT ( 'NONE',  ( -18.09731462108995714, 304.6346555815379133, 8.890781641607192753 ) ) ;
#12069=CARTESIAN_POINT ( 'NONE',  ( 32.88185483055566039, 462.9124542777153692, 11.53073017782671528 ) ) ;
#12074=EDGE_LOOP ( 'NONE', ( #69020, #2368, #105010, #63830 ) ) ;
#12079=( BOUNDED_SURFACE ( )  B_SPLINE_SURFACE ( 3, 2, ( 
 ( #76120, #2216, #35166 ),
 ( #68033, #16289, #33043 ),
 ( #73990, #72, #65909 ),
 ( #98789, #3304, #101471 ) ),
 .UNSPECIFIED., .F., .F., .T. ) 
 B_SPLINE_SURFACE_WITH_KNOTS ( ( 4, 4 ),
 ( 3, 3 ),
 ( 0.000000000000000000, 0.001940382064945962715 ),
 ( 0.000000000000000000, 1.000000000000000000 ),
 .UNSPECIFIED. ) 
 GEOMETRIC_REPRESENTATION_ITEM ( )  RATIONAL_B_SPLINE_SURFACE ( (
 ( 1.000000000000000000, 0.8274249441183172404, 1.000000000000000000),
 ( 1.000000000000000000, 0.8191355677488685316, 1.000000000000000000),
 ( 1.000000000000000000, 0.8101072955758994443, 1.000000000000000000),
 ( 1.000000000000000000, 0.8014084173414376400, 1.000000000000000000) ) ) 
 REPRESENTATION_ITEM ( '' )  SURFACE ( )  );
#12093=CARTESIAN_POINT ( 'NONE',  ( 46.00000000000000000, 437.9690125970931831, 14.09127711025711349 ) ) ;
#12100=EDGE_CURVE ( 'NONE', #48783, #67806, #9093, .T. ) ;
#12127=CARTESIAN_POINT ( 'NONE',  ( -36.66634014091943783, 431.6751349732608105, 5.005327391448617824 ) ) ;
#12128=CARTESIAN_POINT ( 'NONE',  ( 37.83989825151487452, 491.6297408768496666, 12.44743998625079584 ) ) ;
#12133=CARTESIAN_POINT ( 'NONE',  ( 23.73873964903627609, 303.5156351045484371, -9.857263350994356799 ) ) ;
#12134=CARTESIAN_POINT ( 'NONE',  ( 39.24156521425334176, 307.7088117867400001, -7.003459073692002157 ) ) ;
#12144=CARTESIAN_POINT ( 'NONE',  ( 42.49292640382294906, 334.6996552629477151, 7.623548389374787071 ) ) ;
#12147=FACE_OUTER_BOUND ( 'NONE', #69492, .T. ) ;
#12148=CARTESIAN_POINT ( 'NONE',  ( 31.87868955222396750, 439.4198093404291967, 23.54367745888691132 ) ) ;
#12152=DIRECTION ( 'NONE',  ( 1.000000000000000000, -8.034710196240773658E-11, 8.034710196240799507E-11 ) ) ;
#12157=AXIS2_PLACEMENT_3D ( 'NONE', #45491, #33816, #4483 ) ;
#12158=CARTESIAN_POINT ( 'NONE',  ( 32.99999999999995026, 484.0323588803976804, 1.017072797581088262 ) ) ;
#12167=CARTESIAN_POINT ( 'NONE',  ( 34.87679907359152054, 462.5881041932447033, 5.015251600533665588 ) ) ;
#12191=CARTESIAN_POINT ( 'NONE',  ( -45.50351044820315138, 397.4513779159573801, 8.242489876862624243 ) ) ;
#12197=CIRCLE ( 'NONE', #7030, 2.999999999999984457 ) ;
#12203=CARTESIAN_POINT ( 'NONE',  ( 24.56203592210657760, 295.5996828079419743, 10.09760663225323007 ) ) ;
#12218=CARTESIAN_POINT ( 'NONE',  ( -20.05074616892822448, 67.05096163904791240, 10.02537308446411402 ) ) ;
#12227=CARTESIAN_POINT ( 'NONE',  ( 33.89801561537790064, 435.9363418380468715, 7.957186453526370329 ) ) ;
#12235=CARTESIAN_POINT ( 'NONE',  ( 3.493042281569127550, 304.8518027749427119, -10.00000000028269120 ) ) ;
#12236=( BOUNDED_SURFACE ( )  B_SPLINE_SURFACE ( 3, 2, ( 
 ( #23854, #80446, #98231 ),
 ( #56699, #41596, #74481 ),
 ( #97163, #49135, #15185 ),
 ( #33002, #89622, #15720 ) ),
 .UNSPECIFIED., .F., .F., .F. ) 
 B_SPLINE_SURFACE_WITH_KNOTS ( ( 4, 4 ),
 ( 3, 3 ),
 ( -1.561251128379126385E-17, 0.001949576957921161187 ),
 ( 0.000000000000000000, 1.000000000000000000 ),
 .UNSPECIFIED. ) 
 GEOMETRIC_REPRESENTATION_ITEM ( )  RATIONAL_B_SPLINE_SURFACE ( (
 ( 1.000000000000000000, 0.7964405967476665404, 1.000000000000000000),
 ( 1.000000000000000000, 0.8057025330220294324, 1.000000000000000000),
 ( 1.000000000000000000, 0.8148370924185962538, 1.000000000000000000),
 ( 1.000000000000000000, 0.8238944711860057835, 1.000000000000000000) ) ) 
 REPRESENTATION_ITEM ( '' )  SURFACE ( )  );
#12237=FACE_OUTER_BOUND ( 'NONE', #10470, .T. ) ;
#12239=CARTESIAN_POINT ( 'NONE',  ( -43.03185303983482157, 485.3613526602391062, 6.073233449168601972 ) ) ;
#12240=CARTESIAN_POINT ( 'NONE',  ( 46.00000000004322942, 486.6678415250559624, 5.056251502143302545 ) ) ;
#12242=CARTESIAN_POINT ( 'NONE',  ( -46.00000000000000000, 500.0000000000002274, 0.000000000000000000 ) ) ;
#12247=CARTESIAN_POINT ( 'NONE',  ( 40.38854417759264237, 485.1419806746684458, -4.245955111566214413 ) ) ;
#12259=AXIS2_PLACEMENT_3D ( 'NONE', #18220, #17149, #25813 ) ;
#12268=DIRECTION ( 'NONE',  ( -0.2039034312715000408, 0.2189633091458940695, 0.9541899496240715539 ) ) ;
#12272=CARTESIAN_POINT ( 'NONE',  ( 22.83110074884478990, 304.5052821938692773, 10.07833457152883128 ) ) ;
#12293=CARTESIAN_POINT ( 'NONE',  ( 41.16726895037042055, 460.1166845890176660, 2.127318685287079347 ) ) ;
#12300=( NAMED_UNIT ( * ) SI_UNIT ( $, .STERADIAN. ) SOLID_ANGLE_UNIT ( ) );
#12312=FACE_OUTER_BOUND ( 'NONE', #72095, .T. ) ;
#12313=CARTESIAN_POINT ( 'NONE',  ( -46.00000000000000711, 461.5064854449057066, 9.507889913832133999 ) ) ;
#12318=CARTESIAN_POINT ( 'NONE',  ( 44.48436518344927038, 465.3427600001839437, 9.644189083063393397 ) ) ;
#12322=CARTESIAN_POINT ( 'NONE',  ( 42.68463871003257282, 439.3239431036145675, 17.84154235464308158 ) ) ;
#12326=CARTESIAN_POINT ( 'NONE',  ( -43.77364510075356918, 434.9303853139112448, 13.50475697611079973 ) ) ;
#12335=CARTESIAN_POINT ( 'NONE',  ( -40.26971465411892837, 320.4908973235161511, 8.181495172785465897 ) ) ;
#12350=DIRECTION ( 'NONE',  ( -1.000000000000000000, 0.000000000000000000, 0.000000000000000000 ) ) ;
#12354=COLOUR_RGB ( '', 0.31764706, 0.68627451, 0.89019608) ;
#12362=CARTESIAN_POINT ( 'NONE',  ( 2.469322996632425049, 298.9266300817046158, -10.00398374146190861 ) ) ;
#12364=CARTESIAN_POINT ( 'NONE',  ( -42.72731753109085417, 485.8496451746398748, 7.279150061871423105 ) ) ;
#12366=ORIENTED_EDGE ( 'NONE', *, *, #11228, .T. ) ;
#12375=ORIENTED_EDGE ( 'NONE', *, *, #95037, .T. ) ;
#12378=ORIENTED_EDGE ( 'NONE', *, *, #1747, .F. ) ;
#12380=CARTESIAN_POINT ( 'NONE',  ( -46.00000000000000000, 438.4646224975039672, 9.895601460523739235 ) ) ;
#12384=CARTESIAN_POINT ( 'NONE',  ( 30.00000000000000000, 488.8442721620239126, 4.433647275927487641 ) ) ;
#12386=CARTESIAN_POINT ( 'NONE',  ( 20.25321052973721692, 294.7697318699768516, 1.919554895086231117 ) ) ;
#12390=CARTESIAN_POINT ( 'NONE',  ( -42.42823000592670013, 488.6172904996873854, 9.782215989754741159 ) ) ;
#12397=DIRECTION ( 'NONE',  ( 1.000000000000000000, 0.000000000000000000, -1.224646799147353207E-16 ) ) ;
#12421=CARTESIAN_POINT ( 'NONE',  ( 23.43684916743750080, 295.2641918988800285, 10.02474406024658293 ) ) ;
#12425=CARTESIAN_POINT ( 'NONE',  ( 35.56416567323501710, 480.2820146177156175, -4.363888856302766683 ) ) ;
#12437=AXIS2_PLACEMENT_3D ( 'NONE', #58428, #26109, #27695 ) ;
#12445=CARTESIAN_POINT ( 'NONE',  ( -32.05160878076967634, 435.5671699148836638, 16.71734082338229754 ) ) ;
#12472=CARTESIAN_POINT ( 'NONE',  ( 30.00000000000000355, 488.8442721620236853, 4.433647275927599551 ) ) ;
#12475=CARTESIAN_POINT ( 'NONE',  ( -20.33030176445824821, 302.8588253227683822, 9.938492008999505245 ) ) ;
#12476=VERTEX_POINT ( 'NONE', #33694 ) ;
#12477=EDGE_CURVE ( 'NONE', #33657, #101842, #49130, .T. ) ;
#12480=CARTESIAN_POINT ( 'NONE',  ( -6.953544250145660577, 296.7171512541748370, 7.191915520096927139 ) ) ;
#12498=( GEOMETRIC_REPRESENTATION_CONTEXT ( 3 ) GLOBAL_UNCERTAINTY_ASSIGNED_CONTEXT ( ( #47761 ) ) GLOBAL_UNIT_ASSIGNED_CONTEXT ( ( #41269, #48811, #89829 ) ) REPRESENTATION_CONTEXT ( 'NONE', 'WORKASPACE' ) );
#12500=DIRECTION ( 'NONE',  ( 0.000000000000000000, 0.000000000000000000, -1.000000000000000000 ) ) ;
#12504=DIRECTION ( 'NONE',  ( 0.000000000000000000, -0.9971933454386585627, -0.07486943176528132460 ) ) ;
#12545=CARTESIAN_POINT ( 'NONE',  ( 35.98289756235140402, 343.5663561902737797, -0.4926348694814616791 ) ) ;
#12547=CARTESIAN_POINT ( 'NONE',  ( 32.84229071576313430, 485.9543065954273970, 5.517463591349936358 ) ) ;
#12552=CARTESIAN_POINT ( 'NONE',  ( 39.82092066244369022, 436.5808519682737483, 5.503544575420478147 ) ) ;
#12563=EDGE_CURVE ( 'NONE', #91003, #34395, #21816, .T. ) ;
#12570=CARTESIAN_POINT ( 'NONE',  ( -40.20451861284639250, 437.0088225241107693, 5.689194366313575557 ) ) ;
#12576=CARTESIAN_POINT ( 'NONE',  ( 33.00496812083877529, 465.6658704666191966, 15.15901827093884968 ) ) ;
#12592=CARTESIAN_POINT ( 'NONE',  ( -3.291807555861496315, 304.8518027751348995, 8.936999415071573694 ) ) ;
#12603=VERTEX_POINT ( 'NONE', #90191 ) ;
#12628=B_SPLINE_CURVE_WITH_KNOTS ( 'NONE', 3,
 ( #79379, #5500, #38423, #3913 ),
 .UNSPECIFIED., .F., .F.,
 ( 4, 4 ),
 ( 6.938893903907228378E-18, 0.002366282582215003139 ),
 .UNSPECIFIED. ) ;
#12639=CARTESIAN_POINT ( 'NONE',  ( -32.15166163075724626, 486.0589784586660471, 5.199393881400879103 ) ) ;
#12645=CARTESIAN_POINT ( 'NONE',  ( 35.20405031252158068, 355.7307837764093961, 2.598712449362419186 ) ) ;
#12646=CARTESIAN_POINT ( 'NONE',  ( -17.08544069068336668, 304.5690947107618740, -10.06009145438461161 ) ) ;
#12648=CARTESIAN_POINT ( 'NONE',  ( 35.02595189227434247, 491.4435019764543995, 12.32055256812844668 ) ) ;
#12650=DIRECTION ( 'NONE',  ( 0.000000000000000000, 0.000000000000000000, -1.000000000000000000 ) ) ;
#12651=CARTESIAN_POINT ( 'NONE',  ( -31.06063738904513016, 311.6677864819774868, -8.170013517389778102 ) ) ;
#12670=CARTESIAN_POINT ( 'NONE',  ( 35.26778407330819221, 324.1042954016264162, -4.804630642184931411 ) ) ;
#12674=CARTESIAN_POINT ( 'NONE',  ( 31.66834350436152690, 439.0151449066551663, 23.43599344638407800 ) ) ;
#12676=VERTEX_POINT ( 'NONE', #30386 ) ;
#12678=CARTESIAN_POINT ( 'NONE',  ( 44.26028122668510179, 485.3157014729748653, 1.872110468833780406 ) ) ;
#12698=CARTESIAN_POINT ( 'NONE',  ( -32.93513049338658760, 465.6726574193328361, 10.66039033145138326 ) ) ;
#12709=( BOUNDED_SURFACE ( )  B_SPLINE_SURFACE ( 3, 2, ( 
 ( #3638, #69441, #12765 ),
 ( #85083, #4166, #84556 ),
 ( #11167, #76440, #94243 ),
 ( #12239, #10640, #94788 ) ),
 .UNSPECIFIED., .F., .F., .F. ) 
 B_SPLINE_SURFACE_WITH_KNOTS ( ( 4, 4 ),
 ( 3, 3 ),
 ( 1.301042606982605321E-17, 0.002002951328326080076 ),
 ( 0.000000000000000000, 1.000000000000000000 ),
 .UNSPECIFIED. ) 
 GEOMETRIC_REPRESENTATION_ITEM ( )  RATIONAL_B_SPLINE_SURFACE ( (
 ( 1.000000000000000000, 0.7699558187665428433, 1.000000000000000000),
 ( 1.000000000000000000, 0.7788467038584532265, 1.000000000000000000),
 ( 1.000000000000000000, 0.7876570642905753594, 1.000000000000000000),
 ( 1.000000000000000000, 0.7964405967476247961, 1.000000000000000000) ) ) 
 REPRESENTATION_ITEM ( '' )  SURFACE ( )  );
#12730=CARTESIAN_POINT ( 'NONE',  ( 23.98803262824752380, 303.9357235565888686, 10.17341870318404418 ) ) ;
#12731=CARTESIAN_POINT ( 'NONE',  ( 0.2480848965973885545, 295.3545306174075904, -10.00000000001854694 ) ) ;
#12737=DIRECTION ( 'NONE',  ( 0.000000000000000000, 0.09744402424415131436, 0.9952410070626639405 ) ) ;
#12762=CARTESIAN_POINT ( 'NONE',  ( 13.76424046522695122, 304.5457540960956067, -10.06505265514019065 ) ) ;
#12763=CARTESIAN_POINT ( 'NONE',  ( -42.00498316483441386, 460.5526920487833991, 2.538979661987313730 ) ) ;
#12765=CARTESIAN_POINT ( 'NONE',  ( -43.41290683822509067, 487.0833545439620593, 7.569976829064880341 ) ) ;
#12771=AXIS2_PLACEMENT_3D ( 'NONE', #83908, #82312, #8422 ) ;
#12774=CARTESIAN_POINT ( 'NONE',  ( 40.72262571688381882, 485.0559992917314389, -4.084589505546340149 ) ) ;
#12792=EDGE_CURVE ( 'NONE', #84655, #79894, #59287, .T. ) ;
#12798=CARTESIAN_POINT ( 'NONE',  ( 23.15833479403198680, 305.7594302588016149, 10.13509876207107219 ) ) ;
#12830=EDGE_LOOP ( 'NONE', ( #11321, #46813, #34060, #80981 ) ) ;
#12833=ORIENTED_EDGE ( 'NONE', *, *, #99267, .T. ) ;
#12837=CARTESIAN_POINT ( 'NONE',  ( 13.68764148674883430, 294.5450735065955996, 9.871802096439328267 ) ) ;
#12838=ORIENTED_EDGE ( 'NONE', *, *, #73620, .T. ) ;
#12848=CARTESIAN_POINT ( 'NONE',  ( 40.93067809230030463, 381.6511011474903512, 26.75444701802409497 ) ) ;
#12860=CARTESIAN_POINT ( 'NONE',  ( -23.15282783083631202, 305.4172466244119732, -8.878502953368174744 ) ) ;
#12861=CARTESIAN_POINT ( 'NONE',  ( -29.20681473986357446, 312.6947595059442051, 12.31531419807666872 ) ) ;
#12877=DIRECTION ( 'NONE',  ( 0.000000000000000000, 0.000000000000000000, 1.000000000000000000 ) ) ;
#12887=CARTESIAN_POINT ( 'NONE',  ( 3.001409217434625187, 294.8245242021975514, -9.555569693282839339 ) ) ;
#12894=ADVANCED_FACE ( 'NONE', ( #38357 ), #56140, .F. ) ;
#12895=CARTESIAN_POINT ( 'NONE',  ( 40.73953790046563483, -18.92596047533412573, -20.36976895023282097 ) ) ;
#12906=AXIS2_PLACEMENT_3D ( 'NONE', #28222, #101545, #19612 ) ;
#12932=CARTESIAN_POINT ( 'NONE',  ( 43.53992551105506692, 465.2531359679902607, 9.299628767491899595 ) ) ;
#12940=CARTESIAN_POINT ( 'NONE',  ( 42.29287336469166547, 486.6964296286180911, 8.722237745845980328 ) ) ;
#12971=CARTESIAN_POINT ( 'NONE',  ( -33.50732914388991901, 434.8932056792464778, 13.71429463173124219 ) ) ;
#12972=CARTESIAN_POINT ( 'NONE',  ( -33.67444716837086105, 489.3309112354448871, 10.55021651976761987 ) ) ;
#12975=AXIS2_PLACEMENT_3D ( 'NONE', #59485, #83207, #25550 ) ;
#12993=CARTESIAN_POINT ( 'NONE',  ( -33.77559172535808329, 464.7834715296604600, 7.192701217093225630 ) ) ;
#13005=( BOUNDED_SURFACE ( )  B_SPLINE_SURFACE ( 3, 2, ( 
 ( #52722, #86190, #20956 ),
 ( #53788, #29560, #45704 ),
 ( #62431, #54291, #46240 ),
 ( #71036, #103927, #5766 ) ),
 .UNSPECIFIED., .F., .F., .F. ) 
 B_SPLINE_SURFACE_WITH_KNOTS ( ( 4, 4 ),
 ( 3, 3 ),
 ( 2.844946500601963635E-15, 0.001000220508150799449 ),
 ( 0.000000000000000000, 1.000000000000000000 ),
 .UNSPECIFIED. ) 
 GEOMETRIC_REPRESENTATION_ITEM ( )  RATIONAL_B_SPLINE_SURFACE ( (
 ( 1.000000000000000000, 0.9039444415359472185, 1.000000000000000000),
 ( 1.000000000000000000, 0.9074142757225887035, 1.000000000000000000),
 ( 1.000000000000000000, 0.9095719689034493793, 1.000000000000000000),
 ( 1.000000000000000000, 0.9103180234519272496, 1.000000000000000000) ) ) 
 REPRESENTATION_ITEM ( '' )  SURFACE ( )  );
#13008=CARTESIAN_POINT ( 'NONE',  ( -8.083669201034920704, 295.7559805939946500, 5.917592079150272077 ) ) ;
#13011=CARTESIAN_POINT ( 'NONE',  ( 42.91610777304483548, 434.7038292574866887, 17.44089724611159653 ) ) ;
#13018=CARTESIAN_POINT ( 'NONE',  ( 43.00000000000000000, 435.1719937645106029, 7.191579780909999720 ) ) ;
#13020=AXIS2_PLACEMENT_3D ( 'NONE', #1480, #91589, #50558 ) ;
#13036=CARTESIAN_POINT ( 'NONE',  ( 11.80095105920531040, 304.5943220891977035, -9.054726562005919632 ) ) ;
#13082=CARTESIAN_POINT ( 'NONE',  ( 29.83277460719668639, 307.6570928728218632, -8.908988355798932446 ) ) ;
#13089=ORIENTED_EDGE ( 'NONE', *, *, #8896, .T. ) ;
#13090=EDGE_CURVE ( 'NONE', #106028, #61960, #74898, .T. ) ;
#13094=CARTESIAN_POINT ( 'NONE',  ( -34.06332199976886699, 330.0526646846329299, -3.810096259360388427 ) ) ;
#13099=CARTESIAN_POINT ( 'NONE',  ( -46.00000000000000000, 450.0000000000002274, -1.797577426246302013 ) ) ;
#13109=EDGE_CURVE ( 'NONE', #91673, #93450, #57918, .T. ) ;
#13111=ORIENTED_EDGE ( 'NONE', *, *, #40103, .F. ) ;
#13112=DIRECTION ( 'NONE',  ( -1.000000000000000000, 0.000000000000000000, 0.000000000000000000 ) ) ;
#13117=CARTESIAN_POINT ( 'NONE',  ( -44.27627315854449819, 485.3728101450737427, 2.282345336902423583 ) ) ;
#13118=CYLINDRICAL_SURFACE ( 'NONE', #85031, 10.00000000000000355 ) ;
#13157=ADVANCED_FACE ( 'NONE', ( #43910 ), #78852, .T. ) ;
#13158=ORIENTED_EDGE ( 'NONE', *, *, #22066, .T. ) ;
#13169=CARTESIAN_POINT ( 'NONE',  ( 43.71217423904096222, 435.6632154632235938, 9.092528312217307729 ) ) ;
#13170=ADVANCED_FACE ( 'NONE', ( #27241, #60128 ), #18602, .F. ) ;
#13175=CARTESIAN_POINT ( 'NONE',  ( 35.43306991796931271, 355.8922504090353414, 1.638683078167634477 ) ) ;
#13176=CARTESIAN_POINT ( 'NONE',  ( -18.69420657816679210, 304.6310092840336097, -10.04693110555011160 ) ) ;
#13188=CARTESIAN_POINT ( 'NONE',  ( -36.16987904212881944, 464.0305726607188603, 19.55197929207396967 ) ) ;
#13197=AXIS2_PLACEMENT_3D ( 'NONE', #46075, #48171, #40618 ) ;
#13198=CARTESIAN_POINT ( 'NONE',  ( 43.35640344742173369, 355.0162362535172065, 11.71587114036690025 ) ) ;
#13203=CARTESIAN_POINT ( 'NONE',  ( 31.74528079355457777, 439.0126391975445586, 23.49833913028905030 ) ) ;
#13211=B_SPLINE_CURVE_WITH_KNOTS ( 'NONE', 3,
 ( #539, #50194, #91212, #83096 ),
 .UNSPECIFIED., .F., .F.,
 ( 4, 4 ),
 ( 1.734723475976807094E-18, 0.002366282582213706433 ),
 .UNSPECIFIED. ) ;
#13212=CARTESIAN_POINT ( 'NONE',  ( -34.16642289233710983, 463.8422268500497125, 18.98106911353875148 ) ) ;
#13213=ORIENTED_EDGE ( 'NONE', *, *, #57784, .T. ) ;
#13224=CARTESIAN_POINT ( 'NONE',  ( 32.99999999999997868, 463.5362553048591963, 6.739467187734351938 ) ) ;
#13244=CARTESIAN_POINT ( 'NONE',  ( 0.000000000000000000, 304.8518027762758038, 8.936999415352287812 ) ) ;
#13250=ORIENTED_EDGE ( 'NONE', *, *, #99359, .F. ) ;
#13253=ORIENTED_EDGE ( 'NONE', *, *, #105197, .F. ) ;
#13255=DIRECTION ( 'NONE',  ( 0.000000000000000000, 0.000000000000000000, -1.000000000000000000 ) ) ;
#13256=CARTESIAN_POINT ( 'NONE',  ( -38.69275568811816157, 485.6230355318863872, -4.306148472019762252 ) ) ;
#13257=EDGE_CURVE ( 'NONE', #38500, #7327, #64536, .T. ) ;
#13259=CARTESIAN_POINT ( 'NONE',  ( 3.397147169706663750, 299.9647928271241994, -10.00714482582972487 ) ) ;
#13265=DIRECTION ( 'NONE',  ( 0.000000000000000000, 1.000000000000000000, -0.000000000000000000 ) ) ;
#13286=CARTESIAN_POINT ( 'NONE',  ( 43.18901105328356493, 465.6357412882384210, 10.74839809640436350 ) ) ;
#13292=CARTESIAN_POINT ( 'NONE',  ( 46.00000000000000000, 488.5500823953246368, 3.682191395179805316 ) ) ;
#13299=CARTESIAN_POINT ( 'NONE',  ( 38.69275568812167876, 485.6230355318869556, -4.306148472021480877 ) ) ;
#13300=CARTESIAN_POINT ( 'NONE',  ( 33.66378992667857517, 439.0645769355539301, 24.00942065012661786 ) ) ;
#13322=ORIENTED_EDGE ( 'NONE', *, *, #46991, .F. ) ;
#13324=CARTESIAN_POINT ( 'NONE',  ( -24.89405656119140176, 307.3881902170397211, 10.51505289473285742 ) ) ;
#13326=CARTESIAN_POINT ( 'NONE',  ( 21.62181873392152198, 304.1214363623988675, 9.994727137517363857 ) ) ;
#13332=CARTESIAN_POINT ( 'NONE',  ( 46.00000000000000000, 487.9627413807705807, 0.8148295974572986600 ) ) ;
#13345=CIRCLE ( 'NONE', #73629, 3.000000000000009326 ) ;
#13363=CARTESIAN_POINT ( 'NONE',  ( -43.78232966352139499, 435.5778410705178771, 9.443172893404664592 ) ) ;
#13382=COLOUR_RGB ( '', 0.08235294, 0.09019608, 0.10196078) ;
#13390=CARTESIAN_POINT ( 'NONE',  ( -42.35751940687926265, 435.3789575403023377, 19.45706151680432328 ) ) ;
#13391=CARTESIAN_POINT ( 'NONE',  ( -29.60711761872594394, 297.6843837922882017, 2.559186976436628402 ) ) ;
#13401=VERTEX_POINT ( 'NONE', #68891 ) ;
#13404=CARTESIAN_POINT ( 'NONE',  ( 32.28930913498045641, 488.2717154064766873, 9.213726894932154465 ) ) ;
#13405=CARTESIAN_POINT ( 'NONE',  ( -42.74851244753510571, 465.8913837062016796, 12.61547527226740328 ) ) ;
#13416=CARTESIAN_POINT ( 'NONE',  ( 40.93435977689158989, 414.3154843149413296, 27.72243992809649527 ) ) ;
#13417=CARTESIAN_POINT ( 'NONE',  ( 43.67705350351986482, 402.9939091379218894, 16.14668318356454790 ) ) ;
#13418=DIRECTION ( 'NONE',  ( -0.7092840680488620153, -0.7049227693953836749, 0.000000000000000000 ) ) ;
#13427=ADVANCED_FACE ( 'NONE', ( #94763 ), #100279, .F. ) ;
#13432=CARTESIAN_POINT ( 'NONE',  ( -32.84237740334621236, 485.2251842821281116, 5.746442123025396143 ) ) ;
#13435=AXIS2_PLACEMENT_3D ( 'NONE', #85519, #103290, #69338 ) ;
#13442=CARTESIAN_POINT ( 'NONE',  ( 30.00000000000000000, 488.7105273189918648, 4.072454560256274725 ) ) ;
#13444=CARTESIAN_POINT ( 'NONE',  ( 19.30602504899448846, 294.6887084256098888, 1.902826926857465573 ) ) ;
#13449=B_SPLINE_CURVE_WITH_KNOTS ( 'NONE', 3,
 ( #2331, #2865, #69746, #60608, #75696, #28797, #35818, #26659, #1795, #84331, #18012, #85397, #44408, #101038, #43342, #67624, #50877, #83781, #42802, #76225, #35273, #19109, #27193, #68699, #60083, #45480, #95608, #38973, #12545, #55642, #54586, #78351, #29842, #53556, #6047, #96670, #62719, #88577, #46520, #21750, #4473, #62210, #21229, #63251 ),
 .UNSPECIFIED., .F., .F.,
 ( 4, 2, 2, 2, 2, 2, 2, 2, 2, 2, 2, 2, 2, 2, 2, 2, 2, 2, 2, 2, 2, 4 ),
 ( -6.000000002574998152E-08, 0.002244305247072118665, 0.004488670494144262994, 0.005610853117680367035, 0.006733035741216471075, 0.008977400988288671349, 0.01009958361182477539, 0.01122176623536087943, 0.01346613148243323149, 0.01795486197657778643, 0.02019922722365013676, 0.02244359247072248709, 0.02693232296486719121, 0.03590978395315644334, 0.05386470592973494759, 0.06284216691802418930, 0.07181962790631343796, 0.08079708889460268662, 0.08977454988289193527, 0.1077294718594705991, 0.1256843938360492630, 0.1436393158126279268 ),
 .UNSPECIFIED. ) ;
#13455=CARTESIAN_POINT ( 'NONE',  ( -32.88185469562447594, 462.9125115710301088, 11.53071783310444509 ) ) ;
#13480=CARTESIAN_POINT ( 'NONE',  ( 51.01037695545453232, 500.0000000000002274, 5.000000000000001776 ) ) ;
#13490=ORIENTED_EDGE ( 'NONE', *, *, #19731, .T. ) ;
#13496=ORIENTED_EDGE ( 'NONE', *, *, #87929, .T. ) ;
#13503=CARTESIAN_POINT ( 'NONE',  ( -31.32116823360330571, 437.4185521953219791, 20.45661977021549660 ) ) ;
#13509=CARTESIAN_POINT ( 'NONE',  ( -43.43869229197126458, 464.9661605157749591, 13.42065392471462637 ) ) ;
#13510=EDGE_LOOP ( 'NONE', ( #45341, #63609, #28477, #55997 ) ) ;
#13512=CARTESIAN_POINT ( 'NONE',  ( -29.05729197575431755, 306.7584490568243041, -9.121552549401764409 ) ) ;
#13513=CARTESIAN_POINT ( 'NONE',  ( -9.789044728060147804, 294.6486233851416614, -2.043184600577789833 ) ) ;
#13514=CARTESIAN_POINT ( 'NONE',  ( 46.00000000000000000, 488.9831568219304927, 4.757012338623754388 ) ) ;
#13535=CARTESIAN_POINT ( 'NONE',  ( -33.40226379760697029, 315.1786766184623048, -7.050876513733235207 ) ) ;
#13543=CARTESIAN_POINT ( 'NONE',  ( -9.014154628132734715, 295.0480661387584860, 4.340608627653916862 ) ) ;
#13551=CARTESIAN_POINT ( 'NONE',  ( 13.41576242262104302, 302.5494855022793672, -10.06425233116351059 ) ) ;
#13573=CARTESIAN_POINT ( 'NONE',  ( 18.54170707414674979, 304.6552822257318098, -9.041841629248555279 ) ) ;
#13578=EDGE_LOOP ( 'NONE', ( #104440, #54115, #74906, #36727, #85205, #27746 ) ) ;
#13613=EDGE_CURVE ( 'NONE', #18077, #65653, #99077, .T. ) ;
#13614=CARTESIAN_POINT ( 'NONE',  ( -41.71680995862502783, 325.2945054222758472, 5.423733409817787177 ) ) ;
#13615=CARTESIAN_POINT ( 'NONE',  ( 31.58792830376275873, 310.4493673141303702, -8.232059693113699339 ) ) ;
#13627=CARTESIAN_POINT ( 'NONE',  ( -35.76482652855951017, 405.2378813769876729, 6.148826621638260548 ) ) ;
#13628=DIRECTION ( 'NONE',  ( -0.3144882010791185678, 0.9492613820134156999, 0.000000000000000000 ) ) ;
#13635=ORIENTED_EDGE ( 'NONE', *, *, #83797, .F. ) ;
#13639=( BOUNDED_SURFACE ( )  B_SPLINE_SURFACE ( 3, 2, ( 
 ( #26594, #93948, #44332 ),
 ( #85875, #19570, #60010 ),
 ( #91822, #69669, #102567 ),
 ( #28713, #92867, #19035 ) ),
 .UNSPECIFIED., .F., .F., .T. ) 
 B_SPLINE_SURFACE_WITH_KNOTS ( ( 4, 4 ),
 ( 3, 3 ),
 ( 5.160802341031001106E-17, 0.0004290382097890881952 ),
 ( 0.000000000000000000, 1.000000000000000000 ),
 .UNSPECIFIED. ) 
 GEOMETRIC_REPRESENTATION_ITEM ( )  RATIONAL_B_SPLINE_SURFACE ( (
 ( 1.000000000000000000, 0.7888522786293986622, 1.000000000000000000),
 ( 1.000000000000000000, 0.7909287578648700467, 1.000000000000000000),
 ( 1.000000000000000000, 0.7929954621609184295, 1.000000000000000000),
 ( 1.000000000000000000, 0.7950530193018779945, 1.000000000000000000) ) ) 
 REPRESENTATION_ITEM ( '' )  SURFACE ( )  );
#13670=CARTESIAN_POINT ( 'NONE',  ( 15.77372286590048311, 302.5604438122106785, 9.875089768359858411 ) ) ;
#13671=ORIENTED_EDGE ( 'NONE', *, *, #55710, .F. ) ;
#13682=B_SPLINE_CURVE_WITH_KNOTS ( 'NONE', 3,
 ( #66348, #17292, #1049, #83068 ),
 .UNSPECIFIED., .F., .F.,
 ( 4, 4 ),
 ( 0.000000000000000000, 0.001739938677313634333 ),
 .UNSPECIFIED. ) ;
#13685=ORIENTED_EDGE ( 'NONE', *, *, #49238, .T. ) ;
#13691=CARTESIAN_POINT ( 'NONE',  ( -43.00000000000000000, 450.0000000000002274, 1.202422573753698876 ) ) ;
#13694=ORIENTED_EDGE ( 'NONE', *, *, #31258, .T. ) ;
#13710=CARTESIAN_POINT ( 'NONE',  ( 32.83570112080939651, 321.3375211077556060, -5.977635819836277342 ) ) ;
#13732=CARTESIAN_POINT ( 'NONE',  ( 37.51494864192159184, 304.8000952021329226, -7.711197196030624035 ) ) ;
#13736=CARTESIAN_POINT ( 'NONE',  ( 32.02497098277217447, 438.9490321865996521, 23.64594912808245297 ) ) ;
#13747=CARTESIAN_POINT ( 'NONE',  ( 44.08840282922852083, 485.7747746244177733, 4.178803824087951924 ) ) ;
#13757=CARTESIAN_POINT ( 'NONE',  ( -44.14911905790385305, 464.3766534541991859, 9.623404994945861546 ) ) ;
#13768=VERTEX_POINT ( 'NONE', #80932 ) ;
#13776=CARTESIAN_POINT ( 'NONE',  ( -43.65265878650696862, 415.2984488955513598, 15.97998194705296093 ) ) ;
#13777=CARTESIAN_POINT ( 'NONE',  ( -46.00000000000000000, 488.0072389889709257, 1.487873763370969327 ) ) ;
#13780=ORIENTED_EDGE ( 'NONE', *, *, #23812, .T. ) ;
#13785=DIRECTION ( 'NONE',  ( 0.6293714829493385343, 0.5427490687641790545, 0.5561609342679212364 ) ) ;
#13787=CARTESIAN_POINT ( 'NONE',  ( 1.047247153709808698, 296.8411687940693469, -10.00073012113939086 ) ) ;
#13792=CARTESIAN_POINT ( 'NONE',  ( 39.86313086746753243, 464.8578212083490371, 17.96044624995279193 ) ) ;
#13817=EDGE_CURVE ( 'NONE', #66563, #79201, #20752, .T. ) ;
#13824=CARTESIAN_POINT ( 'NONE',  ( -40.69645897022445524, 459.9644416451193933, 1.990281397237554151 ) ) ;
#13828=CARTESIAN_POINT ( 'NONE',  ( 43.71503333927361723, 486.3083204931234604, 5.911991965207032962 ) ) ;
#13835=CARTESIAN_POINT ( 'NONE',  ( 41.68543143493056391, 436.0813452458257871, 20.68254226408532404 ) ) ;
#13844=DIRECTION ( 'NONE',  ( -0.6297424739191580523, 0.1980345732175763651, -0.7511369544581807389 ) ) ;
#13856=CARTESIAN_POINT ( 'NONE',  ( -29.98402147317631972, 322.2345601114735700, 14.46678133052209425 ) ) ;
#13857=VERTEX_POINT ( 'NONE', #53613 ) ;
#13858=CARTESIAN_POINT ( 'NONE',  ( 22.07841018086242357, 305.2842913584914299, 9.030126516642127399 ) ) ;
#13867=CARTESIAN_POINT ( 'NONE',  ( 46.00000000000000000, 488.2691388620956445, 2.804837155789654979 ) ) ;
#13895=CARTESIAN_POINT ( 'NONE',  ( 0.000000000000000000, 294.8518027762758038, 9.936999415352289589 ) ) ;
#13901=ORIENTED_EDGE ( 'NONE', *, *, #53294, .F. ) ;
#13907=CARTESIAN_POINT ( 'NONE',  ( 31.47235159143802719, 326.8924023395367158, 15.83378027818456069 ) ) ;
#13908=CARTESIAN_POINT ( 'NONE',  ( -42.90606796452293992, 465.0680163534665326, 12.12009592787024559 ) ) ;
#13912=CARTESIAN_POINT ( 'NONE',  ( -40.11988102503829623, 460.2461986766760447, 2.235918385955120158 ) ) ;
#13916=CARTESIAN_POINT ( 'NONE',  ( -34.86856670768426625, 461.8421341769301876, 3.992206518671553628 ) ) ;
#13917=CIRCLE ( 'NONE', #41489, 12.00000000000001066 ) ;
#13921=CARTESIAN_POINT ( 'NONE',  ( -35.29817125695181801, 303.6633776229971318, 3.966975762445377196 ) ) ;
#13932=ORIENTED_EDGE ( 'NONE', *, *, #65003, .T. ) ;
#13935=CARTESIAN_POINT ( 'NONE',  ( 35.75766626156808314, 437.8288023593613616, 4.424845182004494504 ) ) ;
#13955=VERTEX_POINT ( 'NONE', #22872 ) ;
#13957=CARTESIAN_POINT ( 'NONE',  ( 0.000000000000000000, 69.00000000000000000, 0.000000000000000000 ) ) ;
#13963=ORIENTED_EDGE ( 'NONE', *, *, #98620, .F. ) ;
#13966=CYLINDRICAL_SURFACE ( 'NONE', #83826, 4.999999999999999112 ) ;
#13969=CARTESIAN_POINT ( 'NONE',  ( 9.789044728060087408, 294.6486233851415477, -2.043184600578025201 ) ) ;
#13975=EDGE_CURVE ( 'NONE', #93114, #26330, #19998, .T. ) ;
#13982=B_SPLINE_CURVE_WITH_KNOTS ( 'NONE', 3,
 ( #67601, #42779, #9867, #10403 ),
 .UNSPECIFIED., .F., .F.,
 ( 4, 4 ),
 ( 0.000000000000000000, 0.0004475792522134777827 ),
 .UNSPECIFIED. ) ;
#13986=AXIS2_PLACEMENT_3D ( 'NONE', #80099, #69382, #77993 ) ;
#13987=CARTESIAN_POINT ( 'NONE',  ( -34.88692374364642035, 481.7037037884593360, 14.61727889479850617 ) ) ;
#13990=CARTESIAN_POINT ( 'NONE',  ( -9.988806003742208617, 294.6431196884677206, 0.5781234520571254532 ) ) ;
#13996=EDGE_LOOP ( 'NONE', ( #61365, #79710, #80191, #61905, #40012, #44100, #97901, #76306, #20082, #46460 ) ) ;
#14008=CARTESIAN_POINT ( 'NONE',  ( -0.9522838070410156730, 294.8487785428199004, 1.936375223474096519 ) ) ;
#14025=ORIENTED_EDGE ( 'NONE', *, *, #56668, .T. ) ;
#14033=CARTESIAN_POINT ( 'NONE',  ( 32.95646543402821749, 485.7809766657146611, 5.067016726498376755 ) ) ;
#14034=FACE_OUTER_BOUND ( 'NONE', #40495, .T. ) ;
#14035=CARTESIAN_POINT ( 'NONE',  ( -30.00000000000000000, 486.4444101590584637, 4.645498354854257883 ) ) ;
#14041=CARTESIAN_POINT ( 'NONE',  ( -32.76713765336180018, 299.3368522934601970, -9.004512236813274839 ) ) ;
#14045=ORIENTED_EDGE ( 'NONE', *, *, #99441, .F. ) ;
#14048=DIRECTION ( 'NONE',  ( -1.000000000000000000, 0.000000000000000000, 0.000000000000000000 ) ) ;
#14049=CARTESIAN_POINT ( 'NONE',  ( 30.96065734108625023, 348.7708920524887617, 19.04886383678881145 ) ) ;
#14059=CARTESIAN_POINT ( 'NONE',  ( -41.98109406947484246, 462.0607394890939759, 3.143716936936614470 ) ) ;
#14061=CARTESIAN_POINT ( 'NONE',  ( -37.69154825673145837, 413.5836300137029298, 6.418259979187027398 ) ) ;
#14063=CARTESIAN_POINT ( 'NONE',  ( 40.35113499395451697, 477.0942685543254242, -2.239294154288959948 ) ) ;
#14090=COLOUR_RGB ( '', 0.31764706, 0.68627451, 0.89019608) ;
#14097=CARTESIAN_POINT ( 'NONE',  ( 30.12932728364529922, 334.4140447340107585, 17.11298374841474867 ) ) ;
#14110=CARTESIAN_POINT ( 'NONE',  ( -11.62074180716757787, 304.6006955855707474, 8.883628396986859244 ) ) ;
#14127=CARTESIAN_POINT ( 'NONE',  ( -32.39813942120886026, 439.6661968104009475, 24.00603005215511843 ) ) ;
#14141=CARTESIAN_POINT ( 'NONE',  ( 33.00000000000000000, 439.7597899781497972, 24.16317522621304192 ) ) ;
#14142=CARTESIAN_POINT ( 'NONE',  ( -43.09506620288802026, 346.7888432250930464, 10.17652556260325447 ) ) ;
#14146=CARTESIAN_POINT ( 'NONE',  ( -35.42320619547098914, 462.9369672597862859, 4.219439332230974671 ) ) ;
#14154=CARTESIAN_POINT ( 'NONE',  ( -31.14694070047868735, 432.3293837220155069, 24.29762062537629319 ) ) ;
#14156=CARTESIAN_POINT ( 'NONE',  ( -34.86892522199585898, 473.1724139605213395, 16.84268715836331864 ) ) ;
#14163=CARTESIAN_POINT ( 'NONE',  ( -44.11327730584680751, 485.7407519190547305, 4.043905406375500000 ) ) ;
#14166=CARTESIAN_POINT ( 'NONE',  ( -33.94429683745519810, 489.7044232354981546, 10.92862313941522601 ) ) ;
#14168=EDGE_CURVE ( 'NONE', #69611, #69218, #21682, .T. ) ;
#14174=CARTESIAN_POINT ( 'NONE',  ( 32.16765183830260355, 415.4432000669583545, 25.54511159463929815 ) ) ;
#14176=CARTESIAN_POINT ( 'NONE',  ( -43.97568020413746126, 485.1298675218507128, -0.2854751263280810858 ) ) ;
#14177=EDGE_CURVE ( 'NONE', #71900, #23399, #30837, .T. ) ;
#14181=B_SPLINE_CURVE_WITH_KNOTS ( 'NONE', 3,
 ( #58023, #66662, #91995, #34333 ),
 .UNSPECIFIED., .F., .F.,
 ( 4, 4 ),
 ( 0.000000000000000000, 0.0002767692171813939143 ),
 .UNSPECIFIED. ) ;
#14192=CARTESIAN_POINT ( 'NONE',  ( 15.57837800091703606, 302.5584965806573337, 9.874655054472732729 ) ) ;
#14195=COLOUR_RGB ( '', 0.31764706, 0.68627451, 0.89019608) ;
#14236=CARTESIAN_POINT ( 'NONE',  ( 34.53439992527028579, 338.2648225848022889, -0.8894174731781776533 ) ) ;
#14242=CARTESIAN_POINT ( 'NONE',  ( 44.20231929237302637, 435.2535292332384529, 14.52165647984069707 ) ) ;
#14245=EDGE_CURVE ( 'NONE', #72492, #13768, #30291, .T. ) ;
#14250=DIRECTION ( 'NONE',  ( -1.000000000000000000, 0.000000000000000000, 0.000000000000000000 ) ) ;
#14253=ORIENTED_EDGE ( 'NONE', *, *, #105091, .T. ) ;
#14258=CARTESIAN_POINT ( 'NONE',  ( 33.46531914086286719, 315.4140312057836582, -6.991426414924862165 ) ) ;
#14268=DIRECTION ( 'NONE',  ( 0.000000000000000000, -0.6177654251562640919, -0.7863624351922594569 ) ) ;
#14272=DIRECTION ( 'NONE',  ( 0.000000000000000000, 0.000000000000000000, -1.000000000000000000 ) ) ;
#14297=ORIENTED_EDGE ( 'NONE', *, *, #83066, .T. ) ;
#14301=CARTESIAN_POINT ( 'NONE',  ( -38.93743777631283365, 438.0716041117389636, 23.12360524549970719 ) ) ;
#14305=CARTESIAN_POINT ( 'NONE',  ( -43.77726364514326463, 485.1149290089483657, -0.7626395446676972334 ) ) ;
#14313=CARTESIAN_POINT ( 'NONE',  ( -40.50232667759595984, 485.1162572728906071, -4.198421296053835405 ) ) ;
#14325=PRESENTATION_STYLE_ASSIGNMENT (( #66075 ) ) ;
#14335=FACE_OUTER_BOUND ( 'NONE', #82054, .T. ) ;
#14342=B_SPLINE_CURVE_WITH_KNOTS ( 'NONE', 3,
 ( #106704, #90534, #51658, #100215, #58158, #91085, #24762, #57609, #74339, #26381, #34466, #75405, #49533, #17193, #92655, #67337, #1502, #9069, #40918, #67855, #73809, #59244, #92120, #59780 ),
 .UNSPECIFIED., .F., .F.,
 ( 4, 2, 2, 2, 2, 2, 2, 2, 2, 2, 2, 4 ),
 ( 0.01655932398363392857, 0.01740833567538811050, 0.01825734736714228895, 0.01995537075065065280, 0.02080438244240483472, 0.02165339413415901665, 0.02335141751766738050, 0.02420042920942156242, 0.02504944090117574435, 0.02674746428468411513, 0.02844548766819248245, 0.03014351105170085324 ),
 .UNSPECIFIED. ) ;
#14344=AXIS2_PLACEMENT_3D ( 'NONE', #8489, #25802, #88889 ) ;
#14351=CARTESIAN_POINT ( 'NONE',  ( -46.00000000000000000, 438.0646818829403060, 14.80758164879957661 ) ) ;
#14355=CARTESIAN_POINT ( 'NONE',  ( 41.90764844430457003, 435.8631799414824854, 20.33131504462095762 ) ) ;
#14359=EDGE_CURVE ( 'NONE', #71900, #105451, #92491, .T. ) ;
#14379=EDGE_CURVE ( 'NONE', #11843, #1378, #6149, .T. ) ;
#14381=CARTESIAN_POINT ( 'NONE',  ( -29.19004656361920880, 323.8257188522660499, 14.61744461631383807 ) ) ;
#14384=CARTESIAN_POINT ( 'NONE',  ( 21.26797753924777012, 304.0416359807921935, 9.977564030807537065 ) ) ;
#14386=DIRECTION ( 'NONE',  ( 1.000000000000000000, 0.000000000000000000, 0.000000000000000000 ) ) ;
#14389=CARTESIAN_POINT ( 'NONE',  ( 46.00000000002251710, 485.7203612215654971, -0.7239266944879970689 ) ) ;
#14402=FACE_OUTER_BOUND ( 'NONE', #64714, .T. ) ;
#14420=ORIENTED_EDGE ( 'NONE', *, *, #13109, .F. ) ;
#14424=CARTESIAN_POINT ( 'NONE',  ( 17.24303157407923237, 294.5700599009814482, 9.877113118490870036 ) ) ;
#14435=CARTESIAN_POINT ( 'NONE',  ( 39.62846356518264201, 316.6287052912528566, 7.214087219703729126 ) ) ;
#14436=CARTESIAN_POINT ( 'NONE',  ( 43.99980723760478440, 434.6400489724846921, 17.20555692211239673 ) ) ;
#14442=CARTESIAN_POINT ( 'NONE',  ( -34.64744136446724099, 462.0025097428029426, 4.201592667583327945 ) ) ;
#14446=CARTESIAN_POINT ( 'NONE',  ( -43.38684324080074362, 436.1115529209241686, 18.84450155852746889 ) ) ;
#14447=CARTESIAN_POINT ( 'NONE',  ( -33.70188103806000157, 302.7179012586964859, 11.74889379020421920 ) ) ;
#14449=DIRECTION ( 'NONE',  ( -1.000000000000000000, 0.000000000000000000, 0.000000000000000000 ) ) ;
#14452=EDGE_CURVE ( 'NONE', #17876, #23615, #23439, .T. ) ;
#14460=CARTESIAN_POINT ( 'NONE',  ( 35.47684105139852306, 436.4843629120485389, 5.043999258398844887 ) ) ;
#14471=CARTESIAN_POINT ( 'NONE',  ( -32.80207110003820503, 464.7310103173836069, 6.970203097363641298 ) ) ;
#14474=CARTESIAN_POINT ( 'NONE',  ( 43.50721599125539285, 484.7945671711811428, 4.126833950650420135 ) ) ;
#14480=CARTESIAN_POINT ( 'NONE',  ( 1.288479777019285939E-15, 37.86482112153537116, 10.52123582012687919 ) ) ;
#14491=ORIENTED_EDGE ( 'NONE', *, *, #31727, .T. ) ;
#14504=CARTESIAN_POINT ( 'NONE',  ( 31.36907200230133697, 433.8648511944086295, 23.03418318384254349 ) ) ;
#14535=CARTESIAN_POINT ( 'NONE',  ( -41.96737725787951945, 484.5368175928758774, -2.772775517605185147 ) ) ;
#14537=CARTESIAN_POINT ( 'NONE',  ( 16.13875682045383542, 303.5610363769735045, -10.06180378987414592 ) ) ;
#14540=CARTESIAN_POINT ( 'NONE',  ( -35.40902385155463605, 484.3229957183393708, -1.494454771033894902 ) ) ;
#14547=ADVANCED_FACE ( 'NONE', ( #8119 ), #100908, .F. ) ;
#14553=CARTESIAN_POINT ( 'NONE',  ( 32.15047201613552375, 464.7337454272250739, 11.12330847294782821 ) ) ;
#14557=CARTESIAN_POINT ( 'NONE',  ( 33.20892452566059205, 484.6201576160617606, 4.300277591678492328 ) ) ;
#14563=EDGE_CURVE ( 'NONE', #73065, #58935, #78361, .T. ) ;
#14566=CARTESIAN_POINT ( 'NONE',  ( -34.62026995421213371, 301.0276281301425456, -8.612034659465027886 ) ) ;
#14575=CARTESIAN_POINT ( 'NONE',  ( 31.44899505358197800, 391.8681076219244801, 24.19046092930541292 ) ) ;
#14576=CARTESIAN_POINT ( 'NONE',  ( -42.41881992943708468, 464.7100687009927924, 16.14946504447264175 ) ) ;
#14586=CARTESIAN_POINT ( 'NONE',  ( -36.55196016430014083, 336.7123902869778362, -1.787123880112916341 ) ) ;
#14611=CARTESIAN_POINT ( 'NONE',  ( -43.00000000000000000, 436.5989882784185170, 19.94133085611150591 ) ) ;
#14655=CARTESIAN_POINT ( 'NONE',  ( -46.00000000000000000, 450.0000000000002274, 13.20242257375370976 ) ) ;
#14668=CARTESIAN_POINT ( 'NONE',  ( 22.35256411763875661, 303.1536920125136589, -9.935383756229917651 ) ) ;
#14676=CARTESIAN_POINT ( 'NONE',  ( 33.68177706158876106, 464.5004658938952957, 17.05886715805488407 ) ) ;
#14688=CARTESIAN_POINT ( 'NONE',  ( -38.39281685574185587, 437.9237591976292947, 4.303444208756491030 ) ) ;
#14694=CARTESIAN_POINT ( 'NONE',  ( -43.47770857297125957, 484.8227827122622102, 4.253339224813452724 ) ) ;
#14718=EDGE_LOOP ( 'NONE', ( #71760, #84124, #22315, #58632 ) ) ;
#14725=EDGE_CURVE ( 'NONE', #69385, #36626, #97640, .T. ) ;
#14758=CARTESIAN_POINT ( 'NONE',  ( -37.54559764570181812, 464.1143081516144662, 19.43664670202813838 ) ) ;
#14761=AXIS2_PLACEMENT_3D ( 'NONE', #62692, #54563, #89615 ) ;
#14762=CARTESIAN_POINT ( 'NONE',  ( -44.43774958859658142, 337.2802145563449017, 0.2445019049555710311 ) ) ;
#14767=CARTESIAN_POINT ( 'NONE',  ( 34.68718586615926824, 326.8403318033771825, -4.364199029797471319 ) ) ;
#14772=ORIENTED_EDGE ( 'NONE', *, *, #86024, .T. ) ;
#14775=CARTESIAN_POINT ( 'NONE',  ( -20.46799911788806625, 303.8501572683899781, -10.00035002725203448 ) ) ;
#14776=CARTESIAN_POINT ( 'NONE',  ( 42.08762648273143014, 487.0030674539048618, 9.106351919857845090 ) ) ;
#14777=CARTESIAN_POINT ( 'NONE',  ( -32.22120753352784561, 464.6691781026584636, 10.60621122532581140 ) ) ;
#14778=DIRECTION ( 'NONE',  ( 0.000000000000000000, 0.1323839925376418813, 0.9911985061125716534 ) ) ;
#14788=ORIENTED_EDGE ( 'NONE', *, *, #8211, .F. ) ;
#14794=CARTESIAN_POINT ( 'NONE',  ( 30.59828542553725583, 308.7413687888409299, -8.648601138669905097 ) ) ;
#14795=CARTESIAN_POINT ( 'NONE',  ( -30.00000000000000000, 461.8887775513397855, 11.55279652844097171 ) ) ;
#14797=B_SPLINE_CURVE_WITH_KNOTS ( 'NONE', 3,
 ( #15283, #55716, #81069, #35217 ),
 .UNSPECIFIED., .F., .F.,
 ( 4, 4 ),
 ( 1.497901326927488094E-16, 0.0002642584603499430781 ),
 .UNSPECIFIED. ) ;
#14816=SURFACE_STYLE_FILL_AREA ( #30512 ) ;
#14831=ORIENTED_EDGE ( 'NONE', *, *, #72563, .F. ) ;
#14836=CARTESIAN_POINT ( 'NONE',  ( -38.16423750294135431, 438.4460316866491212, 23.47818834081018124 ) ) ;
#14837=CARTESIAN_POINT ( 'NONE',  ( 33.14180294099352864, 415.2512948571491620, 25.78082742257582893 ) ) ;
#14838=CARTESIAN_POINT ( 'NONE',  ( -44.78715759568187593, 344.4533273986938298, 1.769479026230448504 ) ) ;
#14840=CARTESIAN_POINT ( 'NONE',  ( -46.00000000000000711, 486.1375394786616084, 2.115994497953515019 ) ) ;
#14843=DIRECTION ( 'NONE',  ( -0.000000000000000000, -1.000000000000000000, -0.000000000000000000 ) ) ;
#14845=ORIENTED_EDGE ( 'NONE', *, *, #11529, .F. ) ;
#14856=CARTESIAN_POINT ( 'NONE',  ( 42.09158233638500235, 465.7816406625409513, 14.79318349170029734 ) ) ;
#14872=CARTESIAN_POINT ( 'NONE',  ( -42.18756898894582719, 484.4522853017719513, -2.425645685620454906 ) ) ;
#14879=DIRECTION ( 'NONE',  ( 1.000000000000000000, 0.000000000000000000, 0.000000000000000000 ) ) ;
#14892=CARTESIAN_POINT ( 'NONE',  ( 33.85195725564128821, 465.2464970902066739, 17.18122764674265568 ) ) ;
#14904=EDGE_CURVE ( 'NONE', #56970, #53610, #54403, .T. ) ;
#14918=CARTESIAN_POINT ( 'NONE',  ( -27.89321753534029824, 311.6752679970134068, 11.81702633892450471 ) ) ;
#14919=VECTOR ( 'NONE', #95707, 1000.000000000000000 ) ;
#14930=CARTESIAN_POINT ( 'NONE',  ( 44.08840282922849241, 485.7747746244180007, 4.178803824087734320 ) ) ;
#14940=CARTESIAN_POINT ( 'NONE',  ( -43.81051912592810282, 434.3294622498371496, 12.62549197245937549 ) ) ;
#14942=CARTESIAN_POINT ( 'NONE',  ( 11.90234461615518491, 304.5915712872084669, -9.055312070383802592 ) ) ;
#14945=ORIENTED_EDGE ( 'NONE', *, *, #34956, .T. ) ;
#14959=CARTESIAN_POINT ( 'NONE',  ( -33.00496812084323750, 465.6658704666174913, 15.15901827095430576 ) ) ;
#14961=CARTESIAN_POINT ( 'NONE',  ( -37.54559764570092995, 464.1143081516180473, 19.43664670202776179 ) ) ;
#14964=VERTEX_POINT ( 'NONE', #49519 ) ;
#14970=CARTESIAN_POINT ( 'NONE',  ( 31.53898829120952030, 327.6230605552352699, 16.00730009383292440 ) ) ;
#14976=CARTESIAN_POINT ( 'NONE',  ( 41.21073348271418979, 328.7814315827667428, 10.19983387948521170 ) ) ;
#14979=CARTESIAN_POINT ( 'NONE',  ( -37.55700377048162153, 460.8426286395056195, 2.817645980328392863 ) ) ;
#14983=CARTESIAN_POINT ( 'NONE',  ( 0.000000000000000000, 0.000000000000000000, 0.000000000000000000 ) ) ;
#14984=CARTESIAN_POINT ( 'NONE',  ( -31.08895332998342198, 299.3338306225929273, 10.94102856163953952 ) ) ;
#14998=CARTESIAN_POINT ( 'NONE',  ( 0.000000000000000000, 67.05096163904791240, -10.02537308446410691 ) ) ;
#15000=EDGE_LOOP ( 'NONE', ( #68305, #69639, #88597, #72238 ) ) ;
#15003=CARTESIAN_POINT ( 'NONE',  ( 36.22735294587279498, 437.9860357368701784, 4.211724321154513007 ) ) ;
#15013=CARTESIAN_POINT ( 'NONE',  ( 9.609724578338589396, 294.6537309100400535, -2.768030809509012258 ) ) ;
#15025=CARTESIAN_POINT ( 'NONE',  ( 1.102182119232618897E-15, -20.00000000000001776, 9.000000000000007105 ) ) ;
#15042=EDGE_CURVE ( 'NONE', #71251, #69309, #26827, .T. ) ;
#15084=CARTESIAN_POINT ( 'NONE',  ( 36.13333162057519843, 491.8038228668837064, 12.56276695384558550 ) ) ;
#15103=CARTESIAN_POINT ( 'NONE',  ( -36.01958551496955607, 344.3887468264661607, -0.3208639796993665860 ) ) ;
#15111=CARTESIAN_POINT ( 'NONE',  ( -27.46538772309321530, 305.3421805592328724, -9.449778543000565634 ) ) ;
#15119=DIRECTION ( 'NONE',  ( -0.9915366780650390899, -0.1269898409407501094, -0.02699252395739001886 ) ) ;
#15120=CARTESIAN_POINT ( 'NONE',  ( 31.39951845036370059, 423.6537597265949557, 23.88519890770611553 ) ) ;
#15126=EDGE_CURVE ( 'NONE', #96664, #67017, #47664, .T. ) ;
#15127=CARTESIAN_POINT ( 'NONE',  ( -33.85195725564127400, 465.2464970902067307, 17.18122764674263436 ) ) ;
#15128=VERTEX_POINT ( 'NONE', #31000 ) ;
#15132=CARTESIAN_POINT ( 'NONE',  ( -33.12944332324994434, 439.4248878830263152, 23.85028906779292868 ) ) ;
#15139=DIRECTION ( 'NONE',  ( -0.000000000000000000, -1.000000000000000000, -0.000000000000000000 ) ) ;
#15147=CARTESIAN_POINT ( 'NONE',  ( 34.85398709568261921, 481.6347222374536727, 14.59797584736199205 ) ) ;
#15159=VERTEX_POINT ( 'NONE', #13169 ) ;
#15163=ORIENTED_EDGE ( 'NONE', *, *, #67207, .T. ) ;
#15171=DIRECTION ( 'NONE',  ( -0.1269898409407502204, -0.9919025243773941236, 0.001721171576547747550 ) ) ;
#15180=CARTESIAN_POINT ( 'NONE',  ( 43.02621584241283870, 434.6128289108255558, 16.97888786058996402 ) ) ;
#15185=CARTESIAN_POINT ( 'NONE',  ( -43.97702309830648915, 485.9235625653078046, 4.765750180334560326 ) ) ;
#15190=VERTEX_POINT ( 'NONE', #22902 ) ;
#15202=ORIENTED_EDGE ( 'NONE', *, *, #70416, .T. ) ;
#15208=CARTESIAN_POINT ( 'NONE',  ( 37.24486667819500241, 485.5941914037273932, -4.198424488985136982 ) ) ;
#15214=CARTESIAN_POINT ( 'NONE',  ( -43.66634721479189807, 409.2520837962942437, 16.13407036732532518 ) ) ;
#15218=CARTESIAN_POINT ( 'NONE',  ( -36.71273542727830375, 461.9574973007366339, 3.152060736416770759 ) ) ;
#15220=TOROIDAL_SURFACE ( 'NONE', #29000, 12.00000000000001066, 3.000000000000000000 ) ;
#15226=DIRECTION ( 'NONE',  ( -0.000000000000000000, -1.000000000000000000, -0.000000000000000000 ) ) ;
#15230=CARTESIAN_POINT ( 'NONE',  ( 24.37088254901632567, 295.3567874699774620, -9.892597027136796228 ) ) ;
#15239=CARTESIAN_POINT ( 'NONE',  ( -43.46689911038884446, 485.4921130117998018, 4.095024577344805294 ) ) ;
#15244=CIRCLE ( 'NONE', #6617, 0.9999999999999811262 ) ;
#15273=CARTESIAN_POINT ( 'NONE',  ( 9.614447121721056533, 294.6546896927073931, 9.895101723320543385 ) ) ;
#15283=CARTESIAN_POINT ( 'NONE',  ( 32.87547266101556431, 465.6993878536748070, 10.91512469976365551 ) ) ;
#15299=EDGE_CURVE ( 'NONE', #56333, #54099, #40642, .T. ) ;
#15300=CARTESIAN_POINT ( 'NONE',  ( 35.67416790563076034, 463.3851398029195252, 19.97299141547252077 ) ) ;
#15305=CARTESIAN_POINT ( 'NONE',  ( -40.73878142687892279, 503.7113041876743864, 10.19672445236252045 ) ) ;
#15307=CARTESIAN_POINT ( 'NONE',  ( -21.51569398614858031, 294.9107018935607130, -9.987480606144490736 ) ) ;
#15310=CARTESIAN_POINT ( 'NONE',  ( 32.02727017616632565, 314.0444030994631248, -7.577622885421612331 ) ) ;
#15311=EDGE_LOOP ( 'NONE', ( #31852, #86351, #49524, #43879 ) ) ;
#15318=VECTOR ( 'NONE', #73776, 1000.000000000000000 ) ;
#15324=CARTESIAN_POINT ( 'NONE',  ( -35.20576575318266066, 464.3971859289012514, 19.03676487905852710 ) ) ;
#15332=CARTESIAN_POINT ( 'NONE',  ( 39.06108710778507032, 311.1868365531275913, 1.892069196330523839 ) ) ;
#15339=FACE_OUTER_BOUND ( 'NONE', #23385, .T. ) ;
#15357=CARTESIAN_POINT ( 'NONE',  ( -43.00000000000000000, 500.0000000000002274, 0.000000000000000000 ) ) ;
#15359=CARTESIAN_POINT ( 'NONE',  ( 42.23079339798727716, 460.7352525929352964, 2.726051457480584972 ) ) ;
#15360=CARTESIAN_POINT ( 'NONE',  ( -30.00000000000000000, 490.5636507776930557, 7.413185101875094496 ) ) ;
#15374=CARTESIAN_POINT ( 'NONE',  ( -32.28552837373656814, 464.7648866755938570, 15.30384310834764428 ) ) ;
#15375=CARTESIAN_POINT ( 'NONE',  ( -39.30528374322037877, 437.8648113156952490, 22.91822685283586125 ) ) ;
#15376=CARTESIAN_POINT ( 'NONE',  ( 24.53406555947808343, 304.2472816665747359, 10.24320745312229164 ) ) ;
#15377=CARTESIAN_POINT ( 'NONE',  ( -41.00068889408650108, 320.1545059241889248, 4.151165785700200672 ) ) ;
#15380=CARTESIAN_POINT ( 'NONE',  ( -46.00000000000000000, 488.1813821183741879, 2.479370420756893623 ) ) ;
#15386=DIRECTION ( 'NONE',  ( 0.000000000000000000, 0.000000000000000000, 1.000000000000000000 ) ) ;
#15387=CARTESIAN_POINT ( 'NONE',  ( -41.72175139495112717, 485.6241823541930103, -4.286260377904754115 ) ) ;
#15393=CARTESIAN_POINT ( 'NONE',  ( 42.00353007817209061, 464.8744261507625311, 15.23981939152684184 ) ) ;
#15394=EDGE_CURVE ( 'NONE', #28630, #70272, #33304, .T. ) ;
#15396=EDGE_CURVE ( 'NONE', #71668, #58013, #32134, .T. ) ;
#15402=CARTESIAN_POINT ( 'NONE',  ( -37.36240688365094798, 491.3429102029593309, 12.25869953513271682 ) ) ;
#15410=CARTESIAN_POINT ( 'NONE',  ( 15.72335261638225035, 304.5560424773130990, 8.874135054364925779 ) ) ;
#15411=ORIENTED_EDGE ( 'NONE', *, *, #65165, .F. ) ;
#15445=CARTESIAN_POINT ( 'NONE',  ( -45.50145573691759182, 405.2496736015978627, 8.430338687477670234 ) ) ;
#15454=CARTESIAN_POINT ( 'NONE',  ( -25.77297728949481126, 308.6353064608509840, 9.816699030083849919 ) ) ;
#15457=CARTESIAN_POINT ( 'NONE',  ( 31.09913253216321749, 439.4710977885268903, 22.91121712903616725 ) ) ;
#15460=VERTEX_POINT ( 'NONE', #51378 ) ;
#15482=CARTESIAN_POINT ( 'NONE',  ( -33.00000000000000000, 464.3970849722209664, 17.41240408234212111 ) ) ;
#15488=CARTESIAN_POINT ( 'NONE',  ( 35.74483125092430669, 413.6409941285803598, 6.029078300230034770 ) ) ;
#15499=ORIENTED_EDGE ( 'NONE', *, *, #18587, .F. ) ;
#15503=CARTESIAN_POINT ( 'NONE',  ( -32.81762910952392787, 465.7339109552316359, 14.50750636005640892 ) ) ;
#15505=CARTESIAN_POINT ( 'NONE',  ( -38.46627235044618942, 463.5297074240463076, 19.68396873923987300 ) ) ;
#15513=CARTESIAN_POINT ( 'NONE',  ( 37.13996112556628759, 311.9295539373470092, 14.05047757564090460 ) ) ;
#15515=CARTESIAN_POINT ( 'NONE',  ( -40.54048956546211713, 460.8805895396322398, 2.213361020665719270 ) ) ;
#15516=CARTESIAN_POINT ( 'NONE',  ( 42.73661845073595345, 422.4026850698294311, 19.47781275723680849 ) ) ;
#15520=CARTESIAN_POINT ( 'NONE',  ( -35.52970765843740963, 407.4888284783144741, 7.046337194675730053 ) ) ;
#15521=CARTESIAN_POINT ( 'NONE',  ( -35.43347100846272468, 303.8941957845916590, 4.023230233832623348 ) ) ;
#15522=DIRECTION ( 'NONE',  ( -0.2255559232117777535, 0.1250062448739086840, 0.9661769839147521521 ) ) ;
#15533=B_SPLINE_CURVE_WITH_KNOTS ( 'NONE', 3,
 ( #38381, #87453, #14059, #23252 ),
 .UNSPECIFIED., .F., .F.,
 ( 4, 4 ),
 ( 7.429119110621935446E-17, 0.001193002000561107449 ),
 .UNSPECIFIED. ) ;
#15536=CARTESIAN_POINT ( 'NONE',  ( 34.62305774441573192, 437.4305192986075213, 5.012907847576154374 ) ) ;
#15564=EDGE_CURVE ( 'NONE', #29160, #26937, #11540, .T. ) ;
#15573=ORIENTED_EDGE ( 'NONE', *, *, #99359, .T. ) ;
#15581=ORIENTED_EDGE ( 'NONE', *, *, #35753, .F. ) ;
#15584=ADVANCED_FACE ( 'NONE', ( #21713 ), #4433, .T. ) ;
#15586=ORIENTED_EDGE ( 'NONE', *, *, #34881, .T. ) ;
#15587=CARTESIAN_POINT ( 'NONE',  ( -42.29361012144100584, 486.6953289214003462, 8.720858923702914822 ) ) ;
#15602=CARTESIAN_POINT ( 'NONE',  ( -7.416584036551215675, 294.7171783682675255, -6.719350101469791170 ) ) ;
#15604=CARTESIAN_POINT ( 'NONE',  ( 42.48678019891497826, 465.9003906206858687, 13.75832259440545435 ) ) ;
#15609=EDGE_CURVE ( 'NONE', #19762, #104952, #12628, .T. ) ;
#15613=CARTESIAN_POINT ( 'NONE',  ( 37.02702338562992423, 490.9575081778457957, 12.45591594067282060 ) ) ;
#15619=ORIENTED_EDGE ( 'NONE', *, *, #16038, .F. ) ;
#15621=CARTESIAN_POINT ( 'NONE',  ( -3.397168681869905615, 299.9648137111082633, -10.00714490978890758 ) ) ;
#15630=CARTESIAN_POINT ( 'NONE',  ( -32.15310320217081141, 439.7024266304582625, 23.94087012106557566 ) ) ;
#15632=CARTESIAN_POINT ( 'NONE',  ( -28.09654795190569132, 307.1907278677510931, -9.251968270002775441 ) ) ;
#15636=CARTESIAN_POINT ( 'NONE',  ( -43.11534632275854761, 435.4435433140274654, 9.329549855370874667 ) ) ;
#15639=CARTESIAN_POINT ( 'NONE',  ( -22.52158133765707149, 295.0395296717392739, -9.960097416559106520 ) ) ;
#15655=VERTEX_POINT ( 'NONE', #86969 ) ;
#15657=CARTESIAN_POINT ( 'NONE',  ( 30.00000000000000000, 488.8442721620239126, 4.433647275927487641 ) ) ;
#15659=ORIENTED_EDGE ( 'NONE', *, *, #92637, .T. ) ;
#15677=CARTESIAN_POINT ( 'NONE',  ( 18.69662128202880069, 302.6591720840974062, -10.04079946497810383 ) ) ;
#15698=CARTESIAN_POINT ( 'NONE',  ( -21.51569398614863715, 294.9107018935607130, -9.987480606144508499 ) ) ;
#15700=CARTESIAN_POINT ( 'NONE',  ( -32.85880617213487653, 464.9534634096118566, 11.16102948071628198 ) ) ;
#15701=( BOUNDED_SURFACE ( )  B_SPLINE_SURFACE ( 3, 2, ( 
 ( #100673, #67785, #33311 ),
 ( #26836, #50515, #58082 ),
 ( #66723, #99062, #74793 ),
 ( #17652, #83962, #83428 ),
 ( #16574, #59708, #92584 ),
 ( #8472, #9525, #74268 ),
 ( #10072, #75327, #34919 ),
 ( #42983, #76392, #49996 ),
 ( #26311, #82903, #27375 ),
 ( #41906, #17119, #101218 ),
 ( #18189, #9000, #49457 ),
 ( #1429, #18739, #51046 ),
 ( #34390, #41377, #84507 ),
 ( #1968, #873, #10596 ),
 ( #91011, #2505, #35452 ),
 ( #99605, #25781, #68324 ),
 ( #60255, #82367, #343 ),
 ( #66183, #25228, #31153 ),
 ( #62965, #105532, #64040 ),
 ( #62438, #97425, #96918 ),
 ( #6832, #79134, #88823 ),
 ( #80715, #14381, #71045 ),
 ( #13856, #7357, #63503 ),
 ( #96402, #79666, #95329 ),
 ( #39751, #72630, #54300 ),
 ( #22534, #95865, #87244 ),
 ( #5774, #103937, #30617 ),
 ( #14918, #47287, #55376 ),
 ( #31673, #56432, #23050 ),
 ( #46247, #64556, #30080 ),
 ( #5259, #38697, #89365 ),
 ( #23586, #88305, #15454 ),
 ( #38186, #21462, #48347 ),
 ( #80186, #6291, #81240 ),
 ( #40268, #13324, #55888 ),
 ( #105011, #73142, #71563 ),
 ( #106046, #47810, #46769 ),
 ( #104469, #21993, #54846 ),
 ( #87775, #39230, #72105 ),
 ( #83382, #83916, #32741 ),
 ( #49948, #89885, #73689 ),
 ( #56969, #65610, #75283 ),
 ( #10027, #32199, #67220 ),
 ( #9478, #42390, #48874 ),
 ( #1379, #66136, #106591 ),
 ( #49414, #7888, #90420 ),
 ( #33264, #99557, #99015 ),
 ( #65075, #34347, #100096 ),
 ( #24124, #25180, #58038 ),
 ( #15995, #26264, #82317 ),
 ( #16523, #75825, #50470 ),
 ( #66676, #59126, #92008 ) ),
 .UNSPECIFIED., .F., .F., .F. ) 
 B_SPLINE_SURFACE_WITH_KNOTS ( ( 4, 2, 2, 2, 2, 2, 2, 2, 2, 2, 2, 2, 2, 2, 2, 2, 2, 2, 2, 2, 2, 2, 2, 2, 2, 4 ),
 ( 3, 3 ),
 ( 0.05020300464300656018, 0.05910007010879590045, 0.06799713557458524071, 0.08579126650616392125, 0.1035853974377426157, 0.1213795283693212962, 0.1391736593008999767, 0.1480707247666893100, 0.1569677902324786711, 0.1614163229653733378, 0.1658648556982680322, 0.1703133884311626989, 0.1747619211640573655, 0.1792104538969520322, 0.1814347202633993517, 0.1836589866298466989, 0.1847711198130703725, 0.1858832529962940461, 0.1869953861795177197, 0.1881075193627413655, 0.1886635859543531746, 0.1892196525459650114, 0.1897757191375768482, 0.1903317857291886850, 0.1914439189124123586, 0.1925560520956360322 ),
 ( 0.000000000000000000, 1.000000000000000000 ),
 .UNSPECIFIED. ) 
 GEOMETRIC_REPRESENTATION_ITEM ( )  RATIONAL_B_SPLINE_SURFACE ( (
 ( 1.000000000000000000, 0.7071068713987338494, 1.000000000000000000),
 ( 1.000000000000000000, 0.7071068931945895253, 1.000000000000000000),
 ( 1.000000000000000000, 0.7071068799682457273, 1.000000000000000000),
 ( 1.000000000000000000, 0.7071068179960090516, 1.000000000000000000),
 ( 1.000000000000000000, 0.7071067808170531377, 1.000000000000000000),
 ( 1.000000000000000000, 0.7071067808170531377, 1.000000000000000000),
 ( 1.000000000000000000, 0.7071067795768681830, 1.000000000000000000),
 ( 1.000000000000000000, 0.7071067795768681830, 1.000000000000000000),
 ( 1.000000000000000000, 0.7071059205153482630, 1.000000000000000000),
 ( 1.000000000000000000, 0.7071040215992112632, 1.000000000000000000),
 ( 1.000000000000000000, 0.7071071097139771666, 1.000000000000000000),
 ( 1.000000000000000000, 0.7071064172135144155, 1.000000000000000000),
 ( 1.000000000000000000, 0.7071032627269669968, 1.000000000000000000),
 ( 1.000000000000000000, 0.7071054807186710756, 1.000000000000000000),
 ( 1.000000000000000000, 0.7071073488286629960, 1.000000000000000000),
 ( 1.000000000000000000, 0.7071060878131381067, 1.000000000000000000),
 ( 1.000000000000000000, 0.7071042701205316749, 1.000000000000000000),
 ( 1.000000000000000000, 0.7071061885472514907, 1.000000000000000000),
 ( 1.000000000000000000, 0.7071092460169422500, 1.000000000000000000),
 ( 1.000000000000000000, 0.7071028304568526268, 1.000000000000000000),
 ( 1.000000000000000000, 0.7070913726372183294, 1.000000000000000000),
 ( 1.000000000000000000, 0.7070821465654113513, 1.000000000000000000),
 ( 1.000000000000000000, 0.7070849791653976979, 1.000000000000000000),
 ( 1.000000000000000000, 0.7071006344750183636, 1.000000000000000000),
 ( 1.000000000000000000, 0.7071084549986811352, 1.000000000000000000),
 ( 1.000000000000000000, 0.7071012737890344235, 1.000000000000000000),
 ( 1.000000000000000000, 0.7071050044716787886, 1.000000000000000000),
 ( 1.000000000000000000, 0.7071073700438799126, 1.000000000000000000),
 ( 1.000000000000000000, 0.7070678821743980880, 1.000000000000000000),
 ( 1.000000000000000000, 0.7070089177333229724, 1.000000000000000000),
 ( 1.000000000000000000, 0.7070191433436773254, 1.000000000000000000),
 ( 1.000000000000000000, 0.7070838732338704524, 1.000000000000000000),
 ( 1.000000000000000000, 0.7071074894229318897, 1.000000000000000000),
 ( 1.000000000000000000, 0.7071058915519934374, 1.000000000000000000),
 ( 1.000000000000000000, 0.7071009288909754220, 1.000000000000000000),
 ( 1.000000000000000000, 0.7071026537070833617, 1.000000000000000000),
 ( 1.000000000000000000, 0.7071047596603757812, 1.000000000000000000),
 ( 1.000000000000000000, 0.7071143613427882668, 1.000000000000000000),
 ( 1.000000000000000000, 0.7071126439119755913, 1.000000000000000000),
 ( 1.000000000000000000, 0.7071061363862406468, 1.000000000000000000),
 ( 1.000000000000000000, 0.7071052386115821431, 1.000000000000000000),
 ( 1.000000000000000000, 0.7070937592812094330, 1.000000000000000000),
 ( 1.000000000000000000, 0.7070897429712678095, 1.000000000000000000),
 ( 1.000000000000000000, 0.7070917291181727515, 1.000000000000000000),
 ( 1.000000000000000000, 0.7070968323554049917, 1.000000000000000000),
 ( 1.000000000000000000, 0.7071053620208651580, 1.000000000000000000),
 ( 1.000000000000000000, 0.7071090935628171481, 1.000000000000000000),
 ( 1.000000000000000000, 0.7070966954647354141, 1.000000000000000000),
 ( 1.000000000000000000, 0.7070788515582973055, 1.000000000000000000),
 ( 1.000000000000000000, 0.7070871700188539055, 1.000000000000000000),
 ( 1.000000000000000000, 0.7071059307897505919, 1.000000000000000000),
 ( 1.000000000000000000, 0.7071067811865311414, 1.000000000000000000) ) ) 
 REPRESENTATION_ITEM ( '' )  SURFACE ( )  );
#15714=B_SPLINE_CURVE_WITH_KNOTS ( 'NONE', 3,
 ( #17736, #13736, #38070, #87126, #13203, #38577, #59796, #26922, #92672, #93747, #36083, #79018, #95737, #47165 ),
 .UNSPECIFIED., .F., .F.,
 ( 4, 2, 2, 2, 2, 2, 4 ),
 ( 1.430489624538199204E-17, 0.0002431197374324345079, 0.0004862394748648547044, 0.0007293592122972748738, 0.0009724789497296950974, 0.001458718424594527630, 0.001944957899459360271 ),
 .UNSPECIFIED. ) ;
#15720=CARTESIAN_POINT ( 'NONE',  ( -44.08840282922863452, 485.7747746244176597, 4.178803824087133911 ) ) ;
#15746=CARTESIAN_POINT ( 'NONE',  ( 32.17646412119353272, 464.6980787822282082, 10.84896803613062666 ) ) ;
#15748=CARTESIAN_POINT ( 'NONE',  ( -33.20189241797189794, 300.3220019530701848, -0.7726951009200400122 ) ) ;
#15758=CIRCLE ( 'NONE', #242, 2.999999999999996447 ) ;
#15761=CARTESIAN_POINT ( 'NONE',  ( 43.00000000000000000, 450.0000000000002274, 13.20242257375370976 ) ) ;
#15762=CARTESIAN_POINT ( 'NONE',  ( 43.29658055318886767, 324.1952503670673877, -2.852919881210743913 ) ) ;
#15790=CARTESIAN_POINT ( 'NONE',  ( 46.00000000000000000, 438.3878896346935790, 16.22878885428537998 ) ) ;
#15807=ADVANCED_FACE ( 'NONE', ( #89076 ), #27899, .F. ) ;
#15829=CARTESIAN_POINT ( 'NONE',  ( 35.20412044861278389, 463.4819191117625792, 19.77841787010871855 ) ) ;
#15835=CARTESIAN_POINT ( 'NONE',  ( -41.58649125062324003, 315.0454808444952732, -5.157136739135766312 ) ) ;
#15837=CARTESIAN_POINT ( 'NONE',  ( -34.95237279327285762, 304.8277712208536627, 12.26231981495593537 ) ) ;
#15840=CARTESIAN_POINT ( 'NONE',  ( 21.12475202124109686, 303.9341318091517223, -9.982500423423047664 ) ) ;
#15842=ORIENTED_EDGE ( 'NONE', *, *, #42618, .F. ) ;
#15844=EDGE_CURVE ( 'NONE', #63495, #73065, #16710, .T. ) ;
#15848=ADVANCED_FACE ( 'NONE', ( #56131 ), #38875, .F. ) ;
#15856=EDGE_CURVE ( 'NONE', #95206, #24536, #65370, .T. ) ;
#15875=CARTESIAN_POINT ( 'NONE',  ( 44.24061507097197676, 485.5299576667521819, 3.142227259635101522 ) ) ;
#15885=CARTESIAN_POINT ( 'NONE',  ( 31.08222273432268068, 314.8424387781652172, -6.614865870714785601 ) ) ;
#15890=CARTESIAN_POINT ( 'NONE',  ( 38.73386039798870684, 460.3889633641978207, 2.371405894923828139 ) ) ;
#15898=CARTESIAN_POINT ( 'NONE',  ( 32.17646412119353272, 464.6980787822282082, 10.84896803613094640 ) ) ;
#15900=CARTESIAN_POINT ( 'NONE',  ( 46.00000000000000000, 461.8820044443820620, 11.41122057645932308 ) ) ;
#15909=CARTESIAN_POINT ( 'NONE',  ( 26.37453794305503152, 306.0354018384379060, 10.66098672490852550 ) ) ;
#15911=CARTESIAN_POINT ( 'NONE',  ( -45.42083050872123096, 373.9457837719378972, 6.495393073555762342 ) ) ;
#15913=CARTESIAN_POINT ( 'NONE',  ( -46.00000000000000000, 485.8996392799547266, 0.4531297708538281621 ) ) ;
#15919=ORIENTED_EDGE ( 'NONE', *, *, #22137, .T. ) ;
#15921=CARTESIAN_POINT ( 'NONE',  ( 19.07845090537422550, 294.6331628770684574, 9.890526070132905190 ) ) ;
#15929=CARTESIAN_POINT ( 'NONE',  ( -32.89379909751026787, 463.7243792478176942, 7.148845075438585717 ) ) ;
#15934=CARTESIAN_POINT ( 'NONE',  ( -34.64166250171392392, 490.4813561613900674, 11.60003975507707175 ) ) ;
#15938=CARTESIAN_POINT ( 'NONE',  ( 32.70825224882159432, 489.1175319723079724, 10.34480600317815835 ) ) ;
#15940=CARTESIAN_POINT ( 'NONE',  ( -43.64534273044682067, 464.9151781295577734, 12.30378483073885221 ) ) ;
#15943=CARTESIAN_POINT ( 'NONE',  ( -6.763850406535977022, 294.7356673863635592, 9.912314076180619438 ) ) ;
#15952=CARTESIAN_POINT ( 'NONE',  ( -40.53459811498787957, 485.1082980165977006, -4.183568619536963240 ) ) ;
#15961=CARTESIAN_POINT ( 'NONE',  ( -44.19868099429154285, 435.2430970659380023, 14.45534906870889991 ) ) ;
#15975=CARTESIAN_POINT ( 'NONE',  ( -46.00000000000000000, 488.7529659943160709, 4.223909611883613913 ) ) ;
#15979=CARTESIAN_POINT ( 'NONE',  ( 33.49531054704386435, 300.6511913297455294, -0.6950156566324289242 ) ) ;
#15985=CARTESIAN_POINT ( 'NONE',  ( -45.29905483467455696, 497.0732240353902398, -8.041250874568902418 ) ) ;
#15991=CARTESIAN_POINT ( 'NONE',  ( -37.24486667819202523, 485.5941914037269953, -4.198424488983384606 ) ) ;
#15995=CARTESIAN_POINT ( 'NONE',  ( -20.56423368124215756, 303.9071437805204710, 9.948769377620161336 ) ) ;
#15998=CARTESIAN_POINT ( 'NONE',  ( 35.23119160525166649, 485.0602108522160734, -1.504563171983482661 ) ) ;
#16019=CARTESIAN_POINT ( 'NONE',  ( 32.11411341898570981, 317.7919323371296514, -6.873671351699469412 ) ) ;
#16020=ORIENTED_EDGE ( 'NONE', *, *, #586, .F. ) ;
#16028=PLANE ( 'NONE',  #51881 ) ;
#16038=EDGE_CURVE ( 'NONE', #101842, #74993, #71857, .T. ) ;
#16043=CARTESIAN_POINT ( 'NONE',  ( 29.02256445720001565, 312.0358488567985660, 12.14896804447468526 ) ) ;
#16067=CARTESIAN_POINT ( 'NONE',  ( 2.422472278927138599E-15, -0.1944580884125599318, 19.78098730681987760 ) ) ;
#16071=CARTESIAN_POINT ( 'NONE',  ( 36.07271708247883168, 437.4941479923609791, 4.311972135659492444 ) ) ;
#16082=CARTESIAN_POINT ( 'NONE',  ( -31.35596682365705945, 438.0939828603719093, 22.55458131664414267 ) ) ;
#16087=CARTESIAN_POINT ( 'NONE',  ( 33.81613602128341967, 485.0484310908490784, 1.468412048127565761 ) ) ;
#16091=ORIENTED_EDGE ( 'NONE', *, *, #89847, .F. ) ;
#16112=EDGE_LOOP ( 'NONE', ( #2964, #24048, #88041, #97993 ) ) ;
#16113=CARTESIAN_POINT ( 'NONE',  ( 29.02089222109925615, 322.4236678735347255, 14.27358046319127283 ) ) ;
#16127=EDGE_CURVE ( 'NONE', #27903, #75855, #70532, .T. ) ;
#16135=CARTESIAN_POINT ( 'NONE',  ( -0.6295717879345569257, 294.8518027745081440, -10.00000000000725109 ) ) ;
#16141=CARTESIAN_POINT ( 'NONE',  ( -4.238144987383360096, 302.8058397689824801, 9.927349000678042046 ) ) ;
#16147=CARTESIAN_POINT ( 'NONE',  ( -31.97926341577425546, 464.8423874313697297, 12.51531747069310363 ) ) ;
#16165=CARTESIAN_POINT ( 'NONE',  ( -29.84737552601459143, 311.4075149060049625, -8.473334882481744046 ) ) ;
#16177=CARTESIAN_POINT ( 'NONE',  ( -33.00000000000000000, 450.0000000000002274, 1.202422573753698876 ) ) ;
#16181=CARTESIAN_POINT ( 'NONE',  ( -42.75482810540037804, 382.1613480202358346, 18.98079264414366918 ) ) ;
#16182=CARTESIAN_POINT ( 'NONE',  ( 28.25162732096593032, 316.4114759038795910, 11.76994533560096556 ) ) ;
#16190=CARTESIAN_POINT ( 'NONE',  ( -41.87449068006959862, 436.7861666052169767, 20.35960683049020048 ) ) ;
#16195=CARTESIAN_POINT ( 'NONE',  ( 40.36577318854557461, 468.8231693121321655, -0.04448211817721040712 ) ) ;
#16197=CARTESIAN_POINT ( 'NONE',  ( 43.00000000000000000, 450.0000000000002274, 13.20242257375370976 ) ) ;
#16198=CARTESIAN_POINT ( 'NONE',  ( -44.20231929237294821, 435.2535292332385097, 14.52165647984114294 ) ) ;
#16223=LINE ( 'NONE', #98208, #87311 ) ;
#16227=CARTESIAN_POINT ( 'NONE',  ( 43.68988669995316343, 484.5122128850408671, 2.637743764868108354 ) ) ;
#16229=CARTESIAN_POINT ( 'NONE',  ( 27.57151080649627417, 314.0751515626058676, 12.18133379269485239 ) ) ;
#16233=CARTESIAN_POINT ( 'NONE',  ( 30.00000000000000355, 489.0575207958582382, 4.971052219124123539 ) ) ;
#16242=CARTESIAN_POINT ( 'NONE',  ( 0.000000000000000000, 80.00000000000000000, 0.000000000000000000 ) ) ;
#16244=CARTESIAN_POINT ( 'NONE',  ( -6.663826174190587537, 304.7444947287337413, 9.914190384935233524 ) ) ;
#16249=DIRECTION ( 'NONE',  ( -0.000000000000000000, -1.000000000000000000, -0.000000000000000000 ) ) ;
#16270=CARTESIAN_POINT ( 'NONE',  ( 45.99999999999999289, 462.0285355451086957, 5.456504273769160918 ) ) ;
#16273=CARTESIAN_POINT ( 'NONE',  ( -32.84237740334621236, 485.2251842821281116, 5.746442123025396143 ) ) ;
#16276=CARTESIAN_POINT ( 'NONE',  ( -35.60192394405001437, 303.3476854347574090, -0.05210932705592784958 ) ) ;
#16289=CARTESIAN_POINT ( 'NONE',  ( -42.89842744829972077, 435.5680593355726842, 8.824050052237332409 ) ) ;
#16295=CARTESIAN_POINT ( 'NONE',  ( -27.41598304250715401, 312.9579576083220900, 10.89685229489437646 ) ) ;
#16298=CARTESIAN_POINT ( 'NONE',  ( -38.86575330739522371, 477.1834804722099079, -1.710715794009403989 ) ) ;
#16313=AXIS2_PLACEMENT_3D ( 'NONE', #42808, #75161, #18561 ) ;
#16328=CARTESIAN_POINT ( 'NONE',  ( -32.63902298026128079, 347.2392149251367641, 20.22000167947927451 ) ) ;
#16337=EDGE_CURVE ( 'NONE', #66185, #3581, #18986, .T. ) ;
#16343=CARTESIAN_POINT ( 'NONE',  ( 37.72766253904391931, 438.6261178958072264, 23.63852112544520523 ) ) ;
#16346=ORIENTED_EDGE ( 'NONE', *, *, #14245, .F. ) ;
#16348=CARTESIAN_POINT ( 'NONE',  ( 43.61212006920802509, 434.3223099624050860, 14.49719201759555354 ) ) ;
#16364=CARTESIAN_POINT ( 'NONE',  ( -22.20318009218133071, 295.0333587257888439, 9.975590323731541531 ) ) ;
#16367=CARTESIAN_POINT ( 'NONE',  ( 23.66013301062279695, 305.5857861401792661, -8.841988464366599132 ) ) ;
#16371=VECTOR ( 'NONE', #37974, 1000.000000000000000 ) ;
#16374=CARTESIAN_POINT ( 'NONE',  ( -43.33388476023132085, 464.9733321035732274, 13.99141793828976610 ) ) ;
#16377=DIRECTION ( 'NONE',  ( 0.000000000000000000, 0.000000000000000000, -1.000000000000000000 ) ) ;
#16382=CARTESIAN_POINT ( 'NONE',  ( -36.57768354961639545, 437.5705742298923724, 4.260889744331883833 ) ) ;
#16395=B_SPLINE_CURVE_WITH_KNOTS ( 'NONE', 3,
 ( #68796, #68251, #92511, #10003 ),
 .UNSPECIFIED., .F., .F.,
 ( 4, 4 ),
 ( 0.000000000000000000, 0.003262827847964568182 ),
 .UNSPECIFIED. ) ;
#16413=CARTESIAN_POINT ( 'NONE',  ( 35.46821841662498542, 430.5464760133320965, 5.814236037882207775 ) ) ;
#16433=CARTESIAN_POINT ( 'NONE',  ( -42.19180677453720563, 462.2931784592652207, 3.389262873192004477 ) ) ;
#16436=CARTESIAN_POINT ( 'NONE',  ( 32.99999999999948130, 488.9035777786946824, 11.52689957822645717 ) ) ;
#16438=CARTESIAN_POINT ( 'NONE',  ( -33.66371007201963295, 439.0645587366565792, 24.00940545830350459 ) ) ;
#16439=CARTESIAN_POINT ( 'NONE',  ( 31.34373427653038746, 325.5152829962089527, 15.50537047965048387 ) ) ;
#16440=CARTESIAN_POINT ( 'NONE',  ( -42.58760755508850337, 320.1910284125954718, -3.858661461815260818 ) ) ;
#16447=CARTESIAN_POINT ( 'NONE',  ( 13.68764148674883430, 294.5450735065955996, 9.871802096439328267 ) ) ;
#16459=SHAPE_REPRESENTATION_RELATIONSHIP ( 'NONE' , 'NONE' ,  #19231, #31828 ) ;
#16463=EDGE_CURVE ( 'NONE', #59429, #63495, #9959, .T. ) ;
#16464=DIRECTION ( 'NONE',  ( -0.000000000000000000, -1.000000000000000000, -0.000000000000000000 ) ) ;
#16472=CARTESIAN_POINT ( 'NONE',  ( 32.46586666336925475, 488.6856797979017415, 9.810357008081247443 ) ) ;
#16490=CARTESIAN_POINT ( 'NONE',  ( -40.19525959765014278, 459.8689882208905146, 1.906254677025774669 ) ) ;
#16507=CARTESIAN_POINT ( 'NONE',  ( 33.15431920332005689, 300.2961132513346456, -0.7782802253148046745 ) ) ;
#16511=CARTESIAN_POINT ( 'NONE',  ( -43.00000000000000000, 461.4080316921935605, 3.462976341553817949 ) ) ;
#16519=CARTESIAN_POINT ( 'NONE',  ( 43.59493452178210759, 373.1075246076704843, 14.23911768532198430 ) ) ;
#16520=CARTESIAN_POINT ( 'NONE',  ( 44.28408485722940924, 463.6816916292668793, 7.557853517648653430 ) ) ;
#16521=ORIENTED_EDGE ( 'NONE', *, *, #53506, .F. ) ;
#16523=CARTESIAN_POINT ( 'NONE',  ( -20.20043710121002078, 303.8503592077864255, 9.936692575589569643 ) ) ;
#16528=CARTESIAN_POINT ( 'NONE',  ( 36.64823341582350480, 437.5392299810053487, 4.281405873620231617 ) ) ;
#16533=CARTESIAN_POINT ( 'NONE',  ( 46.00000000000000000, 438.0901456946865551, 11.29311581785116125 ) ) ;
#16550=CARTESIAN_POINT ( 'NONE',  ( 31.11679462788039530, 441.4271381875185511, 23.27438508043199406 ) ) ;
#16566=CARTESIAN_POINT ( 'NONE',  ( -19.83463548332447601, 303.8035096162418540, 9.926734387303332241 ) ) ;
#16573=CARTESIAN_POINT ( 'NONE',  ( -40.48182439570949498, 464.0838927029486172, 18.36806636631758849 ) ) ;
#16574=CARTESIAN_POINT ( 'NONE',  ( -32.14109322893018827, 425.0905581414837684, 24.99384153588575685 ) ) ;
#16578=CARTESIAN_POINT ( 'NONE',  ( 32.92225573320253318, 439.7404251386080318, 24.14402493977489783 ) ) ;
#16581=CARTESIAN_POINT ( 'NONE',  ( 33.70642115557484431, 302.7255462307956009, 11.75075386443325876 ) ) ;
#16582=CARTESIAN_POINT ( 'NONE',  ( 42.19179521601817839, 485.4956273777428919, -3.824025998174080510 ) ) ;
#16590=CARTESIAN_POINT ( 'NONE',  ( -23.16554820189585229, 303.5579005584135075, 10.08982211509187010 ) ) ;
#16619=CARTESIAN_POINT ( 'NONE',  ( -34.84618260875176787, 489.9833681528637044, 11.97975507378787619 ) ) ;
#16625=FACE_OUTER_BOUND ( 'NONE', #81159, .T. ) ;
#16644=DIRECTION ( 'NONE',  ( 0.9727555100395958165, 0.000000000000000000, -0.2318333834623605982 ) ) ;
#16652=CARTESIAN_POINT ( 'NONE',  ( 32.01718455759882431, 362.9122997726822746, 22.63193864108178488 ) ) ;
#16672=CARTESIAN_POINT ( 'NONE',  ( 0.000000000000000000, 294.8518027762758038, -10.00000000000000178 ) ) ;
#16685=CARTESIAN_POINT ( 'NONE',  ( 35.00143047691824449, 490.1822567707094436, 12.08765882793104574 ) ) ;
#16686=CARTESIAN_POINT ( 'NONE',  ( -35.99391350154813551, 473.1341906942088826, 18.08607326236544921 ) ) ;
#16697=VERTEX_POINT ( 'NONE', #68473 ) ;
#16705=CARTESIAN_POINT ( 'NONE',  ( -31.42089174849851574, 315.4419851189811084, -7.466270551174265968 ) ) ;
#16710=CIRCLE ( 'NONE', #68385, 0.9999999999999984457 ) ;
#16714=CARTESIAN_POINT ( 'NONE',  ( -23.64706605907013781, 295.2260419621491678, -9.920446719441185834 ) ) ;
#16718=CARTESIAN_POINT ( 'NONE',  ( -36.94935132573986891, 484.7118958255200027, -3.060944727314145020 ) ) ;
#16719=CARTESIAN_POINT ( 'NONE',  ( -42.75446687478902419, 415.2909853957704058, 19.76521844420199159 ) ) ;
#16730=CARTESIAN_POINT ( 'NONE',  ( -42.56547585809266110, 436.9993064646045582, 20.73740471268625996 ) ) ;
#16774=CARTESIAN_POINT ( 'NONE',  ( 32.31817526860642431, 488.2662992775009343, 9.217981799629473727 ) ) ;
#16779=EDGE_LOOP ( 'NONE', ( #50340, #16020, #22654, #94734 ) ) ;
#16780=ORIENTED_EDGE ( 'NONE', *, *, #92637, .F. ) ;
#16789=CARTESIAN_POINT ( 'NONE',  ( 30.00000000000000000, 490.5636507777048791, 7.413185101890151785 ) ) ;
#16807=AXIS2_PLACEMENT_3D ( 'NONE', #17375, #24942, #65378 ) ;
#16815=CARTESIAN_POINT ( 'NONE',  ( 33.71029056097465570, 485.0094969250627628, -0.6083101643369144274 ) ) ;
#16820=CARTESIAN_POINT ( 'NONE',  ( 32.12958771267408054, 464.7275665249412100, 11.12424126545838909 ) ) ;
#16823=CARTESIAN_POINT ( 'NONE',  ( -30.49051837336642024, 298.0882550346395874, -1.287325532041848186 ) ) ;
#16830=CARTESIAN_POINT ( 'NONE',  ( 43.04469050570446598, 434.7734435962917132, 9.248231035223279051 ) ) ;
#16837=CARTESIAN_POINT ( 'NONE',  ( 38.68218982724705057, 320.0845437455996603, 16.10279619727025135 ) ) ;
#16841=CARTESIAN_POINT ( 'NONE',  ( -44.11327388758642343, 464.4313852428376777, 9.822198357559813076 ) ) ;
#16852=B_SPLINE_CURVE_WITH_KNOTS ( 'NONE', 3,
 ( #22291, #62221, #97197, #55137, #88067, #14146, #79949, #6059, #15218, #81006, #30915, #38985 ),
 .UNSPECIFIED., .F., .F.,
 ( 4, 2, 2, 2, 2, 4 ),
 ( 0.000000000000000000, 0.001936431260136990684, 0.002904646890205480388, 0.003872862520273970960, 0.005809293780410951236, 0.007745725040547933246 ),
 .UNSPECIFIED. ) ;
#16856=FACE_OUTER_BOUND ( 'NONE', #104468, .T. ) ;
#16858=CARTESIAN_POINT ( 'NONE',  ( 26.35185796998234409, 307.8658938434331844, 10.86782115656190406 ) ) ;
#16871=FACE_OUTER_BOUND ( 'NONE', #93649, .T. ) ;
#16872=CARTESIAN_POINT ( 'NONE',  ( -30.00000000000000000, 450.0000000000002274, 13.20242257375370976 ) ) ;
#16878=CARTESIAN_POINT ( 'NONE',  ( -21.43128638237507388, 303.0517047904468200, 9.980147555062945486 ) ) ;
#16891=CARTESIAN_POINT ( 'NONE',  ( -38.02377251231919075, 490.5703810925436414, 12.25131830484250628 ) ) ;
#16904=CARTESIAN_POINT ( 'NONE',  ( -43.00000000000001421, 461.4080316921935605, 3.462976341553827275 ) ) ;
#16907=CARTESIAN_POINT ( 'NONE',  ( 35.52386467438406470, 464.2380653034119860, 19.26634992204540708 ) ) ;
#16913=CARTESIAN_POINT ( 'NONE',  ( -25.93947128054312756, 296.0094280503604978, 10.18659011856751384 ) ) ;
#16915=CARTESIAN_POINT ( 'NONE',  ( -35.76379064120181539, 307.0162303970107587, 12.81051142610679960 ) ) ;
#16918=B_SPLINE_CURVE_WITH_KNOTS ( 'NONE', 3,
 ( #72027, #104934, #73058, #56881, #7801, #55807, #10463, #33709 ),
 .UNSPECIFIED., .F., .F.,
 ( 4, 2, 2, 4 ),
 ( 2.096953513055919001E-16, 0.002585882924094807904, 0.003878824386142106905, 0.005171765848189405906 ),
 .UNSPECIFIED. ) ;
#16920=ORIENTED_EDGE ( 'NONE', *, *, #26573, .F. ) ;
#16921=CARTESIAN_POINT ( 'NONE',  ( 25.90835893021727898, 306.6868635151020612, -9.596616819076174920 ) ) ;
#16934=CARTESIAN_POINT ( 'NONE',  ( -36.73553355714307145, 438.2340261154905647, 3.898456086346344218 ) ) ;
#16941=VECTOR ( 'NONE', #48553, 1000.000000000000114 ) ;
#16956=ORIENTED_EDGE ( 'NONE', *, *, #60660, .T. ) ;
#16960=CARTESIAN_POINT ( 'NONE',  ( 20.94643265517294850, 304.9211962324576461, -8.985249965551574292 ) ) ;
#16969=CARTESIAN_POINT ( 'NONE',  ( -16.12995111408092441, 294.5641271688412530, -2.061085572538797983 ) ) ;
#16971=CARTESIAN_POINT ( 'NONE',  ( 32.28552837373268147, 464.7648866755951644, 15.30384310833112060 ) ) ;
#16972=CARTESIAN_POINT ( 'NONE',  ( -37.67124221001142814, 463.6239404278534266, 19.49545380201571021 ) ) ;
#16976=CARTESIAN_POINT ( 'NONE',  ( 32.06413248787634274, 464.8630579811580219, 13.97151946468930461 ) ) ;
#16979=VERTEX_POINT ( 'NONE', #81307 ) ;
#16981=ORIENTED_EDGE ( 'NONE', *, *, #34881, .F. ) ;
#16988=CARTESIAN_POINT ( 'NONE',  ( -42.94810946381694805, 342.9651505394211313, 9.411812260929616869 ) ) ;
#16998=CARTESIAN_POINT ( 'NONE',  ( 41.11448970373153600, 464.2845792240962055, 17.78478044672835168 ) ) ;
#17008=B_SPLINE_CURVE_WITH_KNOTS ( 'NONE', 3,
 ( #10845, #28156, #69125, #35717, #101479, #86381, #27630, #52922, #93396, #4369, #36781, #11380, #44304, #100936 ),
 .UNSPECIFIED., .F., .F.,
 ( 4, 2, 2, 2, 2, 2, 4 ),
 ( 8.482014475176614844E-15, 0.003029464007163871000, 0.004544196010741614541, 0.006058928014319358082, 0.007573660017897102491, 0.009088392021474845164, 0.01211785602863033745 ),
 .UNSPECIFIED. ) ;
#17012=CIRCLE ( 'NONE', #78972, 1.000000000000023981 ) ;
#17014=CARTESIAN_POINT ( 'NONE',  ( -34.98071605568955533, 490.8360413343443724, 11.88490725385787705 ) ) ;
#17018=CARTESIAN_POINT ( 'NONE',  ( 33.38504658727612906, 488.8572893496567531, 10.16177171493806952 ) ) ;
#17028=EDGE_CURVE ( 'NONE', #61182, #96036, #66012, .T. ) ;
#17038=CARTESIAN_POINT ( 'NONE',  ( -38.51282804766191248, 490.3045649922998450, 12.08595093631691952 ) ) ;
#17042=CARTESIAN_POINT ( 'NONE',  ( 34.64581139903178553, 463.6418748650359589, 19.44242283797247239 ) ) ;
#17055=CARTESIAN_POINT ( 'NONE',  ( 36.48153863437710243, 303.2350093248795702, -8.088982545662673829 ) ) ;
#17067=CARTESIAN_POINT ( 'NONE',  ( 43.66704108187254008, 409.2854991616131315, 16.12724780824946791 ) ) ;
#17073=CARTESIAN_POINT ( 'NONE',  ( 35.40294873602728387, 484.3215194930215830, -1.486762578860570283 ) ) ;
#17075=CARTESIAN_POINT ( 'NONE',  ( 32.80261435968075290, 487.0248074982611115, 8.977354182173554520 ) ) ;
#17081=CARTESIAN_POINT ( 'NONE',  ( 46.00000000000000000, 438.0166301925371499, 11.64259471674452229 ) ) ;
#17087=CARTESIAN_POINT ( 'NONE',  ( 34.14662298548351771, 464.2250883195994220, 6.054123830998662470 ) ) ;
#17096=CARTESIAN_POINT ( 'NONE',  ( 31.19652432992544888, 378.3327707670021027, 24.28948218791313707 ) ) ;
#17098=CARTESIAN_POINT ( 'NONE',  ( -30.00000000000000355, 489.4338083968330579, 5.745752720312972350 ) ) ;
#17105=UNCERTAINTY_MEASURE_WITH_UNIT (LENGTH_MEASURE( 1.000000000000000082E-05 ), #57913, 'distance_accuracy_value', 'NONE');
#17118=CARTESIAN_POINT ( 'NONE',  ( -41.35772432385135033, 464.3624544568689316, 17.55089308074047949 ) ) ;
#17119=CARTESIAN_POINT ( 'NONE',  ( -31.19347262973593615, 380.6645121172051631, 24.42694056262163116 ) ) ;
#17123=CARTESIAN_POINT ( 'NONE',  ( 42.43166099483027409, 436.1632441641384617, 19.16791492759929838 ) ) ;
#17124=ORIENTED_EDGE ( 'NONE', *, *, #92804, .F. ) ;
#17128=CARTESIAN_POINT ( 'NONE',  ( 29.32203595473246693, 297.8341598778472985, 10.59484822235428325 ) ) ;
#17131=B_SPLINE_CURVE_WITH_KNOTS ( 'NONE', 3,
 ( #100098, #7890, #40798, #26266 ),
 .UNSPECIFIED., .F., .F.,
 ( 4, 4 ),
 ( 2.409751485173049940E-15, 0.0004300933845494213218 ),
 .UNSPECIFIED. ) ;
#17133=CARTESIAN_POINT ( 'NONE',  ( 42.62984607896018474, 365.9487680686676754, 17.22660553029483665 ) ) ;
#17134=( BOUNDED_SURFACE ( )  B_SPLINE_SURFACE ( 3, 2, ( 
 ( #686, #82713, #89223 ),
 ( #73539, #83239, #162 ),
 ( #17467, #32063, #81622 ),
 ( #8816, #24517, #66530 ) ),
 .UNSPECIFIED., .F., .F., .F. ) 
 B_SPLINE_SURFACE_WITH_KNOTS ( ( 4, 4 ),
 ( 3, 3 ),
 ( 4.640385298237958978E-17, 0.002473307515785300430 ),
 ( 0.000000000000000000, 1.000000000000000000 ),
 .UNSPECIFIED. ) 
 GEOMETRIC_REPRESENTATION_ITEM ( )  RATIONAL_B_SPLINE_SURFACE ( (
 ( 1.000000000000000000, 0.7904469216846371493, 1.000000000000000000),
 ( 1.000000000000000000, 0.7997328579911862079, 1.000000000000000000),
 ( 1.000000000000000000, 0.8083744009265905195, 1.000000000000000000),
 ( 1.000000000000000000, 0.8138888783291118312, 1.000000000000000000) ) ) 
 REPRESENTATION_ITEM ( '' )  SURFACE ( )  );
#17139=CARTESIAN_POINT ( 'NONE',  ( -27.42347756180437557, 296.7082162746293648, 10.34135678911163048 ) ) ;
#17145=EDGE_CURVE ( 'NONE', #46054, #96778, #3476, .T. ) ;
#17147=CARTESIAN_POINT ( 'NONE',  ( 1.406471811252868021, 302.0905290902286424, 9.901083696907180709 ) ) ;
#17149=DIRECTION ( 'NONE',  ( 0.000000000000000000, 1.000000000000000000, 0.000000000000000000 ) ) ;
#17151=B_SPLINE_CURVE_WITH_KNOTS ( 'NONE', 3,
 ( #69813, #35895, #36430, #93567 ),
 .UNSPECIFIED., .F., .F.,
 ( 4, 4 ),
 ( 4.906538933386797242E-17, 0.001346487449956126773 ),
 .UNSPECIFIED. ) ;
#17164=DIRECTION ( 'NONE',  ( 0.000000000000000000, 0.000000000000000000, -1.000000000000000000 ) ) ;
#17166=CARTESIAN_POINT ( 'NONE',  ( 33.00000000000000000, 461.8887775513397855, 11.55279652844103566 ) ) ;
#17188=CARTESIAN_POINT ( 'NONE',  ( 37.50059943756055247, 490.7879993827821181, 12.38039871356680344 ) ) ;
#17192=CARTESIAN_POINT ( 'NONE',  ( 8.604130785002874120E-16, 67.00000000000002842, 7.025805963803935406 ) ) ;
#17193=CARTESIAN_POINT ( 'NONE',  ( -6.086036594375756614, 294.7541636957752758, -7.939907524234526726 ) ) ;
#17200=CARTESIAN_POINT ( 'NONE',  ( 31.18696128861778760, 357.2396685113180865, 20.55154636943739632 ) ) ;
#17213=CARTESIAN_POINT ( 'NONE',  ( -23.61963550967466574, 306.0340374937824777, 10.19690224617928287 ) ) ;
#17214=DIRECTION ( 'NONE',  ( -1.000000000000000000, 0.000000000000000000, 0.000000000000000000 ) ) ;
#17220=AXIS2_PLACEMENT_3D ( 'NONE', #75025, #85821, #62594 ) ;
#17225=FACE_OUTER_BOUND ( 'NONE', #71537, .T. ) ;
#17226=CIRCLE ( 'NONE', #70643, 1.000000000000014877 ) ;
#17233=CARTESIAN_POINT ( 'NONE',  ( -17.19041072168119300, 294.5876824650746357, 9.880858205605974831 ) ) ;
#17236=CARTESIAN_POINT ( 'NONE',  ( -41.46910480219105466, 484.7338956289799512, -3.418960549710621244 ) ) ;
#17238=CARTESIAN_POINT ( 'NONE',  ( 35.47838770905575956, 490.5979824477001330, 12.29204623667445340 ) ) ;
#17254=CARTESIAN_POINT ( 'NONE',  ( -31.03678703374875525, 438.6650838204938623, 21.86890379898548176 ) ) ;
#17255=CARTESIAN_POINT ( 'NONE',  ( -33.77559172535808329, 464.7834715296605737, 7.192701217093241617 ) ) ;
#17256=CARTESIAN_POINT ( 'NONE',  ( -32.96072870876664496, 317.2200023992991191, -6.776755668305763258 ) ) ;
#17259=CARTESIAN_POINT ( 'NONE',  ( -43.42366826522957268, 435.2488004288641719, 10.12833319149509315 ) ) ;
#17262=CARTESIAN_POINT ( 'NONE',  ( -24.69387026086019432, 295.5389138248296490, -1.852611171248429445 ) ) ;
#17266=CARTESIAN_POINT ( 'NONE',  ( -36.37693845632723111, 485.4380683983963536, -3.604171430931530029 ) ) ;
#17267=CARTESIAN_POINT ( 'NONE',  ( -32.85315808798738146, 354.3401018246705689, 21.52737482615226483 ) ) ;
#17277=CARTESIAN_POINT ( 'NONE',  ( 30.00000000000000000, 489.8676322012278774, 6.488549987513861694 ) ) ;
#17278=CARTESIAN_POINT ( 'NONE',  ( -40.49327943412436071, 437.8143148761543557, 21.96882124328788066 ) ) ;
#17280=CARTESIAN_POINT ( 'NONE',  ( 0.000000000000000000, 70.00000000000000000, -10.00000000000000178 ) ) ;
#17284=CARTESIAN_POINT ( 'NONE',  ( 0.000000000000000000, 67.00000000000002842, 0.000000000000000000 ) ) ;
#17289=B_SPLINE_CURVE_WITH_KNOTS ( 'NONE', 3,
 ( #58001, #66103, #17038, #50966, #34308, #9992, #26754, #76851, #33230, #66638, #68240, #25700 ),
 .UNSPECIFIED., .F., .F.,
 ( 4, 2, 2, 2, 2, 4 ),
 ( 4.993455085690288581E-15, 0.001726505353950908653, 0.002589758030923909431, 0.003453010707896910208, 0.005179516061842909594, 0.006906021415788908546 ),
 .UNSPECIFIED. ) ;
#17292=CARTESIAN_POINT ( 'NONE',  ( 46.00000000000000000, 488.7529659943156162, 4.223909611882176840 ) ) ;
#17301=VERTEX_POINT ( 'NONE', #42458 ) ;
#17309=DIRECTION ( 'NONE',  ( -1.000000000000000000, -0.000000000000000000, -0.000000000000000000 ) ) ;
#17320=CARTESIAN_POINT ( 'NONE',  ( 40.44189562491348511, 465.0930618392404199, 17.36238218226302621 ) ) ;
#17321=CARTESIAN_POINT ( 'NONE',  ( -34.54755545858651544, 435.5422147998195896, 9.163155746809447777 ) ) ;
#17339=CARTESIAN_POINT ( 'NONE',  ( 43.58525529925911712, 435.7810014872755460, 17.82021598409033913 ) ) ;
#17354=CARTESIAN_POINT ( 'NONE',  ( 34.88900972249397370, 464.6206820655982028, 18.69027339340997784 ) ) ;
#17375=CARTESIAN_POINT ( 'NONE',  ( 42.99999999999997868, 465.8747179598608454, 15.20075430169040231 ) ) ;
#17379=DIRECTION ( 'NONE',  ( 1.000000000000000000, 0.000000000000000000, 0.000000000000000000 ) ) ;
#17383=CARTESIAN_POINT ( 'NONE',  ( -43.18901105325944201, 465.6357412884333939, 10.74839809646403488 ) ) ;
#17396=CARTESIAN_POINT ( 'NONE',  ( 27.25733410137293689, 309.8297720804826554, 11.35386381468975614 ) ) ;
#17401=EDGE_CURVE ( 'NONE', #75237, #101842, #81537, .T. ) ;
#17407=FACE_OUTER_BOUND ( 'NONE', #76475, .T. ) ;
#17414=CARTESIAN_POINT ( 'NONE',  ( -31.01653611012242706, 322.5997654333527294, 14.79674070695548060 ) ) ;
#17418=CARTESIAN_POINT ( 'NONE',  ( -1.128238012697766912, 300.0000000000000000, 9.936150108905552614 ) ) ;
#17423=CARTESIAN_POINT ( 'NONE',  ( 19.38947238167622089, 294.6924519132794558, -2.033477040682234893 ) ) ;
#17434=CARTESIAN_POINT ( 'NONE',  ( -33.07276483573667747, 438.9325140356154975, 23.89537236861306013 ) ) ;
#17442=CARTESIAN_POINT ( 'NONE',  ( -43.27198366478794611, 461.7520071969213404, 3.865882560831350290 ) ) ;
#17445=EDGE_CURVE ( 'NONE', #73295, #78525, #29872, .T. ) ;
#17447=CARTESIAN_POINT ( 'NONE',  ( 33.50694624596046367, 434.8929047988108323, 13.71597635161211848 ) ) ;
#17453=CARTESIAN_POINT ( 'NONE',  ( -27.47093694407817210, 296.2799286419132727, -9.692114557243211692 ) ) ;
#17457=CARTESIAN_POINT ( 'NONE',  ( 24.91130217974400196, 306.1405592189659046, -8.719263803201467766 ) ) ;
#17467=CARTESIAN_POINT ( 'NONE',  ( -33.21051451599209514, 465.5912171658555394, 15.87385029336180509 ) ) ;
#17470=CARTESIAN_POINT ( 'NONE',  ( -35.41405072743933147, 437.5080630478298076, 4.889382217448016377 ) ) ;
#17525=CARTESIAN_POINT ( 'NONE',  ( -30.58328632870184549, 308.7181655071192949, -8.654209201893030112 ) ) ;
#17535=CARTESIAN_POINT ( 'NONE',  ( 38.99314007804239424, 463.6591011809805991, 19.41136731754987821 ) ) ;
#17539=VERTEX_POINT ( 'NONE', #1312 ) ;
#17548=CARTESIAN_POINT ( 'NONE',  ( -43.00000000000000000, 450.0000000000002274, 13.20242257375370976 ) ) ;
#17550=CARTESIAN_POINT ( 'NONE',  ( -36.08160016962256833, 491.3801102092016890, 12.28496641015634872 ) ) ;
#17577=CARTESIAN_POINT ( 'NONE',  ( 35.69355135759132480, 463.3819780847712195, 19.97922827668278245 ) ) ;
#17580=EDGE_CURVE ( 'NONE', #63495, #15128, #4131, .T. ) ;
#17586=CARTESIAN_POINT ( 'NONE',  ( -37.48079203514996038, 473.0293823827626056, 17.43706145210287062 ) ) ;
#17593=CARTESIAN_POINT ( 'NONE',  ( 30.93562973191455612, 298.0458768196136248, -9.298557881189427832 ) ) ;
#17604=CARTESIAN_POINT ( 'NONE',  ( 37.64398511886353305, 375.6922506333542060, 4.851078712600862985 ) ) ;
#17609=CARTESIAN_POINT ( 'NONE',  ( 34.28461378013923166, 484.9851079380702572, 0.1119777429318196682 ) ) ;
#17611=CARTESIAN_POINT ( 'NONE',  ( 37.29743259733411520, 437.4067882691435898, 4.451017177258780322 ) ) ;
#17630=CARTESIAN_POINT ( 'NONE',  ( -43.04469050570867239, 434.7734435962895532, 9.248231035232468145 ) ) ;
#17631=CARTESIAN_POINT ( 'NONE',  ( 30.12932728364529922, 334.4140447340107585, 17.11298374841474867 ) ) ;
#17635=CARTESIAN_POINT ( 'NONE',  ( -29.99999999996959588, 488.4085301725142472, 8.313477165056513130 ) ) ;
#17636=VERTEX_POINT ( 'NONE', #33732 ) ;
#17647=EDGE_LOOP ( 'NONE', ( #50301, #13111, #91000, #33393 ) ) ;
#17652=CARTESIAN_POINT ( 'NONE',  ( -32.13233948541094520, 428.0625681181319919, 24.77049652713832728 ) ) ;
#17658=CARTESIAN_POINT ( 'NONE',  ( 26.18291261871826237, 305.7871056458065482, 10.60176253965241777 ) ) ;
#17663=CARTESIAN_POINT ( 'NONE',  ( 28.69273362649255077, 297.1307134239958714, 2.434641731654969110 ) ) ;
#17665=ORIENTED_EDGE ( 'NONE', *, *, #58972, .T. ) ;
#17667=CARTESIAN_POINT ( 'NONE',  ( -24.44168859681608907, 295.5650463862446600, 10.09009199608876983 ) ) ;
#17679=ORIENTED_EDGE ( 'NONE', *, *, #15564, .F. ) ;
#17687=EDGE_CURVE ( 'NONE', #58935, #16697, #93448, .T. ) ;
#17699=CARTESIAN_POINT ( 'NONE',  ( 41.44325323473465517, 477.1522009800042952, -1.085119017178377554 ) ) ;
#17721=CARTESIAN_POINT ( 'NONE',  ( 5.862635191369047760, 294.7602340196642103, -8.121464904941849028 ) ) ;
#17725=AXIS2_PLACEMENT_3D ( 'NONE', #41939, #65692, #58672 ) ;
#17729=CARTESIAN_POINT ( 'NONE',  ( 28.62319560939385710, 318.3944600039412194, 12.26906456063335149 ) ) ;
#17733=EDGE_CURVE ( 'NONE', #97465, #26579, #25265, .T. ) ;
#17736=CARTESIAN_POINT ( 'NONE',  ( 32.09911992168216699, 438.9232547152094526, 23.66653216045977359 ) ) ;
#17745=CARTESIAN_POINT ( 'NONE',  ( -43.51084452654468748, 465.2903130129675446, 9.421687747985348693 ) ) ;
#17751=CARTESIAN_POINT ( 'NONE',  ( -7.196962703048771282, 302.2659962052633773, -10.02664813804980959 ) ) ;
#17759=CARTESIAN_POINT ( 'NONE',  ( -41.66301127302556750, 485.3863426732056041, -3.409513628938169116 ) ) ;
#17761=( BOUNDED_SURFACE ( )  B_SPLINE_SURFACE ( 3, 2, ( 
 ( #76991, #44101, #95310 ),
 ( #87220, #38162, #85634 ),
 ( #3646, #70505, #36050 ),
 ( #103394, #79113, #27962 ),
 ( #36581, #103912, #12774 ),
 ( #61899, #86175, #69447 ),
 ( #29546, #28478, #12247 ),
 ( #102329, #29033, #86703 ),
 ( #45177, #60825, #68921 ),
 ( #4706, #4172, #71021 ),
 ( #61359, #20413, #94794 ),
 ( #45692, #62416, #94252 ),
 ( #101795, #54277, #21969 ),
 ( #21442, #13299, #30060 ) ),
 .UNSPECIFIED., .F., .F., .F. ) 
 B_SPLINE_SURFACE_WITH_KNOTS ( ( 4, 2, 2, 2, 2, 2, 4 ),
 ( 3, 3 ),
 ( 1.019150042136374168E-17, 0.001037790322792903758, 0.001556685484189350649, 0.002075580645585797541, 0.002594475806982244649, 0.003113370968378691324, 0.004151161291171584673 ),
 ( 0.000000000000000000, 1.000000000000000000 ),
 .UNSPECIFIED. ) 
 GEOMETRIC_REPRESENTATION_ITEM ( )  RATIONAL_B_SPLINE_SURFACE ( (
 ( 1.000000000000000000, 0.8266506655096989009, 1.000000000000000000),
 ( 1.000000000000000000, 0.8403402121222391941, 1.000000000000000000),
 ( 1.000000000000000000, 0.8527375874874671968, 1.000000000000000000),
 ( 1.000000000000000000, 0.8685816477866979968, 1.000000000000000000),
 ( 1.000000000000000000, 0.8733924426142005704, 1.000000000000000000),
 ( 1.000000000000000000, 0.8815965360735344980, 1.000000000000000000),
 ( 1.000000000000000000, 0.8850417602701512454, 1.000000000000000000),
 ( 1.000000000000000000, 0.8904811663267429012, 1.000000000000000000),
 ( 1.000000000000000000, 0.8924856662909712579, 1.000000000000000000),
 ( 1.000000000000000000, 0.8947492012709854503, 1.000000000000000000),
 ( 1.000000000000000000, 0.8950270886654364544, 1.000000000000000000),
 ( 1.000000000000000000, 0.8933353874799748739, 1.000000000000000000),
 ( 1.000000000000000000, 0.8887179207583161267, 1.000000000000000000),
 ( 1.000000000000000000, 0.8812198548864902392, 1.000000000000000000) ) ) 
 REPRESENTATION_ITEM ( '' )  SURFACE ( )  );
#17765=CARTESIAN_POINT ( 'NONE',  ( -34.56726037194436429, 484.1545686971863347, -0.1516737162322892851 ) ) ;
#17783=CARTESIAN_POINT ( 'NONE',  ( -25.62494917502693781, 306.5451325936110152, -8.628440507281284866 ) ) ;
#17788=CARTESIAN_POINT ( 'NONE',  ( -43.37695759419973740, 434.6160983767828725, 10.05510951421886645 ) ) ;
#17796=CARTESIAN_POINT ( 'NONE',  ( -33.16875022513573867, 397.0288761002586284, 25.82781127675604438 ) ) ;
#17801=AXIS2_PLACEMENT_3D ( 'NONE', #37096, #4164, #84553 ) ;
#17805=CARTESIAN_POINT ( 'NONE',  ( 34.47678062874019389, 437.1474145881098821, 5.468662283308706407 ) ) ;
#17828=ADVANCED_FACE ( 'NONE', ( #64244 ), #35176, .T. ) ;
#17851=CARTESIAN_POINT ( 'NONE',  ( 35.69739812508499455, 430.4862580793411553, 4.964222856391316441 ) ) ;
#17852=CARTESIAN_POINT ( 'NONE',  ( 40.06570913991743765, 460.7366702961331839, 2.123561850760146363 ) ) ;
#17853=CARTESIAN_POINT ( 'NONE',  ( -34.47678062873981730, 437.1474145881089157, 5.468662283310409045 ) ) ;
#17854=CARTESIAN_POINT ( 'NONE',  ( 32.04172522544141088, 487.4996691821121431, 8.071286837385784452 ) ) ;
#17859=ORIENTED_EDGE ( 'NONE', *, *, #15564, .T. ) ;
#17861=CARTESIAN_POINT ( 'NONE',  ( 33.94783393359906398, 484.1261039197348737, 1.321740980885009353 ) ) ;
#17864=B_SPLINE_CURVE_WITH_KNOTS ( 'NONE', 3,
 ( #78220, #46391, #37807, #30221 ),
 .UNSPECIFIED., .F., .F.,
 ( 4, 4 ),
 ( 1.734723475976807094E-17, 0.002002602941643040913 ),
 .UNSPECIFIED. ) ;
#17873=EDGE_CURVE ( 'NONE', #67806, #63037, #33385, .T. ) ;
#17876=VERTEX_POINT ( 'NONE', #66888 ) ;
#17897=SURFACE_STYLE_USAGE ( .BOTH. , #65892 ) ;
#17901=UNCERTAINTY_MEASURE_WITH_UNIT (LENGTH_MEASURE( 1.000000000000000082E-05 ), #28830, 'distance_accuracy_value', 'NONE');
#17906=CARTESIAN_POINT ( 'NONE',  ( 43.63911886419051456, 435.1012159695193873, 10.95008075557279170 ) ) ;
#17914=CARTESIAN_POINT ( 'NONE',  ( 35.60955124828987550, 461.3429156349023970, 3.374284740307414765 ) ) ;
#17916=CARTESIAN_POINT ( 'NONE',  ( -22.21408712632129934, 305.3228438409180967, 9.038496626227296105 ) ) ;
#17917=EDGE_CURVE ( 'NONE', #7512, #21702, #20127, .T. ) ;
#17928=CARTESIAN_POINT ( 'NONE',  ( 43.10371592040107203, 462.6168321841715283, 4.970041475426227429 ) ) ;
#17929=CARTESIAN_POINT ( 'NONE',  ( 21.29199042761633365, 304.0466698332161855, 9.978644581415256454 ) ) ;
#17935=CARTESIAN_POINT ( 'NONE',  ( -38.83537165123732393, 468.9475234385650992, 0.4936731619138239324 ) ) ;
#17936=ORIENTED_EDGE ( 'NONE', *, *, #76722, .T. ) ;
#17940=CARTESIAN_POINT ( 'NONE',  ( -20.49977525862259142, 302.8459220885798686, -10.00124997875687427 ) ) ;
#17945=CARTESIAN_POINT ( 'NONE',  ( -22.51188458451504104, 303.3301420540304321, 10.03976258024267842 ) ) ;
#17946=ORIENTED_EDGE ( 'NONE', *, *, #34162, .F. ) ;
#17948=EDGE_CURVE ( 'NONE', #65653, #23677, #67941, .T. ) ;
#17963=EDGE_CURVE ( 'NONE', #62284, #66822, #54133, .T. ) ;
#17966=EDGE_CURVE ( 'NONE', #23615, #4842, #35590, .T. ) ;
#17970=CARTESIAN_POINT ( 'NONE',  ( -30.00000000000000355, 462.0200324021746496, 12.95089283450024276 ) ) ;
#17993=CARTESIAN_POINT ( 'NONE',  ( 20.97754405179131254, 294.8763868968453608, 9.942224931492251727 ) ) ;
#18012=CARTESIAN_POINT ( 'NONE',  ( 27.79797611564797322, 306.8793823578155298, -9.324996632398045548 ) ) ;
#18025=CARTESIAN_POINT ( 'NONE',  ( 27.63197730200188218, 308.2542597069073622, -8.233497725011043045 ) ) ;
#18029=B_SPLINE_CURVE_WITH_KNOTS ( 'NONE', 3,
 ( #39981, #87483, #71795, #7063, #39463, #95565, #88536, #63740 ),
 .UNSPECIFIED., .F., .F.,
 ( 4, 2, 2, 4 ),
 ( 3.469446951953614189E-18, 0.002719188179122917007, 0.004078782268684381582, 0.005438376358245846157 ),
 .UNSPECIFIED. ) ;
#18030=ORIENTED_EDGE ( 'NONE', *, *, #104943, .T. ) ;
#18039=FACE_OUTER_BOUND ( 'NONE', #46361, .T. ) ;
#18047=CARTESIAN_POINT ( 'NONE',  ( -43.04469050570867239, 434.7734435962895532, 9.248231035232468145 ) ) ;
#18055=( NAMED_UNIT ( * ) PLANE_ANGLE_UNIT ( ) SI_UNIT ( $, .RADIAN. ) );
#18059=CARTESIAN_POINT ( 'NONE',  ( -39.01698735643275029, 311.0398647938606587, 1.855041891536996834 ) ) ;
#18067=CARTESIAN_POINT ( 'NONE',  ( 42.43284980134657047, 464.7153848364305873, 16.15301860174535165 ) ) ;
#18077=VERTEX_POINT ( 'NONE', #28580 ) ;
#18091=DIRECTION ( 'NONE',  ( 0.000000000000000000, 0.3049629831704142591, 0.9523642049635221429 ) ) ;
#18111=CIRCLE ( 'NONE', #31892, 0.9999999999999994449 ) ;
#18117=CARTESIAN_POINT ( 'NONE',  ( -42.50679667587944266, 460.9583926513354868, 2.954705527095128126 ) ) ;
#18122=CARTESIAN_POINT ( 'NONE',  ( -42.71758075471695548, 375.2456527110321076, 18.33958921108564155 ) ) ;
#18129=CARTESIAN_POINT ( 'NONE',  ( 29.07128654445882887, 296.9339959557834163, -9.548856946219741459 ) ) ;
#18138=CARTESIAN_POINT ( 'NONE',  ( 19.73463816634110657, 304.7971333121958537, 8.925379062039144884 ) ) ;
#18139=CARTESIAN_POINT ( 'NONE',  ( -42.48678019891495694, 465.9003906206858119, 13.75832259440540284 ) ) ;
#18148=CARTESIAN_POINT ( 'NONE',  ( 36.97265860262990600, 437.4722588954304570, 4.366279915526031452 ) ) ;
#18151=DIRECTION ( 'NONE',  ( -1.000000000000000000, 0.000000000000000000, 0.000000000000000000 ) ) ;
#18158=CARTESIAN_POINT ( 'NONE',  ( 33.00000000000000000, 488.6481008951279250, 3.890293910850408210 ) ) ;
#18163=CARTESIAN_POINT ( 'NONE',  ( 43.00000000000000000, 500.0000000000002274, 15.00000000000000711 ) ) ;
#18164=CARTESIAN_POINT ( 'NONE',  ( -43.69697758767997442, 434.4335448986656729, 11.30914782517130668 ) ) ;
#18165=CARTESIAN_POINT ( 'NONE',  ( 40.07586470527510158, 337.7832441655235129, 20.21182470898328631 ) ) ;
#18168=CARTESIAN_POINT ( 'NONE',  ( -32.15166163075724626, 486.0589784586660471, 5.199393881400879103 ) ) ;
#18178=CARTESIAN_POINT ( 'NONE',  ( -31.69405040003880814, 348.1944610541558518, 20.16544092466686777 ) ) ;
#18183=CARTESIAN_POINT ( 'NONE',  ( -32.71046359557016103, 465.7618366408448765, 11.82978892796183246 ) ) ;
#18186=CIRCLE ( 'NONE', #57704, 3.000000000000019096 ) ;
#18187=CARTESIAN_POINT ( 'NONE',  ( 36.53955443788006363, 439.8193023638518753, 24.21875945428991272 ) ) ;
#18189=CARTESIAN_POINT ( 'NONE',  ( -32.13665136737670736, 374.7280873276972102, 24.09185903376077320 ) ) ;
#18193=ORIENTED_EDGE ( 'NONE', *, *, #85036, .T. ) ;
#18200=CARTESIAN_POINT ( 'NONE',  ( 34.73580866203639061, 304.6300892602635031, 12.21738039697267553 ) ) ;
#18206=AXIS2_PLACEMENT_3D ( 'NONE', #2260, #2804, #34151 ) ;
#18213=CARTESIAN_POINT ( 'NONE',  ( -23.45191171818318665, 303.6749378929117711, 10.11563714018844884 ) ) ;
#18220=CARTESIAN_POINT ( 'NONE',  ( 0.000000000000000000, 70.00000000000000000, 0.000000000000000000 ) ) ;
#18225=FACE_BOUND ( 'NONE', #21696, .T. ) ;
#18237=CARTESIAN_POINT ( 'NONE',  ( 43.00000000000000000, 487.9285348210859752, 8.903916466042430145 ) ) ;
#18255=CARTESIAN_POINT ( 'NONE',  ( -36.42556657147747501, 437.5919504960684776, 4.247212042401131704 ) ) ;
#18262=ORIENTED_EDGE ( 'NONE', *, *, #55586, .T. ) ;
#18263=FILL_AREA_STYLE_COLOUR ( '', #53221 ) ;
#18268=CARTESIAN_POINT ( 'NONE',  ( 9.091052096490022549, 294.6686584899208583, -4.203955522403658662 ) ) ;
#18275=CARTESIAN_POINT ( 'NONE',  ( 31.43460747645193010, 410.2298262219391063, 24.47801356763874026 ) ) ;
#18286=CARTESIAN_POINT ( 'NONE',  ( -31.14694070047868735, 432.3293837220155069, 24.29762062537629319 ) ) ;
#18289=CARTESIAN_POINT ( 'NONE',  ( -43.54570344706616680, 464.5919001249994835, 9.427857144821919277 ) ) ;
#18292=ORIENTED_EDGE ( 'NONE', *, *, #89285, .F. ) ;
#18301=CARTESIAN_POINT ( 'NONE',  ( -16.55845859191752112, 294.5717093170194403, 1.877662430929134096 ) ) ;
#18307=CARTESIAN_POINT ( 'NONE',  ( -32.87547266101557852, 465.6993878536674742, 10.91512469976539279 ) ) ;
#18312=CARTESIAN_POINT ( 'NONE',  ( -44.23147267340018374, 435.1968787606626847, 14.01185548270382242 ) ) ;
#18315=VERTEX_POINT ( 'NONE', #76428 ) ;
#18333=DIRECTION ( 'NONE',  ( 0.000000000000000000, -0.9591753627735369880, 0.2828119931124806197 ) ) ;
#18336=CARTESIAN_POINT ( 'NONE',  ( -42.76735375558020280, 409.2590350599533622, 19.91209603463725131 ) ) ;
#18351=CARTESIAN_POINT ( 'NONE',  ( -20.05074616892822803, 67.05096163904791240, -10.02537308446410869 ) ) ;
#18355=VECTOR ( 'NONE', #31526, 1000.000000000000227 ) ;
#18366=CARTESIAN_POINT ( 'NONE',  ( 27.18908553330205180, 296.5274986157688772, 10.30015177545897842 ) ) ;
#18369=ORIENTED_EDGE ( 'NONE', *, *, #7559, .F. ) ;
#18371=AXIS2_PLACEMENT_3D ( 'NONE', #12242, #46742, #94249 ) ;
#18389=CARTESIAN_POINT ( 'NONE',  ( 28.76346532419124458, 309.5219921958590135, -8.933260212751790164 ) ) ;
#18390=CARTESIAN_POINT ( 'NONE',  ( 41.75908120488439579, 460.3944608375876442, 2.386179269085898724 ) ) ;
#18424=EDGE_LOOP ( 'NONE', ( #86864, #39861, #7781, #63691 ) ) ;
#18434=CARTESIAN_POINT ( 'NONE',  ( 43.27801297234275779, 485.1608390498441850, -2.258185464242984608 ) ) ;
#18442=CARTESIAN_POINT ( 'NONE',  ( -32.68648381768493039, 486.2785269687576601, 6.276066868102866181 ) ) ;
#18454=CARTESIAN_POINT ( 'NONE',  ( 42.20540931547681396, 464.9254549434355681, 14.73500713293389985 ) ) ;
#18466=CARTESIAN_POINT ( 'NONE',  ( 42.61140200160144786, 465.9030374194822457, 13.21253569360410829 ) ) ;
#18479=CARTESIAN_POINT ( 'NONE',  ( 42.18756898894580587, 484.4522853017719513, -2.425645685620450909 ) ) ;
#18484=CARTESIAN_POINT ( 'NONE',  ( -27.80732017476346130, 308.5520240896025825, 11.27696741942652281 ) ) ;
#18489=TOROIDAL_SURFACE ( 'NONE', #78729, 7.999999999999983125, 1.000000000000000888 ) ;
#18509=CARTESIAN_POINT ( 'NONE',  ( -30.00000000000000000, 464.1571281261997797, 12.55969758983369822 ) ) ;
#18510=CARTESIAN_POINT ( 'NONE',  ( -42.89089171642230980, 462.3282028663734877, 4.511925770446329587 ) ) ;
#18512=CARTESIAN_POINT ( 'NONE',  ( 32.84970661036780371, 435.2659274799900686, 16.49359760587357826 ) ) ;
#18516=CARTESIAN_POINT ( 'NONE',  ( 1.128077836147720614, 302.8478239976497548, 9.936168295454386623 ) ) ;
#18532=FACE_OUTER_BOUND ( 'NONE', #74365, .T. ) ;
#18549=ORIENTED_EDGE ( 'NONE', *, *, #1841, .F. ) ;
#18561=DIRECTION ( 'NONE',  ( -0.2021170706129989947, -0.9793613683246955581, 0.000000000000000000 ) ) ;
#18570=CARTESIAN_POINT ( 'NONE',  ( -32.17646412119387378, 464.6980787822280377, 10.84896803612861227 ) ) ;
#18572=EDGE_CURVE ( 'NONE', #76499, #79477, #93813, .T. ) ;
#18576=DIRECTION ( 'NONE',  ( -0.2246406655633630400, 0.2919586099462053164, 0.9296756108737761481 ) ) ;
#18579=CARTESIAN_POINT ( 'NONE',  ( -43.59536836168519613, 485.3411848761405736, 3.528079522969483239 ) ) ;
#18583=CARTESIAN_POINT ( 'NONE',  ( -36.57468857844283860, 463.9816243198204688, 19.61678995109673806 ) ) ;
#18587=EDGE_CURVE ( 'NONE', #57189, #20836, #90346, .T. ) ;
#18593=CARTESIAN_POINT ( 'NONE',  ( -42.79755424932065466, 462.9502418795178755, 4.193817862666615603 ) ) ;
#18597=FACE_OUTER_BOUND ( 'NONE', #79359, .T. ) ;
#18601=CARTESIAN_POINT ( 'NONE',  ( -33.53347886086262264, 315.6494051702701427, -6.932048779613169565 ) ) ;
#18602=PLANE ( 'NONE',  #33599 ) ;
#18632=CARTESIAN_POINT ( 'NONE',  ( -37.39037644056123355, 437.8315769264678465, 4.421099621100916366 ) ) ;
#18663=CARTESIAN_POINT ( 'NONE',  ( 35.44354944450248723, 438.5272207030965887, 4.908769030776976905 ) ) ;
#18667=CARTESIAN_POINT ( 'NONE',  ( -28.70957337361108230, 297.0740850577855667, 2.420696489529333917 ) ) ;
#18670=CARTESIAN_POINT ( 'NONE',  ( -36.71681843521122346, 414.0170306961729239, 6.175275802599538899 ) ) ;
#18675=CARTESIAN_POINT ( 'NONE',  ( 45.48126212248870814, 413.7349014071057240, 8.309231847991947362 ) ) ;
#18688=CARTESIAN_POINT ( 'NONE',  ( 31.35596682365820342, 438.0939828603633828, 22.55458131664035548 ) ) ;
#18704=CARTESIAN_POINT ( 'NONE',  ( 37.58431281695580140, 369.0522562676452480, 4.070271502429146260 ) ) ;
#18714=CARTESIAN_POINT ( 'NONE',  ( 43.00000000000000000, 450.0000000000002274, 28.20242257375372219 ) ) ;
#18716=CARTESIAN_POINT ( 'NONE',  ( -30.00000000000000355, 488.8442721620238558, 4.433647275927455667 ) ) ;
#18728=CARTESIAN_POINT ( 'NONE',  ( -30.17217689282319881, 323.8004284941208653, 14.85062082350430046 ) ) ;
#18739=CARTESIAN_POINT ( 'NONE',  ( -31.04379474421510920, 362.9620158108600094, 22.40809114958081238 ) ) ;
#18747=CARTESIAN_POINT ( 'NONE',  ( 31.88024914789805564, 435.8785884660822489, 17.60509251234928030 ) ) ;
#18748=CARTESIAN_POINT ( 'NONE',  ( 31.56243845224520683, 299.8233007605157354, 11.05572696249486064 ) ) ;
#18751=ORIENTED_EDGE ( 'NONE', *, *, #92804, .T. ) ;
#18754=CARTESIAN_POINT ( 'NONE',  ( 38.23020739000291712, 310.6548857871646305, 5.705730873200064224 ) ) ;
#18762=CARTESIAN_POINT ( 'NONE',  ( 43.54152071275301239, 464.9591243512723509, 12.86066780444667579 ) ) ;
#18764=CARTESIAN_POINT ( 'NONE',  ( 2.477036783837432310, 294.8392925584320210, 1.934412769351830041 ) ) ;
#18767=EDGE_CURVE ( 'NONE', #85790, #84655, #94604, .T. ) ;
#18768=CIRCLE ( 'NONE', #70392, 0.9999999999999986677 ) ;
#18789=CARTESIAN_POINT ( 'NONE',  ( -36.66272501223257052, 491.8430924522253349, 12.58828741394581030 ) ) ;
#18811=CARTESIAN_POINT ( 'NONE',  ( 32.82691535583474973, 485.1045372766795367, 1.724905475515037701 ) ) ;
#18812=ORIENTED_EDGE ( 'NONE', *, *, #87659, .T. ) ;
#18813=EDGE_CURVE ( 'NONE', #62559, #37271, #103973, .T. ) ;
#18820=EDGE_LOOP ( 'NONE', ( #74209, #53660, #865, #20708, #86154, #47691 ) ) ;
#18824=CARTESIAN_POINT ( 'NONE',  ( 26.43220986894085911, 308.0179851418885164, 10.90514003825779099 ) ) ;
#18833=CARTESIAN_POINT ( 'NONE',  ( -30.35537264529554946, 338.7115663565144246, 18.05293407820170515 ) ) ;
#18836=CARTESIAN_POINT ( 'NONE',  ( -44.11327388758688528, 464.4313852428373934, 9.822198357558601600 ) ) ;
#18839=ORIENTED_EDGE ( 'NONE', *, *, #10442, .F. ) ;
#18855=ADVANCED_FACE ( 'NONE', ( #76302 ), #60933, .F. ) ;
#18856=CARTESIAN_POINT ( 'NONE',  ( 37.54559764570182523, 464.1143081516207189, 19.43664670202678835 ) ) ;
#18859=ORIENTED_EDGE ( 'NONE', *, *, #81367, .F. ) ;
#18861=CARTESIAN_POINT ( 'NONE',  ( -46.00000000000000000, 436.0273486662516689, 12.60673985408120323 ) ) ;
#18873=CARTESIAN_POINT ( 'NONE',  ( -21.91220694774618849, 304.0706505179387023, -9.953496567762948999 ) ) ;
#18880=ORIENTED_EDGE ( 'NONE', *, *, #91198, .F. ) ;
#18886=CARTESIAN_POINT ( 'NONE',  ( -28.87333700207125986, 311.5295170219202419, 12.02128803619848263 ) ) ;
#18900=CARTESIAN_POINT ( 'NONE',  ( -32.95589646111152149, 464.8957215206404499, 10.75300444715534987 ) ) ;
#18902=CARTESIAN_POINT ( 'NONE',  ( 13.16264097910227981, 304.5561373339386932, 8.874147965172166863 ) ) ;
#18915=B_SPLINE_CURVE_WITH_KNOTS ( 'NONE', 3,
 ( #97125, #54523, #15147, #96081 ),
 .UNSPECIFIED., .F., .F.,
 ( 4, 4 ),
 ( 0.0007388461703411279557, 0.02697940549969501944 ),
 .UNSPECIFIED. ) ;
#18916=CARTESIAN_POINT ( 'NONE',  ( 0.5082004253310246078, 295.8543628272474280, -10.00017741440575669 ) ) ;
#18917=CARTESIAN_POINT ( 'NONE',  ( 35.76379064120181539, 307.0162303970107587, 12.81051142610679960 ) ) ;
#18918=FACE_BOUND ( 'NONE', #1463, .T. ) ;
#18931=CARTESIAN_POINT ( 'NONE',  ( 9.881544152755356691, 294.6462802181998200, 1.569702982030937610 ) ) ;
#18932=CARTESIAN_POINT ( 'NONE',  ( -43.47539510892337944, 487.0683238468439527, 3.561594968384696802 ) ) ;
#18940=CARTESIAN_POINT ( 'NONE',  ( -34.16642289233710983, 463.8422268500497125, 18.98106911353875148 ) ) ;
#18941=CARTESIAN_POINT ( 'NONE',  ( 35.59667163540026280, 463.9592197885497171, -0.04846191499040426731 ) ) ;
#18942=CARTESIAN_POINT ( 'NONE',  ( 39.17204790861331531, 459.8623611124623949, 1.900463024344650087 ) ) ;
#18952=CARTESIAN_POINT ( 'NONE',  ( -19.53131398207814939, 303.7300551578738919, -10.02587845849555492 ) ) ;
#18986=B_SPLINE_CURVE_WITH_KNOTS ( 'NONE', 3,
 ( #104665, #45389, #30817, #36793, #69660, #61583, #94475, #20633, #53473, #86393, #78270, #4382 ),
 .UNSPECIFIED., .F., .F.,
 ( 4, 2, 2, 2, 2, 4 ),
 ( 2.255140518769849223E-17, 0.001518988062909442825, 0.002278482094364125531, 0.003037976125818808455, 0.004556964188728219838, 0.006075952251637632522 ),
 .UNSPECIFIED. ) ;
#19002=FACE_OUTER_BOUND ( 'NONE', #26650, .T. ) ;
#19005=CARTESIAN_POINT ( 'NONE',  ( -19.73463816634111012, 304.7971333121958537, 8.925379062039116462 ) ) ;
#19019=CARTESIAN_POINT ( 'NONE',  ( 43.04469050570450150, 434.7734435962914290, 9.248231035223298591 ) ) ;
#19020=CARTESIAN_POINT ( 'NONE',  ( 43.71037717921926458, 462.3391554988761527, 4.824299547763559737 ) ) ;
#19021=CARTESIAN_POINT ( 'NONE',  ( 22.71376002812208839, 304.4529191814661431, 10.06675239557364065 ) ) ;
#19035=CARTESIAN_POINT ( 'NONE',  ( -32.15166163075724626, 486.0589784586661040, 5.199393881400821371 ) ) ;
#19049=CARTESIAN_POINT ( 'NONE',  ( -42.08762648273019380, 487.0030674539067945, 9.106351919860287580 ) ) ;
#19051=DIRECTION ( 'NONE',  ( 0.000000000000000000, 0.000000000000000000, 1.000000000000000000 ) ) ;
#19056=( BOUNDED_SURFACE ( )  B_SPLINE_SURFACE ( 3, 2, ( 
 ( #13455, #70653, #46892 ),
 ( #45849, #21084, #30752 ),
 ( #39879, #88958, #13987 ),
 ( #72239, #78722, #5895 ) ),
 .UNSPECIFIED., .F., .F., .F. ) 
 B_SPLINE_SURFACE_WITH_KNOTS ( ( 4, 4 ),
 ( 3, 3 ),
 ( 0.1191486731993773723, 0.1451922720400707911 ),
 ( 0.000000000000000000, 0.6299180599692617566 ),
 .UNSPECIFIED. ) 
 GEOMETRIC_REPRESENTATION_ITEM ( )  RATIONAL_B_SPLINE_SURFACE ( (
 ( 1.000000000000000000, 0.8155016339198950526, 0.8634409734971468797),
 ( 1.000000000000000000, 0.8155019444343304391, 0.8634412033287162114),
 ( 1.000000000000000000, 0.8155018689791531106, 0.8634411474795193886),
 ( 1.000000000000000000, 0.8155015613424223542, 0.8634409197779229217) ) ) 
 REPRESENTATION_ITEM ( '' )  SURFACE ( )  );
#19062=CARTESIAN_POINT ( 'NONE',  ( 34.86931356687689032, 472.8464800566460440, 16.94524670509526132 ) ) ;
#19067=CARTESIAN_POINT ( 'NONE',  ( 31.55511120193260055, 436.6792952284608873, 19.27130410701429852 ) ) ;
#19072=CARTESIAN_POINT ( 'NONE',  ( -45.49982102694234953, 388.3127959276886827, 7.886590035822850453 ) ) ;
#19086=DIRECTION ( 'NONE',  ( 1.000000000000000000, 0.000000000000000000, 0.000000000000000000 ) ) ;
#19109=CARTESIAN_POINT ( 'NONE',  ( 33.09767504420651818, 317.8536043559706741, -6.616321532221737911 ) ) ;
#19116=CARTESIAN_POINT ( 'NONE',  ( 40.95645226493660118, 436.0015890305569428, 6.362679593776062070 ) ) ;
#19129=VERTEX_POINT ( 'NONE', #69599 ) ;
#19131=DIRECTION ( 'NONE',  ( 0.000000000000000000, -0.9540597841379402366, 0.2996163017772344728 ) ) ;
#19132=CARTESIAN_POINT ( 'NONE',  ( 11.72694920408448560, 302.5954528286877689, -10.05449594607857655 ) ) ;
#19138=SURFACE_STYLE_USAGE ( .BOTH. , #20747 ) ;
#19143=AXIS2_PLACEMENT_3D ( 'NONE', #80221, #6325, #62472 ) ;
#19149=DIRECTION ( 'NONE',  ( -1.000000000000000000, -0.000000000000000000, -0.000000000000000000 ) ) ;
#19153=CARTESIAN_POINT ( 'NONE',  ( -37.72597192858580684, 305.1524505036002211, -7.625521618108728639 ) ) ;
#19156=CARTESIAN_POINT ( 'NONE',  ( -13.16254534550195565, 304.5561388177458184, 8.874148279916250104 ) ) ;
#19184=CARTESIAN_POINT ( 'NONE',  ( -37.29743189576421258, 437.4067884073531332, 4.451016994673306471 ) ) ;
#19187=CARTESIAN_POINT ( 'NONE',  ( 33.77559172535811172, 464.7834715296606873, 7.192701217093182997 ) ) ;
#19202=CARTESIAN_POINT ( 'NONE',  ( 46.00000000000004263, 436.1058985003094222, 16.82352493621293377 ) ) ;
#19215=CARTESIAN_POINT ( 'NONE',  ( -42.16858620285800185, 461.4629983908308191, 3.513115262080999557 ) ) ;
#19221=CARTESIAN_POINT ( 'NONE',  ( -42.11927462130235966, 344.1102093767603947, 13.55314436600152739 ) ) ;
#19229=CARTESIAN_POINT ( 'NONE',  ( 23.58450237658830417, 303.4694747804686017, -9.867290210144552987 ) ) ;
#19230=CARTESIAN_POINT ( 'NONE',  ( 43.74855578046756222, 328.6220886837048170, -1.765109843966993441 ) ) ;
#19231=SHAPE_REPRESENTATION ( '4. Handle', ( #10728 ), #60740 ) ;
#19241=CARTESIAN_POINT ( 'NONE',  ( 43.81783411079661050, 329.5522331351167509, -1.551972439396806402 ) ) ;
#19246=CIRCLE ( 'NONE', #62322, 15.00000000000000711 ) ;
#19248=CARTESIAN_POINT ( 'NONE',  ( 31.29338602784115864, 439.6455612451725870, 23.30856287163057772 ) ) ;
#19285=CARTESIAN_POINT ( 'NONE',  ( -32.01437930851541580, 362.7125307742095970, 22.60227621942590304 ) ) ;
#19289=ORIENTED_EDGE ( 'NONE', *, *, #30933, .F. ) ;
#19290=CARTESIAN_POINT ( 'NONE',  ( -31.99294114632805019, 464.8457910465705822, 12.87241426108672826 ) ) ;
#19304=CARTESIAN_POINT ( 'NONE',  ( 25.78003121851679680, 295.8949495087512673, 2.161690327135773693 ) ) ;
#19313=EDGE_LOOP ( 'NONE', ( #61054, #37164, #27980, #29933 ) ) ;
#19320=PRODUCT_DEFINITION ( 'UNKNOWN', '', #25007, #99571 ) ;
#19333=AXIS2_PLACEMENT_3D ( 'NONE', #89246, #95744, #14272 ) ;
#19336=CARTESIAN_POINT ( 'NONE',  ( 36.63387181268254977, 490.9973753891291040, 12.47313570402020666 ) ) ;
#19340=CARTESIAN_POINT ( 'NONE',  ( -37.51625577700188074, 491.7333577044544768, 12.51656167145504384 ) ) ;
#19352=CARTESIAN_POINT ( 'NONE',  ( 40.17970824403359842, 485.1790858365317263, -4.313947164402517132 ) ) ;
#19353=ORIENTED_EDGE ( 'NONE', *, *, #98620, .T. ) ;
#19368=CARTESIAN_POINT ( 'NONE',  ( 23.79145413011031351, 304.9699511662212785, 10.18164519790058442 ) ) ;
#19369=( BOUNDED_SURFACE ( )  B_SPLINE_SURFACE ( 3, 2, ( 
 ( #20608, #3298, #60498 ),
 ( #59424, #69635, #27618 ),
 ( #11910, #61020, #44839 ),
 ( #92829, #51835, #85834 ),
 ( #93381, #52367, #77726 ),
 ( #34641, #18442, #85278 ),
 ( #100920, #51298, #84217 ),
 ( #68027, #36769, #84750 ) ),
 .UNSPECIFIED., .F., .F., .F. ) 
 B_SPLINE_SURFACE_WITH_KNOTS ( ( 4, 2, 2, 4 ),
 ( 3, 3 ),
 ( 2.732189474663471174E-17, 0.002319727980540720394, 0.003479591970811066713, 0.004639455961081413032 ),
 ( 0.000000000000000000, 1.000000000000000000 ),
 .UNSPECIFIED. ) 
 GEOMETRIC_REPRESENTATION_ITEM ( )  RATIONAL_B_SPLINE_SURFACE ( (
 ( 1.000000000000000000, 0.8162384603571204433, 1.000000000000000000),
 ( 1.000000000000000000, 0.8233098591466496696, 1.000000000000000000),
 ( 1.000000000000000000, 0.8247006568295612849, 1.000000000000000000),
 ( 1.000000000000000000, 0.8207129887246857880, 1.000000000000000000),
 ( 1.000000000000000000, 0.8182997519107459983, 1.000000000000000000),
 ( 1.000000000000000000, 0.8111528056794476971, 1.000000000000000000),
 ( 1.000000000000000000, 0.8064385712637164305, 1.000000000000000000),
 ( 1.000000000000000000, 0.8001746426091337350, 1.000000000000000000) ) ) 
 REPRESENTATION_ITEM ( '' )  SURFACE ( )  );
#19371=DIRECTION ( 'NONE',  ( -0.2517716543986441846, 0.000000000000000000, 0.9677866676294779591 ) ) ;
#19378=CARTESIAN_POINT ( 'NONE',  ( -35.76482652855951017, 405.2378813769876729, 6.148826621638260548 ) ) ;
#19381=FACE_OUTER_BOUND ( 'NONE', #20191, .T. ) ;
#19388=CARTESIAN_POINT ( 'NONE',  ( -4.023953349588704320, 300.5162199157759915, -10.00978861085819460 ) ) ;
#19400=CARTESIAN_POINT ( 'NONE',  ( 43.22624402987835879, 434.6924416827904452, 9.644670084733055759 ) ) ;
#19402=CARTESIAN_POINT ( 'NONE',  ( -30.00000000000000000, 450.0000000000002274, 13.20242257375370976 ) ) ;
#19409=ORIENTED_EDGE ( 'NONE', *, *, #20951, .T. ) ;
#19416=DIRECTION ( 'NONE',  ( -1.000000000000000000, 0.000000000000000000, 0.000000000000000000 ) ) ;
#19418=EDGE_CURVE ( 'NONE', #66185, #16979, #81165, .T. ) ;
#19420=CARTESIAN_POINT ( 'NONE',  ( -43.81062608880512244, 434.3289934330967981, 12.63519120573293542 ) ) ;
#19428=CARTESIAN_POINT ( 'NONE',  ( -32.45536069360919385, 439.3279843089443943, 23.70254088333128450 ) ) ;
#19430=CARTESIAN_POINT ( 'NONE',  ( -32.23866588128408495, 319.2897111165075898, -5.491189000399069542 ) ) ;
#19431=CARTESIAN_POINT ( 'NONE',  ( -29.01992505677934275, 312.0266740597124340, 12.14665302515488143 ) ) ;
#19437=CIRCLE ( 'NONE', #40018, 0.9999999999999965583 ) ;
#19446=CARTESIAN_POINT ( 'NONE',  ( 46.00000000000000000, 500.0000000000002274, 0.000000000000000000 ) ) ;
#19455=CARTESIAN_POINT ( 'NONE',  ( 7.886225516951638426, 296.0473068317901379, -10.02775466922195413 ) ) ;
#19465=CARTESIAN_POINT ( 'NONE',  ( -42.76230833568499179, 461.1825766694569211, 3.198895819599639978 ) ) ;
#19469=ORIENTED_EDGE ( 'NONE', *, *, #53088, .T. ) ;
#19470=CARTESIAN_POINT ( 'NONE',  ( 9.789044728060087408, 294.6486233851415477, -2.043184600578025201 ) ) ;
#19480=CARTESIAN_POINT ( 'NONE',  ( 38.98764044590114963, 460.2978347093389289, 2.283752696535007232 ) ) ;
#19481=CARTESIAN_POINT ( 'NONE',  ( -35.23234612623826223, 435.7070084737468392, 6.197831874882719916 ) ) ;
#19486=EDGE_LOOP ( 'NONE', ( #98849, #19795, #12833, #57901 ) ) ;
#19522=CARTESIAN_POINT ( 'NONE',  ( -29.01988888469873018, 321.8047804620298393, 14.12772110426748284 ) ) ;
#19534=CARTESIAN_POINT ( 'NONE',  ( 42.69811214730273718, 434.9611672192513652, 18.34625614733210242 ) ) ;
#19542=CARTESIAN_POINT ( 'NONE',  ( 42.18756898894580587, 484.4522853017719513, -2.425645685620450909 ) ) ;
#19558=AXIS2_PLACEMENT_3D ( 'NONE', #90471, #32793, #65132 ) ;
#19570=CARTESIAN_POINT ( 'NONE',  ( -32.92521947952602090, 485.8269030686984706, 5.191998501979409930 ) ) ;
#19572=EDGE_CURVE ( 'NONE', #29309, #99399, #74307, .T. ) ;
#19583=CARTESIAN_POINT ( 'NONE',  ( -3.042178694127982475, 300.3091518900824326, 9.528975082528521767 ) ) ;
#19589=DIRECTION ( 'NONE',  ( 0.2270551762890646308, 0.1092888915761187629, 0.9677302749725282816 ) ) ;
#19603=CARTESIAN_POINT ( 'NONE',  ( 32.82178245385870952, 434.5289685218765499, 16.70197725476643313 ) ) ;
#19612=DIRECTION ( 'NONE',  ( 0.000000000000000000, -0.8813945903476978483, 0.4723807533185641061 ) ) ;
#19613=B_SPLINE_CURVE_WITH_KNOTS ( 'NONE', 3,
 ( #19534, #83672, #43235, #9780 ),
 .UNSPECIFIED., .F., .F.,
 ( 4, 4 ),
 ( 1.868354362588067661E-17, 0.001851782051266549116 ),
 .UNSPECIFIED. ) ;
#19616=AXIS2_PLACEMENT_3D ( 'NONE', #33791, #74738, #67213 ) ;
#19618=CARTESIAN_POINT ( 'NONE',  ( -19.96162532426521352, 302.8116070918646301, 9.928455558879880627 ) ) ;
#19652=EDGE_CURVE ( 'NONE', #26711, #66185, #54408, .T. ) ;
#19664=CARTESIAN_POINT ( 'NONE',  ( -35.69739812508499455, 430.4862580793411553, 4.964222856391316441 ) ) ;
#19666=CARTESIAN_POINT ( 'NONE',  ( -43.09948196127317033, 484.9577458347782226, -0.8563396247089051228 ) ) ;
#19667=CARTESIAN_POINT ( 'NONE',  ( 32.65804572401750505, 465.7880960007718727, 12.84163515238255826 ) ) ;
#19668=CARTESIAN_POINT ( 'NONE',  ( -34.63438812788589871, 463.6460534741191282, 19.43326544948470769 ) ) ;
#19672=CARTESIAN_POINT ( 'NONE',  ( 17.35892867067943257, 294.5707697310705839, -10.05973541782409342 ) ) ;
#19676=ADVANCED_FACE ( 'NONE', ( #58596 ), #58387, .F. ) ;
#19684=CARTESIAN_POINT ( 'NONE',  ( -38.86088754547002111, 310.5264066565887333, 1.725813668771058351 ) ) ;
#19685=DIRECTION ( 'NONE',  ( 0.000000000000000000, 0.000000000000000000, -1.000000000000000000 ) ) ;
#19714=DIRECTION ( 'NONE',  ( -1.000000000000000000, 0.000000000000000000, 0.000000000000000000 ) ) ;
#19717=CYLINDRICAL_SURFACE ( 'NONE', #71141, 15.00000000000000711 ) ;
#19722=CIRCLE ( 'NONE', #60952, 3.000000000000000000 ) ;
#19731=EDGE_CURVE ( 'NONE', #67017, #5193, #50291, .T. ) ;
#19744=B_SPLINE_SURFACE_WITH_KNOTS ( 'NONE', 1, 3, ( 
 ( #60428, #93306, #61483, #100317, #20539, #59353, #101915, #36701 ),
 ( #69564, #11293, #60944, #76569, #26478, #2682, #36173, #67961 ) ),
 .UNSPECIFIED., .F., .F., .F.,
 ( 2, 2 ),
 ( 4, 2, 2, 4 ),
 ( 0.000000000000000000, 1.000000000000000000 ),
 ( 0.000000000000000000, 0.04450745600790868145, 0.06676118401186306728, 0.08901491201581737678 ),
 .UNSPECIFIED. ) ;
#19745=CARTESIAN_POINT ( 'NONE',  ( -33.70641995125998136, 301.3514140349557238, 3.410652409991425049 ) ) ;
#19754=CARTESIAN_POINT ( 'NONE',  ( 25.63523488843089737, 295.8087761051020834, -1.794239459488054633 ) ) ;
#19755=CARTESIAN_POINT ( 'NONE',  ( 42.09210974227526947, 317.4093497706929270, -4.557617623460385126 ) ) ;
#19762=VERTEX_POINT ( 'NONE', #64445 ) ;
#19770=CARTESIAN_POINT ( 'NONE',  ( 39.80833478160801064, 313.8620429462365564, 2.567395400256364812 ) ) ;
#19773=CARTESIAN_POINT ( 'NONE',  ( -3.587928128302542596, 304.8518027750386636, 9.936999415048941131 ) ) ;
#19790=CARTESIAN_POINT ( 'NONE',  ( -33.00000000000000000, 500.0000000000002274, 0.000000000000000000 ) ) ;
#19791=CARTESIAN_POINT ( 'NONE',  ( -43.03357534758770697, 463.2291678140051658, 4.675918524147543387 ) ) ;
#19795=ORIENTED_EDGE ( 'NONE', *, *, #5532, .T. ) ;
#19803=CARTESIAN_POINT ( 'NONE',  ( -23.71062927693709099, 304.9117331807381106, 10.16837944912345648 ) ) ;
#19807=EDGE_LOOP ( 'NONE', ( #91930, #4123, #14845, #49665 ) ) ;
#19814=EDGE_CURVE ( 'NONE', #7327, #66563, #85406, .T. ) ;
#19823=DIRECTION ( 'NONE',  ( -1.000000000000000000, 0.000000000000000000, 0.000000000000000000 ) ) ;
#19824=CARTESIAN_POINT ( 'NONE',  ( 22.31492703060326477, 303.2773340566886304, 10.02844635004729135 ) ) ;
#19831=CARTESIAN_POINT ( 'NONE',  ( -30.00000000000000000, 500.0000000000002274, 0.000000000000000000 ) ) ;
#19832=CARTESIAN_POINT ( 'NONE',  ( 22.76441849112663007, 295.0913517417525895, 1.987917119805708843 ) ) ;
#19858=MANIFOLD_SOLID_BREP ( 'Cut-Extrude1', #34330 ) ;
#19860=CARTESIAN_POINT ( 'NONE',  ( 19.70764564238367100, 304.7954121406193053, 9.925013215726757210 ) ) ;
#19883=EDGE_LOOP ( 'NONE', ( #54757, #74515, #6207, #53340 ) ) ;
#19890=ORIENTED_EDGE ( 'NONE', *, *, #52061, .T. ) ;
#19892=ORIENTED_EDGE ( 'NONE', *, *, #41496, .T. ) ;
#19894=CARTESIAN_POINT ( 'NONE',  ( 22.39167605158363372, 305.3927309438643078, 9.053801646461055341 ) ) ;
#19909=ORIENTED_EDGE ( 'NONE', *, *, #103082, .T. ) ;
#19917=CARTESIAN_POINT ( 'NONE',  ( -6.930002047141902821, 302.1778385080101543, -10.02505617572823304 ) ) ;
#19918=CARTESIAN_POINT ( 'NONE',  ( 0.000000000000000000, 0.000000000000000000, 0.000000000000000000 ) ) ;
#19947=CARTESIAN_POINT ( 'NONE',  ( 41.62074773851009724, 334.2059636480821609, 11.44767655643080140 ) ) ;
#19956=CARTESIAN_POINT ( 'NONE',  ( -33.07276483573514980, 438.9325140356083352, 23.89537236861354685 ) ) ;
#19958=CARTESIAN_POINT ( 'NONE',  ( -26.15748752718828385, 306.9073039913806156, -8.546226797207475911 ) ) ;
#19959=CARTESIAN_POINT ( 'NONE',  ( -40.84349315627966348, 325.1007658372994911, 9.312971402044151858 ) ) ;
#19963=ORIENTED_EDGE ( 'NONE', *, *, #47214, .T. ) ;
#19973=CARTESIAN_POINT ( 'NONE',  ( 18.09733584172112231, 304.6346571588649681, 8.890781977549927717 ) ) ;
#19977=AXIS2_PLACEMENT_3D ( 'NONE', #50367, #18576, #19131 ) ;
#19984=CARTESIAN_POINT ( 'NONE',  ( 4.544092624809295877, 294.7929985550215974, -8.922686206446940105 ) ) ;
#19986=CARTESIAN_POINT ( 'NONE',  ( 22.91651842568168362, 295.0901107613288445, -9.949346074078583513 ) ) ;
#19994=CIRCLE ( 'NONE', #71594, 3.000000000000024425 ) ;
#19998=CIRCLE ( 'NONE', #33753, 5.000000000000003553 ) ;
#19999=CARTESIAN_POINT ( 'NONE',  ( -43.00000000000000000, 461.4080316921935605, 3.462976341553817949 ) ) ;
#20007=ORIENTED_EDGE ( 'NONE', *, *, #67614, .T. ) ;
#20008=DIRECTION ( 'NONE',  ( 0.000000000000000000, 0.000000000000000000, -1.000000000000000000 ) ) ;
#20012=CARTESIAN_POINT ( 'NONE',  ( 30.00000000000000000, 488.6481008951278113, 3.890293910850189274 ) ) ;
#20050=CARTESIAN_POINT ( 'NONE',  ( 27.18908553330205180, 296.5274986157688772, 10.30015177545897842 ) ) ;
#20052=CARTESIAN_POINT ( 'NONE',  ( -31.00389226249483698, 502.9289871839745842, 8.047326149841639520 ) ) ;
#20060=CARTESIAN_POINT ( 'NONE',  ( -42.20041562234357002, 435.2369744135583574, 7.788607701745487333 ) ) ;
#20073=CARTESIAN_POINT ( 'NONE',  ( -32.82923042684467418, 434.9827582799806009, 12.60815599139151111 ) ) ;
#20075=CARTESIAN_POINT ( 'NONE',  ( 42.61140200160144076, 465.9030374194823594, 13.21253569360416691 ) ) ;
#20080=ADVANCED_FACE ( 'NONE', ( #25476 ), #63121, .F. ) ;
#20082=ORIENTED_EDGE ( 'NONE', *, *, #50364, .T. ) ;
#20089=CARTESIAN_POINT ( 'NONE',  ( 43.02661387979727436, 465.7449615347604208, 11.43319743843670544 ) ) ;
#20104=DIRECTION ( 'NONE',  ( 0.000000000000000000, 0.000000000000000000, 1.000000000000000000 ) ) ;
#20115=ADVANCED_FACE ( 'NONE', ( #42143 ), #92088, .T. ) ;
#20117=CARTESIAN_POINT ( 'NONE',  ( 16.25962063600091412, 302.5670250583751795, -10.06049463409325107 ) ) ;
#20119=DIRECTION ( 'NONE',  ( 1.000000000000000000, -0.000000000000000000, -0.000000000000000000 ) ) ;
#20124=ADVANCED_FACE ( 'NONE', ( #48629 ), #91775, .F. ) ;
#20127=B_SPLINE_CURVE_WITH_KNOTS ( 'NONE', 3,
 ( #69025, #10227, #26463, #52277 ),
 .UNSPECIFIED., .F., .F.,
 ( 4, 4 ),
 ( 0.000000000000000000, 0.0002485318720385933230 ),
 .UNSPECIFIED. ) ;
#20129=CARTESIAN_POINT ( 'NONE',  ( 36.01601968523547015, 463.8931034503634692, 20.04842029783048929 ) ) ;
#20142=EDGE_CURVE ( 'NONE', #93551, #22579, #12031, .T. ) ;
#20152=CARTESIAN_POINT ( 'NONE',  ( -32.00946877229060306, 486.4631725509864850, 6.108882930589409455 ) ) ;
#20166=EDGE_LOOP ( 'NONE', ( #92144, #20316, #50562, #64207, #27230, #7143 ) ) ;
#20175=CARTESIAN_POINT ( 'NONE',  ( 32.12958771267400948, 464.7275665249413237, 11.12424126545837133 ) ) ;
#20185=CARTESIAN_POINT ( 'NONE',  ( 38.69545490169056023, 437.5444261471850496, 4.829293893634224233 ) ) ;
#20191=EDGE_LOOP ( 'NONE', ( #52124, #7045, #68536, #46885 ) ) ;
#20196=CARTESIAN_POINT ( 'NONE',  ( -43.39367449997198634, 484.9145775485452532, -0.08602995367264502924 ) ) ;
#20198=DIRECTION ( 'NONE',  ( -1.000000000000000000, -0.000000000000000000, -0.000000000000000000 ) ) ;
#20205=CARTESIAN_POINT ( 'NONE',  ( 51.01037695545453232, 450.0000000000002274, 13.20242257375370976 ) ) ;
#20206=CARTESIAN_POINT ( 'NONE',  ( 32.82691535583475684, 485.1045372766794799, 1.724905475515027264 ) ) ;
#20226=CARTESIAN_POINT ( 'NONE',  ( 32.83963058357245046, 487.9259959563239022, 4.912446691208849359 ) ) ;
#20231=B_SPLINE_CURVE_WITH_KNOTS ( 'NONE', 3,
 ( #45697, #78059, #44649, #85092, #102335, #76454, #44105, #37110, #19352, #54283, #28483, #4176, #2563, #20942 ),
 .UNSPECIFIED., .F., .F.,
 ( 4, 2, 2, 2, 2, 2, 4 ),
 ( 2.934965519869990483E-17, 0.0003840169304677532383, 0.0007680338609354772032, 0.001152050791403200951, 0.001536067721870924916, 0.002304101582806372412, 0.003072135443741819474 ),
 .UNSPECIFIED. ) ;
#20246=ADVANCED_FACE ( 'NONE', ( #101974 ), #74723, .F. ) ;
#20252=CARTESIAN_POINT ( 'NONE',  ( -36.97265860262993442, 437.4722588954306843, 4.366279915526011024 ) ) ;
#20253=PLANE ( 'NONE',  #56806 ) ;
#20264=ORIENTED_EDGE ( 'NONE', *, *, #17966, .T. ) ;
#20265=B_SPLINE_CURVE_WITH_KNOTS ( 'NONE', 3,
 ( #106728, #32878, #65753, #98634 ),
 .UNSPECIFIED., .F., .F.,
 ( 4, 4 ),
 ( 1.734723475976807094E-18, 0.0001964870061279678343 ),
 .UNSPECIFIED. ) ;
#20271=DIRECTION ( 'NONE',  ( -0.5516836157922502260, -0.3133352674422915096, 0.7729593768389489972 ) ) ;
#20290=ORIENTED_EDGE ( 'NONE', *, *, #63763, .T. ) ;
#20308=CARTESIAN_POINT ( 'NONE',  ( 37.12174742129960947, 348.0611237983079036, 0.6179234092325384120 ) ) ;
#20309=CARTESIAN_POINT ( 'NONE',  ( 43.55333112596304090, 465.2342844084865874, 9.238213423009668190 ) ) ;
#20312=B_SPLINE_CURVE_WITH_KNOTS ( 'NONE', 3,
 ( #5922, #22684, #105163, #38850 ),
 .UNSPECIFIED., .F., .F.,
 ( 4, 4 ),
 ( 5.386030058153475923E-17, 0.0001964870061225198268 ),
 .UNSPECIFIED. ) ;
#20314=CARTESIAN_POINT ( 'NONE',  ( 31.36162942603217019, 438.6301898249564601, 22.30086042418462711 ) ) ;
#20316=ORIENTED_EDGE ( 'NONE', *, *, #14379, .T. ) ;
#20318=CIRCLE ( 'NONE', #37472, 5.000000000000000888 ) ;
#20333=CARTESIAN_POINT ( 'NONE',  ( 33.50665702490327647, 462.9566363596913448, 5.621882783608548984 ) ) ;
#20348=( BOUNDED_SURFACE ( )  B_SPLINE_SURFACE ( 3, 2, ( 
 ( #21218, #29310, #37403 ),
 ( #54048, #4462, #53016 ),
 ( #62200, #61669, #46510 ),
 ( #70264, #95086, #86993 ) ),
 .UNSPECIFIED., .F., .F., .T. ) 
 B_SPLINE_SURFACE_WITH_KNOTS ( ( 4, 4 ),
 ( 3, 3 ),
 ( 1.934216675714139910E-16, 0.0007499009164755209749 ),
 ( 0.000000000000000000, 1.000000000000000000 ),
 .UNSPECIFIED. ) 
 GEOMETRIC_REPRESENTATION_ITEM ( )  RATIONAL_B_SPLINE_SURFACE ( (
 ( 1.000000000000000000, 0.7301269460247277188, 1.000000000000000000),
 ( 1.000000000000000000, 0.7327382575064924630, 1.000000000000000000),
 ( 1.000000000000000000, 0.7350727526496084741, 1.000000000000000000),
 ( 1.000000000000000000, 0.7370557512816053869, 1.000000000000000000) ) ) 
 REPRESENTATION_ITEM ( '' )  SURFACE ( )  );
#20361=EDGE_CURVE ( 'NONE', #86195, #72492, #10674, .T. ) ;
#20368=CARTESIAN_POINT ( 'NONE',  ( -41.31161337382455656, 484.8232235214489378, -3.619187650532241562 ) ) ;
#20370=CARTESIAN_POINT ( 'NONE',  ( 24.65765876571508031, 295.6277211468342898, 10.10369318520652193 ) ) ;
#20378=EDGE_CURVE ( 'NONE', #103206, #91640, #7246, .T. ) ;
#20389=CARTESIAN_POINT ( 'NONE',  ( 44.28985889617170102, 463.6758032475478899, 7.532946519189393619 ) ) ;
#20412=ORIENTED_EDGE ( 'NONE', *, *, #99802, .F. ) ;
#20413=CARTESIAN_POINT ( 'NONE',  ( 39.65885301127772067, 485.6927826267698833, -4.533530942913213124 ) ) ;
#20423=EDGE_CURVE ( 'NONE', #71461, #71251, #75059, .T. ) ;
#20436=ADVANCED_FACE ( 'NONE', ( #850 ), #95561, .T. ) ;
#20439=CARTESIAN_POINT ( 'NONE',  ( 22.75333575518925855, 305.5577985524777773, 10.09022899150792973 ) ) ;
#20465=ORIENTED_EDGE ( 'NONE', *, *, #27705, .T. ) ;
#20475=CIRCLE ( 'NONE', #39362, 15.00000000000001243 ) ;
#20493=CARTESIAN_POINT ( 'NONE',  ( 40.93034849641253459, 415.5868670752544176, 27.59989424832417626 ) ) ;
#20495=CARTESIAN_POINT ( 'NONE',  ( -43.80679553850465169, 434.9371637098606698, 12.86766421698907514 ) ) ;
#20503=CARTESIAN_POINT ( 'NONE',  ( -20.96340531204895186, 304.9350079645578262, -8.982323148433966509 ) ) ;
#20504=AXIS2_PLACEMENT_3D ( 'NONE', #55600, #95566, #87484 ) ;
#20505=CARTESIAN_POINT ( 'NONE',  ( -39.21858437040845757, 325.7412493439550758, 17.46750275458761692 ) ) ;
#20532=CARTESIAN_POINT ( 'NONE',  ( 8.984970058459877507, 294.6717433611685237, -4.394086705239145907 ) ) ;
#20539=CARTESIAN_POINT ( 'NONE',  ( -13.68764148674883430, 294.5450735065955996, 9.871802096439328267 ) ) ;
#20563=CARTESIAN_POINT ( 'NONE',  ( 9.819056950928633398, 294.6481068335447731, 1.893705519456528208 ) ) ;
#20566=ORIENTED_EDGE ( 'NONE', *, *, #91617, .T. ) ;
#20602=CARTESIAN_POINT ( 'NONE',  ( 35.59667163540026280, 463.9592197885497171, -0.04846191499040426731 ) ) ;
#20608=CARTESIAN_POINT ( 'NONE',  ( -32.28930913497459443, 488.2717154064632723, 9.213726894912742438 ) ) ;
#20618=CARTESIAN_POINT ( 'NONE',  ( -33.97359119245064107, 434.1099241184709285, 11.80501937577160732 ) ) ;
#20625=B_SPLINE_CURVE_WITH_KNOTS ( 'NONE', 3,
 ( #26231, #76317, #77396, #50438, #27297, #3510, #9995, #60699, #75794, #36451, #2429, #43437, #34842, #51514 ),
 .UNSPECIFIED., .F., .F.,
 ( 4, 2, 2, 2, 2, 2, 4 ),
 ( 0.000000000000000000, 0.0003608396711012821904, 0.0007216793422025643808, 0.001082519013303846409, 0.001443358684405128762, 0.002165038026607684143, 0.002886717368810240176 ),
 .UNSPECIFIED. ) ;
#20630=CARTESIAN_POINT ( 'NONE',  ( 32.12958771267400948, 464.7275665249413237, 11.12424126545837133 ) ) ;
#20633=CARTESIAN_POINT ( 'NONE',  ( 40.60713025163710910, 436.1947416310474637, 6.060763751012176570 ) ) ;
#20639=EDGE_LOOP ( 'NONE', ( #60036, #26389, #48259, #6310 ) ) ;
#20642=CARTESIAN_POINT ( 'NONE',  ( -46.00000000000000000, 462.6038693158056390, 6.978327855974978178 ) ) ;
#20645=CARTESIAN_POINT ( 'NONE',  ( -29.60697198811803688, 307.3530822094822952, -8.981721099768231298 ) ) ;
#20654=DIRECTION ( 'NONE',  ( 0.000000000000000000, 0.000000000000000000, 1.000000000000000000 ) ) ;
#20661=CARTESIAN_POINT ( 'NONE',  ( 15.42276584910590920, 294.5569213128695196, -2.062679874220467724 ) ) ;
#20667=CARTESIAN_POINT ( 'NONE',  ( 43.64534273044669277, 464.9151781295577734, 12.30378483073953966 ) ) ;
#20687=ADVANCED_FACE ( 'NONE', ( #66039 ), #81054, .F. ) ;
#20708=ORIENTED_EDGE ( 'NONE', *, *, #4616, .T. ) ;
#20716=CARTESIAN_POINT ( 'NONE',  ( -39.13466327772848530, 485.8437493838396790, -4.960055907049729207 ) ) ;
#20721=CARTESIAN_POINT ( 'NONE',  ( -44.12472801210821416, 485.7238370326489871, 3.975897585127424527 ) ) ;
#20726=CARTESIAN_POINT ( 'NONE',  ( 40.02090011478166076, 436.4865077410170784, 5.635628130754340326 ) ) ;
#20727=VERTEX_POINT ( 'NONE', #51970 ) ;
#20728=DIRECTION ( 'NONE',  ( -1.000000000000000000, -0.000000000000000000, -0.000000000000000000 ) ) ;
#20735=EDGE_CURVE ( 'NONE', #22409, #78525, #28824, .T. ) ;
#20741=CARTESIAN_POINT ( 'NONE',  ( -41.61741820144500537, 435.6127172585689777, 7.033059668058291969 ) ) ;
#20747=SURFACE_SIDE_STYLE ('',( #10978 ) ) ;
#20752=B_SPLINE_CURVE_WITH_KNOTS ( 'NONE', 3,
 ( #90095, #16198, #97638, #32949 ),
 .UNSPECIFIED., .F., .F.,
 ( 4, 4 ),
 ( 0.000000000000000000, 0.0002045283294089406535 ),
 .UNSPECIFIED. ) ;
#20762=CARTESIAN_POINT ( 'NONE',  ( 31.84798808520906022, 480.8473942020407321, 11.59524609927768957 ) ) ;
#20763=ORIENTED_EDGE ( 'NONE', *, *, #55871, .T. ) ;
#20785=CARTESIAN_POINT ( 'NONE',  ( 42.19179521601841287, 485.4956273777429487, -3.824025998174274577 ) ) ;
#20804=CARTESIAN_POINT ( 'NONE',  ( 46.00000000000000000, 438.3878896346934653, 16.22878885428544038 ) ) ;
#20816=CARTESIAN_POINT ( 'NONE',  ( 35.73709257329849720, 382.3453677267265221, 5.045156307748890789 ) ) ;
#20821=CARTESIAN_POINT ( 'NONE',  ( -32.23979701228631001, 314.7547567211047976, -7.398542135358657568 ) ) ;
#20823=CARTESIAN_POINT ( 'NONE',  ( 40.46549058525986453, 490.2743938847165737, 11.42162415461235447 ) ) ;
#20824=DIRECTION ( 'NONE',  ( 1.000000000000000000, 0.000000000000000000, 0.000000000000000000 ) ) ;
#20836=VERTEX_POINT ( 'NONE', #88082 ) ;
#20841=CARTESIAN_POINT ( 'NONE',  ( 37.50518029089035821, 362.5804478665973534, 3.197089636230608267 ) ) ;
#20842=CARTESIAN_POINT ( 'NONE',  ( 43.63213036654197197, 464.4895599185542210, 9.038982508271296012 ) ) ;
#20843=ORIENTED_EDGE ( 'NONE', *, *, #44168, .T. ) ;
#20845=CARTESIAN_POINT ( 'NONE',  ( 31.67687266298273130, 439.4050284403294881, 23.39876501491971439 ) ) ;
#20850=ADVANCED_FACE ( 'NONE', ( #39536 ), #88605, .F. ) ;
#20865=CARTESIAN_POINT ( 'NONE',  ( 35.23463026195637582, 462.2854383349875320, 4.568931904893218210 ) ) ;
#20884=DIRECTION ( 'NONE',  ( -1.000000000000000000, 0.000000000000000000, 0.000000000000000000 ) ) ;
#20897=CARTESIAN_POINT ( 'NONE',  ( -41.66301127302475749, 485.3863426732057746, -3.409513628938614982 ) ) ;
#20898=CARTESIAN_POINT ( 'NONE',  ( 28.51814700840726857, 297.3184951835715424, 10.47819064956899204 ) ) ;
#20899=CARTESIAN_POINT ( 'NONE',  ( 4.925903578703449526, 301.1861660590338943, -10.01402232597611608 ) ) ;
#20924=CARTESIAN_POINT ( 'NONE',  ( 33.26935678862407997, 435.1895192765533693, 10.58170431744235884 ) ) ;
#20930=CARTESIAN_POINT ( 'NONE',  ( 3.587928128302542596, 304.8518027750386636, 9.936999415048941131 ) ) ;
#20942=CARTESIAN_POINT ( 'NONE',  ( 41.46910480218704009, 484.7338956289814860, -3.418960549715446717 ) ) ;
#20951=EDGE_CURVE ( 'NONE', #58013, #457, #41819, .T. ) ;
#20955=ORIENTED_EDGE ( 'NONE', *, *, #57357, .F. ) ;
#20956=CARTESIAN_POINT ( 'NONE',  ( 32.88333705524289741, 439.7317646416726689, 24.13381181826147071 ) ) ;
#20963=CARTESIAN_POINT ( 'NONE',  ( 24.30353620171109341, 306.6619372981346032, 10.34251987938447748 ) ) ;
#20964=EDGE_LOOP ( 'NONE', ( #22639, #64641, #90698, #55674 ) ) ;
#20982=CARTESIAN_POINT ( 'NONE',  ( 39.68467815576448743, 459.8383127612376029, 1.879537633271029851 ) ) ;
#20999=CARTESIAN_POINT ( 'NONE',  ( 13.63130828375568981, 294.5445729804733901, -10.06530370901874072 ) ) ;
#21010=CARTESIAN_POINT ( 'NONE',  ( -39.86761651079807223, 459.8416857619844222, 1.882458089121660905 ) ) ;
#21020=CARTESIAN_POINT ( 'NONE',  ( -31.93573408248750312, 317.9195443334689344, -5.838035979257788277 ) ) ;
#21021=CARTESIAN_POINT ( 'NONE',  ( -39.62459902451224991, 316.6078743528785253, 7.208843829914820311 ) ) ;
#21030=CARTESIAN_POINT ( 'NONE',  ( 40.30492368078588328, 437.3365155501883237, 5.155601643837086634 ) ) ;
#21041=AXIS2_PLACEMENT_3D ( 'NONE', #23311, #16249, #64292 ) ;
#21045=CARTESIAN_POINT ( 'NONE',  ( 37.45944789261785957, 486.5137780151753759, 13.75061995631740963 ) ) ;
#21048=CARTESIAN_POINT ( 'NONE',  ( 9.218636978371788970, 294.6649786875626660, -3.878494680376622483 ) ) ;
#21051=CARTESIAN_POINT ( 'NONE',  ( -16.46333734837338270, 294.5649015166168283, 1.876035010524102820 ) ) ;
#21055=CARTESIAN_POINT ( 'NONE',  ( 46.00000000000000000, 488.2683853232034039, 2.802483919472203766 ) ) ;
#21057=CARTESIAN_POINT ( 'NONE',  ( 2.494577234427376227E-15, -18.92596047533412573, 20.36976895023282097 ) ) ;
#21084=CARTESIAN_POINT ( 'NONE',  ( -31.86301241941225726, 472.3478509189352508, 13.84919938057076294 ) ) ;
#21085=CARTESIAN_POINT ( 'NONE',  ( -33.00000000000000000, 488.6481008951270155, 3.890293910847612668 ) ) ;
#21088=FACE_OUTER_BOUND ( 'NONE', #57393, .T. ) ;
#21094=EDGE_CURVE ( 'NONE', #58946, #26193, #17008, .T. ) ;
#21098=VERTEX_POINT ( 'NONE', #101998 ) ;
#21112=CARTESIAN_POINT ( 'NONE',  ( -32.35336999986095208, 300.6590557721156642, 11.25190399080426751 ) ) ;
#21131=CARTESIAN_POINT ( 'NONE',  ( -33.06850474076788515, 435.0785904875464780, 15.57666385384312413 ) ) ;
#21144=CARTESIAN_POINT ( 'NONE',  ( 46.00000000000001421, 438.2677368034359233, 10.58177734929973290 ) ) ;
#21153=ORIENTED_EDGE ( 'NONE', *, *, #40644, .T. ) ;
#21160=CARTESIAN_POINT ( 'NONE',  ( -33.97150963885389530, 317.2836215396021089, -6.519267954480356231 ) ) ;
#21170=CARTESIAN_POINT ( 'NONE',  ( -9.678462853824605361, 294.6717994822394644, 2.536598382984742273 ) ) ;
#21171=CARTESIAN_POINT ( 'NONE',  ( 0.000000000000000000, 0.000000000000000000, -6.999999999999993783 ) ) ;
#21176=CARTESIAN_POINT ( 'NONE',  ( -30.00000000000000000, 488.7759337287078552, 4.253621113604353354 ) ) ;
#21178=ORIENTED_EDGE ( 'NONE', *, *, #95616, .F. ) ;
#21179=CARTESIAN_POINT ( 'NONE',  ( 38.79830821498527627, 485.8176106091541442, -4.884814968350399411 ) ) ;
#21180=CARTESIAN_POINT ( 'NONE',  ( 43.75010090114224681, 464.8337800386878484, 11.75004750934975029 ) ) ;
#21188=ADVANCED_FACE ( 'NONE', ( #53962 ), #70681, .T. ) ;
#21194=CARTESIAN_POINT ( 'NONE',  ( 20.21880305278369150, 304.8280059657581660, -9.005058168222337400 ) ) ;
#21195=AXIS2_PLACEMENT_3D ( 'NONE', #49195, #32528, #104793 ) ;
#21204=CARTESIAN_POINT ( 'NONE',  ( -31.96729082391632559, 486.9543932134526472, 7.084325681754340742 ) ) ;
#21218=CARTESIAN_POINT ( 'NONE',  ( -33.00000000000000000, 463.5362553048592531, 6.739467187734391906 ) ) ;
#21227=CARTESIAN_POINT ( 'NONE',  ( -40.81956795959430906, 485.7841149218988335, -4.786840289928851355 ) ) ;
#21229=CARTESIAN_POINT ( 'NONE',  ( 36.66638760098313554, 431.6597644233127085, 5.007224883190088960 ) ) ;
#21237=CARTESIAN_POINT ( 'NONE',  ( 36.55294322374219718, 336.7270298077904727, -1.783817123648057335 ) ) ;
#21238=ORIENTED_EDGE ( 'NONE', *, *, #24588, .T. ) ;
#21240=CIRCLE ( 'NONE', #97018, 0.9999999999999998890 ) ;
#21270=CARTESIAN_POINT ( 'NONE',  ( -44.19651249026929918, 485.6203925269955448, 3.557660179964223790 ) ) ;
#21277=ORIENTED_EDGE ( 'NONE', *, *, #31314, .T. ) ;
#21287=DIRECTION ( 'NONE',  ( 1.000000000000000000, 0.000000000000000000, 0.000000000000000000 ) ) ;
#21293=B_SPLINE_CURVE_WITH_KNOTS ( 'NONE', 3,
 ( #37428, #35834, #102656, #28815 ),
 .UNSPECIFIED., .F., .F.,
 ( 4, 4 ),
 ( 0.000000000000000000, 0.001831984915194361310 ),
 .UNSPECIFIED. ) ;
#21321=CARTESIAN_POINT ( 'NONE',  ( 36.62596431772431060, 370.5219051594085045, 4.028350488951735642 ) ) ;
#21322=CARTESIAN_POINT ( 'NONE',  ( -19.36103579130787367, 294.6347466944262692, -10.04613669444748680 ) ) ;
#21325=CIRCLE ( 'NONE', #95362, 3.000000000000017764 ) ;
#21327=CARTESIAN_POINT ( 'NONE',  ( -20.70564462400559336, 303.8824169543686367, -9.993494645898625350 ) ) ;
#21343=CARTESIAN_POINT ( 'NONE',  ( 36.06705365364255300, 330.6635994761463166, -3.195544000931108908 ) ) ;
#21346=ORIENTED_EDGE ( 'NONE', *, *, #22619, .T. ) ;
#21347=CARTESIAN_POINT ( 'NONE',  ( -32.28930913497458022, 488.2717154064632723, 9.213726894912692700 ) ) ;
#21352=CARTESIAN_POINT ( 'NONE',  ( -21.19348424345033521, 294.8901562694577478, 1.945151701991089332 ) ) ;
#21358=CARTESIAN_POINT ( 'NONE',  ( -36.53813723229947641, 463.3027015936762041, 20.13340496300980931 ) ) ;
#21388=CARTESIAN_POINT ( 'NONE',  ( 35.45036406932566564, 436.3203772529585649, 5.179456583034234285 ) ) ;
#21389=CARTESIAN_POINT ( 'NONE',  ( -43.67905695453814019, 391.1919955517727772, 15.78495246862232371 ) ) ;
#21397=CARTESIAN_POINT ( 'NONE',  ( -40.86966971611449395, 485.5857298029526419, -4.179518346797930661 ) ) ;
#21403=DIRECTION ( 'NONE',  ( 0.000000000000000000, 0.000000000000000000, -1.000000000000000000 ) ) ;
#21404=CARTESIAN_POINT ( 'NONE',  ( -41.17613404335627081, 436.9855557163879212, 5.736539807628611598 ) ) ;
#21408=ORIENTED_EDGE ( 'NONE', *, *, #105099, .T. ) ;
#21422=CARTESIAN_POINT ( 'NONE',  ( 34.50115457526765539, 434.4752522064443383, 9.494722064492803426 ) ) ;
#21426=CARTESIAN_POINT ( 'NONE',  ( -36.87655955837857391, 438.2068510013161244, 3.933030107424709598 ) ) ;
#21429=EDGE_CURVE ( 'NONE', #19762, #36055, #21240, .T. ) ;
#21432=DIRECTION ( 'NONE',  ( 0.9730146112117565860, 0.000000000000000000, 0.2307435077492631936 ) ) ;
#21433=CIRCLE ( 'NONE', #49186, 3.000000000000002220 ) ;
#21434=CARTESIAN_POINT ( 'NONE',  ( -46.00000000000000000, 461.8820044443818347, 11.41122057645802990 ) ) ;
#21441=ORIENTED_EDGE ( 'NONE', *, *, #17580, .F. ) ;
#21442=CARTESIAN_POINT ( 'NONE',  ( 38.47428897412591198, 485.7788508071993760, -4.770630528148357641 ) ) ;
#21443=CARTESIAN_POINT ( 'NONE',  ( 33.21174982057957692, 465.5907685032113363, 15.87814633359622540 ) ) ;
#21446=CARTESIAN_POINT ( 'NONE',  ( -39.75288494767817582, 438.7659461435675325, 23.14726008740691299 ) ) ;
#21447=ADVANCED_FACE ( 'NONE', ( #30675 ), #54904, .F. ) ;
#21450=CARTESIAN_POINT ( 'NONE',  ( 43.41290683822508356, 487.0833545439620593, 7.569976829064907875 ) ) ;
#21460=AXIS2_PLACEMENT_3D ( 'NONE', #36153, #51746, #68489 ) ;
#21462=CARTESIAN_POINT ( 'NONE',  ( -25.40811296394797125, 308.2121404732505425, 10.71478048255157312 ) ) ;
#21481=ADVANCED_FACE ( 'NONE', ( #4246 ), #47353, .F. ) ;
#21487=CARTESIAN_POINT ( 'NONE',  ( 40.36516081888879626, 459.8940149412731557, 1.928085546549638929 ) ) ;
#21518=CARTESIAN_POINT ( 'NONE',  ( 42.08346088162276999, 343.2171893020684479, 13.37295717174569099 ) ) ;
#21530=EDGE_LOOP ( 'NONE', ( #69089, #57750, #66040, #48114 ) ) ;
#21532=CARTESIAN_POINT ( 'NONE',  ( -29.45300615175912284, 297.5885148576093115, 2.537559088144822006 ) ) ;
#21537=CARTESIAN_POINT ( 'NONE',  ( 41.17613404335629212, 436.9855557163879780, 5.736539807628617815 ) ) ;
#21542=ORIENTED_EDGE ( 'NONE', *, *, #41496, .F. ) ;
#21549=EDGE_CURVE ( 'NONE', #2695, #46619, #100480, .T. ) ;
#21554=CARTESIAN_POINT ( 'NONE',  ( 37.48079164320805035, 473.0294839324634495, 17.43702840686824729 ) ) ;
#21557=CARTESIAN_POINT ( 'NONE',  ( 7.196962703002473205, 302.2659962052679248, -10.02664813804953248 ) ) ;
#21558=CARTESIAN_POINT ( 'NONE',  ( 43.66633623381847684, 409.2573964131182152, 16.13396782784120376 ) ) ;
#21559=CARTESIAN_POINT ( 'NONE',  ( -42.87890296919689348, 485.5827577773663393, 6.686241925529927244 ) ) ;
#21578=B_SPLINE_CURVE_WITH_KNOTS ( 'NONE', 3,
 ( #52288, #44216, #77107, #44756, #3223, #69033, #28065, #77645 ),
 .UNSPECIFIED., .F., .F.,
 ( 4, 2, 2, 4 ),
 ( 6.071532165918824830E-18, 0.001701937957019037306, 0.003403875914038068540, 0.006807751828076084172 ),
 .UNSPECIFIED. ) ;
#21593=CARTESIAN_POINT ( 'NONE',  ( -41.71840012517714769, 489.3048647944248728, 10.52957302900678904 ) ) ;
#21601=VERTEX_POINT ( 'NONE', #41915 ) ;
#21624=DIRECTION ( 'NONE',  ( 0.5401002696853186569, -0.5464483025172026665, -0.6400671459791652529 ) ) ;
#21626=CARTESIAN_POINT ( 'NONE',  ( -30.55228927099183522, 298.7536840786443690, 10.80461237140096209 ) ) ;
#21632=ORIENTED_EDGE ( 'NONE', *, *, #97991, .T. ) ;
#21642=CARTESIAN_POINT ( 'NONE',  ( -42.70777704799414209, 431.8248371325450989, 18.68372644223032353 ) ) ;
#21645=CARTESIAN_POINT ( 'NONE',  ( -32.15713331982922796, 435.6530683308595826, 19.42064546954540916 ) ) ;
#21647=CARTESIAN_POINT ( 'NONE',  ( -30.00000000000994405, 486.6562833505550998, 5.030808486074148433 ) ) ;
#21652=CARTESIAN_POINT ( 'NONE',  ( -30.73227349664980323, 297.9212584795371868, -9.326660378782543503 ) ) ;
#21675=CARTESIAN_POINT ( 'NONE',  ( -38.28124992147791517, 438.9555075391706964, 23.36623646420498090 ) ) ;
#21677=CARTESIAN_POINT ( 'NONE',  ( -22.35039165680892381, 303.1532478080135320, -9.935478914023770258 ) ) ;
#21682=CIRCLE ( 'NONE', #18206, 2.999999999999982236 ) ;
#21684=ADVANCED_FACE ( 'NONE', ( #28845 ), #13118, .T. ) ;
#21696=EDGE_LOOP ( 'NONE', ( #58513, #11991 ) ) ;
#21701=PLANE ( 'NONE',  #27708 ) ;
#21702=VERTEX_POINT ( 'NONE', #4515 ) ;
#21713=FACE_OUTER_BOUND ( 'NONE', #105377, .T. ) ;
#21721=CIRCLE ( 'NONE', #83731, 7.999999999999989342 ) ;
#21724=CARTESIAN_POINT ( 'NONE',  ( -32.01678793614195939, 487.4833407576300033, 8.028904756518427277 ) ) ;
#21744=ORIENTED_EDGE ( 'NONE', *, *, #81569, .T. ) ;
#21748=CARTESIAN_POINT ( 'NONE',  ( -40.16087957073754211, 485.8454018306724720, -4.964645702805049687 ) ) ;
#21750=CARTESIAN_POINT ( 'NONE',  ( 36.73048575021757500, 408.0658092706848947, 6.298725112593818842 ) ) ;
#21752=EDGE_CURVE ( 'NONE', #78525, #23615, #28694, .T. ) ;
#21753=CARTESIAN_POINT ( 'NONE',  ( 32.80551872593211726, 486.0171861992458844, 5.671217483528002923 ) ) ;
#21757=CARTESIAN_POINT ( 'NONE',  ( -46.00000000000000711, 437.9209086209079373, 12.30656597848518885 ) ) ;
#21769=CARTESIAN_POINT ( 'NONE',  ( -35.76320840016588676, 388.4727839510825333, 5.610592865731860002 ) ) ;
#21772=CARTESIAN_POINT ( 'NONE',  ( -41.81614247337329004, 436.2534677952782545, 7.171297734019188574 ) ) ;
#21808=CARTESIAN_POINT ( 'NONE',  ( 9.965951495596808485, 294.6437651480115960, 1.892775183163956543 ) ) ;
#21814=CARTESIAN_POINT ( 'NONE',  ( 33.00000000000000000, 461.8163627757383551, 11.11111419091032460 ) ) ;
#21816=CIRCLE ( 'NONE', #73414, 12.00000000000000711 ) ;
#21818=STYLED_ITEM ( 'NONE', ( #91924 ), #23822 ) ;
#21834=DIRECTION ( 'NONE',  ( 0.000000000000000000, 0.000000000000000000, -1.000000000000000000 ) ) ;
#21848=AXIS2_PLACEMENT_3D ( 'NONE', #71438, #55251, #88175 ) ;
#21851=CARTESIAN_POINT ( 'NONE',  ( 33.19417746838672656, 318.2631342106616898, -6.512803730419179260 ) ) ;
#21858=DIRECTION ( 'NONE',  ( 0.2284631855477637086, 0.3307511317731879896, 0.9156463627843030029 ) ) ;
#21874=CARTESIAN_POINT ( 'NONE',  ( 30.82100972494468394, 309.0976561879820110, -8.562264960266007918 ) ) ;
#21884=( BOUNDED_SURFACE ( )  B_SPLINE_SURFACE ( 3, 2, ( 
 ( #16672, #7497, #97569 ),
 ( #16135, #99169, #106734 ),
 ( #8037, #8573, #58190 ),
 ( #49021, #56585, #106191 ),
 ( #39894, #65758, #66284 ),
 ( #50098, #98639, #65226 ),
 ( #973, #98118, #74363 ),
 ( #31813, #57642, #73840 ),
 ( #83003, #9098, #89508 ),
 ( #32883, #24267, #90563 ),
 ( #42006, #33955, #47958 ),
 ( #15602, #97054, #442 ),
 ( #81918, #23199, #74888 ),
 ( #40950, #81387, #80865 ),
 ( #6977, #72769, #105674 ),
 ( #1529, #68967, #19388 ),
 ( #60871, #101323, #35019 ),
 ( #77036, #100242, #101840 ),
 ( #85131, #2605, #93759 ),
 ( #25885, #66826, #43082 ),
 ( #100771, #26935, #91638 ),
 ( #34495, #9626, #19917 ),
 ( #27472, #75971, #17751 ),
 ( #67364, #51688, #10168 ),
 ( #28002, #10690, #60350 ),
 ( #93226, #51150, #50607 ),
 ( #43605, #3153, #84608 ),
 ( #99715, #35554, #58743 ) ),
 .UNSPECIFIED., .F., .F., .F. ) 
 B_SPLINE_SURFACE_WITH_KNOTS ( ( 4, 2, 2, 2, 2, 2, 2, 2, 2, 2, 2, 2, 2, 4 ),
 ( 3, 3 ),
 ( -1.788854400197697518E-05, 0.0008258451467760102556, 0.001669578837553997415, 0.002513312528331984683, 0.003357046219109971735, 0.004200779909887959220, 0.005044513600665946271, 0.006731980982221920373, 0.007575714672999907424, 0.008419448363777894476, 0.01010691574533386858, 0.01095064943611185650, 0.01179438312688984442, 0.01348185050844581852 ),
 ( 0.000000000000000000, 1.000000000000000000 ),
 .UNSPECIFIED. ) 
 GEOMETRIC_REPRESENTATION_ITEM ( )  RATIONAL_B_SPLINE_SURFACE ( (
 ( 1.000000000000000000, 1.000000000000000000, 1.000000000000000000),
 ( 1.000000000000000000, 1.000005597032284976, 1.000000000000000000),
 ( 1.000000000000000000, 0.9981174035053985705, 1.000000000000000000),
 ( 1.000000000000000000, 0.9910941550115122123, 1.000000000000000000),
 ( 1.000000000000000000, 0.9859587391819751856, 1.000000000000000000),
 ( 1.000000000000000000, 0.9732073139009395080, 1.000000000000000000),
 ( 1.000000000000000000, 0.9655956055815202443, 1.000000000000000000),
 ( 1.000000000000000000, 0.9487954604282968774, 1.000000000000000000),
 ( 1.000000000000000000, 0.9396125312366238047, 1.000000000000000000),
 ( 1.000000000000000000, 0.9205547400728270047, 1.000000000000000000),
 ( 1.000000000000000000, 0.9106598259483166258, 1.000000000000000000),
 ( 1.000000000000000000, 0.8910166268681486423, 1.000000000000000000),
 ( 1.000000000000000000, 0.8812839758754353880, 1.000000000000000000),
 ( 1.000000000000000000, 0.8530381836181091249, 1.000000000000000000),
 ( 1.000000000000000000, 0.8355499924272906664, 1.000000000000000000),
 ( 1.000000000000000000, 0.8121180734272108737, 1.000000000000000000),
 ( 1.000000000000000000, 0.8047528071544994832, 1.000000000000000000),
 ( 1.000000000000000000, 0.7908772856458535783, 1.000000000000000000),
 ( 1.000000000000000000, 0.7843397418763655704, 1.000000000000000000),
 ( 1.000000000000000000, 0.7662143347336847210, 1.000000000000000000),
 ( 1.000000000000000000, 0.7560053113360732935, 1.000000000000000000),
 ( 1.000000000000000000, 0.7426428230152902765, 1.000000000000000000),
 ( 1.000000000000000000, 0.7385160411530290459, 1.000000000000000000),
 ( 1.000000000000000000, 0.7308023910617710284, 1.000000000000000000),
 ( 1.000000000000000000, 0.7272503285417218910, 1.000000000000000000),
 ( 1.000000000000000000, 0.7174350756258216499, 1.000000000000000000),
 ( 1.000000000000000000, 0.7119478818699274125, 1.000000000000000000),
 ( 1.000000000000000000, 0.7071066567438195616, 1.000000000000000000) ) ) 
 REPRESENTATION_ITEM ( '' )  SURFACE ( )  );
#21899=CARTESIAN_POINT ( 'NONE',  ( -43.72316710615100277, 464.1667603278365277, 8.066774506823993107 ) ) ;
#21930=CARTESIAN_POINT ( 'NONE',  ( 41.86592229012135391, 465.6952443684891705, 15.31587819977333886 ) ) ;
#21952=CARTESIAN_POINT ( 'NONE',  ( 34.77793752178678943, 435.8715891072652084, 8.130587104768295603 ) ) ;
#21959=CARTESIAN_POINT ( 'NONE',  ( 43.75010090113823225, 464.8337800386758545, 11.75004750935514686 ) ) ;
#21969=CARTESIAN_POINT ( 'NONE',  ( 39.04140135028778502, 485.1684443570251801, -4.294922607834593009 ) ) ;
#21974=CARTESIAN_POINT ( 'NONE',  ( 46.00000000000000000, 500.0000000000002274, -5.000000000000001776 ) ) ;
#21976=CARTESIAN_POINT ( 'NONE',  ( -43.69392749306696544, 464.9769837083814537, 8.436995239877180808 ) ) ;
#21981=CARTESIAN_POINT ( 'NONE',  ( -41.58649125062324003, 315.0454808444952732, -5.157136739128146630 ) ) ;
#21993=CARTESIAN_POINT ( 'NONE',  ( -23.88426421104139763, 306.2535832371898437, 10.24728475601139976 ) ) ;
#21997=CARTESIAN_POINT ( 'NONE',  ( -41.35836404316634685, 461.4284568614622231, 2.579347946915543588 ) ) ;
#22001=CARTESIAN_POINT ( 'NONE',  ( 44.14489099987147824, 485.6019929922275082, 3.572971381548252889 ) ) ;
#22012=CARTESIAN_POINT ( 'NONE',  ( 36.47247920115664499, 437.5953975496288422, 4.244884750893885617 ) ) ;
#22029=CARTESIAN_POINT ( 'NONE',  ( 44.12472801211155371, 485.7238370326410859, 3.975897585125152123 ) ) ;
#22030=CARTESIAN_POINT ( 'NONE',  ( 19.07845090537422550, 294.6331628770684574, 9.890526070132905190 ) ) ;
#22041=CARTESIAN_POINT ( 'NONE',  ( 42.75497199330776255, 415.3167855576094212, 19.81357880037930030 ) ) ;
#22043=CARTESIAN_POINT ( 'NONE',  ( -43.00000000000000000, 461.4080316921935605, 3.462976341553817949 ) ) ;
#22047=EDGE_LOOP ( 'NONE', ( #91033, #72469, #95253, #99096 ) ) ;
#22050=CARTESIAN_POINT ( 'NONE',  ( -34.23250573208579794, 462.3234378130318305, 4.646251724931845573 ) ) ;
#22055=CARTESIAN_POINT ( 'NONE',  ( -35.49987330852459166, 304.0097181485430156, 4.051457700508126258 ) ) ;
#22066=EDGE_CURVE ( 'NONE', #98501, #5193, #89390, .T. ) ;
#22080=CARTESIAN_POINT ( 'NONE',  ( -42.69811214730272297, 434.9611672192513652, 18.34625614733208820 ) ) ;
#22082=CARTESIAN_POINT ( 'NONE',  ( 9.659964574192086317, 294.6522956596213021, -2.587254427043884419 ) ) ;
#22085=CARTESIAN_POINT ( 'NONE',  ( -21.19348424345033521, 294.8901562694577478, 1.945151701991089332 ) ) ;
#22095=VERTEX_POINT ( 'NONE', #23072 ) ;
#22137=EDGE_CURVE ( 'NONE', #87652, #38500, #63357, .T. ) ;
#22143=CARTESIAN_POINT ( 'NONE',  ( -43.00000000000000000, 485.2629658518202405, -2.796394914059407100 ) ) ;
#22147=CARTESIAN_POINT ( 'NONE',  ( 32.43164319908647286, 464.5283015133045978, 9.485638277864474333 ) ) ;
#22155=ORIENTED_EDGE ( 'NONE', *, *, #56964, .T. ) ;
#22166=CARTESIAN_POINT ( 'NONE',  ( 30.00000000000000355, 461.8665156241228260, 11.40533150091922820 ) ) ;
#22169=CARTESIAN_POINT ( 'NONE',  ( -32.42294576121290817, 435.8436782518352288, 18.25571606399968516 ) ) ;
#22170=CARTESIAN_POINT ( 'NONE',  ( 32.42656933071582159, 485.5064012031800189, 3.828740380144981081 ) ) ;
#22179=CARTESIAN_POINT ( 'NONE',  ( -35.45950249840887381, 303.1341283215246563, -0.1035848689192439415 ) ) ;
#22185=CARTESIAN_POINT ( 'NONE',  ( -42.68467435370097718, 439.3123962055185530, 17.84297149534227955 ) ) ;
#22186=CARTESIAN_POINT ( 'NONE',  ( 27.42085833529588257, 312.9751210562151300, 10.90118510545367414 ) ) ;
#22198=CARTESIAN_POINT ( 'NONE',  ( -35.50355603268687332, 439.1325461877797238, 24.06453856846038519 ) ) ;
#22200=CARTESIAN_POINT ( 'NONE',  ( -28.32351931790351429, 306.0343727091704977, -9.290635017633318782 ) ) ;
#22202=CARTESIAN_POINT ( 'NONE',  ( 1.224646799147353651E-15, 300.0000000000000000, 10.00000000000000178 ) ) ;
#22245=VERTEX_POINT ( 'NONE', #100649 ) ;
#22275=CARTESIAN_POINT ( 'NONE',  ( -41.12904442321463705, 485.7386261246312529, -4.649563818468734233 ) ) ;
#22277=DIRECTION ( 'NONE',  ( 1.000000000000000000, 0.000000000000000000, 0.000000000000000000 ) ) ;
#22284=CARTESIAN_POINT ( 'NONE',  ( -36.20959526385565397, 304.3379572843515461, 0.1881653396831703962 ) ) ;
#22286=CARTESIAN_POINT ( 'NONE',  ( 20.87268443183278421, 302.8961289238256427, -9.990552340451243296 ) ) ;
#22291=CARTESIAN_POINT ( 'NONE',  ( -33.95156263172582101, 464.5083255208627975, 6.608064661821575037 ) ) ;
#22298=ORIENTED_EDGE ( 'NONE', *, *, #41302, .T. ) ;
#22300=CARTESIAN_POINT ( 'NONE',  ( 41.58649125062324003, 315.0454808444952732, -5.157136739135766312 ) ) ;
#22304=CARTESIAN_POINT ( 'NONE',  ( -41.20010578034021620, 436.9751675121757444, 5.754626909160545090 ) ) ;
#22305=FACE_OUTER_BOUND ( 'NONE', #104011, .T. ) ;
#22309=B_SPLINE_CURVE_WITH_KNOTS ( 'NONE', 3,
 ( #74074, #23447, #56283, #73537 ),
 .UNSPECIFIED., .F., .F.,
 ( 4, 4 ),
 ( 0.000000000000000000, 0.001448684797825257461 ),
 .UNSPECIFIED. ) ;
#22313=VERTEX_POINT ( 'NONE', #10050 ) ;
#22315=ORIENTED_EDGE ( 'NONE', *, *, #11495, .T. ) ;
#22320=CARTESIAN_POINT ( 'NONE',  ( 32.13489264513381727, 427.2002522300152805, 24.83829134347774215 ) ) ;
#22325=CARTESIAN_POINT ( 'NONE',  ( 34.90210058998459175, 473.1145171525240585, 16.89534907407908548 ) ) ;
#22338=CARTESIAN_POINT ( 'NONE',  ( 16.93821050485266611, 302.5835677207606409, 9.880234544770994276 ) ) ;
#22359=ORIENTED_EDGE ( 'NONE', *, *, #58751, .F. ) ;
#22367=EDGE_CURVE ( 'NONE', #34982, #2439, #78376, .T. ) ;
#22384=CARTESIAN_POINT ( 'NONE',  ( 35.74123987347093845, 414.7932616781445745, 5.921579997229594383 ) ) ;
#22385=B_SPLINE_SURFACE_WITH_KNOTS ( 'NONE', 1, 3, ( 
 ( #93893, #45353, #12421, #37281, #20050, #103052, #102516, #37818, #28660, #70676, #29719, #83939, #41352, #66157, #25756, #50491, #18165, #100121, #58615, #98521, #74246, #24667, #67243, #82344, #56993, #26287, #90984, #57520 ),
 ( #90441, #25207, #66698, #99039, #42415, #59148, #51027, #58060, #65635, #322, #91516, #8452, #33285, #81789, #89908, #17631, #10051, #33825, #32764, #17096, #74769, #83404, #1403, #9502, #16550, #49435, #75308, #92031 ) ),
 .UNSPECIFIED., .F., .F., .F.,
 ( 2, 2 ),
 ( 4, 2, 2, 2, 2, 2, 2, 2, 2, 2, 2, 2, 2, 4 ),
 ( 0.000000000000000000, 1.000000000000000000 ),
 ( 0.08901491201581737678, 0.1032490540155679704, 0.1174831960153185778, 0.1317173380150691853, 0.1459514800148197788, 0.1744197640143299588, 0.2028880480138401388, 0.2598246160128514504, 0.3167611840118632616, 0.4306343200098861623, 0.5445074560079088410, 0.6583805920059359051, 0.7722537280039543095, 1.000000000000000000 ),
 .UNSPECIFIED. ) ;
#22398=CARTESIAN_POINT ( 'NONE',  ( -35.59180895336101003, 464.2025721804453724, 19.31791767298735252 ) ) ;
#22406=CARTESIAN_POINT ( 'NONE',  ( 37.98379125797355016, 307.9909936412415163, 1.091397535864746970 ) ) ;
#22409=VERTEX_POINT ( 'NONE', #32638 ) ;
#22432=CARTESIAN_POINT ( 'NONE',  ( 36.09139106816682130, 461.0566049081365350, 3.057441095446108648 ) ) ;
#22454=CARTESIAN_POINT ( 'NONE',  ( -46.00000000000000000, 485.7784312020116886, -0.3394844618430318262 ) ) ;
#22457=ORIENTED_EDGE ( 'NONE', *, *, #91161, .F. ) ;
#22461=CARTESIAN_POINT ( 'NONE',  ( 32.91522635463719837, 465.6822307888475052, 10.74522530471245041 ) ) ;
#22462=CARTESIAN_POINT ( 'NONE',  ( -40.83002285428302969, 485.0211005501724912, -4.017563975490292982 ) ) ;
#22463=CARTESIAN_POINT ( 'NONE',  ( 6.144704265756976369, 301.8764918330675187, -10.02047951298166240 ) ) ;
#22467=CARTESIAN_POINT ( 'NONE',  ( 40.49255712025206577, 464.0858896352993952, 18.37716086306491903 ) ) ;
#22479=ADVANCED_FACE ( 'NONE', ( #73578 ), #87092, .T. ) ;
#22484=EDGE_CURVE ( 'NONE', #93970, #65357, #85387, .T. ) ;
#22489=CARTESIAN_POINT ( 'NONE',  ( -42.51305782313426818, 484.3273291304232089, -1.912516135270148743 ) ) ;
#22505=CARTESIAN_POINT ( 'NONE',  ( -46.00000000000000000, 437.9690125970931831, 14.09127711025708507 ) ) ;
#22534=CARTESIAN_POINT ( 'NONE',  ( -28.80272083960844043, 315.1418830885958187, 12.69311001326675736 ) ) ;
#22535=ORIENTED_EDGE ( 'NONE', *, *, #42754, .F. ) ;
#22543=CARTESIAN_POINT ( 'NONE',  ( 46.00000000000570566, 485.9629172155148922, 0.8649761565702976940 ) ) ;
#22556=CARTESIAN_POINT ( 'NONE',  ( 40.19525959764776957, 459.8689882208901736, 1.906254677025529531 ) ) ;
#22558=CARTESIAN_POINT ( 'NONE',  ( -38.85446894546474539, 460.8903912184078422, 2.218456751110488678 ) ) ;
#22562=CARTESIAN_POINT ( 'NONE',  ( 30.95643954367146833, 313.8918926584737505, -7.857037206977866006 ) ) ;
#22578=DIRECTION ( 'NONE',  ( 0.1270361284032394955, -0.9918980905719678720, 0.000000000000000000 ) ) ;
#22579=VERTEX_POINT ( 'NONE', #1813 ) ;
#22583=CARTESIAN_POINT ( 'NONE',  ( 0.000000000000000000, 70.00000000000000000, -10.00000000000000178 ) ) ;
#22589=CARTESIAN_POINT ( 'NONE',  ( 35.76362145159366435, 307.1564523868753440, 12.84684258606850271 ) ) ;
#22596=CARTESIAN_POINT ( 'NONE',  ( -34.05871433650573010, 463.4203836794940230, 6.469249789599879286 ) ) ;
#22601=CARTESIAN_POINT ( 'NONE',  ( -31.74043077603787921, 299.2833385164202582, 2.924916184740101510 ) ) ;
#22609=CARTESIAN_POINT ( 'NONE',  ( 15.71080878184230301, 303.5558203657541299, 9.874086874886266685 ) ) ;
#22619=EDGE_CURVE ( 'NONE', #96778, #71668, #50867, .T. ) ;
#22620=VECTOR ( 'NONE', #79458, 1000.000000000000227 ) ;
#22623=EDGE_CURVE ( 'NONE', #81976, #19129, #67162, .T. ) ;
#22628=CARTESIAN_POINT ( 'NONE',  ( 37.50105657201422105, 463.9558240680319159, 19.48687553971743469 ) ) ;
#22631=LINE ( 'NONE', #105624, #69875 ) ;
#22633=CARTESIAN_POINT ( 'NONE',  ( 43.52075891743746894, 484.7805561108181109, 4.063293749111048569 ) ) ;
#22639=ORIENTED_EDGE ( 'NONE', *, *, #57916, .T. ) ;
#22653=ORIENTED_EDGE ( 'NONE', *, *, #586, .T. ) ;
#22654=ORIENTED_EDGE ( 'NONE', *, *, #51592, .F. ) ;
#22683=CARTESIAN_POINT ( 'NONE',  ( -7.169728294440821159, 294.7252185496461721, 1.910214800425284132 ) ) ;
#22684=CARTESIAN_POINT ( 'NONE',  ( 43.52578837347088836, 465.2717874277798842, 9.360669990306849542 ) ) ;
#22688=DIRECTION ( 'NONE',  ( 0.000000000000000000, 0.000000000000000000, 1.000000000000000000 ) ) ;
#22691=CARTESIAN_POINT ( 'NONE',  ( -37.69506754384124747, 484.8919167041191827, -3.620297613827866190 ) ) ;
#22707=CARTESIAN_POINT ( 'NONE',  ( 33.21585456055980501, 485.3968598104756325, 4.030361751232280909 ) ) ;
#22715=CARTESIAN_POINT ( 'NONE',  ( -34.86904551647302242, 301.2900558943937881, -8.550442243075442761 ) ) ;
#22719=EDGE_LOOP ( 'NONE', ( #63136, #84451, #89028, #93403, #57815, #21346, #105398 ) ) ;
#22723=CARTESIAN_POINT ( 'NONE',  ( 31.41956315632691599, 380.3354942127950835, 23.41885142240392881 ) ) ;
#22726=STYLED_ITEM ( 'NONE', ( #80611 ), #93555 ) ;
#22733=ORIENTED_EDGE ( 'NONE', *, *, #104657, .T. ) ;
#22734=CARTESIAN_POINT ( 'NONE',  ( -24.15840962162803507, 303.6456723108300366, -9.828972323003243972 ) ) ;
#22736=CARTESIAN_POINT ( 'NONE',  ( 38.85520749938564933, 460.5777845577952689, 2.285580541808310162 ) ) ;
#22744=ADVANCED_FACE ( 'NONE', ( #62231 ), #43882, .T. ) ;
#22770=CARTESIAN_POINT ( 'NONE',  ( 22.91885868373643831, 305.6172567281201964, 10.10309701371861912 ) ) ;
#22782=CARTESIAN_POINT ( 'NONE',  ( -13.25308349978780598, 303.5542394377912956, 9.873748767567704476 ) ) ;
#22790=AXIS2_PLACEMENT_3D ( 'NONE', #7594, #7075, #41047 ) ;
#22795=ORIENTED_EDGE ( 'NONE', *, *, #33666, .T. ) ;
#22808=CARTESIAN_POINT ( 'NONE',  ( 32.78741055188843490, 485.3331003366700998, 5.977022408747314053 ) ) ;
#22815=CARTESIAN_POINT ( 'NONE',  ( -43.28593744481448624, 352.9831048051240714, 11.32485626521906141 ) ) ;
#22816=CARTESIAN_POINT ( 'NONE',  ( 35.45719195239888677, 325.1427260202198113, -4.543212221563117659 ) ) ;
#22826=B_SPLINE_CURVE_WITH_KNOTS ( 'NONE', 3,
 ( #16433, #66583, #18593, #84368 ),
 .UNSPECIFIED., .F., .F.,
 ( 4, 4 ),
 ( 2.602085213965210642E-18, 0.001800036990427380601 ),
 .UNSPECIFIED. ) ;
#22830=CARTESIAN_POINT ( 'NONE',  ( -23.96375140441108442, 306.3052962357393199, 10.25885168886986243 ) ) ;
#22834=CARTESIAN_POINT ( 'NONE',  ( -41.60090381918462299, 436.7951626062874197, 6.075960697891537698 ) ) ;
#22840=FACE_OUTER_BOUND ( 'NONE', #34044, .T. ) ;
#22849=CARTESIAN_POINT ( 'NONE',  ( 32.16538097803554308, 380.2609445124364811, 24.62016063048157832 ) ) ;
#22864=CARTESIAN_POINT ( 'NONE',  ( 43.00000000000000000, 487.9285348210859752, 8.903916466042430145 ) ) ;
#22866=CARTESIAN_POINT ( 'NONE',  ( 19.15449903924667652, 294.6774112952710993, 1.900463839854222847 ) ) ;
#22872=CARTESIAN_POINT ( 'NONE',  ( 1.128238012697730275, 300.0000000000000000, 9.936150108905557943 ) ) ;
#22887=CARTESIAN_POINT ( 'NONE',  ( -39.21279148650070567, 436.8435004666161490, 5.150741822288940952 ) ) ;
#22901=CARTESIAN_POINT ( 'NONE',  ( -39.24156521425334176, 307.7088117867400001, -7.003459073692002157 ) ) ;
#22902=CARTESIAN_POINT ( 'NONE',  ( 46.00000000000000000, 461.9428920847514632, 12.03309428281642823 ) ) ;
#22907=CARTESIAN_POINT ( 'NONE',  ( 35.73673605237448214, 338.3594419497471790, -1.628405847195040668 ) ) ;
#22908=ORIENTED_EDGE ( 'NONE', *, *, #43207, .T. ) ;
#22911=CARTESIAN_POINT ( 'NONE',  ( -21.88406739194823913, 304.0791269202651392, -9.951548237181681245 ) ) ;
#22913=CARTESIAN_POINT ( 'NONE',  ( -42.31186848673717549, 465.8659795009672280, 14.28293630011528137 ) ) ;
#22920=CARTESIAN_POINT ( 'NONE',  ( -36.55165400673971732, 463.9825939691005487, 19.61553332823773133 ) ) ;
#22924=ORIENTED_EDGE ( 'NONE', *, *, #87040, .F. ) ;
#22929=CARTESIAN_POINT ( 'NONE',  ( 36.03799849557760382, 304.0525444531467087, 0.1188115607976301946 ) ) ;
#22937=CARTESIAN_POINT ( 'NONE',  ( 43.98494780483915889, 485.1299400071267769, -0.2561545284547621093 ) ) ;
#22938=AXIS2_PLACEMENT_3D ( 'NONE', #42078, #39585, #23405 ) ;
#22945=CARTESIAN_POINT ( 'NONE',  ( 43.03185303983483578, 485.3613526602389356, 6.073233449168498055 ) ) ;
#22950=VERTEX_POINT ( 'NONE', #84882 ) ;
#22971=CARTESIAN_POINT ( 'NONE',  ( -41.68589585752227578, 436.0808743425936882, 20.68176223068306285 ) ) ;
#22972=CARTESIAN_POINT ( 'NONE',  ( 33.13272883738260788, 379.7391572186269855, 24.76066166452115169 ) ) ;
#22973=CARTESIAN_POINT ( 'NONE',  ( -41.66500103013587619, 324.8107132651804818, 5.306019078252184329 ) ) ;
#22975=CARTESIAN_POINT ( 'NONE',  ( -46.00000000000000000, 488.3725375423296668, 3.127739281037493768 ) ) ;
#22998=EDGE_CURVE ( 'NONE', #29831, #86195, #100931, .T. ) ;
#23003=UNCERTAINTY_MEASURE_WITH_UNIT (LENGTH_MEASURE( 1.000000000000000082E-05 ), #7295, 'distance_accuracy_value', 'NONE');
#23007=CARTESIAN_POINT ( 'NONE',  ( 11.62660349859606868, 304.6006130031697126, 9.883607381091580990 ) ) ;
#23017=CARTESIAN_POINT ( 'NONE',  ( -40.05511244076242150, 485.1954865622287230, -4.343528235245400992 ) ) ;
#23022=CARTESIAN_POINT ( 'NONE',  ( -30.00000000000000355, 461.9590195980672434, 14.34002891082236708 ) ) ;
#23033=CARTESIAN_POINT ( 'NONE',  ( -36.54024843362181940, 439.8191410655647360, 24.21861018269294163 ) ) ;
#23034=ORIENTED_EDGE ( 'NONE', *, *, #40940, .F. ) ;
#23035=CARTESIAN_POINT ( 'NONE',  ( -43.03357534758885095, 463.2291678140052227, 4.675918524150252331 ) ) ;
#23050=CARTESIAN_POINT ( 'NONE',  ( -26.97187310779845504, 311.5034665361333168, 10.53023658691173026 ) ) ;
#23052=VERTEX_POINT ( 'NONE', #46544 ) ;
#23054=DIRECTION ( 'NONE',  ( 0.6181567188929438794, 0.3028222199723830110, -0.7253833289913049764 ) ) ;
#23057=ADVANCED_FACE ( 'NONE', ( #48117 ), #10792, .F. ) ;
#23060=CARTESIAN_POINT ( 'NONE',  ( 45.99999999999428013, 486.2727346241949249, 2.946729464013586597 ) ) ;
#23065=EDGE_CURVE ( 'NONE', #81556, #22579, #66442, .T. ) ;
#23072=CARTESIAN_POINT ( 'NONE',  ( 33.95156263172584943, 464.5083255208626838, 6.608064661821377861 ) ) ;
#23074=CARTESIAN_POINT ( 'NONE',  ( 6.779931853646243844, 303.7378069780689884, -10.02423311839737607 ) ) ;
#23096=CARTESIAN_POINT ( 'NONE',  ( -46.00000000000000000, 461.5923542530184704, 9.841579728281992345 ) ) ;
#23105=CARTESIAN_POINT ( 'NONE',  ( 27.64945316933048147, 308.2090964242639757, 11.19157541975697967 ) ) ;
#23106=CARTESIAN_POINT ( 'NONE',  ( 42.15357157744617211, 485.2432036427202320, -2.744622672851878775 ) ) ;
#23109=CARTESIAN_POINT ( 'NONE',  ( 42.12169488795439776, 344.1724850039262833, 13.56560836097746403 ) ) ;
#23112=CARTESIAN_POINT ( 'NONE',  ( -38.85446894546556962, 460.8903912184119349, 2.218456751109251890 ) ) ;
#23115=DIRECTION ( 'NONE',  ( 0.9807128367232246235, 0.000000000000000000, -0.1954541682499656707 ) ) ;
#23119=CARTESIAN_POINT ( 'NONE',  ( -26.95874670891568670, 306.9337786011216167, 10.87796326698635241 ) ) ;
#23134=CARTESIAN_POINT ( 'NONE',  ( 35.31443409317389381, 437.2805527638817011, 5.244185069633229723 ) ) ;
#23137=( BOUNDED_SURFACE ( )  B_SPLINE_SURFACE ( 3, 2, ( 
 ( #90860, #56873, #32648 ),
 ( #65519, #98407, #41765 ),
 ( #16976, #74121, #99458 ),
 ( #106491, #83287, #24558 ),
 ( #82218, #50904, #735 ),
 ( #97877, #24032, #49853 ),
 ( #91914, #90320, #81671 ),
 ( #33171, #26169, #57404 ) ),
 .UNSPECIFIED., .F., .F., .F. ) 
 B_SPLINE_SURFACE_WITH_KNOTS ( ( 4, 2, 2, 4 ),
 ( 3, 3 ),
 ( 0.006715319241937533351, 0.008391857906702646086, 0.009230127239085202454, 0.01006839657146775882 ),
 ( 0.1556289876074680167, 1.000000000000000000 ),
 .UNSPECIFIED. ) 
 GEOMETRIC_REPRESENTATION_ITEM ( )  RATIONAL_B_SPLINE_SURFACE ( (
 ( 0.9230226209209920762, 0.7526894563075792188, 1.000000000000000000),
 ( 0.9285426880689180429, 0.7704241573834766932, 1.000000000000000000),
 ( 0.9321341943958372234, 0.7819628378765275389, 1.000000000000000000),
 ( 0.9333181995231564221, 0.7857667729451842664, 1.000000000000000000),
 ( 0.9330118842454382388, 0.7847826526908945333, 1.000000000000000000),
 ( 0.9309453891092112077, 0.7781434810044502992, 1.000000000000000000),
 ( 0.9291880512466714759, 0.7724975602490826709, 1.000000000000000000),
 ( 0.9267827504115082604, 0.7647698840875247761, 1.000000000000000000) ) ) 
 REPRESENTATION_ITEM ( '' )  SURFACE ( )  );
#23144=CARTESIAN_POINT ( 'NONE',  ( 9.766195837854356299, 294.6492712292731539, -2.152655282857795616 ) ) ;
#23150=CARTESIAN_POINT ( 'NONE',  ( -19.96162532426521352, 302.8116070918646301, 9.928455558879880627 ) ) ;
#23155=DIRECTION ( 'NONE',  ( 0.9745656835855570632, 0.000000000000000000, -0.2241020490254743425 ) ) ;
#23193=AXIS2_PLACEMENT_3D ( 'NONE', #11000, #43394, #93000 ) ;
#23199=CARTESIAN_POINT ( 'NONE',  ( -5.800920608303504977, 296.2164713808596161, -10.01425861749949320 ) ) ;
#23206=CARTESIAN_POINT ( 'NONE',  ( -10.01511786699015438, 294.6430527449200554, 9.892628225130204456 ) ) ;
#23211=DIRECTION ( 'NONE',  ( 1.000000000000000000, -0.000000000000000000, -0.000000000000000000 ) ) ;
#23212=CARTESIAN_POINT ( 'NONE',  ( 36.08160016961308969, 491.3801102092154451, 12.28496641016068835 ) ) ;
#23215=ORIENTED_EDGE ( 'NONE', *, *, #30661, .T. ) ;
#23228=CARTESIAN_POINT ( 'NONE',  ( 32.94021323899735165, 485.0599191339526328, 5.361609822540882142 ) ) ;
#23230=CARTESIAN_POINT ( 'NONE',  ( -30.00000000000000355, 488.7759232732886403, 4.253593570507368860 ) ) ;
#23236=CARTESIAN_POINT ( 'NONE',  ( -31.85803618339147647, 298.6540356601998951, -9.160706982464283499 ) ) ;
#23243=CARTESIAN_POINT ( 'NONE',  ( 31.18772345825684056, 357.3324404125347087, 20.56444635957918265 ) ) ;
#23251=CARTESIAN_POINT ( 'NONE',  ( -46.00000000000000000, 461.5923978621302695, 9.841791816127033243 ) ) ;
#23252=CARTESIAN_POINT ( 'NONE',  ( -42.19180677453720563, 462.2931784592652207, 3.389262873192004477 ) ) ;
#23298=CARTESIAN_POINT ( 'NONE',  ( 35.17658899013087392, 491.5165241545285539, 12.37078523472800207 ) ) ;
#23300=ORIENTED_EDGE ( 'NONE', *, *, #62905, .T. ) ;
#23310=LINE ( 'NONE', #82584, #33905 ) ;
#23311=CARTESIAN_POINT ( 'NONE',  ( 0.000000000000000000, 80.00000000000000000, 0.000000000000000000 ) ) ;
#23315=EDGE_LOOP ( 'NONE', ( #13490, #58704 ) ) ;
#23321=CARTESIAN_POINT ( 'NONE',  ( -32.64147241561564528, 439.6779429780672217, 24.07034118911103349 ) ) ;
#23322=VERTEX_POINT ( 'NONE', #99059 ) ;
#23337=CARTESIAN_POINT ( 'NONE',  ( -43.61009301646220138, 374.8108257898446141, 14.43920481438196468 ) ) ;
#23339=CARTESIAN_POINT ( 'NONE',  ( 20.49977525862259142, 302.8459220885798686, -10.00124997875687427 ) ) ;
#23347=CARTESIAN_POINT ( 'NONE',  ( 34.15253942429875877, 465.0582672257839363, 17.72214182034170094 ) ) ;
#23364=CARTESIAN_POINT ( 'NONE',  ( -43.52075891743668734, 484.7805561108187931, 4.063293749114571085 ) ) ;
#23369=ORIENTED_EDGE ( 'NONE', *, *, #74805, .T. ) ;
#23385=EDGE_LOOP ( 'NONE', ( #21441, #32523, #86415, #60832, #81030, #8727, #90650, #50462 ) ) ;
#23390=AXIS2_PLACEMENT_3D ( 'NONE', #99113, #49512, #25833 ) ;
#23392=CARTESIAN_POINT ( 'NONE',  ( 16.52192859150929749, 294.5714182157683467, 9.877401045508872102 ) ) ;
#23399=VERTEX_POINT ( 'NONE', #89003 ) ;
#23405=DIRECTION ( 'NONE',  ( 0.000000000000000000, 0.000000000000000000, 1.000000000000000000 ) ) ;
#23406=CARTESIAN_POINT ( 'NONE',  ( 34.01853213578340984, 439.9180697526190897, 24.30896811189926154 ) ) ;
#23407=AXIS2_PLACEMENT_3D ( 'NONE', #105754, #63197, #80408 ) ;
#23423=CARTESIAN_POINT ( 'NONE',  ( 37.07355662510760652, 464.0045528213532293, 19.58584291727852644 ) ) ;
#23430=CIRCLE ( 'NONE', #76749, 0.9999999999999854561 ) ;
#23431=CARTESIAN_POINT ( 'NONE',  ( -40.17205142263708240, 310.2804317922712016, -6.358608209523628929 ) ) ;
#23433=CARTESIAN_POINT ( 'NONE',  ( -45.48003679188781234, 379.8448106960472614, 7.220331889307936457 ) ) ;
#23437=CARTESIAN_POINT ( 'NONE',  ( 20.93475926104522600, 304.9197011768563925, -8.985567749925818859 ) ) ;
#23439=CIRCLE ( 'NONE', #83686, 1.000000000000000888 ) ;
#23445=B_SPLINE_CURVE_WITH_KNOTS ( 'NONE', 3,
 ( #46173, #71489, #79063, #80637 ),
 .UNSPECIFIED., .F., .F.,
 ( 4, 4 ),
 ( 0.000000000000000000, 0.002170046543158816663 ),
 .UNSPECIFIED. ) ;
#23447=CARTESIAN_POINT ( 'NONE',  ( 42.91610780537346415, 434.7038292309374015, 17.44089711044166435 ) ) ;
#23456=ORIENTED_EDGE ( 'NONE', *, *, #40686, .T. ) ;
#23461=CARTESIAN_POINT ( 'NONE',  ( 31.00757884493366134, 309.4105030836295782, -8.486170584823613083 ) ) ;
#23483=VERTEX_POINT ( 'NONE', #26832 ) ;
#23485=CARTESIAN_POINT ( 'NONE',  ( 38.85446894546156926, 460.8903912184132992, 2.218456751110441605 ) ) ;
#23486=CARTESIAN_POINT ( 'NONE',  ( -44.26701432268654202, 464.1304138491120170, 8.787925729972910105 ) ) ;
#23501=CARTESIAN_POINT ( 'NONE',  ( -34.12291542400680555, 439.1280893533294147, 24.06048014402972512 ) ) ;
#23502=CARTESIAN_POINT ( 'NONE',  ( 27.81431368193088005, 308.5680772048329459, 11.28096045510426748 ) ) ;
#23504=CARTESIAN_POINT ( 'NONE',  ( -43.55139821557366275, 368.5580705440897873, 13.69133376421734383 ) ) ;
#23506=CARTESIAN_POINT ( 'NONE',  ( -46.00000000000000000, 487.9627413807708081, 0.8148295974594718105 ) ) ;
#23514=CARTESIAN_POINT ( 'NONE',  ( -41.29724588151401576, 485.7091420655430056, -4.558554568099082438 ) ) ;
#23525=CARTESIAN_POINT ( 'NONE',  ( 41.74148791219703725, 464.4898036148945266, 17.08834101213432533 ) ) ;
#23535=FACE_OUTER_BOUND ( 'NONE', #74298, .T. ) ;
#23539=CARTESIAN_POINT ( 'NONE',  ( 15.73174254031733987, 303.5560491714110753, 9.874135506282730290 ) ) ;
#23547=CARTESIAN_POINT ( 'NONE',  ( -39.42128877452295654, 485.2094636432215111, -4.368416090031590926 ) ) ;
#23550=CARTESIAN_POINT ( 'NONE',  ( 43.51084452654482249, 465.2903130129674878, 9.421687747984014649 ) ) ;
#23559=ORIENTED_EDGE ( 'NONE', *, *, #72357, .T. ) ;
#23574=CARTESIAN_POINT ( 'NONE',  ( -45.48126212248870814, 413.7349014071057240, 8.309231847991947362 ) ) ;
#23579=AXIS2_PLACEMENT_3D ( 'NONE', #8516, #41420, #99109 ) ;
#23584=ORIENTED_EDGE ( 'NONE', *, *, #74108, .T. ) ;
#23586=CARTESIAN_POINT ( 'NONE',  ( -26.43366826923012169, 308.0207211451966032, 10.90581097607394057 ) ) ;
#23589=DIRECTION ( 'NONE',  ( 0.000000000000000000, -1.000000000000000000, 0.000000000000000000 ) ) ;
#23591=VERTEX_POINT ( 'NONE', #27371 ) ;
#23611=CARTESIAN_POINT ( 'NONE',  ( 26.97491686565329161, 307.4599153070161606, -9.420584459367196573 ) ) ;
#23615=VERTEX_POINT ( 'NONE', #13244 ) ;
#23634=CARTESIAN_POINT ( 'NONE',  ( 37.31779904297146544, 312.7144339071508057, 14.24890093005832625 ) ) ;
#23636=CIRCLE ( 'NONE', #58094, 15.00000000000001421 ) ;
#23638=AXIS2_PLACEMENT_3D ( 'NONE', #78935, #69794, #55175 ) ;
#23644=CARTESIAN_POINT ( 'NONE',  ( -35.34812152312258604, 364.3443896332000804, 3.939155806205292265 ) ) ;
#23646=CARTESIAN_POINT ( 'NONE',  ( -32.64021143431507710, 300.1493399910716562, 3.126861728487528413 ) ) ;
#23677=VERTEX_POINT ( 'NONE', #37582 ) ;
#23679=CARTESIAN_POINT ( 'NONE',  ( 42.57704743493903266, 486.1612337113410263, 7.852296464539683107 ) ) ;
#23689=DIRECTION ( 'NONE',  ( -0.000000000000000000, -1.000000000000000000, -0.000000000000000000 ) ) ;
#23707=ORIENTED_EDGE ( 'NONE', *, *, #90654, .F. ) ;
#23710=CARTESIAN_POINT ( 'NONE',  ( 31.35087791607053020, 439.7411499371610830, 22.35627675531413061 ) ) ;
#23732=AXIS2_PLACEMENT_3D ( 'NONE', #5101, #87090, #28893 ) ;
#23736=CARTESIAN_POINT ( 'NONE',  ( -31.80704930621334370, 485.2748291366696662, 5.788617803630615732 ) ) ;
#23742=CARTESIAN_POINT ( 'NONE',  ( -15.66789899020478849, 294.5588784006489504, 1.874736099250551957 ) ) ;
#23748=CARTESIAN_POINT ( 'NONE',  ( 33.00000000000000000, 450.0000000000002274, 13.20242257375370976 ) ) ;
#23749=CARTESIAN_POINT ( 'NONE',  ( 35.46673095356709382, 491.6344107835774366, 12.45081314981930909 ) ) ;
#23750=CARTESIAN_POINT ( 'NONE',  ( -34.89132489497384171, 463.6439613888530289, 18.89948583901070123 ) ) ;
#23753=ORIENTED_EDGE ( 'NONE', *, *, #67936, .T. ) ;
#23756=CARTESIAN_POINT ( 'NONE',  ( -2.289807569700440748, 298.7146840682374318, -10.00340823979563609 ) ) ;
#23765=CARTESIAN_POINT ( 'NONE',  ( 30.00000000000000711, 464.1062179653382032, 10.70584622103039329 ) ) ;
#23769=CARTESIAN_POINT ( 'NONE',  ( -31.35792916284521681, 312.3233365065780163, -8.007654514793925316 ) ) ;
#23774=( BOUNDED_SURFACE ( )  B_SPLINE_SURFACE ( 3, 2, ( 
 ( #14959, #47853, #89408 ),
 ( #15503, #67781, #52115 ),
 ( #27905, #60771, #93659 ),
 ( #60250, #101213, #19290 ),
 ( #100670, #1964, #50511 ),
 ( #18183, #59168, #66719 ),
 ( #93118, #85029, #68319 ),
 ( #76386, #11652, #59702 ) ),
 .UNSPECIFIED., .F., .F., .T. ) 
 B_SPLINE_SURFACE_WITH_KNOTS ( ( 4, 2, 2, 4 ),
 ( 3, 3 ),
 ( 0.000000000000000000, 0.002244734355339991771, 0.003367101533009987657, 0.004489468710679983543 ),
 ( 0.000000000000000000, 1.000000000000000000 ),
 .UNSPECIFIED. ) 
 GEOMETRIC_REPRESENTATION_ITEM ( )  RATIONAL_B_SPLINE_SURFACE ( (
 ( 1.000000000000000000, 0.8138888783288348305, 1.000000000000000000),
 ( 1.000000000000000000, 0.8201127045460194775, 1.000000000000000000),
 ( 1.000000000000000000, 0.8211215022295521582, 1.000000000000000000),
 ( 1.000000000000000000, 0.8168533336244402365, 1.000000000000000000),
 ( 1.000000000000000000, 0.8144062529141679052, 1.000000000000000000),
 ( 1.000000000000000000, 0.8072737967831881134, 1.000000000000000000),
 ( 1.000000000000000000, 0.8026171117791235377, 1.000000000000000000),
 ( 1.000000000000000000, 0.7964893136846482591, 1.000000000000000000) ) ) 
 REPRESENTATION_ITEM ( '' )  SURFACE ( )  );
#23775=VERTEX_POINT ( 'NONE', #73597 ) ;
#23777=CARTESIAN_POINT ( 'NONE',  ( -29.95916737693520915, 297.7500670450060625, -1.363754256076671334 ) ) ;
#23785=CARTESIAN_POINT ( 'NONE',  ( 23.05647306551357190, 305.6773795875058681, 9.116627575657666682 ) ) ;
#23789=CARTESIAN_POINT ( 'NONE',  ( -33.50220463782434166, 465.4655183566870846, 16.55182854116007718 ) ) ;
#23812=EDGE_CURVE ( 'NONE', #69611, #8963, #87599, .T. ) ;
#23815=CARTESIAN_POINT ( 'NONE',  ( 21.29975379448952211, 294.8969325209483259, -1.990407376643346327 ) ) ;
#23819=EDGE_CURVE ( 'NONE', #62559, #93551, #16918, .T. ) ;
#23822=ADVANCED_FACE ( 'NONE', ( #18597 ), #84902, .F. ) ;
#23826=CARTESIAN_POINT ( 'NONE',  ( -30.00000000000000000, 461.8802764867013479, 14.89328939273681662 ) ) ;
#23827=CARTESIAN_POINT ( 'NONE',  ( -44.17836536378457168, 435.2619773020560956, 14.65562696767996087 ) ) ;
#23854=CARTESIAN_POINT ( 'NONE',  ( -43.03185303983481447, 485.3613526602391630, 6.073233449168583320 ) ) ;
#23869=CARTESIAN_POINT ( 'NONE',  ( 35.20565090456888413, 464.3972607891108169, 19.03665261460805169 ) ) ;
#23871=CARTESIAN_POINT ( 'NONE',  ( -46.00000000000000711, 488.0476234683169992, 1.803521264818849668 ) ) ;
#23876=CARTESIAN_POINT ( 'NONE',  ( 46.00000000000000000, 460.8575856737739969, 7.929402417993718366 ) ) ;
#23879=FILL_AREA_STYLE ('',( #90171 ) ) ;
#23887=DIRECTION ( 'NONE',  ( -0.9639005798659543434, 0.1664520902827338611, 0.2078205326106775386 ) ) ;
#23891=CARTESIAN_POINT ( 'NONE',  ( 43.61263226029653595, 434.4864728595456427, 10.89080223165081662 ) ) ;
#23901=CARTESIAN_POINT ( 'NONE',  ( -29.34015253733962680, 323.3386329294219195, 13.49677481019017478 ) ) ;
#23920=AXIS2_PLACEMENT_3D ( 'NONE', #99051, #20198, #91527 ) ;
#23930=ORIENTED_EDGE ( 'NONE', *, *, #77415, .F. ) ;
#23937=CARTESIAN_POINT ( 'NONE',  ( 18.46952720637950307, 302.6549406408472009, 9.895497875268649324 ) ) ;
#23951=AXIS2_PLACEMENT_3D ( 'NONE', #13691, #80548, #21834 ) ;
#23952=CARTESIAN_POINT ( 'NONE',  ( 35.05535456316795972, 439.9564985210690224, 24.34373081590672427 ) ) ;
#23968=CARTESIAN_POINT ( 'NONE',  ( 37.40828998627038970, 463.5731143434501291, 19.60478905908873415 ) ) ;
#23971=CARTESIAN_POINT ( 'NONE',  ( 34.13947300040292987, 489.1610961117067973, 11.38003656226467619 ) ) ;
#23975=CARTESIAN_POINT ( 'NONE',  ( -24.37088254901632567, 295.3567874699774620, -9.892597027136796228 ) ) ;
#23977=CARTESIAN_POINT ( 'NONE',  ( -45.49982102694234953, 388.3127959276886827, 7.886590035822850453 ) ) ;
#23981=CARTESIAN_POINT ( 'NONE',  ( 30.40875718013408857, 312.9039625323161431, -7.101849360686649959 ) ) ;
#23993=CARTESIAN_POINT ( 'NONE',  ( -32.82691535583476394, 485.1045372766794799, 1.724905475514959097 ) ) ;
#23997=VERTEX_POINT ( 'NONE', #1710 ) ;
#24005=CARTESIAN_POINT ( 'NONE',  ( 0.000000000000000000, 0.000000000000000000, -10.00000000000000178 ) ) ;
#24007=CARTESIAN_POINT ( 'NONE',  ( 43.65008909229851497, 485.2536725492909682, 3.136905111439891147 ) ) ;
#24009=FILL_AREA_STYLE ('',( #40676 ) ) ;
#24021=DIRECTION ( 'NONE',  ( 0.000000000000000000, 0.000000000000000000, -1.000000000000000000 ) ) ;
#24022=CARTESIAN_POINT ( 'NONE',  ( 36.51699212156835017, 461.3945476718891996, 3.425852496309615525 ) ) ;
#24025=CARTESIAN_POINT ( 'NONE',  ( 42.50585811106661538, 460.9576338508423987, 2.953927975892467472 ) ) ;
#24031=CARTESIAN_POINT ( 'NONE',  ( 32.91521444485818648, 465.6822365171199181, 10.74527606630968357 ) ) ;
#24032=CARTESIAN_POINT ( 'NONE',  ( 30.00000000000035527, 464.1529070875457137, 11.87753652825273143 ) ) ;
#24042=CARTESIAN_POINT ( 'NONE',  ( 33.14480304713701742, 382.6980963264236379, 25.00621942273273746 ) ) ;
#24043=CARTESIAN_POINT ( 'NONE',  ( -42.84559671612151988, 321.7670785502716626, -3.464489948122500884 ) ) ;
#24048=ORIENTED_EDGE ( 'NONE', *, *, #96576, .F. ) ;
#24058=EDGE_LOOP ( 'NONE', ( #86323, #89254, #60885, #59379, #44454 ) ) ;
#24064=CARTESIAN_POINT ( 'NONE',  ( -35.67925427714555298, 491.2490127027255653, 12.19183392504566044 ) ) ;
#24079=ADVANCED_FACE ( 'NONE', ( #16856 ), #43897, .F. ) ;
#24080=CIRCLE ( 'NONE', #89575, 3.000000000000015543 ) ;
#24081=FACE_OUTER_BOUND ( 'NONE', #100536, .T. ) ;
#24083=ADVANCED_FACE ( 'NONE', ( #26581 ), #106218, .T. ) ;
#24093=CARTESIAN_POINT ( 'NONE',  ( 37.88504238421471371, 463.4171042825133213, 19.90923349043903556 ) ) ;
#24103=B_SPLINE_CURVE_WITH_KNOTS ( 'NONE', 3,
 ( #36724, #94401, #78196, #62046 ),
 .UNSPECIFIED., .F., .F.,
 ( 4, 4 ),
 ( 2.693015029076737962E-17, 0.0002092826938343774910 ),
 .UNSPECIFIED. ) ;
#24108=CARTESIAN_POINT ( 'NONE',  ( 34.64323721803893363, 301.0516837800478811, -8.606392057058632972 ) ) ;
#24113=CARTESIAN_POINT ( 'NONE',  ( -32.11411341898570981, 317.7919323371296514, -6.873671351699469412 ) ) ;
#24117=CARTESIAN_POINT ( 'NONE',  ( -43.67170302692484540, 434.9885551707871514, 18.57290719901140363 ) ) ;
#24121=EDGE_CURVE ( 'NONE', #6722, #10424, #82425, .T. ) ;
#24124=CARTESIAN_POINT ( 'NONE',  ( -21.28260013279781759, 304.0447176871748525, 9.978225629331577196 ) ) ;
#24126=CARTESIAN_POINT ( 'NONE',  ( 37.82041704037612107, 485.6919130818703252, -4.511470998796305309 ) ) ;
#24150=FACE_OUTER_BOUND ( 'NONE', #18820, .T. ) ;
#24152=CARTESIAN_POINT ( 'NONE',  ( 21.23684446602550935, 304.9566545053270943, -9.977713076987674512 ) ) ;
#24169=CARTESIAN_POINT ( 'NONE',  ( -43.00000000000000000, 464.8825480873695710, 15.07585856869431851 ) ) ;
#24172=CARTESIAN_POINT ( 'NONE',  ( 43.38684324084172772, 436.1115529209311603, 18.84450155852645636 ) ) ;
#24178=CARTESIAN_POINT ( 'NONE',  ( 36.39978974708674997, 309.1571451204594041, 13.35031817374169805 ) ) ;
#24188=CARTESIAN_POINT ( 'NONE',  ( -22.15408181022044687, 295.0131836217579462, 1.971301972191277896 ) ) ;
#24201=CARTESIAN_POINT ( 'NONE',  ( 36.28420329445040693, 437.5777248398098891, 4.256696328373720917 ) ) ;
#24247=CARTESIAN_POINT ( 'NONE',  ( 31.04372800095298501, 362.9570874249782833, 22.40737358240867749 ) ) ;
#24252=CARTESIAN_POINT ( 'NONE',  ( -42.19618372163387221, 487.7264399052799604, 8.629926728122912394 ) ) ;
#24254=CARTESIAN_POINT ( 'NONE',  ( -32.81992448453860334, 465.7192846569213884, 11.17271167765305862 ) ) ;
#24267=CARTESIAN_POINT ( 'NONE',  ( -4.598202642515742511, 296.0917469169227729, -10.00877229851206707 ) ) ;
#24269=CARTESIAN_POINT ( 'NONE',  ( -34.47678062873981020, 437.1474145881089157, 5.468662283310369077 ) ) ;
#24273=CARTESIAN_POINT ( 'NONE',  ( -7.218639321055465352, 294.7245701161654665, 9.909955229536505428 ) ) ;
#24295=CARTESIAN_POINT ( 'NONE',  ( -6.615709386635189482, 303.7455146892042421, 9.914404184983467871 ) ) ;
#24297=CARTESIAN_POINT ( 'NONE',  ( -31.81126046617210434, 439.4148073498083704, 23.49515931950221059 ) ) ;
#24299=CARTESIAN_POINT ( 'NONE',  ( -29.30744343150515618, 310.6405753734469499, -7.659872152243718979 ) ) ;
#24309=CARTESIAN_POINT ( 'NONE',  ( -21.29121868248358851, 302.9472852280009079, -9.979704577517333419 ) ) ;
#24316=CARTESIAN_POINT ( 'NONE',  ( 31.38879778682737154, 374.5724854738020326, 22.86450524640430615 ) ) ;
#24327=EDGE_LOOP ( 'NONE', ( #102925, #83103, #100579, #8533, #29293 ) ) ;
#24335=VECTOR ( 'NONE', #15171, 1000.000000000000227 ) ;
#24340=ADVANCED_FACE ( 'NONE', ( #89022 ), #87968, .T. ) ;
#24359=EDGE_CURVE ( 'NONE', #81976, #64080, #68452, .T. ) ;
#24365=CARTESIAN_POINT ( 'NONE',  ( 23.61963550967466574, 306.0340374937824777, 10.19690224617928287 ) ) ;
#24372=CARTESIAN_POINT ( 'NONE',  ( 46.00000000000000000, 500.0000000000002274, 12.00000000000000711 ) ) ;
#24380=B_SPLINE_CURVE_WITH_KNOTS ( 'NONE', 3,
 ( #54278, #14355, #13835, #47267, #104442, #87221, #95839, #55864, #30592, #4707, #39728, #80690, #63482, #6810, #80163, #72606, #13300, #38163 ),
 .UNSPECIFIED., .F., .F.,
 ( 4, 2, 2, 2, 2, 2, 2, 2, 4 ),
 ( 0.000000000000000000, 0.001407658255260105370, 0.002815316510520210740, 0.004222974765780315894, 0.005630633021040421481, 0.007038291276300527068, 0.008445949531560631787, 0.009853607786820737374, 0.01126126604208084296 ),
 .UNSPECIFIED. ) ;
#24381=CARTESIAN_POINT ( 'NONE',  ( -3.334877097134691049, 304.8518027755578146, 8.936999414895272054 ) ) ;
#24389=EDGE_CURVE ( 'NONE', #942, #22409, #52963, .T. ) ;
#24412=DIRECTION ( 'NONE',  ( 0.000000000000000000, 0.000000000000000000, 1.000000000000000000 ) ) ;
#24414=CARTESIAN_POINT ( 'NONE',  ( -28.82368679149679025, 297.0884870745862258, -1.512235082149814946 ) ) ;
#24432=CARTESIAN_POINT ( 'NONE',  ( 45.31383884518383098, 362.9196860876334085, 5.161789940898600548 ) ) ;
#24437=CARTESIAN_POINT ( 'NONE',  ( -39.20264847829642463, 436.8475545326365932, 5.145470557645624332 ) ) ;
#24443=EDGE_CURVE ( 'NONE', #47515, #78613, #1412, .T. ) ;
#24462=ORIENTED_EDGE ( 'NONE', *, *, #54679, .F. ) ;
#24470=CARTESIAN_POINT ( 'NONE',  ( -33.16850225799807106, 397.3870901570517162, 25.83374077364281973 ) ) ;
#24477=ADVANCED_FACE ( 'NONE', ( #104129 ), #88002, .T. ) ;
#24483=CARTESIAN_POINT ( 'NONE',  ( -39.40891928560527191, 489.7148911633813100, 11.67978059220125076 ) ) ;
#24485=CARTESIAN_POINT ( 'NONE',  ( 39.83339193442425596, 438.7265728230044033, 23.10267571010011878 ) ) ;
#24488=ORIENTED_EDGE ( 'NONE', *, *, #62905, .F. ) ;
#24494=CARTESIAN_POINT ( 'NONE',  ( -43.51233770565556114, 462.0554640178127670, 4.320559117850118369 ) ) ;
#24498=CARTESIAN_POINT ( 'NONE',  ( 34.68490551323855442, 463.9993046474232301, 18.60480341024936024 ) ) ;
#24504=CARTESIAN_POINT ( 'NONE',  ( -23.43684916743750080, 295.2641918988800285, 10.02474406024658293 ) ) ;
#24506=CARTESIAN_POINT ( 'NONE',  ( -38.68218982724705057, 320.0845437455996603, 16.10279619727025135 ) ) ;
#24509=CARTESIAN_POINT ( 'NONE',  ( 28.42669129514683135, 309.2334035236105478, -8.000929056396238082 ) ) ;
#24517=CARTESIAN_POINT ( 'NONE',  ( -32.94994279514382640, 464.9549361168403152, 15.12478419439365851 ) ) ;
#24523=ORIENTED_EDGE ( 'NONE', *, *, #38504, .F. ) ;
#24527=ORIENTED_EDGE ( 'NONE', *, *, #13257, .T. ) ;
#24528=DIRECTION ( 'NONE',  ( 0.000000000000000000, -0.2013748291394190093, -0.9795142562459567825 ) ) ;
#24533=CARTESIAN_POINT ( 'NONE',  ( 44.26939524491439926, 485.3791217652536716, 2.298766312369611153 ) ) ;
#24536=VERTEX_POINT ( 'NONE', #65141 ) ;
#24544=EDGE_CURVE ( 'NONE', #10763, #51428, #1186, .T. ) ;
#24545=TOROIDAL_SURFACE ( 'NONE', #38320, 7.999999999999983125, 1.000000000000000888 ) ;
#24547=ORIENTED_EDGE ( 'NONE', *, *, #84348, .F. ) ;
#24549=CARTESIAN_POINT ( 'NONE',  ( 38.11830511241422670, 460.5921607997356659, 2.566192292264859010 ) ) ;
#24550=CARTESIAN_POINT ( 'NONE',  ( 0.000000000000000000, 80.00000000000000000, 0.000000000000000000 ) ) ;
#24551=CARTESIAN_POINT ( 'NONE',  ( -13.28202820877807433, 294.5488970812774596, -10.06438453904008945 ) ) ;
#24554=CARTESIAN_POINT ( 'NONE',  ( -35.96642943166444439, 464.0782432590693247, 19.48772549671483389 ) ) ;
#24558=CARTESIAN_POINT ( 'NONE',  ( 30.00000000000000355, 462.0200324021747065, 12.95089283449304496 ) ) ;
#24570=CARTESIAN_POINT ( 'NONE',  ( 28.35254126057398594, 309.9120444834643990, 11.61584289200398956 ) ) ;
#24571=CARTESIAN_POINT ( 'NONE',  ( -36.70796720182337225, 339.3380366985459773, -1.209698081358119071 ) ) ;
#24587=CARTESIAN_POINT ( 'NONE',  ( -36.15790072655923382, 490.9284497187053944, 12.44298047260288165 ) ) ;
#24588=EDGE_CURVE ( 'NONE', #64324, #73045, #32196, .T. ) ;
#24620=VERTEX_POINT ( 'NONE', #32545 ) ;
#24633=CARTESIAN_POINT ( 'NONE',  ( 33.29811181468569004, 300.4441021725457404, -0.7436061328819506544 ) ) ;
#24644=CARTESIAN_POINT ( 'NONE',  ( 43.58517788116362368, 464.0093709438414180, 6.089361716052055229 ) ) ;
#24648=ORIENTED_EDGE ( 'NONE', *, *, #58884, .F. ) ;
#24649=CARTESIAN_POINT ( 'NONE',  ( 35.03683940498239480, 484.2356779365860575, -0.9730041317311258764 ) ) ;
#24655=CARTESIAN_POINT ( 'NONE',  ( 46.00000000000000000, 437.9222508511570595, 13.74115800020442002 ) ) ;
#24661=DIRECTION ( 'NONE',  ( 0.000000000000000000, 0.000000000000000000, -1.000000000000000000 ) ) ;
#24667=CARTESIAN_POINT ( 'NONE',  ( 40.95595929481465447, 405.2208686710653183, 27.85131585683114963 ) ) ;
#24691=CARTESIAN_POINT ( 'NONE',  ( -37.67124221001134288, 463.6239404278531993, 19.49545380201589850 ) ) ;
#24692=ORIENTED_EDGE ( 'NONE', *, *, #90396, .F. ) ;
#24695=CARTESIAN_POINT ( 'NONE',  ( 33.21102376836596903, 438.9613914113129454, 23.92328486949907429 ) ) ;
#24698=CARTESIAN_POINT ( 'NONE',  ( 29.99982483545057121, 316.1377075229455613, 13.18505363741200753 ) ) ;
#24707=ORIENTED_EDGE ( 'NONE', *, *, #11819, .F. ) ;
#24710=CARTESIAN_POINT ( 'NONE',  ( -25.05418058866352382, 295.6716560995653822, 2.113063722413087042 ) ) ;
#24718=EDGE_CURVE ( 'NONE', #71251, #76425, #97668, .T. ) ;
#24722=ORIENTED_EDGE ( 'NONE', *, *, #12792, .T. ) ;
#24737=B_SPLINE_CURVE_WITH_KNOTS ( 'NONE', 3,
 ( #86170, #45169, #53767, #4699 ),
 .UNSPECIFIED., .F., .F.,
 ( 4, 4 ),
 ( 2.525795506525165703E-17, 0.0002485318720365765443 ),
 .UNSPECIFIED. ) ;
#24754=ORIENTED_EDGE ( 'NONE', *, *, #69328, .T. ) ;
#24762=CARTESIAN_POINT ( 'NONE',  ( -8.838593709200374349, 294.6759896675590653, -4.712412173198521792 ) ) ;
#24768=EDGE_LOOP ( 'NONE', ( #16920, #65199, #18030, #67492 ) ) ;
#24769=CARTESIAN_POINT ( 'NONE',  ( 30.82873539022197562, 330.8540204601990240, 16.52588298193462180 ) ) ;
#24772=ORIENTED_EDGE ( 'NONE', *, *, #15126, .T. ) ;
#24796=CARTESIAN_POINT ( 'NONE',  ( -19.99639985080580118, 294.7507280618032155, 9.915515321361612067 ) ) ;
#24799=B_SPLINE_SURFACE_WITH_KNOTS ( 'NONE', 1, 3, ( 
 ( #29861, #86506, #29340, #95111, #87022, #94590, #53575, #45503, #93517, #85970, #53049, #102117, #27755, #12040, #13094, #46021, #78903, #95631, #5030, #87546, #21769, #13627, #60629, #19664, #28274, #52497, #11500, #3435 ),
 ( #36380, #69244, #104776, #96693, #64848, #65383, #22830, #97728, #72407, #48643, #80483, #88076, #30925, #88599, #6070, #71871, #6601, #73451, #56191, #106349, #97205, #7652, #5548, #14154, #55662, #96170, #48116, #39530 ) ),
 .UNSPECIFIED., .F., .F., .F.,
 ( 2, 2 ),
 ( 4, 2, 2, 2, 2, 2, 2, 2, 2, 2, 2, 2, 2, 4 ),
 ( 0.000000000000000000, 1.000000000000000000 ),
 ( 0.08901491201581737678, 0.1032490540155679704, 0.1174831960153185778, 0.1317173380150691853, 0.1459514800148197788, 0.1744197640143299588, 0.2028880480138401388, 0.2598246160128514504, 0.3167611840118632616, 0.4306343200098861623, 0.5445074560079088410, 0.6583805920059359051, 0.7722537280039543095, 1.000000000000000000 ),
 .UNSPECIFIED. ) ;
#24800=CARTESIAN_POINT ( 'NONE',  ( 37.36240688364735973, 491.3429102029600699, 12.25869953513177357 ) ) ;
#24819=CARTESIAN_POINT ( 'NONE',  ( -32.01559026740443414, 317.5007976905572491, -6.946860387831226724 ) ) ;
#24832=CARTESIAN_POINT ( 'NONE',  ( -38.69275568811735866, 485.6230355318863872, -4.306148472019582840 ) ) ;
#24833=CARTESIAN_POINT ( 'NONE',  ( -42.57247758682796501, 361.1230050982096031, 16.58080135936016930 ) ) ;
#24835=CARTESIAN_POINT ( 'NONE',  ( -41.32787293365091585, 464.3526374298369888, 17.58299175745637299 ) ) ;
#24839=CARTESIAN_POINT ( 'NONE',  ( -19.83463548332447601, 303.8035096162418540, 9.926734387303332241 ) ) ;
#24843=CARTESIAN_POINT ( 'NONE',  ( -43.00000000000000000, 436.5989882784185738, 19.94133085611151301 ) ) ;
#24861=CARTESIAN_POINT ( 'NONE',  ( 19.12955214649078428, 294.6724190044754437, -2.037676829496062769 ) ) ;
#24883=CARTESIAN_POINT ( 'NONE',  ( -20.21880305278369150, 304.8280059657581660, -9.005058168222323189 ) ) ;
#24886=CARTESIAN_POINT ( 'NONE',  ( -32.84088564781220043, 464.9638558180865857, 11.24476942535982005 ) ) ;
#24898=CARTESIAN_POINT ( 'NONE',  ( -16.55743558489286826, 303.5680260445984686, 9.876668833592542995 ) ) ;
#24919=CARTESIAN_POINT ( 'NONE',  ( -46.00000000000000000, 488.0336798547363628, -0.8984331811837280579 ) ) ;
#24924=CARTESIAN_POINT ( 'NONE',  ( 46.00000000000000000, 460.3195313667369533, 7.040850765614101725 ) ) ;
#24929=CARTESIAN_POINT ( 'NONE',  ( 32.87547266101574195, 465.6993878536675879, 10.91512469976464850 ) ) ;
#24931=CARTESIAN_POINT ( 'NONE',  ( -29.50656783759020740, 297.4601869455973997, -1.429291789817593861 ) ) ;
#24937=B_SPLINE_CURVE_WITH_KNOTS ( 'NONE', 3,
 ( #4986, #60583, #37916, #78328 ),
 .UNSPECIFIED., .F., .F.,
 ( 4, 4 ),
 ( 6.071532165918824830E-18, 0.0006696797651157682238 ),
 .UNSPECIFIED. ) ;
#24942=DIRECTION ( 'NONE',  ( 0.3968475291348044776, 0.1146398630990837497, -0.9106973923363477219 ) ) ;
#24946=CARTESIAN_POINT ( 'NONE',  ( 35.76379064120181539, 307.0162303970107587, 12.81051142610679960 ) ) ;
#24949=CARTESIAN_POINT ( 'NONE',  ( -43.99295543319385615, 464.6035880629004282, 10.45302038923090748 ) ) ;
#24951=CARTESIAN_POINT ( 'NONE',  ( -39.86396139244069303, 437.4902212974461690, 4.924226175446892562 ) ) ;
#24952=CARTESIAN_POINT ( 'NONE',  ( -31.44900114652979184, 397.6410742345365747, 24.40761942929495021 ) ) ;
#24956=CARTESIAN_POINT ( 'NONE',  ( 43.00000000000000000, 436.0987441542287115, 7.567257455462724991 ) ) ;
#24964=CARTESIAN_POINT ( 'NONE',  ( 32.01443999233854498, 362.7175041558164708, 22.60295584479863962 ) ) ;
#24965=CARTESIAN_POINT ( 'NONE',  ( -33.20902353462242473, 484.6199955813539759, 4.299886535036168134 ) ) ;
#24984=CARTESIAN_POINT ( 'NONE',  ( -32.88644894021390996, 356.0147610692134776, 21.80302539000014050 ) ) ;
#25000=CARTESIAN_POINT ( 'NONE',  ( -34.89857526195044102, 437.7187790665907983, 4.586527422595223058 ) ) ;
#25007=PRODUCT_DEFINITION_FORMATION_WITH_SPECIFIED_SOURCE ( 'ANY', '', #99384, .NOT_KNOWN. ) ;
#25012=ADVANCED_FACE ( 'NONE', ( #9684 ), #3263, .F. ) ;
#25013=CARTESIAN_POINT ( 'NONE',  ( 35.96642943166446571, 464.0782432590749522, 19.48772549671354781 ) ) ;
#25019=CARTESIAN_POINT ( 'NONE',  ( -20.97754405179121662, 294.8763868968453608, 9.942224931492262385 ) ) ;
#25024=CARTESIAN_POINT ( 'NONE',  ( 20.21880305278368439, 304.8280059657581660, -9.005058168222323189 ) ) ;
#25053=SURFACE_STYLE_FILL_AREA ( #82730 ) ;
#25062=ORIENTED_EDGE ( 'NONE', *, *, #30294, .T. ) ;
#25065=CARTESIAN_POINT ( 'NONE',  ( 33.83623258902267850, 330.0920146021361461, -2.810346497816497369 ) ) ;
#25069=ORIENTED_EDGE ( 'NONE', *, *, #90324, .T. ) ;
#25072=CARTESIAN_POINT ( 'NONE',  ( 20.06460911473395470, 302.7901891854631913, -10.01309647120555013 ) ) ;
#25076=CARTESIAN_POINT ( 'NONE',  ( -35.85615118283770641, 463.5955582468936882, 19.55698106745636977 ) ) ;
#25081=CARTESIAN_POINT ( 'NONE',  ( 17.08544069068336668, 304.5690947107618740, -10.06009145438461161 ) ) ;
#25088=ORIENTED_EDGE ( 'NONE', *, *, #11819, .T. ) ;
#25093=CARTESIAN_POINT ( 'NONE',  ( -37.64383558481692660, 375.6724030661061988, 4.848939086997407166 ) ) ;
#25124=DIRECTION ( 'NONE',  ( -0.2266275398141938957, 0.09415776302217854221, 0.9694195551258625310 ) ) ;
#25126=CARTESIAN_POINT ( 'NONE',  ( -13.68764148674883430, 294.5450735065955996, 9.871802096439328267 ) ) ;
#25151=ORIENTED_EDGE ( 'NONE', *, *, #56144, .T. ) ;
#25165=CARTESIAN_POINT ( 'NONE',  ( 34.73933834331388937, 301.1522517439193507, -8.582803626330811397 ) ) ;
#25176=CARTESIAN_POINT ( 'NONE',  ( 43.63769803434600902, 379.1446434011715496, 14.87092719457540113 ) ) ;
#25180=CARTESIAN_POINT ( 'NONE',  ( -21.07176076349410820, 305.0225856740397035, 9.973527527123424719 ) ) ;
#25182=CARTESIAN_POINT ( 'NONE',  ( 34.22523139975753281, 485.0580393423874170, -1.439874417901405135 ) ) ;
#25184=CARTESIAN_POINT ( 'NONE',  ( 32.72014288347716615, 485.4774019870154120, 6.282418260585018288 ) ) ;
#25190=CARTESIAN_POINT ( 'NONE',  ( 46.00000000000000000, 437.9690125970931831, 14.09127711025715080 ) ) ;
#25207=CARTESIAN_POINT ( 'NONE',  ( 20.52350613252515643, 304.8999024697870937, 9.947223320822450532 ) ) ;
#25210=DIRECTION ( 'NONE',  ( 0.000000000000000000, 0.000000000000000000, -1.000000000000000000 ) ) ;
#25227=CARTESIAN_POINT ( 'NONE',  ( -40.97817787413512036, 465.3187661920380265, 16.73602713972349676 ) ) ;
#25228=CARTESIAN_POINT ( 'NONE',  ( -29.96292276380026465, 332.4061231152326172, 16.64388083012304875 ) ) ;
#25236=CARTESIAN_POINT ( 'NONE',  ( 34.53878426067466734, 302.4591013005480136, 3.675451461037441359 ) ) ;
#25248=CARTESIAN_POINT ( 'NONE',  ( -24.37690711297229740, 295.5467921614321085, 10.08613426303809923 ) ) ;
#25253=CARTESIAN_POINT ( 'NONE',  ( 44.13343456913768392, 464.3829732007686175, 9.622105740879975500 ) ) ;
#25265=B_SPLINE_CURVE_WITH_KNOTS ( 'NONE', 3,
 ( #2399, #35345, #68206, #27263 ),
 .UNSPECIFIED., .F., .F.,
 ( 4, 4 ),
 ( 1.760524696717142919E-15, 0.001000218973296797091 ),
 .UNSPECIFIED. ) ;
#25270=CARTESIAN_POINT ( 'NONE',  ( -32.92227116393205932, 439.7404285724725241, 24.14402898922834240 ) ) ;
#25274=CARTESIAN_POINT ( 'NONE',  ( -33.84761347220299399, 488.7471039746336032, 11.01988148152527103 ) ) ;
#25281=CIRCLE ( 'NONE', #85568, 0.9999999999999961142 ) ;
#25287=EDGE_CURVE ( 'NONE', #38837, #88625, #59124, .T. ) ;
#25300=DIRECTION ( 'NONE',  ( 0.2276885448027893277, 0.1882482561681191047, 0.9553640775197957957 ) ) ;
#25308=CARTESIAN_POINT ( 'NONE',  ( 30.95257640470975602, 348.4999900758657532, 18.99904917110374214 ) ) ;
#25318=CARTESIAN_POINT ( 'NONE',  ( -20.52350613252515643, 304.8999024697870937, 9.947223320822450532 ) ) ;
#25324=CARTESIAN_POINT ( 'NONE',  ( 43.17545047952468451, 487.6211760455611284, 8.487215481668586747 ) ) ;
#25335=DIRECTION ( 'NONE',  ( 0.9788760387920804051, 0.000000000000000000, 0.2044546421060805530 ) ) ;
#25339=CARTESIAN_POINT ( 'NONE',  ( 36.50840931121960153, 491.4427145161587873, 12.32866606331501202 ) ) ;
#25346=CIRCLE ( 'NONE', #75263, 0.9999999999999985567 ) ;
#25347=CARTESIAN_POINT ( 'NONE',  ( -33.00000000000000000, 464.3970849722209664, 17.41240408234212111 ) ) ;
#25358=CARTESIAN_POINT ( 'NONE',  ( -31.30848237729719230, 439.0139854832817150, 22.67909095395106789 ) ) ;
#25360=CARTESIAN_POINT ( 'NONE',  ( -27.48025251572867234, 308.0883985054451841, -8.272527303563915524 ) ) ;
#25368=ORIENTED_EDGE ( 'NONE', *, *, #30661, .F. ) ;
#25370=EDGE_CURVE ( 'NONE', #45699, #73133, #91425, .T. ) ;
#25371=CARTESIAN_POINT ( 'NONE',  ( -23.56457664856237599, 303.4636367812840376, -9.868556678049921871 ) ) ;
#25376=CARTESIAN_POINT ( 'NONE',  ( -42.70159805713172574, 373.1387034520102475, 18.11088861087180391 ) ) ;
#25383=ORIENTED_EDGE ( 'NONE', *, *, #94369, .T. ) ;
#25385=CARTESIAN_POINT ( 'NONE',  ( 30.00000000000000355, 489.0498425200157158, 4.975187970393438519 ) ) ;
#25386=CIRCLE ( 'NONE', #101198, 3.000000000000013323 ) ;
#25387=B_SPLINE_CURVE_WITH_KNOTS ( 'NONE', 3,
 ( #25811, #75354, #58665, #82392, #99090, #91567, #74294, #8498, #9023, #57040, #81312, #90489, #73219, #74815, #33874, #89955, #41401, #66205, #98568, #50538, #1455, #17147, #63168, #48942, #9554, #7424 ),
 .UNSPECIFIED., .F., .F.,
 ( 4, 2, 2, 2, 2, 2, 2, 2, 2, 2, 2, 2, 4 ),
 ( 6.942281208919283290E-18, 0.001948376510295373376, 0.002922564765443056919, 0.003896753020590740680, 0.005845129530886042715, 0.007793506041181345184, 0.009741882551476647653, 0.01169025906177195012, 0.01266444731691965947, 0.01363863557206736535, 0.01461282382721507296, 0.01509991795478892590, 0.01558701208236277884 ),
 .UNSPECIFIED. ) ;
#25391=CARTESIAN_POINT ( 'NONE',  ( 43.11534632275463963, 435.4435433140298528, 9.329549855361591426 ) ) ;
#25433=CARTESIAN_POINT ( 'NONE',  ( 34.94338628507543376, 342.5355909536760350, -0.9693026116843473927 ) ) ;
#25434=CARTESIAN_POINT ( 'NONE',  ( 40.90837589346737957, 460.4813280201769885, 2.460853848284856760 ) ) ;
#25441=B_SPLINE_CURVE_WITH_KNOTS ( 'NONE', 3,
 ( #16273, #30906, #63787, #72386 ),
 .UNSPECIFIED., .F., .F.,
 ( 4, 4 ),
 ( 1.600194022572398637E-15, 0.0002604505668095903267 ),
 .UNSPECIFIED. ) ;
#25449=CARTESIAN_POINT ( 'NONE',  ( -18.20176702087010057, 303.6397689725556575, 9.891910795295462577 ) ) ;
#25454=CARTESIAN_POINT ( 'NONE',  ( -32.15310320217076878, 439.7024266304582625, 23.94087012106557211 ) ) ;
#25472=CARTESIAN_POINT ( 'NONE',  ( 46.00000000000000000, 461.1597079622285946, 8.544206286667911598 ) ) ;
#25476=FACE_OUTER_BOUND ( 'NONE', #12074, .T. ) ;
#25478=EDGE_CURVE ( 'NONE', #65653, #68930, #16223, .T. ) ;
#25479=CARTESIAN_POINT ( 'NONE',  ( -34.71762651478146466, 302.0735516083713037, -0.3584149496404396840 ) ) ;
#25486=CARTESIAN_POINT ( 'NONE',  ( 44.34415387544843412, 435.2422591719042657, 12.20585227837244702 ) ) ;
#25487=CIRCLE ( 'NONE', #37588, 0.9999999999999966693 ) ;
#25496=CARTESIAN_POINT ( 'NONE',  ( 33.51920064736375338, 462.9438705373632388, 5.599630057702720265 ) ) ;
#25498=CARTESIAN_POINT ( 'NONE',  ( -29.90889627134798090, 328.9483774411300487, 14.84562707069868637 ) ) ;
#25503=CARTESIAN_POINT ( 'NONE',  ( -33.78214696080224400, 461.9283447517260015, 7.821959111644967599 ) ) ;
#25505=EDGE_CURVE ( 'NONE', #15460, #52539, #70055, .T. ) ;
#25509=CARTESIAN_POINT ( 'NONE',  ( 42.63927665717513804, 462.0185602173703501, 4.112661701976962902 ) ) ;
#25510=CARTESIAN_POINT ( 'NONE',  ( 30.93990408052894381, 332.3813973617133684, 16.87533365184100376 ) ) ;
#25533=CARTESIAN_POINT ( 'NONE',  ( -33.15394466697068054, 409.2619214805569641, 25.87672194516226654 ) ) ;
#25538=CARTESIAN_POINT ( 'NONE',  ( -1.407990191586397932, 302.0882495255234517, 9.900872584904373497 ) ) ;
#25547=CARTESIAN_POINT ( 'NONE',  ( 38.08110185299304362, 439.4416046545700851, 23.85860822400425363 ) ) ;
#25550=DIRECTION ( 'NONE',  ( 0.000000000000000000, 0.000000000000000000, 1.000000000000000000 ) ) ;
#25556=CARTESIAN_POINT ( 'NONE',  ( 46.00000000000001421, 487.9843608680976104, -0.2179797824887820534 ) ) ;
#25559=CARTESIAN_POINT ( 'NONE',  ( -42.63927665720805749, 462.0185602173216353, 4.112661701945640402 ) ) ;
#25563=CARTESIAN_POINT ( 'NONE',  ( 36.69926874265758698, 463.5184712008513657, 19.71956904107949882 ) ) ;
#25566=CARTESIAN_POINT ( 'NONE',  ( 31.35596682365711274, 438.0939828603570732, 22.55458131664589061 ) ) ;
#25575=CARTESIAN_POINT ( 'NONE',  ( 28.98194489702799004, 310.1023937361698017, -7.790637802078380858 ) ) ;
#25589=CARTESIAN_POINT ( 'NONE',  ( -35.73700087854410867, 437.1201388800316181, 4.567739269148499481 ) ) ;
#25600=ORIENTED_EDGE ( 'NONE', *, *, #61740, .F. ) ;
#25616=CARTESIAN_POINT ( 'NONE',  ( 21.67097115919219519, 305.0473406493022139, -8.958495691138132599 ) ) ;
#25624=CARTESIAN_POINT ( 'NONE',  ( -15.42316984156294168, 294.5569238556877849, -2.062679335141809123 ) ) ;
#25637=CARTESIAN_POINT ( 'NONE',  ( -46.00000000000000000, 438.3878896346936358, 16.22878885428542262 ) ) ;
#25644=CARTESIAN_POINT ( 'NONE',  ( -30.75264184865481809, 308.9867225161979718, -8.589175589975059921 ) ) ;
#25651=EDGE_LOOP ( 'NONE', ( #50758, #83381, #76385, #43658, #92654, #57045 ) ) ;
#25663=( BOUNDED_SURFACE ( )  B_SPLINE_SURFACE ( 3, 2, ( 
 ( #25253, #33875, #41933 ),
 ( #27405, #1996, #60283 ),
 ( #66752, #93152, #67292 ),
 ( #58667, #99091, #75899 ) ),
 .UNSPECIFIED., .F., .F., .T. ) 
 B_SPLINE_SURFACE_WITH_KNOTS ( ( 4, 4 ),
 ( 3, 3 ),
 ( 0.01114851999726041223, 0.01303042415394033669 ),
 ( 0.1618064000426147064, 1.000000000000000000 ),
 .UNSPECIFIED. ) 
 GEOMETRIC_REPRESENTATION_ITEM ( )  RATIONAL_B_SPLINE_SURFACE ( (
 ( 0.9362898844563825040, 0.8031285674520963758, 1.000000000000000000),
 ( 0.9312276682860366472, 0.7874857493404125997, 1.000000000000000000),
 ( 0.9259581024412342209, 0.7712021973813599773, 1.000000000000000000),
 ( 0.9205526622925819247, 0.7544987785202129649, 1.000000000000000000) ) ) 
 REPRESENTATION_ITEM ( '' )  SURFACE ( )  );
#25670=CARTESIAN_POINT ( 'NONE',  ( -36.47828316237969659, 491.8387149836262324, 12.58546224878396735 ) ) ;
#25681=VERTEX_POINT ( 'NONE', #12380 ) ;
#25700=CARTESIAN_POINT ( 'NONE',  ( -42.08762648273019380, 487.0030674539066808, 9.106351919860241395 ) ) ;
#25719=CARTESIAN_POINT ( 'NONE',  ( 27.02761694636049583, 305.0378212988403561, -9.518998403309037570 ) ) ;
#25732=AXIS2_PLACEMENT_3D ( 'NONE', #106274, #72847, #41033 ) ;
#25741=CARTESIAN_POINT ( 'NONE',  ( 31.96724538747933764, 486.9512181893505272, 7.078368790602016070 ) ) ;
#25745=CARTESIAN_POINT ( 'NONE',  ( 46.00000000000000000, 437.8919113138612147, 12.69150955564872874 ) ) ;
#25746=EDGE_LOOP ( 'NONE', ( #86958, #48012, #106109, #9469, #68177, #3623 ) ) ;
#25756=CARTESIAN_POINT ( 'NONE',  ( 39.13885763974980136, 324.4948203046521371, 17.18769520460729439 ) ) ;
#25759=CARTESIAN_POINT ( 'NONE',  ( 20.24579557674104890, 304.8297271373346575, -10.00469232190994084 ) ) ;
#25760=CARTESIAN_POINT ( 'NONE',  ( -32.10528697966012857, 486.1671898930081852, 5.449875171704860577 ) ) ;
#25771=CARTESIAN_POINT ( 'NONE',  ( -32.18152649027052803, 409.5700136857448683, 25.68904360494498462 ) ) ;
#25773=ADVANCED_FACE ( 'NONE', ( #46359 ), #13966, .T. ) ;
#25781=CARTESIAN_POINT ( 'NONE',  ( -30.38822253705984977, 339.6140856355796132, 18.22937297894274522 ) ) ;
#25786=CARTESIAN_POINT ( 'NONE',  ( 42.73089261237365832, 435.7309723475635224, 18.11242468272458339 ) ) ;
#25787=EDGE_CURVE ( 'NONE', #63799, #35905, #80869, .T. ) ;
#25788=ORIENTED_EDGE ( 'NONE', *, *, #73923, .T. ) ;
#25792=CARTESIAN_POINT ( 'NONE',  ( 24.42072771677381127, 304.1864907082163541, 10.22967129747842385 ) ) ;
#25800=CARTESIAN_POINT ( 'NONE',  ( 33.96616553272742323, 301.6615848611037904, 3.484217928160723954 ) ) ;
#25801=DIRECTION ( 'NONE',  ( 0.2042951644570906167, 0.03948950745688053349, 0.9781125009835337503 ) ) ;
#25802=DIRECTION ( 'NONE',  ( 1.000000000000000000, 0.000000000000000000, 0.000000000000000000 ) ) ;
#25805=CARTESIAN_POINT ( 'NONE',  ( -25.49348957563488227, 295.8024135625230429, 2.141455523061916999 ) ) ;
#25810=CARTESIAN_POINT ( 'NONE',  ( 33.00000000000000000, 500.0000000000002274, 0.000000000000000000 ) ) ;
#25811=CARTESIAN_POINT ( 'NONE',  ( 9.819056950928633398, 294.6481068335447731, 1.893705519456528208 ) ) ;
#25813=DIRECTION ( 'NONE',  ( 0.000000000000000000, 0.000000000000000000, 1.000000000000000000 ) ) ;
#25815=CARTESIAN_POINT ( 'NONE',  ( 43.71037717921923615, 462.3391554988761527, 4.824299547763561513 ) ) ;
#25830=CARTESIAN_POINT ( 'NONE',  ( -31.62289491507650041, 439.0131222673971365, 23.39481604279367488 ) ) ;
#25833=DIRECTION ( 'NONE',  ( 0.7611201562151608258, 0.000000000000000000, -0.6486109063244381856 ) ) ;
#25834=CARTESIAN_POINT ( 'NONE',  ( 44.51476414916738378, 462.1216129963507910, 5.766699645629802973 ) ) ;
#25836=CARTESIAN_POINT ( 'NONE',  ( 33.94783393359901424, 484.1261039197349305, 1.321740980884986039 ) ) ;
#25857=CARTESIAN_POINT ( 'NONE',  ( 9.730534315287435732, 294.6502823553246344, -2.323512206574427807 ) ) ;
#25864=CARTESIAN_POINT ( 'NONE',  ( 28.39284659809811373, 318.1946778488376140, 13.22144771204134095 ) ) ;
#25870=CARTESIAN_POINT ( 'NONE',  ( -32.66130572512955865, 465.7845731394322115, 12.51261058353286515 ) ) ;
#25875=CARTESIAN_POINT ( 'NONE',  ( -35.56416567323501710, 480.2820146177156175, -4.363888856302766683 ) ) ;
#25883=VERTEX_POINT ( 'NONE', #53904 ) ;
#25884=CARTESIAN_POINT ( 'NONE',  ( 35.98123173773587524, 437.4058846046290796, 4.371064750171454349 ) ) ;
#25885=CARTESIAN_POINT ( 'NONE',  ( -9.398978598902781201, 294.6597737643588744, -3.429745804552094324 ) ) ;
#25893=DIRECTION ( 'NONE',  ( -0.2042951644570322467, 0.03948950745649387750, 0.9781125009835615058 ) ) ;
#25903=CARTESIAN_POINT ( 'NONE',  ( -4.023896803983132209, 300.5161690456517363, -10.00978837624883155 ) ) ;
#25913=CARTESIAN_POINT ( 'NONE',  ( -31.43208348565051935, 438.4707862388146395, 22.17802677911202380 ) ) ;
#25914=CARTESIAN_POINT ( 'NONE',  ( 32.75411547143891511, 465.7435926370463903, 11.50418982276139879 ) ) ;
#25915=CARTESIAN_POINT ( 'NONE',  ( -28.76324779970338241, 309.5459823743811398, -8.926984934462732113 ) ) ;
#25920=CARTESIAN_POINT ( 'NONE',  ( -43.86611073477271816, 435.5752409525268831, 9.535927547476964250 ) ) ;
#25926=LINE ( 'NONE', #31858, #86623 ) ;
#25928=CARTESIAN_POINT ( 'NONE',  ( -33.10739874314164410, 427.7875163274654255, 25.07383443705004922 ) ) ;
#25929=CARTESIAN_POINT ( 'NONE',  ( -32.86259851300427215, 485.9239370913668949, 5.440925357814620611 ) ) ;
#25941=CARTESIAN_POINT ( 'NONE',  ( 43.51047069090565600, 435.7684321374258616, 8.546621873845968054 ) ) ;
#25959=CARTESIAN_POINT ( 'NONE',  ( 37.83989825151499531, 491.6297408768496098, 12.44743998625077630 ) ) ;
#25969=LINE ( 'NONE', #1067, #1338 ) ;
#25978=CARTESIAN_POINT ( 'NONE',  ( 34.06332199976886699, 330.0526646846329299, -3.810096259360388427 ) ) ;
#25989=( BOUNDED_SURFACE ( )  B_SPLINE_SURFACE ( 3, 2, ( 
 ( #64192, #55519, #88460 ),
 ( #14535, #47444, #982 ),
 ( #57652, #42014, #84075 ),
 ( #17236, #17759, #42543 ) ),
 .UNSPECIFIED., .F., .F., .F. ) 
 B_SPLINE_SURFACE_WITH_KNOTS ( ( 4, 4 ),
 ( 3, 3 ),
 ( 4.336808689942017736E-19, 0.001384307398009136702 ),
 ( 0.000000000000000000, 1.000000000000000000 ),
 .UNSPECIFIED. ) 
 GEOMETRIC_REPRESENTATION_ITEM ( )  RATIONAL_B_SPLINE_SURFACE ( (
 ( 1.000000000000000000, 0.7976994903569329942, 1.000000000000000000),
 ( 1.000000000000000000, 0.8073889694077948098, 1.000000000000000000),
 ( 1.000000000000000000, 0.8171087964275586257, 1.000000000000000000),
 ( 1.000000000000000000, 0.8266506655095640088, 1.000000000000000000) ) ) 
 REPRESENTATION_ITEM ( '' )  SURFACE ( )  );
#25993=CARTESIAN_POINT ( 'NONE',  ( -18.15175992912209324, 304.6383698585960929, 8.891572390514982160 ) ) ;
#26012=ORIENTED_EDGE ( 'NONE', *, *, #42280, .F. ) ;
#26013=CARTESIAN_POINT ( 'NONE',  ( -46.00000000000002132, 487.9826193845792659, -0.2183537434872499794 ) ) ;
#26025=CARTESIAN_POINT ( 'NONE',  ( 32.85889741710023060, 464.9534104978457094, 11.16060310718602544 ) ) ;
#26039=DIRECTION ( 'NONE',  ( 0.000000000000000000, 0.000000000000000000, -1.000000000000000000 ) ) ;
#26058=CARTESIAN_POINT ( 'NONE',  ( 27.74070829223574464, 311.1873351945520199, 11.69411441391677009 ) ) ;
#26074=CARTESIAN_POINT ( 'NONE',  ( -23.55598625820995196, 303.7182208366987197, 10.12520193139073577 ) ) ;
#26100=CARTESIAN_POINT ( 'NONE',  ( -42.79891897445037330, 462.9518546950670270, 4.196605471987052027 ) ) ;
#26104=CARTESIAN_POINT ( 'NONE',  ( 33.00000000000000000, 435.0774731480752280, 11.67986145722081304 ) ) ;
#26109=DIRECTION ( 'NONE',  ( -1.000000000000000000, 0.000000000000000000, 0.000000000000000000 ) ) ;
#26130=CARTESIAN_POINT ( 'NONE',  ( -35.05271644150329280, 437.8393516193276582, 4.418594605291610300 ) ) ;
#26155=CARTESIAN_POINT ( 'NONE',  ( 31.84958088623538686, 317.5633087689430454, -5.928141683191124223 ) ) ;
#26167=CARTESIAN_POINT ( 'NONE',  ( 32.95589646111110937, 464.8957215206408478, 10.75300444715717951 ) ) ;
#26169=CARTESIAN_POINT ( 'NONE',  ( 29.99999999999995381, 464.1568293259584834, 11.21040210117823399 ) ) ;
#26182=CARTESIAN_POINT ( 'NONE',  ( -35.91510745124932669, 303.8491723658412411, 0.06940248214010066863 ) ) ;
#26185=EDGE_CURVE ( 'NONE', #21601, #75683, #54625, .T. ) ;
#26193=VERTEX_POINT ( 'NONE', #92116 ) ;
#26205=AXIS2_PLACEMENT_3D ( 'NONE', #100597, #9445, #1889 ) ;
#26206=CARTESIAN_POINT ( 'NONE',  ( 30.00000000000000000, 450.0000000000002274, 13.20242257375370976 ) ) ;
#26222=ORIENTED_EDGE ( 'NONE', *, *, #54776, .F. ) ;
#26231=CARTESIAN_POINT ( 'NONE',  ( -32.15310320217076878, 439.7024266304582625, 23.94087012106557211 ) ) ;
#26232=CARTESIAN_POINT ( 'NONE',  ( 37.22806219797154625, 463.3233819687148980, 20.09366234602714840 ) ) ;
#26240=CARTESIAN_POINT ( 'NONE',  ( -41.57853049034962112, 486.1006523484328454, 12.35204812598594160 ) ) ;
#26241=CARTESIAN_POINT ( 'NONE',  ( -36.66795030846187586, 306.3035926564865008, 4.617914666504396415 ) ) ;
#26247=CARTESIAN_POINT ( 'NONE',  ( 33.41308119780744335, 300.5641305218781554, -0.7154550005598049323 ) ) ;
#26249=EDGE_CURVE ( 'NONE', #48477, #54135, #25346, .T. ) ;
#26252=CARTESIAN_POINT ( 'NONE',  ( 46.00000000000000000, 500.0000000000002274, 0.000000000000000000 ) ) ;
#26260=CARTESIAN_POINT ( 'NONE',  ( 37.61995183727506031, 438.1738172413044481, 4.432413526166450346 ) ) ;
#26264=CARTESIAN_POINT ( 'NONE',  ( -20.39914337211097006, 304.8937497850257614, 9.945937256050433106 ) ) ;
#26266=CARTESIAN_POINT ( 'NONE',  ( 32.94021323899734455, 485.0599191339525191, 5.361609822540892800 ) ) ;
#26268=CARTESIAN_POINT ( 'NONE',  ( 32.10528697966010014, 486.1671898930082421, 5.449875171705066634 ) ) ;
#26271=CARTESIAN_POINT ( 'NONE',  ( 44.31720021651388919, 435.2315751315647958, 12.07978424043336929 ) ) ;
#26274=AXIS2_PLACEMENT_3D ( 'NONE', #75041, #71, #97727 ) ;
#26287=CARTESIAN_POINT ( 'NONE',  ( 40.77380256327629837, 468.8478597483947965, 21.13608272249925690 ) ) ;
#26300=( BOUNDED_SURFACE ( )  B_SPLINE_SURFACE ( 3, 2, ( 
 ( #65041, #41296, #55854 ),
 ( #89331, #82281, #65577 ),
 ( #14351, #6260, #97939 ),
 ( #22505, #90383, #15961 ) ),
 .UNSPECIFIED., .F., .F., .F. ) 
 B_SPLINE_SURFACE_WITH_KNOTS ( ( 4, 4 ),
 ( 3, 3 ),
 ( 0.01611645847898578870, 0.01831749139115683780 ),
 ( 0.000000000000000000, 0.8386188628085423646 ),
 .UNSPECIFIED. ) 
 GEOMETRIC_REPRESENTATION_ITEM ( )  RATIONAL_B_SPLINE_SURFACE ( (
 ( 1.000000000000000000, 0.7543742219143267924, 0.9207212652179949108),
 ( 1.000000000000000000, 0.7738259253571172502, 0.9269995412618118324),
 ( 1.000000000000000000, 0.7927721361627113605, 0.9331146633523637046),
 ( 1.000000000000000000, 0.8105494169260334392, 0.9388524989238771212) ) ) 
 REPRESENTATION_ITEM ( '' )  SURFACE ( )  );
#26311=CARTESIAN_POINT ( 'NONE',  ( -32.19533475021953706, 392.4752074454114563, 25.42422936412204493 ) ) ;
#26320=CARTESIAN_POINT ( 'NONE',  ( 26.96170002121218801, 306.9387515484356186, 10.87917313509033335 ) ) ;
#26326=CARTESIAN_POINT ( 'NONE',  ( 24.30812977188561419, 295.4061218410959100, 2.054700292315147170 ) ) ;
#26330=VERTEX_POINT ( 'NONE', #56419 ) ;
#26332=CARTESIAN_POINT ( 'NONE',  ( -24.62889686368193765, 295.5521682776166585, 2.087298195416544377 ) ) ;
#26335=CARTESIAN_POINT ( 'NONE',  ( -32.83703342409244641, 465.7129651006319477, 11.08653443108803138 ) ) ;
#26340=FACE_OUTER_BOUND ( 'NONE', #94558, .T. ) ;
#26380=VERTEX_POINT ( 'NONE', #10540 ) ;
#26381=CARTESIAN_POINT ( 'NONE',  ( -7.895830884676383832, 294.7033644922051963, -6.143025603150206848 ) ) ;
#26384=CARTESIAN_POINT ( 'NONE',  ( 3.887627447353766641, 294.8076638163112762, -9.231226148363823825 ) ) ;
#26389=ORIENTED_EDGE ( 'NONE', *, *, #71650, .F. ) ;
#26390=CARTESIAN_POINT ( 'NONE',  ( 31.59989307617499321, 345.3384981963453129, 19.62160995718464207 ) ) ;
#26398=CARTESIAN_POINT ( 'NONE',  ( -43.99225961071505253, 464.6045839418125638, 10.45666854317281036 ) ) ;
#26400=CARTESIAN_POINT ( 'NONE',  ( 38.81358894280276672, 485.1131561813238591, -4.191378885298274959 ) ) ;
#26413=CARTESIAN_POINT ( 'NONE',  ( 32.88333705524082973, 439.7317646416722141, 24.13381181826093069 ) ) ;
#26421=CARTESIAN_POINT ( 'NONE',  ( -32.93513049338658760, 465.6726574193328361, 10.66039033145138326 ) ) ;
#26424=EDGE_LOOP ( 'NONE', ( #92241, #83269, #21277, #62668, #55551, #58225, #103599, #89473, #88990, #40187 ) ) ;
#26426=CARTESIAN_POINT ( 'NONE',  ( -46.00000000000000000, 437.9690125970932399, 14.09127711025738883 ) ) ;
#26436=CARTESIAN_POINT ( 'NONE',  ( 35.45036406932566564, 436.3203772529585649, 5.179456583034234285 ) ) ;
#26437=CARTESIAN_POINT ( 'NONE',  ( -23.41949505512490504, 304.4436526223547048, -9.872909214488972296 ) ) ;
#26446=CARTESIAN_POINT ( 'NONE',  ( -33.88237199998296489, 485.0486819176492759, 1.241522336454282227 ) ) ;
#26447=CARTESIAN_POINT ( 'NONE',  ( -42.19277509307554652, 346.1477229841391363, 13.95430603839016648 ) ) ;
#26458=CARTESIAN_POINT ( 'NONE',  ( -39.28083343692465945, 437.8791283697678409, 22.93287928653034058 ) ) ;
#26463=CARTESIAN_POINT ( 'NONE',  ( 32.20627895475151092, 464.6794106235104209, 10.68705400064636812 ) ) ;
#26475=CARTESIAN_POINT ( 'NONE',  ( 22.08400538955477899, 294.9973745800270990, -1.969057594002644906 ) ) ;
#26478=CARTESIAN_POINT ( 'NONE',  ( -13.63130828375568981, 294.5445729804733901, -10.06530370901874072 ) ) ;
#26488=VERTEX_POINT ( 'NONE', #50986 ) ;
#26493=ORIENTED_EDGE ( 'NONE', *, *, #61984, .F. ) ;
#26502=CARTESIAN_POINT ( 'NONE',  ( 31.14694070047868735, 432.3293837220155069, 24.29762062537629319 ) ) ;
#26503=CARTESIAN_POINT ( 'NONE',  ( 39.32386068305349625, 460.7288320239697441, 2.118193558184886083 ) ) ;
#26516=CARTESIAN_POINT ( 'NONE',  ( -19.02089907821467918, 303.6992913295931658, 9.904582106010233034 ) ) ;
#26555=CARTESIAN_POINT ( 'NONE',  ( -43.03265099499957813, 484.2747968070553384, -0.8099405866661226749 ) ) ;
#26573=EDGE_CURVE ( 'NONE', #96657, #68930, #104604, .T. ) ;
#26574=ORIENTED_EDGE ( 'NONE', *, *, #45255, .T. ) ;
#26579=VERTEX_POINT ( 'NONE', #75677 ) ;
#26581=FACE_OUTER_BOUND ( 'NONE', #69273, .T. ) ;
#26594=CARTESIAN_POINT ( 'NONE',  ( -32.94021323899823983, 485.0599191339509844, 5.361609822537348080 ) ) ;
#26599=CARTESIAN_POINT ( 'NONE',  ( -33.51634086989047745, 434.0198194387172634, 13.77974706611873223 ) ) ;
#26610=CARTESIAN_POINT ( 'NONE',  ( 41.68941770529601598, 436.0776509569181485, 20.67692828010792994 ) ) ;
#26613=CARTESIAN_POINT ( 'NONE',  ( 43.63899620156487202, 434.3182181978403946, 14.37213632273145336 ) ) ;
#26619=CARTESIAN_POINT ( 'NONE',  ( -30.00000000000000000, 464.1958267128339344, 14.61098489593202920 ) ) ;
#26622=CARTESIAN_POINT ( 'NONE',  ( 33.74590849135869064, 434.0087241940787521, 12.79517754095366477 ) ) ;
#26629=DIRECTION ( 'NONE',  ( -0.000000000000000000, 1.000000000000000000, -0.000000000000000000 ) ) ;
#26650=EDGE_LOOP ( 'NONE', ( #42081, #30079, #103166, #27982 ) ) ;
#26652=EDGE_CURVE ( 'NONE', #67620, #27128, #69253, .T. ) ;
#26659=CARTESIAN_POINT ( 'NONE',  ( 26.01965034449775516, 305.5777608012918449, -9.622097568370508114 ) ) ;
#26671=CARTESIAN_POINT ( 'NONE',  ( 35.53638905438354101, 390.1040284153648940, 6.613863457673663682 ) ) ;
#26681=CARTESIAN_POINT ( 'NONE',  ( -34.02541642150921319, 436.1155524591087556, 7.421587081314565459 ) ) ;
#26687=CARTESIAN_POINT ( 'NONE',  ( -37.07355662510683914, 464.0045528213379384, 19.58584291728184823 ) ) ;
#26702=CARTESIAN_POINT ( 'NONE',  ( 51.01037695545453232, 500.0000000000002274, 0.000000000000000000 ) ) ;
#26706=CARTESIAN_POINT ( 'NONE',  ( -40.15721392778465315, 315.4447579100735197, 2.968104171095417243 ) ) ;
#26707=CARTESIAN_POINT ( 'NONE',  ( -18.67438172734769353, 303.6203036519360694, -10.04920665861971507 ) ) ;
#26710=CARTESIAN_POINT ( 'NONE',  ( 33.74271564777244237, 484.1802673187708592, 2.058285076122321922 ) ) ;
#26711=VERTEX_POINT ( 'NONE', #30210 ) ;
#26714=CARTESIAN_POINT ( 'NONE',  ( -42.19179521602280403, 485.4956273777414708, -3.824025998168937512 ) ) ;
#26725=AXIS2_PLACEMENT_3D ( 'NONE', #101149, #35391, #75262 ) ;
#26727=DIRECTION ( 'NONE',  ( 0.000000000000000000, 0.000000000000000000, -1.000000000000000000 ) ) ;
#26739=CARTESIAN_POINT ( 'NONE',  ( 31.80704930621342541, 485.2748291366697231, 5.788617803630847547 ) ) ;
#26740=ORIENTED_EDGE ( 'NONE', *, *, #32190, .F. ) ;
#26754=CARTESIAN_POINT ( 'NONE',  ( -40.04008949875484547, 489.2273486934108178, 11.31296313617192517 ) ) ;
#26766=CARTESIAN_POINT ( 'NONE',  ( -42.77939692685449558, 390.9255358409083669, 19.61564233301173843 ) ) ;
#26768=ADVANCED_FACE ( 'NONE', ( #6961 ), #19056, .T. ) ;
#26773=CARTESIAN_POINT ( 'NONE',  ( 25.45638573206032618, 295.6828782483409555, -9.821760129149877727 ) ) ;
#26775=CARTESIAN_POINT ( 'NONE',  ( 45.31383884518383098, 362.9196860876334085, 5.161789940898600548 ) ) ;
#26776=( BOUNDED_SURFACE ( )  B_SPLINE_SURFACE ( 3, 2, ( 
 ( #104262, #30408, #12069 ),
 ( #22325, #46046, #69791 ),
 ( #45527, #20762, #53598 ),
 ( #78930, #88099, #20226 ) ),
 .UNSPECIFIED., .F., .F., .F. ) 
 B_SPLINE_SURFACE_WITH_KNOTS ( ( 4, 4 ),
 ( 3, 3 ),
 ( 0.05778559309751216816, 0.08382991918232818307 ),
 ( 0.3700819400308131280, 1.000000000000000000 ),
 .UNSPECIFIED. ) 
 GEOMETRIC_REPRESENTATION_ITEM ( )  RATIONAL_B_SPLINE_SURFACE ( (
 ( 0.8634409734957675386, 0.8155016339180689577, 1.000000000000000000),
 ( 0.8634412033712403067, 0.8155019444918201188, 1.000000000000000000),
 ( 0.8634411474490393257, 0.8155018689380103547, 1.000000000000000000),
 ( 0.8634409197777686007, 0.8155015613422507137, 1.000000000000000000) ) ) 
 REPRESENTATION_ITEM ( '' )  SURFACE ( )  );
#26792=DIRECTION ( 'NONE',  ( -1.000000000000000000, -0.000000000000000000, -0.000000000000000000 ) ) ;
#26794=CARTESIAN_POINT ( 'NONE',  ( 37.62251730745840916, 437.3427388312647395, 4.535622330043188377 ) ) ;
#26802=CARTESIAN_POINT ( 'NONE',  ( 37.66154869537736261, 377.9587457276326177, 5.098102565965574762 ) ) ;
#26813=CARTESIAN_POINT ( 'NONE',  ( -34.90665437305706575, 461.8152559346092971, 3.957791774131551144 ) ) ;
#26816=ORIENTED_EDGE ( 'NONE', *, *, #24544, .F. ) ;
#26823=CARTESIAN_POINT ( 'NONE',  ( -32.10816233020364052, 435.9969136641942100, 24.01734164033964092 ) ) ;
#26827=B_SPLINE_CURVE_WITH_KNOTS ( 'NONE', 3,
 ( #12639, #38035, #87622, #63882 ),
 .UNSPECIFIED., .F., .F.,
 ( 4, 4 ),
 ( 6.938893903907228378E-18, 0.0004064560158441167894 ),
 .UNSPECIFIED. ) ;
#26829=ORIENTED_EDGE ( 'NONE', *, *, #30294, .F. ) ;
#26832=CARTESIAN_POINT ( 'NONE',  ( 32.87547266101556431, 465.6993878536748070, 10.91512469976365551 ) ) ;
#26836=CARTESIAN_POINT ( 'NONE',  ( -32.10523269976815897, 436.9427959952963647, 23.91264094315748068 ) ) ;
#26841=CARTESIAN_POINT ( 'NONE',  ( 32.88333705524178896, 439.7317646416724415, 24.13381181826117228 ) ) ;
#26846=CARTESIAN_POINT ( 'NONE',  ( 30.76197147106075747, 299.0183610105614775, 10.86750422692454343 ) ) ;
#26882=CARTESIAN_POINT ( 'NONE',  ( 37.83989825151499531, 491.6297408768496098, 12.44743998625077630 ) ) ;
#26893=CARTESIAN_POINT ( 'NONE',  ( 43.52560603733946465, 486.7876375777498197, 7.034422870327473376 ) ) ;
#26897=CARTESIAN_POINT ( 'NONE',  ( -36.47337843289997039, 437.5890141897104400, 4.249048303382426894 ) ) ;
#26914=CARTESIAN_POINT ( 'NONE',  ( 27.18297321513363940, 309.6406833422096270, 11.30666984776100925 ) ) ;
#26916=CARTESIAN_POINT ( 'NONE',  ( -39.33042632267828509, 460.7392826591625408, 2.124562382289973961 ) ) ;
#26919=ADVANCED_FACE ( 'NONE', ( #41459 ), #62494, .F. ) ;
#26922=CARTESIAN_POINT ( 'NONE',  ( 31.47314211086991165, 438.9571839453554389, 23.21193214522953951 ) ) ;
#26926=CARTESIAN_POINT ( 'NONE',  ( -22.42417502586373246, 305.3961751430792333, 10.05444931189341773 ) ) ;
#26929=CARTESIAN_POINT ( 'NONE',  ( -43.53206229128350202, 464.6078677241816877, 9.489307009109641200 ) ) ;
#26935=CARTESIAN_POINT ( 'NONE',  ( -9.041223236741398495, 295.5670253727008685, -10.03755077321278222 ) ) ;
#26937=VERTEX_POINT ( 'NONE', #49547 ) ;
#26950=CARTESIAN_POINT ( 'NONE',  ( -45.99999999997621103, 435.9911642595333774, 13.93550065361152690 ) ) ;
#26969=FACE_OUTER_BOUND ( 'NONE', #82225, .T. ) ;
#26972=CARTESIAN_POINT ( 'NONE',  ( -40.93023141354418470, 381.5373706023750628, 26.74524372019637752 ) ) ;
#26994=CARTESIAN_POINT ( 'NONE',  ( 3.292161566725979593, 304.8518027751346722, 8.936999415071538166 ) ) ;
#27003=CARTESIAN_POINT ( 'NONE',  ( 7.088826403996534076, 296.1964324881835751, -10.02186216631562843 ) ) ;
#27004=CARTESIAN_POINT ( 'NONE',  ( 33.08751701378358945, 301.6823158026044780, 11.49690784967660662 ) ) ;
#27030=CARTESIAN_POINT ( 'NONE',  ( 31.19652432992544888, 378.3327707670021027, 24.28948218791313707 ) ) ;
#27031=CARTESIAN_POINT ( 'NONE',  ( 41.50820411079202188, 461.5963371455320612, 2.703439750996334823 ) ) ;
#27032=CARTESIAN_POINT ( 'NONE',  ( -34.50213009991706059, 434.5101795678424992, 9.485856115010102840 ) ) ;
#27047=CARTESIAN_POINT ( 'NONE',  ( -37.85084083633361729, 438.0234350436313093, 4.171260309356228824 ) ) ;
#27075=CARTESIAN_POINT ( 'NONE',  ( -31.21759734847655210, 387.2566916973277671, 24.99345285570965913 ) ) ;
#27088=CARTESIAN_POINT ( 'NONE',  ( 40.93292669599463096, 378.0706848361106722, 26.55786848468904537 ) ) ;
#27092=CARTESIAN_POINT ( 'NONE',  ( 34.90201944348623897, 461.8185193995851137, 3.961962287866056087 ) ) ;
#27128=VERTEX_POINT ( 'NONE', #100227 ) ;
#27143=CARTESIAN_POINT ( 'NONE',  ( -37.50059943756144776, 490.7879993827797307, 12.38039871356719246 ) ) ;
#27147=TOROIDAL_SURFACE ( 'NONE', #58124, 12.00000000000001066, 3.000000000000000000 ) ;
#27153=CARTESIAN_POINT ( 'NONE',  ( 33.17685491218571769, 435.0131028569089722, 15.11923937554624153 ) ) ;
#27161=CIRCLE ( 'NONE', #85653, 1.000000000000008660 ) ;
#27170=CARTESIAN_POINT ( 'NONE',  ( 20.64244187944548159, 302.8988018313013413, 9.946989373691105030 ) ) ;
#27193=CARTESIAN_POINT ( 'NONE',  ( 33.26095177349862553, 318.5585020271619783, -6.438101968021065602 ) ) ;
#27200=CARTESIAN_POINT ( 'NONE',  ( 40.60010613376692845, 436.1985323639532339, 6.054933560615542554 ) ) ;
#27216=CARTESIAN_POINT ( 'NONE',  ( 13.48376080047430392, 302.5481724856162487, -10.06453332316872284 ) ) ;
#27223=VERTEX_POINT ( 'NONE', #10675 ) ;
#27225=( NAMED_UNIT ( * ) SI_UNIT ( $, .STERADIAN. ) SOLID_ANGLE_UNIT ( ) );
#27226=CARTESIAN_POINT ( 'NONE',  ( 38.51282804765381940, 490.3045649923045062, 12.08595093631995532 ) ) ;
#27228=MECHANICAL_DESIGN_GEOMETRIC_PRESENTATION_REPRESENTATION('',(#82294),#87478);
#27230=ORIENTED_EDGE ( 'NONE', *, *, #10407, .T. ) ;
#27231=AXIS2_PLACEMENT_3D ( 'NONE', #40497, #98195, #64776 ) ;
#27240=CARTESIAN_POINT ( 'NONE',  ( -36.72214694598457640, 305.2241286510804912, 0.4044219380610372672 ) ) ;
#27241=FACE_BOUND ( 'NONE', #88310, .T. ) ;
#27254=VERTEX_POINT ( 'NONE', #52204 ) ;
#27263=CARTESIAN_POINT ( 'NONE',  ( 32.09911992168216699, 438.9232547152094526, 23.66653216045977359 ) ) ;
#27281=CARTESIAN_POINT ( 'NONE',  ( 43.62838954006723213, 434.9736691849515751, 14.34345830637718322 ) ) ;
#27285=ORIENTED_EDGE ( 'NONE', *, *, #54593, .F. ) ;
#27297=CARTESIAN_POINT ( 'NONE',  ( -31.61648724296877688, 439.7300051528717972, 23.66942472547106391 ) ) ;
#27305=CARTESIAN_POINT ( 'NONE',  ( -38.24569826024678321, 310.6312515531008671, 5.698628603124755720 ) ) ;
#27310=CARTESIAN_POINT ( 'NONE',  ( 38.42890617179530466, 491.4184709533606110, 12.30537189783381358 ) ) ;
#27315=CARTESIAN_POINT ( 'NONE',  ( 23.95564068939877345, 305.6666757346319514, -9.824255363916352124 ) ) ;
#27327=CARTESIAN_POINT ( 'NONE',  ( 43.51858057942322944, 326.4877523563876593, -2.294238957344378882 ) ) ;
#27332=CARTESIAN_POINT ( 'NONE',  ( 0.000000000000000000, 304.8518027762758038, -10.00000000000000178 ) ) ;
#27333=CARTESIAN_POINT ( 'NONE',  ( 31.75936052488420458, 439.7430734213018013, 23.78634771736264142 ) ) ;
#27348=CARTESIAN_POINT ( 'NONE',  ( 37.34256500486003461, 354.2819331376351215, 1.821034110566981390 ) ) ;
#27359=ORIENTED_EDGE ( 'NONE', *, *, #46714, .T. ) ;
#27365=CARTESIAN_POINT ( 'NONE',  ( -32.09911992168218831, 438.9232547152092252, 23.66653216045979491 ) ) ;
#27371=CARTESIAN_POINT ( 'NONE',  ( -38.47428897412184767, 485.7788508071988645, -4.770630528146724281 ) ) ;
#27373=CIRCLE ( 'NONE', #63517, 1.000000000000000888 ) ;
#27375=CARTESIAN_POINT ( 'NONE',  ( -31.44965265175576974, 392.5298586342441922, 24.22355757266445053 ) ) ;
#27384=CARTESIAN_POINT ( 'NONE',  ( 22.56285362583756893, 303.3507920709804466, 10.04438543891975577 ) ) ;
#27390=CARTESIAN_POINT ( 'NONE',  ( 30.65126007668194319, 298.3960702967059433, 2.720726122834696170 ) ) ;
#27394=VERTEX_POINT ( 'NONE', #31042 ) ;
#27405=CARTESIAN_POINT ( 'NONE',  ( 43.99399868442856842, 464.5851102539050999, 10.32278593046345705 ) ) ;
#27417=CARTESIAN_POINT ( 'NONE',  ( 17.08544069068336668, 304.5690947107618740, -10.06009145438460983 ) ) ;
#27421=CARTESIAN_POINT ( 'NONE',  ( 38.95242300084920117, 491.1731620564962668, 12.13306966136837062 ) ) ;
#27436=ORIENTED_EDGE ( 'NONE', *, *, #86024, .F. ) ;
#27444=CARTESIAN_POINT ( 'NONE',  ( 9.496329878501317268, 294.6569770103990891, -3.146524261899395825 ) ) ;
#27450=CARTESIAN_POINT ( 'NONE',  ( 24.90254304838390453, 305.8449809694421333, 10.38262587369874268 ) ) ;
#27459=DIRECTION ( 'NONE',  ( 0.6293714829493110008, -0.5427490687642032574, -0.5561609342679288970 ) ) ;
#27460=CARTESIAN_POINT ( 'NONE',  ( -27.57151080649627417, 314.0751515626058676, 12.18133379269485239 ) ) ;
#27465=CARTESIAN_POINT ( 'NONE',  ( -43.52581800834794024, 465.2717506914920023, 9.360548986731394905 ) ) ;
#27472=CARTESIAN_POINT ( 'NONE',  ( -9.609724578342728307, 294.6537309100401671, -2.768030809497829203 ) ) ;
#27485=CARTESIAN_POINT ( 'NONE',  ( 43.37536761788344819, 434.6169042472851061, 10.05068736165323351 ) ) ;
#27486=DIRECTION ( 'NONE',  ( 0.000000000000000000, 0.000000000000000000, -1.000000000000000000 ) ) ;
#27488=B_SPLINE_CURVE_WITH_KNOTS ( 'NONE', 3,
 ( #15360, #39133, #48246, #62874, #87680, #30518 ),
 .UNSPECIFIED., .F., .F.,
 ( 4, 2, 4 ),
 ( 0.000000000000000000, 0.001720022418478405661, 0.003440044836956811323 ),
 .UNSPECIFIED. ) ;
#27503=CARTESIAN_POINT ( 'NONE',  ( -26.27395767078098388, 305.7318160080068310, -9.587391517416717690 ) ) ;
#27513=ORIENTED_EDGE ( 'NONE', *, *, #43704, .F. ) ;
#27515=CARTESIAN_POINT ( 'NONE',  ( -30.71792534725271651, 320.3613057377743303, 14.24394111771609950 ) ) ;
#27531=DIRECTION ( 'NONE',  ( 0.000000000000000000, 0.000000000000000000, 1.000000000000000000 ) ) ;
#27542=CARTESIAN_POINT ( 'NONE',  ( 1.487796992647206995, 297.5563421047799579, -10.00151720974370129 ) ) ;
#27543=CARTESIAN_POINT ( 'NONE',  ( 42.09210974227526947, 317.4093497706929270, -4.557617623460385126 ) ) ;
#27544=CARTESIAN_POINT ( 'NONE',  ( 39.24609676134105030, 311.8013972301173453, 2.046850167889632921 ) ) ;
#27548=CARTESIAN_POINT ( 'NONE',  ( -43.85205561063334301, 464.7392644986606456, 11.03676161964631319 ) ) ;
#27551=DIRECTION ( 'NONE',  ( 0.4753313241819922541, 0.2469313775204109718, -0.8444436198155955697 ) ) ;
#27554=( BOUNDED_SURFACE ( )  B_SPLINE_SURFACE ( 3, 2, ( 
 ( #104492, #63528, #80211 ),
 ( #55399, #88330, #72131 ),
 ( #105040, #31181, #23074 ),
 ( #14942, #47836, #80743 ),
 ( #6858, #106616, #82346 ),
 ( #49973, #82881, #1406 ),
 ( #8979, #34372, #48897 ),
 ( #8454, #25759, #58617 ) ),
 .UNSPECIFIED., .F., .F., .T. ) 
 B_SPLINE_SURFACE_WITH_KNOTS ( ( 4, 2, 2, 4 ),
 ( 3, 3 ),
 ( 0.009824648773345148398, 0.02000824059645995093, 0.02510003650801735306, 0.03019183241957475519 ),
 ( 0.000000000000000000, 1.000000000000000000 ),
 .UNSPECIFIED. ) 
 GEOMETRIC_REPRESENTATION_ITEM ( )  RATIONAL_B_SPLINE_SURFACE ( (
 ( 1.000000000000000000, 0.7071067811865475727, 1.000000000000000000),
 ( 1.000000000000000000, 0.7071067811865475727, 1.000000000000000000),
 ( 1.000000000000000000, 0.7071080532101867711, 1.000000000000000000),
 ( 1.000000000000000000, 0.7071061931969254699, 1.000000000000000000),
 ( 1.000000000000000000, 0.7071074416173600552, 1.000000000000000000),
 ( 1.000000000000000000, 0.7071061821613239262, 1.000000000000000000),
 ( 1.000000000000000000, 0.7071482299271628635, 1.000000000000000000),
 ( 1.000000000000000000, 0.7071067811865643371, 1.000000000000000000) ) ) 
 REPRESENTATION_ITEM ( '' )  SURFACE ( )  );
#27576=DIRECTION ( 'NONE',  ( 0.2039034312721268727, 0.2189633091458398073, 0.9541899496239500955 ) ) ;
#27600=B_SPLINE_CURVE_WITH_KNOTS ( 'NONE', 3,
 ( #31199, #23096, #12313, #30120, #45239, #4233, #78119, #37168, #70029, #102931 ),
 .UNSPECIFIED., .F., .F.,
 ( 4, 2, 2, 2, 4 ),
 ( 0.000000000000000000, 0.001026607246098428655, 0.002053214492196857310, 0.003079821738295285966, 0.004106428984393714621 ),
 .UNSPECIFIED. ) ;
#27610=CARTESIAN_POINT ( 'NONE',  ( -22.91885868373643831, 305.6172567281201964, 10.10309701371861912 ) ) ;
#27615=CARTESIAN_POINT ( 'NONE',  ( 33.00000000000000000, 485.0303364503728289, 0.9535057477322557151 ) ) ;
#27618=CARTESIAN_POINT ( 'NONE',  ( -32.80261435968446904, 487.0248074981827244, 8.977354182202281763 ) ) ;
#27623=DIRECTION ( 'NONE',  ( 0.000000000000000000, 0.2013748291391406209, 0.9795142562460140701 ) ) ;
#27630=CARTESIAN_POINT ( 'NONE',  ( 32.48439440699409886, 435.0131534033402545, 18.09282574846879044 ) ) ;
#27643=CARTESIAN_POINT ( 'NONE',  ( 46.00000000000000711, 437.8938411292168666, 13.38357595664191813 ) ) ;
#27653=CARTESIAN_POINT ( 'NONE',  ( -38.81331594050915612, 485.4121048083255232, -4.285540015901212030 ) ) ;
#27657=CARTESIAN_POINT ( 'NONE',  ( -46.00000000000000000, 459.9277931459674278, 6.461582622316496938 ) ) ;
#27664=CARTESIAN_POINT ( 'NONE',  ( -42.61140200160144786, 465.9030374194822457, 13.21253569360411895 ) ) ;
#27674=CARTESIAN_POINT ( 'NONE',  ( 42.83167223033138526, 435.5834305853641695, 17.69761675603227857 ) ) ;
#27676=CARTESIAN_POINT ( 'NONE',  ( -41.74378088170519874, 488.3362766135676338, 9.453202772108019403 ) ) ;
#27678=CARTESIAN_POINT ( 'NONE',  ( 41.91039677604278069, 435.8602217528023743, 20.32597409357570584 ) ) ;
#27688=CARTESIAN_POINT ( 'NONE',  ( -34.49820706003161064, 464.8461132930464714, 18.22442427693934519 ) ) ;
#27689=CARTESIAN_POINT ( 'NONE',  ( 32.70848551668328952, 434.6726260045710433, 17.17137052634237193 ) ) ;
#27695=DIRECTION ( 'NONE',  ( 0.000000000000000000, 0.000000000000000000, 1.000000000000000000 ) ) ;
#27705=EDGE_CURVE ( 'NONE', #36676, #56041, #78294, .T. ) ;
#27708=AXIS2_PLACEMENT_3D ( 'NONE', #72849, #37893, #30856 ) ;
#27746=ORIENTED_EDGE ( 'NONE', *, *, #18767, .T. ) ;
#27755=CARTESIAN_POINT ( 'NONE',  ( -32.54922218626916930, 319.8023524069591303, -6.363686095274232457 ) ) ;
#27757=CARTESIAN_POINT ( 'NONE',  ( -43.69141235711237670, 485.1129823701677992, 2.341835213801349624 ) ) ;
#27764=( NAMED_UNIT ( * ) PLANE_ANGLE_UNIT ( ) SI_UNIT ( $, .RADIAN. ) );
#27765=CARTESIAN_POINT ( 'NONE',  ( -36.73972469232126770, 391.2873159729405188, 5.934521470291739043 ) ) ;
#27778=CARTESIAN_POINT ( 'NONE',  ( -37.76134924625720402, 305.2126739483049960, -7.610856539317000014 ) ) ;
#27779=CARTESIAN_POINT ( 'NONE',  ( -11.89662026262662842, 304.5916488899262617, -10.05529741525224452 ) ) ;
#27783=CARTESIAN_POINT ( 'NONE',  ( -42.73089261237365832, 435.7309723475635792, 18.11242468272465089 ) ) ;
#27784=EDGE_CURVE ( 'NONE', #20727, #2280, #59371, .T. ) ;
#27794=CARTESIAN_POINT ( 'NONE',  ( -30.00000000000000000, 500.0000000000002274, 12.00000000000000888 ) ) ;
#27803=AXIS2_PLACEMENT_3D ( 'NONE', #29638, #46318, #86268 ) ;
#27838=CARTESIAN_POINT ( 'NONE',  ( -32.96172342428652513, 300.4657064437288341, 3.200647364369005654 ) ) ;
#27842=DIRECTION ( 'NONE',  ( 0.000000000000000000, 0.000000000000000000, 1.000000000000000000 ) ) ;
#27846=CARTESIAN_POINT ( 'NONE',  ( 25.83562903227484497, 295.7929986566709886, -9.797862988238321691 ) ) ;
#27847=CARTESIAN_POINT ( 'NONE',  ( 34.94338628507543376, 342.5355909536760350, -0.9693026116538068226 ) ) ;
#27848=EDGE_CURVE ( 'NONE', #25681, #46054, #48568, .T. ) ;
#27851=EDGE_CURVE ( 'NONE', #93450, #62342, #45923, .T. ) ;
#27859=CARTESIAN_POINT ( 'NONE',  ( 41.99603398301461255, 317.0185905804366939, -4.657216470168420663 ) ) ;
#27860=CARTESIAN_POINT ( 'NONE',  ( 34.74668892571865086, 477.5740991570432925, -0.3050944403155617657 ) ) ;
#27887=FILL_AREA_STYLE_COLOUR ( '', #13382 ) ;
#27899=( BOUNDED_SURFACE ( )  B_SPLINE_SURFACE ( 3, 2, ( 
 ( #31402, #13, #98213 ),
 ( #32981, #82568, #65852 ),
 ( #49116, #15700, #6540 ),
 ( #98730, #24886, #81477 ) ),
 .UNSPECIFIED., .F., .F., .F. ) 
 B_SPLINE_SURFACE_WITH_KNOTS ( ( 4, 4 ),
 ( 3, 3 ),
 ( 1.734723475976807094E-18, 0.0002932394964387638383 ),
 ( 0.000000000000000000, 1.000000000000000000 ),
 .UNSPECIFIED. ) 
 GEOMETRIC_REPRESENTATION_ITEM ( )  RATIONAL_B_SPLINE_SURFACE ( (
 ( 1.000000000000000000, 0.7912633096140038180, 1.000000000000000000),
 ( 1.000000000000000000, 0.7930984581161097946, 1.000000000000000000),
 ( 1.000000000000000000, 0.7948408637866294368, 1.000000000000000000),
 ( 1.000000000000000000, 0.7964893136847220889, 1.000000000000000000) ) ) 
 REPRESENTATION_ITEM ( '' )  SURFACE ( )  );
#27900=CARTESIAN_POINT ( 'NONE',  ( -32.14349642894332248, 424.2545041670527439, 25.05049640504120845 ) ) ;
#27903=VERTEX_POINT ( 'NONE', #38461 ) ;
#27905=CARTESIAN_POINT ( 'NONE',  ( -32.70701262249002639, 465.7750753107770265, 13.84670167514589068 ) ) ;
#27908=CARTESIAN_POINT ( 'NONE',  ( 41.61220833757316484, 437.6913339738342756, 21.78352536266461925 ) ) ;
#27910=CARTESIAN_POINT ( 'NONE',  ( 6.123233995736761352E-16, 69.00000000000000000, 4.999999999999993783 ) ) ;
#27912=EDGE_LOOP ( 'NONE', ( #79261, #105882, #35327, #58434 ) ) ;
#27915=AXIS2_PLACEMENT_3D ( 'NONE', #95421, #4822, #38279 ) ;
#27920=CARTESIAN_POINT ( 'NONE',  ( 22.39204233095570729, 303.2998958009682724, 10.03333151357952424 ) ) ;
#27925=CARTESIAN_POINT ( 'NONE',  ( 38.82758694742345540, 312.8745823789997189, 6.266461510169453852 ) ) ;
#27932=FACE_OUTER_BOUND ( 'NONE', #86636, .T. ) ;
#27949=B_SPLINE_CURVE_WITH_KNOTS ( 'NONE', 3,
 ( #90479, #65136, #57028, #80242, #98554, #64101, #81827, #31731 ),
 .UNSPECIFIED., .F., .F.,
 ( 4, 2, 2, 4 ),
 ( 0.000000000000000000, 0.002068697987604109587, 0.003103046981406205364, 0.004137395975208301574 ),
 .UNSPECIFIED. ) ;
#27956=CARTESIAN_POINT ( 'NONE',  ( 39.71213755904409481, 490.7526980994978203, 11.81179577511769097 ) ) ;
#27958=CARTESIAN_POINT ( 'NONE',  ( 44.47476154325583764, 485.8001484721103793, -0.4986663365551948224 ) ) ;
#27962=CARTESIAN_POINT ( 'NONE',  ( 40.83002285427885880, 485.0211005501694785, -4.017563975491787787 ) ) ;
#27963=CARTESIAN_POINT ( 'NONE',  ( 33.00000000000000000, 500.0000000000002274, 15.00000000000000711 ) ) ;
#27966=CARTESIAN_POINT ( 'NONE',  ( -41.93285660804859560, 437.4666891908580624, 21.45432292391068430 ) ) ;
#27980=ORIENTED_EDGE ( 'NONE', *, *, #14904, .F. ) ;
#27982=ORIENTED_EDGE ( 'NONE', *, *, #60950, .F. ) ;
#27983=CARTESIAN_POINT ( 'NONE',  ( 22.54520074857146383, 305.4514246655992338, 9.066665743933437938 ) ) ;
#27990=CARTESIAN_POINT ( 'NONE',  ( 41.75331920095265303, 461.8277566036529720, 2.915730576367065119 ) ) ;
#27998=ORIENTED_EDGE ( 'NONE', *, *, #38653, .T. ) ;
#28002=CARTESIAN_POINT ( 'NONE',  ( -9.681569006903592012, 294.6516795043967250, -2.504656372063916780 ) ) ;
#28012=AXIS2_PLACEMENT_3D ( 'NONE', #48683, #106388, #34684 ) ;
#28018=FACE_OUTER_BOUND ( 'NONE', #18424, .T. ) ;
#28029=CARTESIAN_POINT ( 'NONE',  ( 40.35868996910548390, 344.7914381055520607, 21.62271489072101360 ) ) ;
#28030=CARTESIAN_POINT ( 'NONE',  ( -26.87630176750905164, 307.4199632232798649, -9.428850274614722693 ) ) ;
#28040=CARTESIAN_POINT ( 'NONE',  ( -32.88333705524179607, 439.7317646416723846, 24.13381181826116517 ) ) ;
#28042=CARTESIAN_POINT ( 'NONE',  ( -26.73681790852576867, 307.3696589980178260, -8.440011308043008142 ) ) ;
#28043=CARTESIAN_POINT ( 'NONE',  ( -29.29569811498970466, 313.0313481771436841, 12.40036593387712927 ) ) ;
#28058=CARTESIAN_POINT ( 'NONE',  ( 16.45451579217936811, 304.5657612144941027, 8.876165602381572484 ) ) ;
#28065=CARTESIAN_POINT ( 'NONE',  ( 33.26922818042641694, 435.1894657785401819, 10.58222864814420383 ) ) ;
#28067=CARTESIAN_POINT ( 'NONE',  ( 0.3768998597285306840, 294.9778291297479882, -9.999929723870947029 ) ) ;
#28070=CARTESIAN_POINT ( 'NONE',  ( 33.20657005241940851, 300.3266200210385932, -0.7716179031724232917 ) ) ;
#28076=EDGE_LOOP ( 'NONE', ( #82666, #7623, #28216, #71205, #94406 ) ) ;
#28078=CARTESIAN_POINT ( 'NONE',  ( 46.00000000000000000, 488.3725375423206287, 3.127739281036224117 ) ) ;
#28097=DIRECTION ( 'NONE',  ( -0.9081249930074554166, 0.3474488548219246686, 0.2336413712469223303 ) ) ;
#28106=ORIENTED_EDGE ( 'NONE', *, *, #61270, .T. ) ;
#28107=CARTESIAN_POINT ( 'NONE',  ( 33.21102376836596193, 438.9613914113129454, 23.92328486949907784 ) ) ;
#28111=AXIS2_PLACEMENT_3D ( 'NONE', #53208, #38121, #54772 ) ;
#28138=EDGE_CURVE ( 'NONE', #22950, #91205, #67887, .T. ) ;
#28139=CARTESIAN_POINT ( 'NONE',  ( 36.87655955837855259, 438.2068510013161813, 3.933030107424693167 ) ) ;
#28154=CARTESIAN_POINT ( 'NONE',  ( -33.16955188770710095, 434.2034342956006299, 15.24725034886469466 ) ) ;
#28155=CARTESIAN_POINT ( 'NONE',  ( 42.54181027558946226, 465.0722614357431439, 13.76085909084874892 ) ) ;
#28156=CARTESIAN_POINT ( 'NONE',  ( 31.53897358591923350, 437.3651574122892498, 21.86285002934833699 ) ) ;
#28175=CARTESIAN_POINT ( 'NONE',  ( -33.22740183690338256, 464.7219767745360173, 9.606361102862551959 ) ) ;
#28195=VECTOR ( 'NONE', #3191, 1000.000000000000000 ) ;
#28196=CARTESIAN_POINT ( 'NONE',  ( -2.360737205864155364, 300.9840656762371509, 9.719989882648539137 ) ) ;
#28197=LINE ( 'NONE', #21171, #46182 ) ;
#28199=EDGE_CURVE ( 'NONE', #49452, #62342, #56198, .T. ) ;
#28203=CARTESIAN_POINT ( 'NONE',  ( 16.39985520464312785, 294.5680733035314915, -10.06030923778802411 ) ) ;
#28216=ORIENTED_EDGE ( 'NONE', *, *, #102114, .T. ) ;
#28217=CARTESIAN_POINT ( 'NONE',  ( 32.52812566731132904, 435.6745906244506159, 17.82476273229491426 ) ) ;
#28222=CARTESIAN_POINT ( 'NONE',  ( 43.94716957229235987, 463.1429429498418813, 4.278538522906490726 ) ) ;
#28224=CIRCLE ( 'NONE', #71291, 0.9999999999999966693 ) ;
#28227=ORIENTED_EDGE ( 'NONE', *, *, #88787, .F. ) ;
#28232=CARTESIAN_POINT ( 'NONE',  ( -32.12146351642663689, 487.8665243855083986, 8.631703203532680391 ) ) ;
#28259=VECTOR ( 'NONE', #13265, 1000.000000000000000 ) ;
#28264=CARTESIAN_POINT ( 'NONE',  ( 42.11386565848213337, 436.0925768526452089, 7.550517934394086694 ) ) ;
#28274=CARTESIAN_POINT ( 'NONE',  ( -35.66932529116966322, 438.9565575286536045, 4.011496722538590909 ) ) ;
#28276=CARTESIAN_POINT ( 'NONE',  ( -19.24689719943499355, 294.6758623120367133, -10.03739701883414526 ) ) ;
#28284=CARTESIAN_POINT ( 'NONE',  ( -36.62762355347277321, 370.6867356965224189, 4.048972153900439963 ) ) ;
#28286=DIRECTION ( 'NONE',  ( 0.000000000000000000, 0.000000000000000000, -1.000000000000000000 ) ) ;
#28287=ORIENTED_EDGE ( 'NONE', *, *, #38414, .F. ) ;
#28299=ORIENTED_EDGE ( 'NONE', *, *, #22367, .F. ) ;
#28320=CARTESIAN_POINT ( 'NONE',  ( -45.99999999995579003, 486.5369520445917146, 4.408549137160468590 ) ) ;
#28321=CARTESIAN_POINT ( 'NONE',  ( -37.85084083633360308, 438.0234350436312525, 4.171260309356210172 ) ) ;
#28328=EDGE_CURVE ( 'NONE', #48464, #91003, #39001, .T. ) ;
#28334=B_SPLINE_CURVE_WITH_KNOTS ( 'NONE', 3,
 ( #27615, #11907, #3834, #1683 ),
 .UNSPECIFIED., .F., .F.,
 ( 4, 4 ),
 ( 2.122407100861210359E-17, 0.0007940539003705733134 ),
 .UNSPECIFIED. ) ;
#28347=CARTESIAN_POINT ( 'NONE',  ( -41.50820411079205741, 461.5963371455321749, 2.703439750996430302 ) ) ;
#28350=B_SPLINE_SURFACE_WITH_KNOTS ( 'NONE', 1, 3, ( 
 ( #58430, #16364, #65459, #99387, #73525, #105898, #48719, #98351, #8803, #15837, #16915, #7734, #91339, #24506, #32049, #7209, #97812, #57340, #89208, #82697, #90261, #40118, #33116, #74593, #82156, #670, #81096, #41711 ),
 ( #15307, #33634, #66515, #17453, #97281, #81607, #8269, #50319, #41182, #83225, #74060, #72993, #65983, #64926, #9319, #42230, #105387, #31527, #64408, #23433, #23977, #56818, #89742, #77270, #42768, #85914, #69193, #34182 ) ),
 .UNSPECIFIED., .F., .F., .F.,
 ( 2, 2 ),
 ( 4, 2, 2, 2, 2, 2, 2, 2, 2, 2, 2, 2, 2, 4 ),
 ( 0.000000000000000000, 1.000000000000000000 ),
 ( 0.08901491201581737678, 0.1032490540155679704, 0.1174831960153185778, 0.1317173380150691853, 0.1459514800148197788, 0.1744197640143299588, 0.2028880480138401388, 0.2598246160128514504, 0.3167611840118632616, 0.4306343200098861623, 0.5445074560079088410, 0.6583805920059359051, 0.7722537280039543095, 1.000000000000000000 ),
 .UNSPECIFIED. ) ;
#28352=ORIENTED_EDGE ( 'NONE', *, *, #97106, .T. ) ;
#28360=FACE_OUTER_BOUND ( 'NONE', #57493, .T. ) ;
#28363=CARTESIAN_POINT ( 'NONE',  ( 33.63427961064055438, 325.9154870834976236, -4.827994974213513757 ) ) ;
#28371=CARTESIAN_POINT ( 'NONE',  ( 42.18756898894579876, 484.4522853017719513, -2.425645685620453129 ) ) ;
#28375=AXIS2_PLACEMENT_3D ( 'NONE', #59905, #33494, #44239 ) ;
#28376=CARTESIAN_POINT ( 'NONE',  ( 43.55162665249213205, 368.5793226304579093, 13.69405092322887540 ) ) ;
#28377=CARTESIAN_POINT ( 'NONE',  ( 34.76127829571465355, 469.3283515771897783, 1.881857718270027346 ) ) ;
#28402=CARTESIAN_POINT ( 'NONE',  ( -43.58517788116170522, 464.0093709437825851, 6.089361716058439455 ) ) ;
#28404=CARTESIAN_POINT ( 'NONE',  ( 0.000000000000000000, 300.0000000000000000, 9.936999415352289589 ) ) ;
#28421=CARTESIAN_POINT ( 'NONE',  ( -43.61936128191153017, 427.3462587541194466, 15.28103652271592416 ) ) ;
#28422=CARTESIAN_POINT ( 'NONE',  ( -31.31579387245123058, 439.0805111990142109, 22.75910752502478118 ) ) ;
#28429=CARTESIAN_POINT ( 'NONE',  ( -42.19179521602254823, 485.4956273777415277, -3.824025998169165330 ) ) ;
#28430=CARTESIAN_POINT ( 'NONE',  ( 22.37268651138633402, 303.2941807803410370, 10.03209224172512748 ) ) ;
#28442=CARTESIAN_POINT ( 'NONE',  ( 30.00000000000000000, 461.8665070935973063, 11.40527499426175062 ) ) ;
#28447=B_SPLINE_CURVE_WITH_KNOTS ( 'NONE', 3,
 ( #102956, #86261, #70589, #20503, #62504, #77618, #103479, #12860, #93801, #3194, #29119, #43646, #19958, #28042, #68470, #45260, #3735, #4259, #2646, #86789, #36664, #53341, #85174, #101360, #37188, #60391, #70050, #21020, #19430, #95391, #51730, #52800, #44730, #84647, #76535, #35593, #44190, #47359, #23644, #55437, #63030, #64622, #56500, #71628, #31221, #15520, #89429, #72173, #88891, #38761 ),
 .UNSPECIFIED., .F., .F.,
 ( 4, 2, 2, 2, 2, 2, 2, 2, 2, 2, 2, 2, 2, 2, 2, 2, 2, 2, 2, 2, 2, 2, 2, 2, 4 ),
 ( -6.000000000098130878E-08, 0.0005605446129132989497, 0.001121149225826598844, 0.002242358451653208608, 0.004484776903306437676, 0.005605986129133047439, 0.006727195354959656336, 0.007848404580786266099, 0.008969613806612876730, 0.01121203225826622636, 0.01233324148409289597, 0.01345445070991956732, 0.01569686916157306267, 0.01793928761322655802, 0.02242412451653353830, 0.02690896141984051512, 0.03587863522645447917, 0.05381798283968223379, 0.06278765664629612497, 0.07175733045291000922, 0.08072700425952387959, 0.08969667806613777772, 0.1076360256793653380, 0.1255753732925929123, 0.1435147209058204865 ),
 .UNSPECIFIED. ) ;
#28461=CARTESIAN_POINT ( 'NONE',  ( -46.00000000000000000, 450.0000000000002274, 13.20242257375370976 ) ) ;
#28468=CARTESIAN_POINT ( 'NONE',  ( 35.15995658827085890, 490.3459154101568629, 12.17011141540134211 ) ) ;
#28469=CARTESIAN_POINT ( 'NONE',  ( 16.96954359408614366, 304.5683848806726814, 9.876757081930351845 ) ) ;
#28477=ORIENTED_EDGE ( 'NONE', *, *, #43950, .F. ) ;
#28478=CARTESIAN_POINT ( 'NONE',  ( 40.49428179616492685, 485.6422782434408418, -4.370491944107985915 ) ) ;
#28481=( BOUNDED_SURFACE ( )  B_SPLINE_SURFACE ( 3, 2, ( 
 ( #98688, #90623, #49618 ),
 ( #56094, #82527, #42059 ),
 ( #41529, #74419, #494 ),
 ( #1035, #66881, #66337 ) ),
 .UNSPECIFIED., .F., .F., .T. ) 
 B_SPLINE_SURFACE_WITH_KNOTS ( ( 4, 4 ),
 ( 3, 3 ),
 ( 3.903127820947815962E-16, 0.0002239690292486364140 ),
 ( 0.000000000000000000, 1.000000000000000000 ),
 .UNSPECIFIED. ) 
 GEOMETRIC_REPRESENTATION_ITEM ( )  RATIONAL_B_SPLINE_SURFACE ( (
 ( 1.000000000000000000, 0.8238944711859870207, 1.000000000000000000),
 ( 1.000000000000000000, 0.8250855524373764682, 1.000000000000000000),
 ( 1.000000000000000000, 0.8262263977136614646, 1.000000000000000000),
 ( 1.000000000000000000, 0.8273155905872641158, 1.000000000000000000) ) ) 
 REPRESENTATION_ITEM ( '' )  SURFACE ( )  );
#28483=CARTESIAN_POINT ( 'NONE',  ( 40.75856060348023391, 485.0489837854431698, -4.073182915998790676 ) ) ;
#28487=ADVANCED_FACE ( 'NONE', ( #100626 ), #84545, .F. ) ;
#28488=CARTESIAN_POINT ( 'NONE',  ( -43.63933387927399821, 486.5321090506437827, 6.480556376458819656 ) ) ;
#28498=ORIENTED_EDGE ( 'NONE', *, *, #6384, .F. ) ;
#28499=CARTESIAN_POINT ( 'NONE',  ( 23.26573150479070762, 305.7875708879445824, 9.141252083811004070 ) ) ;
#28502=DIRECTION ( 'NONE',  ( -0.9508028509851106369, 0.1865215626109575919, -0.2473532802284052201 ) ) ;
#28548=ORIENTED_EDGE ( 'NONE', *, *, #34956, .F. ) ;
#28549=CARTESIAN_POINT ( 'NONE',  ( -33.94783393359910662, 484.1261039197349305, 1.321740980884785532 ) ) ;
#28553=CARTESIAN_POINT ( 'NONE',  ( 40.87706463175591409, 434.1066599708036051, 26.33551600060701858 ) ) ;
#28556=CARTESIAN_POINT ( 'NONE',  ( -44.35819766388001284, 435.2221642642158486, 12.65712761108313522 ) ) ;
#28561=CARTESIAN_POINT ( 'NONE',  ( -32.09911992168216699, 438.9232547152094526, 23.66653216045977004 ) ) ;
#28564=CARTESIAN_POINT ( 'NONE',  ( -38.19251921417566109, 310.5472675333638790, 5.678690236465158137 ) ) ;
#28580=CARTESIAN_POINT ( 'NONE',  ( 0.000000000000000000, 273.9999999999999432, -6.999999999999982236 ) ) ;
#28583=ADVANCED_FACE ( 'NONE', ( #84987 ), #91470, .T. ) ;
#28593=CARTESIAN_POINT ( 'NONE',  ( 4.023953349526805390, 300.5162199157299483, -10.00978861085792104 ) ) ;
#28594=CARTESIAN_POINT ( 'NONE',  ( 45.50145573691759182, 405.2496736015978627, 8.430338687477670234 ) ) ;
#28596=CARTESIAN_POINT ( 'NONE',  ( 43.51697068632529408, 365.4421646331526858, 13.28917352912563032 ) ) ;
#28597=CARTESIAN_POINT ( 'NONE',  ( -42.57704743493907529, 486.1612337113410831, 7.852296464539637810 ) ) ;
#28599=AXIS2_PLACEMENT_3D ( 'NONE', #72108, #23589, #30620 ) ;
#28600=CARTESIAN_POINT ( 'NONE',  ( -33.00000000000000000, 450.0000000000002274, 13.20242257375370976 ) ) ;
#28624=DIRECTION ( 'NONE',  ( 0.000000000000000000, 0.000000000000000000, 1.000000000000000000 ) ) ;
#28628=ORIENTED_EDGE ( 'NONE', *, *, #46991, .T. ) ;
#28630=VERTEX_POINT ( 'NONE', #4604 ) ;
#28632=ORIENTED_EDGE ( 'NONE', *, *, #37700, .T. ) ;
#28646=B_SPLINE_CURVE_WITH_KNOTS ( 'NONE', 3,
 ( #74657, #743, #54100, #37446 ),
 .UNSPECIFIED., .F., .F.,
 ( 4, 4 ),
 ( 4.718958039861916012E-17, 0.002032023592278147089 ),
 .UNSPECIFIED. ) ;
#28649=CARTESIAN_POINT ( 'NONE',  ( 42.08762648273149409, 487.0030674539048618, 9.106351919857861077 ) ) ;
#28660=CARTESIAN_POINT ( 'NONE',  ( 33.08751701378358945, 301.6823158026044780, 11.49690784967660662 ) ) ;
#28661=DIRECTION ( 'NONE',  ( 0.000000000000000000, 0.7605354461462350280, -0.6492964154799772958 ) ) ;
#28676=ORIENTED_EDGE ( 'NONE', *, *, #51316, .F. ) ;
#28677=CARTESIAN_POINT ( 'NONE',  ( -41.46910480218704009, 484.7338956289818270, -3.418960549715579500 ) ) ;
#28684=CARTESIAN_POINT ( 'NONE',  ( -33.74590002647645548, 434.0087204318717795, 12.79521435343652236 ) ) ;
#28686=CARTESIAN_POINT ( 'NONE',  ( -32.46586666335682736, 488.6856797978888380, 9.810357008062371875 ) ) ;
#28694=B_SPLINE_CURVE_WITH_KNOTS ( 'NONE', 3,
 ( #51993, #85994, #12067, #62252, #2906, #19156, #86530, #46045, #12592, #37455 ),
 .UNSPECIFIED., .F., .F.,
 ( 4, 2, 2, 2, 4 ),
 ( -5.999999999514162541E-08, 0.002466202848293326880, 0.004932465696586649066, 0.009864991393173294307, 0.01973004278634659173 ),
 .UNSPECIFIED. ) ;
#28699=CARTESIAN_POINT ( 'NONE',  ( 32.02014133911703908, 464.7988840750959980, 11.81894500396711933 ) ) ;
#28700=CARTESIAN_POINT ( 'NONE',  ( 46.00000000000000000, 437.9690125970931831, 14.09127711025711349 ) ) ;
#28706=CARTESIAN_POINT ( 'NONE',  ( 0.000000000000000000, 274.9999999999999432, -10.00000000000000533 ) ) ;
#28709=CARTESIAN_POINT ( 'NONE',  ( -45.99999999999999289, 462.1567080628744293, 5.830853676147882858 ) ) ;
#28713=CARTESIAN_POINT ( 'NONE',  ( -32.84237740334658895, 485.2251842821276568, 5.746442123023856041 ) ) ;
#28720=EDGE_CURVE ( 'NONE', #24620, #69218, #43244, .T. ) ;
#28722=CARTESIAN_POINT ( 'NONE',  ( -3.271359168585607158, 300.0885221343756371, 9.452922326459093583 ) ) ;
#28729=CARTESIAN_POINT ( 'NONE',  ( 11.46329167404285343, 294.5997526591420410, -10.05357486629153030 ) ) ;
#28769=CARTESIAN_POINT ( 'NONE',  ( -13.69034148509428839, 302.5483970265941593, 9.872518330349395299 ) ) ;
#28786=ORIENTED_EDGE ( 'NONE', *, *, #67309, .T. ) ;
#28793=ORIENTED_EDGE ( 'NONE', *, *, #90396, .T. ) ;
#28797=CARTESIAN_POINT ( 'NONE',  ( 25.02598631787318695, 305.0623641175172338, -9.737168983575548609 ) ) ;
#28805=CARTESIAN_POINT ( 'NONE',  ( 32.88333705524082973, 439.7317646416722141, 24.13381181826093069 ) ) ;
#28806=CARTESIAN_POINT ( 'NONE',  ( 40.32369798409568062, 437.3250542437401123, 5.179402639110887385 ) ) ;
#28815=CARTESIAN_POINT ( 'NONE',  ( -42.18756898894582719, 484.4522853017719513, -2.425645685620470449 ) ) ;
#28819=CARTESIAN_POINT ( 'NONE',  ( -20.49977525862255590, 302.8459220885798686, -10.00124997875689203 ) ) ;
#28821=CARTESIAN_POINT ( 'NONE',  ( -40.60010613376132937, 436.1985323639528360, 6.054933560611875265 ) ) ;
#28822=CARTESIAN_POINT ( 'NONE',  ( 32.03720899076503059, 464.7921976803871758, 11.81820142135948437 ) ) ;
#28824=LINE ( 'NONE', #84886, #81310 ) ;
#28827=B_SPLINE_CURVE_WITH_KNOTS ( 'NONE', 3,
 ( #105652, #80307, #48474, #88953 ),
 .UNSPECIFIED., .F., .F.,
 ( 4, 4 ),
 ( 0.000000000000000000, 0.001935030059085813409 ),
 .UNSPECIFIED. ) ;
#28830=( LENGTH_UNIT ( ) NAMED_UNIT ( * ) SI_UNIT ( .MILLI., .METRE. ) );
#28845=FACE_OUTER_BOUND ( 'NONE', #57861, .T. ) ;
#28858=AXIS2_PLACEMENT_3D ( 'NONE', #103140, #30323, #71813 ) ;
#28861=EDGE_CURVE ( 'NONE', #26579, #91673, #71763, .T. ) ;
#28893=DIRECTION ( 'NONE',  ( 0.000000000000000000, 0.000000000000000000, -1.000000000000000000 ) ) ;
#28896=CARTESIAN_POINT ( 'NONE',  ( 0.000000000000000000, 0.000000000000000000, -10.00000000000000355 ) ) ;
#28901=CARTESIAN_POINT ( 'NONE',  ( 35.51316232729440259, 414.8269433707833969, 6.894890188973520573 ) ) ;
#28907=CARTESIAN_POINT ( 'NONE',  ( 38.67643969787641822, 490.7806551866269160, 11.84688141262719441 ) ) ;
#28908=CARTESIAN_POINT ( 'NONE',  ( 44.17836536378482748, 435.2619773020558682, 14.65562696767865170 ) ) ;
#28912=CARTESIAN_POINT ( 'NONE',  ( 21.29592979798552577, 302.9478885984597127, -9.979576327195278651 ) ) ;
#28926=CARTESIAN_POINT ( 'NONE',  ( 41.66809339685227087, 324.8386627565116100, 5.312837162286244919 ) ) ;
#28949=ORIENTED_EDGE ( 'NONE', *, *, #74261, .F. ) ;
#28951=CARTESIAN_POINT ( 'NONE',  ( -43.71037717921183230, 462.3391554988663756, 4.824299547743598815 ) ) ;
#28967=B_SPLINE_CURVE_WITH_KNOTS ( 'NONE', 3,
 ( #104664, #30816, #56632, #55561, #90075, #80379, #106239, #23785, #48540, #98161, #88497, #6491, #39942, #64743, #32399, #7545, #72813, #5962, #55037, #38886, #40461, #30273, #22186, #56081, #16182, #63702, #73341, #96589, #39422, #80914, #105720, #87969, #7025, #72297, #14049, #23243, #65271, #24316, #22723, #14575, #47481, #57163, #79329, #15120, #105204, #5448, #31350, #97619 ),
 .UNSPECIFIED., .F., .F.,
 ( 4, 2, 2, 2, 2, 2, 2, 2, 2, 2, 2, 2, 2, 2, 2, 2, 2, 2, 2, 2, 2, 2, 2, 4 ),
 ( -5.999999999670915252E-08, 0.001090263057642365876, 0.002180586115284728361, 0.003270909172927090412, 0.003816070701748271003, 0.004361232230569451161, 0.004906393759390633054, 0.005451555288211814079, 0.006541878345854297561, 0.008722524461139262789, 0.01090317057642422628, 0.01308381669170918804, 0.01744510892227911850, 0.02616769338341913553, 0.03052898561398914926, 0.03489027784455915604, 0.04361286230569918348, 0.05233544676683919011, 0.06978061568911922419, 0.08722578461139925132, 0.1046709535336792785, 0.1221161224559593056, 0.1308387069170994232, 0.1395612913782395270 ),
 .UNSPECIFIED. ) ;
#28985=CARTESIAN_POINT ( 'NONE',  ( 25.04416970470931147, 295.6688433518704642, 2.112457367892493831 ) ) ;
#28994=EDGE_CURVE ( 'NONE', #44795, #25681, #61484, .T. ) ;
#28996=B_SPLINE_CURVE_WITH_KNOTS ( 'NONE', 3,
 ( #92112, #85094, #60313, #26897, #18255, #75935, #76456, #59772, #51651, #84575, #68392, #51114, #10134, #10652, #43570, #101286 ),
 .UNSPECIFIED., .F., .F.,
 ( 4, 2, 2, 2, 2, 2, 2, 4 ),
 ( 6.992893892674702526E-18, 0.0001384951335132145981, 0.0002769902670264222030, 0.0005539805340528701017, 0.0008309708010793181087, 0.001107961068105766007, 0.001661941602158780850, 0.002215922136211795259 ),
 .UNSPECIFIED. ) ;
#29000=AXIS2_PLACEMENT_3D ( 'NONE', #60081, #33672, #9892 ) ;
#29005=CARTESIAN_POINT ( 'NONE',  ( -4.989154468854752454E-15, -18.92596047533412573, -20.36976895023282097 ) ) ;
#29008=AXIS2_PLACEMENT_3D ( 'NONE', #35581, #19416, #52250 ) ;
#29033=CARTESIAN_POINT ( 'NONE',  ( 40.22629662633006831, 485.6695299958086594, -4.459425866601474553 ) ) ;
#29056=CARTESIAN_POINT ( 'NONE',  ( 26.49263286547231644, 310.1913357440211030, 10.20160702900524008 ) ) ;
#29077=CARTESIAN_POINT ( 'NONE',  ( 41.74778363246261392, 460.3875427940046166, 2.379529480111751916 ) ) ;
#29082=EDGE_LOOP ( 'NONE', ( #72035, #39931, #47091, #65842 ) ) ;
#29087=ADVANCED_FACE ( 'NONE', ( #66542 ), #66009, .T. ) ;
#29101=AXIS2_PLACEMENT_3D ( 'NONE', #81397, #83536, #8586 ) ;
#29108=CARTESIAN_POINT ( 'NONE',  ( 33.14162648300398928, 381.8286340670186405, 24.93812587160989480 ) ) ;
#29112=CARTESIAN_POINT ( 'NONE',  ( -39.17204790862007968, 459.8623611124606896, 1.900463024343122420 ) ) ;
#29119=CARTESIAN_POINT ( 'NONE',  ( -25.22202552652619190, 306.3045764116132545, -8.682614143662695128 ) ) ;
#29121=CARTESIAN_POINT ( 'NONE',  ( -28.62134865195630695, 310.7073307092337586, 11.81453451529568888 ) ) ;
#29127=ORIENTED_EDGE ( 'NONE', *, *, #44168, .F. ) ;
#29144=CARTESIAN_POINT ( 'NONE',  ( 8.557829126397788144, 294.6841484303158154, -5.194105103951514479 ) ) ;
#29146=CARTESIAN_POINT ( 'NONE',  ( 38.56934373940381988, 309.6127934295942623, 1.496663477255220531 ) ) ;
#29159=CARTESIAN_POINT ( 'NONE',  ( -43.51602118134770336, 463.0217804479698884, 9.924213970829672604 ) ) ;
#29160=VERTEX_POINT ( 'NONE', #94009 ) ;
#29166=VERTEX_POINT ( 'NONE', #36352 ) ;
#29176=CARTESIAN_POINT ( 'NONE',  ( -37.83989825151947173, 491.6297408768480750, 12.44743998624971049 ) ) ;
#29181=ORIENTED_EDGE ( 'NONE', *, *, #5026, .T. ) ;
#29182=CARTESIAN_POINT ( 'NONE',  ( -43.21667697146752118, 434.4554196591588493, 16.17972000939132116 ) ) ;
#29212=EDGE_CURVE ( 'NONE', #4725, #36986, #76657, .T. ) ;
#29229=CARTESIAN_POINT ( 'NONE',  ( -33.17861982450024527, 435.0122478756496207, 15.11176251742224608 ) ) ;
#29252=CARTESIAN_POINT ( 'NONE',  ( -36.89065814680163413, 342.5445545919167785, -0.5098802229861002511 ) ) ;
#29258=ORIENTED_EDGE ( 'NONE', *, *, #1653, .T. ) ;
#29262=DIRECTION ( 'NONE',  ( 1.000000000000000000, 0.000000000000000000, -1.224646799147353207E-16 ) ) ;
#29267=CARTESIAN_POINT ( 'NONE',  ( 13.31041225640290548, 294.5490349693251346, -2.064332924270082970 ) ) ;
#29272=CARTESIAN_POINT ( 'NONE',  ( -37.02109538778312725, 490.9589098422684401, 12.45652899166105243 ) ) ;
#29275=ADVANCED_FACE ( 'NONE', ( #79930 ), #3897, .F. ) ;
#29279=CARTESIAN_POINT ( 'NONE',  ( -33.72687874427343502, 464.0440927327247209, 18.49751758948643499 ) ) ;
#29291=EDGE_CURVE ( 'NONE', #52539, #9067, #30463, .T. ) ;
#29293=ORIENTED_EDGE ( 'NONE', *, *, #73248, .T. ) ;
#29309=VERTEX_POINT ( 'NONE', #104208 ) ;
#29310=CARTESIAN_POINT ( 'NONE',  ( -33.89250494191498575, 463.6575930728432127, 6.993601543837932866 ) ) ;
#29336=CARTESIAN_POINT ( 'NONE',  ( 34.16218064238238128, 484.1154536690855821, 0.7177099017922428104 ) ) ;
#29340=CARTESIAN_POINT ( 'NONE',  ( -22.18906107735381283, 305.1406206946286943, -9.938500898754245583 ) ) ;
#29343=CARTESIAN_POINT ( 'NONE',  ( -46.00000000000000000, 500.0000000000002274, 0.000000000000000000 ) ) ;
#29344=CARTESIAN_POINT ( 'NONE',  ( -39.82092066244458550, 436.5808519682735209, 5.503544575421002172 ) ) ;
#29380=B_SPLINE_CURVE_WITH_KNOTS ( 'NONE', 3,
 ( #104853, #78976, #87088, #38030 ),
 .UNSPECIFIED., .F., .F.,
 ( 4, 4 ),
 ( 6.651595791536764171E-17, 0.003677212860670132834 ),
 .UNSPECIFIED. ) ;
#29397=CIRCLE ( 'NONE', #39694, 1.000000000000000000 ) ;
#29402=ORIENTED_EDGE ( 'NONE', *, *, #65588, .T. ) ;
#29406=DIRECTION ( 'NONE',  ( 0.2021170706129989947, -0.9793613683246955581, 0.000000000000000000 ) ) ;
#29407=EDGE_CURVE ( 'NONE', #104315, #71046, #46073, .T. ) ;
#29410=EDGE_CURVE ( 'NONE', #44580, #103542, #65007, .T. ) ;
#29420=VERTEX_POINT ( 'NONE', #64823 ) ;
#29421=CARTESIAN_POINT ( 'NONE',  ( 36.69625031493811917, 379.3716818342556394, 5.006538804195920456 ) ) ;
#29424=CARTESIAN_POINT ( 'NONE',  ( 37.51625577699761038, 491.7333577044556705, 12.51656167145575083 ) ) ;
#29426=CARTESIAN_POINT ( 'NONE',  ( -32.01402575875847845, 314.0648241496062951, -7.572118188761770341 ) ) ;
#29429=B_SPLINE_CURVE_WITH_KNOTS ( 'NONE', 3,
 ( #21180, #20667, #95045, #70747 ),
 .UNSPECIFIED., .F., .F.,
 ( 4, 4 ),
 ( 1.486235917163331928E-15, 0.001704530934783209063 ),
 .UNSPECIFIED. ) ;
#29446=CARTESIAN_POINT ( 'NONE',  ( 44.17878650602291657, 334.0442197469624830, -0.5072527954545905660 ) ) ;
#29447=CARTESIAN_POINT ( 'NONE',  ( 44.29460294111461138, 463.8401613562670605, 7.966579552400246733 ) ) ;
#29453=( BOUNDED_SURFACE ( )  B_SPLINE_SURFACE ( 3, 2, ( 
 ( #87550, #79440, #29864 ),
 ( #94593, #6076, #104241 ),
 ( #20741, #21772, #70302 ),
 ( #103198, #53578, #22834 ),
 ( #28821, #96175, #22304 ),
 ( #86510, #12570, #78378 ),
 ( #29344, #41113, #98280 ),
 ( #40576, #81532, #24951 ),
 ( #24437, #31975, #65388 ),
 ( #31457, #88603, #32516 ),
 ( #64852, #33048, #14688 ),
 ( #90192, #57269, #106354 ) ),
 .UNSPECIFIED., .F., .F., .F. ) 
 B_SPLINE_SURFACE_WITH_KNOTS ( ( 4, 2, 2, 2, 2, 4 ),
 ( 3, 3 ),
 ( 4.336808689942017736E-18, 0.001679904595664889885, 0.003359809191329775433, 0.004199761489162218316, 0.005039713786994660764, 0.006719618382659546529 ),
 ( 0.000000000000000000, 1.000000000000000000 ),
 .UNSPECIFIED. ) 
 GEOMETRIC_REPRESENTATION_ITEM ( )  RATIONAL_B_SPLINE_SURFACE ( (
 ( 1.000000000000000000, 0.8014084173415133572, 1.000000000000000000),
 ( 1.000000000000000000, 0.8133474198053308735, 1.000000000000000000),
 ( 1.000000000000000000, 0.8251589633820495262, 1.000000000000000000),
 ( 1.000000000000000000, 0.8478574907211462452, 1.000000000000000000),
 ( 1.000000000000000000, 0.8587488926515607357, 1.000000000000000000),
 ( 1.000000000000000000, 0.8739423948897212524, 1.000000000000000000),
 ( 1.000000000000000000, 0.8787956638559124567, 1.000000000000000000),
 ( 1.000000000000000000, 0.8878757020716896431, 1.000000000000000000),
 ( 1.000000000000000000, 0.8921241670187577411, 1.000000000000000000),
 ( 1.000000000000000000, 0.9038999154881867115, 1.000000000000000000),
 ( 1.000000000000000000, 0.9104653308039090120, 1.000000000000000000),
 ( 1.000000000000000000, 0.9153908114177995436, 1.000000000000000000) ) ) 
 REPRESENTATION_ITEM ( '' )  SURFACE ( )  );
#29460=CARTESIAN_POINT ( 'NONE',  ( -37.05595180434684011, 463.3109355731702408, 20.11755950910318447 ) ) ;
#29461=ORIENTED_EDGE ( 'NONE', *, *, #94904, .F. ) ;
#29474=ORIENTED_EDGE ( 'NONE', *, *, #60499, .F. ) ;
#29475=CARTESIAN_POINT ( 'NONE',  ( 43.00000000000000000, 436.0987441542287115, 7.567257455462724991 ) ) ;
#29482=ORIENTED_EDGE ( 'NONE', *, *, #13975, .F. ) ;
#29486=EDGE_LOOP ( 'NONE', ( #38209, #61098, #8146, #94621 ) ) ;
#29490=CARTESIAN_POINT ( 'NONE',  ( -43.67962475666660538, 397.2192610118504490, 16.03014433720793264 ) ) ;
#29495=ORIENTED_EDGE ( 'NONE', *, *, #51592, .T. ) ;
#29502=CARTESIAN_POINT ( 'NONE',  ( 31.63326088424243920, 436.4600345790572078, 18.87307648235493573 ) ) ;
#29503=CARTESIAN_POINT ( 'NONE',  ( 22.10125386972620376, 303.2174250443505343, 10.01554689547207744 ) ) ;
#29507=CARTESIAN_POINT ( 'NONE',  ( 42.20540931547678554, 464.9254549434356250, 14.73500713293391229 ) ) ;
#29509=CARTESIAN_POINT ( 'NONE',  ( -37.85084083633361729, 438.0234350436313093, 4.171260309356228824 ) ) ;
#29511=EDGE_CURVE ( 'NONE', #63262, #73090, #97703, .T. ) ;
#29514=DIRECTION ( 'NONE',  ( 0.2255559232117683721, 0.1250062448739182319, 0.9661769839147531513 ) ) ;
#29525=CARTESIAN_POINT ( 'NONE',  ( -42.79914298581935839, 484.2777690190095541, -1.375851118298070164 ) ) ;
#29531=DIRECTION ( 'NONE',  ( 0.000000000000000000, 0.000000000000000000, -1.000000000000000000 ) ) ;
#29538=DIRECTION ( 'NONE',  ( -0.2280158659362349349, 0.1533051183515994065, 0.9615125093146479340 ) ) ;
#29539=FACE_OUTER_BOUND ( 'NONE', #88590, .T. ) ;
#29546=CARTESIAN_POINT ( 'NONE',  ( 40.67924138885037166, 485.8013567632063996, -4.837443355053446581 ) ) ;
#29558=CARTESIAN_POINT ( 'NONE',  ( -42.09210974227526947, 317.4093497706929270, -4.557617623460385126 ) ) ;
#29560=CARTESIAN_POINT ( 'NONE',  ( 32.73226863436134693, 439.3384463444876360, 23.76670009903627800 ) ) ;
#29568=CARTESIAN_POINT ( 'NONE',  ( -40.89305344739149461, 461.0673237560018833, 2.333915627062479903 ) ) ;
#29606=CARTESIAN_POINT ( 'NONE',  ( -46.00000000000000000, 438.0901456946749022, 11.29311581785933072 ) ) ;
#29608=EDGE_CURVE ( 'NONE', #23483, #73133, #7105, .T. ) ;
#29617=CARTESIAN_POINT ( 'NONE',  ( 42.70246075394577900, 373.2460375941973894, 18.12284514452785089 ) ) ;
#29619=EDGE_CURVE ( 'NONE', #70575, #55309, #25386, .T. ) ;
#29630=CARTESIAN_POINT ( 'NONE',  ( -30.94128241318078665, 298.6042193091406602, 2.768098133593460908 ) ) ;
#29638=CARTESIAN_POINT ( 'NONE',  ( -43.00000000000000000, 488.3725375423296100, 3.127739281037506647 ) ) ;
#29643=ORIENTED_EDGE ( 'NONE', *, *, #9276, .T. ) ;
#29652=MECHANICAL_DESIGN_GEOMETRIC_PRESENTATION_REPRESENTATION('',(#22726),#45121);
#29660=CARTESIAN_POINT ( 'NONE',  ( 8.849035312350377325, 302.6218124188690126, -10.03679229143238594 ) ) ;
#29662=CARTESIAN_POINT ( 'NONE',  ( 37.12595521884477989, 306.0480932226964796, 0.6086346269186700964 ) ) ;
#29663=CARTESIAN_POINT ( 'NONE',  ( -43.03185303983481447, 485.3613526602391062, 6.073233449168579767 ) ) ;
#29696=EDGE_CURVE ( 'NONE', #71461, #85977, #27161, .T. ) ;
#29702=CARTESIAN_POINT ( 'NONE',  ( 43.55333112596304090, 465.2342844084867011, 9.238213423009598912 ) ) ;
#29709=ORIENTED_EDGE ( 'NONE', *, *, #48303, .T. ) ;
#29714=ADVANCED_FACE ( 'NONE', ( #17225 ), #21884, .T. ) ;
#29717=CARTESIAN_POINT ( 'NONE',  ( -42.75139825103929070, 485.3314578938633304, -3.157348782696939971 ) ) ;
#29719=CARTESIAN_POINT ( 'NONE',  ( 35.76379064120181539, 307.0162303970107587, 12.81051142610679960 ) ) ;
#29723=DIRECTION ( 'NONE',  ( 0.000000000000000000, -0.6886991506751505288, 0.7250472259510594153 ) ) ;
#29742=CARTESIAN_POINT ( 'NONE',  ( -31.88073664226197934, 435.8776075131638663, 17.60257548430462293 ) ) ;
#29748=( BOUNDED_SURFACE ( )  B_SPLINE_SURFACE ( 3, 2, ( 
 ( #73463, #49731, #25503 ),
 ( #99879, #50773, #33572 ),
 ( #16298, #33053, #59442 ),
 ( #74533, #75057, #1152 ) ),
 .UNSPECIFIED., .F., .F., .F. ) 
 B_SPLINE_SURFACE_WITH_KNOTS ( ( 4, 4 ),
 ( 3, 3 ),
 ( 0.05518226518917336565, 0.08125438797488282461 ),
 ( 0.3700808604202216467, 1.000000000000000000 ),
 .UNSPECIFIED. ) 
 GEOMETRIC_REPRESENTATION_ITEM ( )  RATIONAL_B_SPLINE_SURFACE ( (
 ( 0.8634406061711257241, 0.8155005994179043149, 1.000000000000000000),
 ( 0.8634403698514303560, 0.8155002801367408072, 1.000000000000000000),
 ( 0.8634404275997331624, 0.8155003581579370886, 1.000000000000000000),
 ( 0.8634406601346265031, 0.8155006723256206236, 1.000000000000000000) ) ) 
 REPRESENTATION_ITEM ( '' )  SURFACE ( )  );
#29751=CARTESIAN_POINT ( 'NONE',  ( -34.96345651127622034, 302.4133583293575498, -0.2769688069068840242 ) ) ;
#29758=CARTESIAN_POINT ( 'NONE',  ( 43.18793366350566032, 465.6364658675358328, 10.75294125769881148 ) ) ;
#29762=AXIS2_PLACEMENT_3D ( 'NONE', #62315, #95208, #5129 ) ;
#29769=CARTESIAN_POINT ( 'NONE',  ( -37.67790193267708077, 380.9199617470918611, 5.379015220008868781 ) ) ;
#29782=DIRECTION ( 'NONE',  ( -1.224646799147353454E-16, 0.000000000000000000, -1.000000000000000000 ) ) ;
#29783=EDGE_CURVE ( 'NONE', #52539, #94742, #34088, .T. ) ;
#29784=CARTESIAN_POINT ( 'NONE',  ( -43.00000000000000000, 500.0000000000002274, 12.00000000000000711 ) ) ;
#29831=VERTEX_POINT ( 'NONE', #22558 ) ;
#29835=ORIENTED_EDGE ( 'NONE', *, *, #80933, .F. ) ;
#29842=CARTESIAN_POINT ( 'NONE',  ( 36.54310633446583978, 363.9539195057402594, 3.129522754832409603 ) ) ;
#29846=CARTESIAN_POINT ( 'NONE',  ( -33.07276483573667747, 438.9325140356154975, 23.89537236861306013 ) ) ;
#29850=CARTESIAN_POINT ( 'NONE',  ( -40.31555625028288148, 316.2223002904267446, 3.164403933231767052 ) ) ;
#29851=CARTESIAN_POINT ( 'NONE',  ( 36.34421051467749209, 333.8189236619288067, -2.452241787315455390 ) ) ;
#29861=CARTESIAN_POINT ( 'NONE',  ( -20.24579557674108088, 304.8297271373347144, -10.00469232190996749 ) ) ;
#29864=CARTESIAN_POINT ( 'NONE',  ( -43.00000000000000000, 436.0987441542287115, 7.567257455462743643 ) ) ;
#29872=CIRCLE ( 'NONE', #90107, 1.000000000000016209 ) ;
#29876=ORIENTED_EDGE ( 'NONE', *, *, #31053, .T. ) ;
#29894=CARTESIAN_POINT ( 'NONE',  ( 13.81785577674642873, 302.5467234193154127, 9.872154563399625715 ) ) ;
#29903=CARTESIAN_POINT ( 'NONE',  ( -46.00000000000000000, 488.3725375423296668, 3.127739281037490215 ) ) ;
#29933=ORIENTED_EDGE ( 'NONE', *, *, #49947, .F. ) ;
#29934=CARTESIAN_POINT ( 'NONE',  ( 34.76497128141613047, 338.4643821587915227, -1.841863933405186282 ) ) ;
#29937=CARTESIAN_POINT ( 'NONE',  ( 34.59893540551180990, 491.2022546151283109, 12.15065315885511765 ) ) ;
#29949=CARTESIAN_POINT ( 'NONE',  ( -32.94021323899831799, 485.0599191339510980, 5.361609822536971492 ) ) ;
#29954=CARTESIAN_POINT ( 'NONE',  ( 43.27459526351800179, 485.1620945307548141, -2.264801863435696561 ) ) ;
#29958=CARTESIAN_POINT ( 'NONE',  ( 30.90190637651703653, 309.2317938240619810, -8.529668860358439630 ) ) ;
#29975=ORIENTED_EDGE ( 'NONE', *, *, #2132, .T. ) ;
#29980=ORIENTED_EDGE ( 'NONE', *, *, #8896, .F. ) ;
#29996=CIRCLE ( 'NONE', #104018, 2.999999999999999112 ) ;
#30004=CARTESIAN_POINT ( 'NONE',  ( 33.70427618943720205, 490.4072845429053018, 11.54254722977849745 ) ) ;
#30009=EDGE_LOOP ( 'NONE', ( #29181, #23456, #7233, #19289 ) ) ;
#30014=CARTESIAN_POINT ( 'NONE',  ( -39.65839090363253661, 485.8593493675159039, -5.004208577436008554 ) ) ;
#30037=CARTESIAN_POINT ( 'NONE',  ( 18.15174345153223712, 304.6383688000003076, 8.891572165220576807 ) ) ;
#30040=CARTESIAN_POINT ( 'NONE',  ( 34.89266211578681975, 436.0682616543206223, 7.611940783812184641 ) ) ;
#30044=CARTESIAN_POINT ( 'NONE',  ( -32.15963082908692172, 464.7082849654399865, 10.94047064224899835 ) ) ;
#30046=EDGE_CURVE ( 'NONE', #75387, #7582, #43034, .T. ) ;
#30048=CARTESIAN_POINT ( 'NONE',  ( 43.50250715914180688, 464.6389613228375310, 9.611700240007991169 ) ) ;
#30049=CARTESIAN_POINT ( 'NONE',  ( -42.23079339798738374, 460.7352525929354101, 2.726051457480726636 ) ) ;
#30051=CARTESIAN_POINT ( 'NONE',  ( -41.50820411079202188, 461.5963371455320612, 2.703439750996428081 ) ) ;
#30053=CARTESIAN_POINT ( 'NONE',  ( 46.00000000000000000, 486.4340384878591408, 3.748479173862500513 ) ) ;
#30060=CARTESIAN_POINT ( 'NONE',  ( 38.81358894280344884, 485.1131561813197095, -4.191378885297267765 ) ) ;
#30065=CARTESIAN_POINT ( 'NONE',  ( -34.00007050920425655, 439.9158767981585356, 24.30698066181913575 ) ) ;
#30066=ORIENTED_EDGE ( 'NONE', *, *, #49768, .T. ) ;
#30079=ORIENTED_EDGE ( 'NONE', *, *, #12100, .F. ) ;
#30080=CARTESIAN_POINT ( 'NONE',  ( -26.49347172118876514, 310.1936227282963046, 10.20217970970264609 ) ) ;
#30086=EDGE_CURVE ( 'NONE', #30344, #3187, #21293, .T. ) ;
#30118=CARTESIAN_POINT ( 'NONE',  ( -46.00000000000000000, 438.4646224975035125, 9.895601460523737458 ) ) ;
#30120=CARTESIAN_POINT ( 'NONE',  ( -45.99999999999998579, 461.2896359780384614, 8.857952602228083450 ) ) ;
#30125=CARTESIAN_POINT ( 'NONE',  ( -42.99999999999847944, 487.1237704758270866, 9.497510897114741724 ) ) ;
#30132=CARTESIAN_POINT ( 'NONE',  ( 40.74486364038580888, 360.0828261927184144, 24.30144178707762848 ) ) ;
#30138=AXIS2_PLACEMENT_3D ( 'NONE', #104938, #80110, #87696 ) ;
#30139=CARTESIAN_POINT ( 'NONE',  ( -38.98764044588113364, 460.2978347093127809, 2.283752696491721856 ) ) ;
#30143=CARTESIAN_POINT ( 'NONE',  ( -35.41620593328612188, 462.9429453004491961, 4.226634750751853353 ) ) ;
#30147=CARTESIAN_POINT ( 'NONE',  ( -33.80382396800512623, 301.4638900151607572, 3.437251938379645821 ) ) ;
#30166=ADVANCED_FACE ( 'NONE', ( #54078 ), #6477, .F. ) ;
#30173=ORIENTED_EDGE ( 'NONE', *, *, #97914, .T. ) ;
#30179=EDGE_CURVE ( 'NONE', #72871, #457, #58521, .T. ) ;
#30189=ORIENTED_EDGE ( 'NONE', *, *, #6869, .F. ) ;
#30210=CARTESIAN_POINT ( 'NONE',  ( 36.64823341582350480, 437.5392299810053487, 4.281405873620231617 ) ) ;
#30215=DIRECTION ( 'NONE',  ( 0.000000000000000000, 0.000000000000000000, 1.000000000000000000 ) ) ;
#30221=CARTESIAN_POINT ( 'NONE',  ( 43.75010090114224681, 464.8337800386878484, 11.75004750934975029 ) ) ;
#30230=CARTESIAN_POINT ( 'NONE',  ( -13.68624448364603374, 294.5456259610601251, 1.871922272540206045 ) ) ;
#30243=CARTESIAN_POINT ( 'NONE',  ( 46.00000000000000000, 450.0000000000002274, 25.20242257375371864 ) ) ;
#30244=ADVANCED_FACE ( 'NONE', ( #55658 ), #44544, .F. ) ;
#30254=CARTESIAN_POINT ( 'NONE',  ( -31.61667038019096410, 439.3937981091067968, 23.34452816489683258 ) ) ;
#30256=CARTESIAN_POINT ( 'NONE',  ( -35.46167881839126323, 432.6462199839393179, 5.655415401830411248 ) ) ;
#30261=ADVANCED_FACE ( 'NONE', ( #49715 ), #59661, .F. ) ;
#30265=CARTESIAN_POINT ( 'NONE',  ( -28.74670144010507400, 306.4392983594438533, -9.196308249178452243 ) ) ;
#30268=ORIENTED_EDGE ( 'NONE', *, *, #19572, .F. ) ;
#30273=CARTESIAN_POINT ( 'NONE',  ( 27.22388839005207828, 312.2963372293064026, 10.72986269782501623 ) ) ;
#30287=CARTESIAN_POINT ( 'NONE',  ( -30.87619945487599082, 309.1625279880333892, -8.547083864057238856 ) ) ;
#30290=CARTESIAN_POINT ( 'NONE',  ( 33.00000000000000000, 500.0000000000002274, 0.000000000000000000 ) ) ;
#30291=CIRCLE ( 'NONE', #92219, 15.00000000000001243 ) ;
#30294=EDGE_CURVE ( 'NONE', #1378, #104577, #82241, .T. ) ;
#30303=CARTESIAN_POINT ( 'NONE',  ( 16.92021657089327746, 302.5811070205058968, -10.05744944873218572 ) ) ;
#30323=DIRECTION ( 'NONE',  ( 1.000000000000000000, 0.000000000000000000, 0.000000000000000000 ) ) ;
#30332=AXIS2_PLACEMENT_3D ( 'NONE', #55312, #45139, #21403 ) ;
#30335=DIRECTION ( 'NONE',  ( 0.000000000000000000, 0.000000000000000000, -1.000000000000000000 ) ) ;
#30344=VERTEX_POINT ( 'NONE', #26555 ) ;
#30352=B_SPLINE_CURVE_WITH_KNOTS ( 'NONE', 3,
 ( #106585, #106041, #57490, #31669, #82848, #90415, #89881, #49407, #39746, #40263, #74741, #15991, #105529, #80709 ),
 .UNSPECIFIED., .F., .F.,
 ( 4, 2, 2, 2, 2, 2, 4 ),
 ( 2.602085213965210642E-18, 0.001028561904211934379, 0.002057123808423866156, 0.004114247616847721903, 0.005142809521059639802, 0.006171371425271557701, 0.008228495233695377886 ),
 .UNSPECIFIED. ) ;
#30353=CARTESIAN_POINT ( 'NONE',  ( 32.15166163075743100, 486.0589784586656492, 5.199393881399972273 ) ) ;
#30357=CARTESIAN_POINT ( 'NONE',  ( -43.18056654203904543, 485.1460802498594944, 5.477204712337340631 ) ) ;
#30369=CARTESIAN_POINT ( 'NONE',  ( -37.76893244230605262, 307.4136788487199965, 0.9472622734037586811 ) ) ;
#30383=CARTESIAN_POINT ( 'NONE',  ( 22.20318009218133071, 295.0333587257888439, 9.975590323731541531 ) ) ;
#30386=CARTESIAN_POINT ( 'NONE',  ( 31.03678703375144821, 438.6650838204807314, 21.86890379897223013 ) ) ;
#30408=CARTESIAN_POINT ( 'NONE',  ( 31.88312681400266868, 463.8062021098571677, 15.68963310188262739 ) ) ;
#30409=ORIENTED_EDGE ( 'NONE', *, *, #28861, .T. ) ;
#30419=CARTESIAN_POINT ( 'NONE',  ( 17.24515478965690818, 294.5883438517400918, 1.881387340289478516 ) ) ;
#30435=AXIS2_PLACEMENT_3D ( 'NONE', #94545, #53535, #87505 ) ;
#30454=FACE_OUTER_BOUND ( 'NONE', #43920, .T. ) ;
#30456=CARTESIAN_POINT ( 'NONE',  ( 0.000000000000000000, 69.00000000000000000, 0.000000000000000000 ) ) ;
#30463=CIRCLE ( 'NONE', #44224, 2.999999999999999112 ) ;
#30466=CARTESIAN_POINT ( 'NONE',  ( 36.00963897964896177, 344.1584813113714176, -0.3684565162341075228 ) ) ;
#30469=CARTESIAN_POINT ( 'NONE',  ( 42.44292469749079544, 488.6013120130130005, 9.763388545826034104 ) ) ;
#30476=CARTESIAN_POINT ( 'NONE',  ( -37.43096154125763064, 464.0779267918313735, 19.48675998633273920 ) ) ;
#30485=CARTESIAN_POINT ( 'NONE',  ( 35.48147139702570030, 303.1671216000320328, -0.09562962482448161827 ) ) ;
#30493=FACE_OUTER_BOUND ( 'NONE', #12830, .T. ) ;
#30512=FILL_AREA_STYLE ('',( #40163 ) ) ;
#30518=CARTESIAN_POINT ( 'NONE',  ( -30.00000000000000000, 488.8442721620238558, 4.433647275927475206 ) ) ;
#30533=CARTESIAN_POINT ( 'NONE',  ( 46.00000000000000000, 500.0000000000002274, -15.00000000000000711 ) ) ;
#30536=CARTESIAN_POINT ( 'NONE',  ( -43.65164521923173879, 485.1135274750027406, -1.117678676893244960 ) ) ;
#30544=AXIS2_PLACEMENT_3D ( 'NONE', #51277, #2732, #77169 ) ;
#30548=CARTESIAN_POINT ( 'NONE',  ( 37.88504238421554504, 463.4171042825134919, 19.90923349043870871 ) ) ;
#30566=DIRECTION ( 'NONE',  ( -9.567764352753668770E-16, 0.5617366626193331935, 0.8273160954975393722 ) ) ;
#30567=CARTESIAN_POINT ( 'NONE',  ( -42.88788165701930666, 484.9809715185594996, -1.409177641707331619 ) ) ;
#30585=CIRCLE ( 'NONE', #8137, 0.9999999999999806821 ) ;
#30592=CARTESIAN_POINT ( 'NONE',  ( 38.93727158156521995, 438.0716948385729665, 23.12369454750587749 ) ) ;
#30597=CARTESIAN_POINT ( 'NONE',  ( 38.96902200852336051, 460.8405016383494512, 2.186950304201005224 ) ) ;
#30611=AXIS2_PLACEMENT_3D ( 'NONE', #11756, #59808, #36096 ) ;
#30617=CARTESIAN_POINT ( 'NONE',  ( -27.76738912986519381, 314.2059264268535230, 11.21182569962504694 ) ) ;
#30620=DIRECTION ( 'NONE',  ( 0.000000000000000000, 0.000000000000000000, -1.000000000000000000 ) ) ;
#30625=CARTESIAN_POINT ( 'NONE',  ( 46.00000000000000000, 488.3725375423288710, 3.127739281034839003 ) ) ;
#30641=CARTESIAN_POINT ( 'NONE',  ( 31.19652432992544888, 378.3327707670021027, 24.28948218791313707 ) ) ;
#30645=EDGE_LOOP ( 'NONE', ( #18751, #101509, #45226, #90243 ) ) ;
#30659=CARTESIAN_POINT ( 'NONE',  ( -45.99999999999996447, 436.0910238442153855, 11.28143031774616567 ) ) ;
#30661=EDGE_CURVE ( 'NONE', #66199, #8292, #45534, .T. ) ;
#30673=CARTESIAN_POINT ( 'NONE',  ( 41.07051048954355821, 327.4162906337114691, 9.867383232854635366 ) ) ;
#30675=FACE_OUTER_BOUND ( 'NONE', #99390, .T. ) ;
#30680=ORIENTED_EDGE ( 'NONE', *, *, #39252, .T. ) ;
#30682=CARTESIAN_POINT ( 'NONE',  ( -38.51502786940056211, 460.0233756673464427, 2.043034587342818398 ) ) ;
#30684=ORIENTED_EDGE ( 'NONE', *, *, #106332, .F. ) ;
#30685=AXIS2_PLACEMENT_3D ( 'NONE', #63198, #87476, #55592 ) ;
#30687=CARTESIAN_POINT ( 'NONE',  ( -26.91834224567524814, 306.8661554697472980, 10.86152638338143994 ) ) ;
#30701=CARTESIAN_POINT ( 'NONE',  ( 36.73553355714089008, 438.2340261154861309, 3.898456086351941074 ) ) ;
#30703=( BOUNDED_SURFACE ( )  B_SPLINE_SURFACE ( 3, 2, ( 
 ( #97213, #56200, #23364 ),
 ( #14163, #5557, #54092 ),
 ( #80492, #79445, #89140 ),
 ( #88607, #15239, #14694 ) ),
 .UNSPECIFIED., .F., .F., .F. ) 
 B_SPLINE_SURFACE_WITH_KNOTS ( ( 4, 4 ),
 ( 3, 3 ),
 ( 1.322726650432315409E-17, 0.0002214634272574486900 ),
 ( 0.000000000000000000, 1.000000000000000000 ),
 .UNSPECIFIED. ) 
 GEOMETRIC_REPRESENTATION_ITEM ( )  RATIONAL_B_SPLINE_SURFACE ( (
 ( 1.000000000000000000, 0.8273155905869640225, 1.000000000000000000),
 ( 1.000000000000000000, 0.8262236971337512115, 1.000000000000000000),
 ( 1.000000000000000000, 0.8250826013137413373, 1.000000000000000000),
 ( 1.000000000000000000, 0.8238944711861589942, 1.000000000000000000) ) ) 
 REPRESENTATION_ITEM ( '' )  SURFACE ( )  );
#30705=B_SPLINE_CURVE_WITH_KNOTS ( 'NONE', 3,
 ( #21194, #3912, #13573, #87492, #36845, #45968, #13036, #78844, #4974, #61093 ),
 .UNSPECIFIED., .F., .F.,
 ( 4, 2, 2, 2, 4 ),
 ( -6.000000001405383295E-08, 0.002526620965178684626, 0.005053301930357382774, 0.01010666386071478948, 0.02021338772142960982 ),
 .UNSPECIFIED. ) ;
#30711=CARTESIAN_POINT ( 'NONE',  ( 41.58444831332685254, 481.6520554591356245, 13.64600804804222811 ) ) ;
#30752=CARTESIAN_POINT ( 'NONE',  ( -34.90210962188712074, 473.1106922774044961, 16.89617127990342738 ) ) ;
#30776=CARTESIAN_POINT ( 'NONE',  ( -40.95595929481465447, 405.2208686710653183, 27.85131585683114963 ) ) ;
#30781=ADVANCED_FACE ( 'NONE', ( #45755 ), #89343, .F. ) ;
#30789=EDGE_CURVE ( 'NONE', #95206, #56333, #46222, .T. ) ;
#30797=CARTESIAN_POINT ( 'NONE',  ( -31.52652959927143428, 438.9874841044786535, 23.28591655054718856 ) ) ;
#30799=CARTESIAN_POINT ( 'NONE',  ( 32.22503847990213899, 485.9064490506210632, 4.829857536092947434 ) ) ;
#30800=CARTESIAN_POINT ( 'NONE',  ( -32.70825224878974780, 489.1175319723178632, 10.34480600318775068 ) ) ;
#30808=CARTESIAN_POINT ( 'NONE',  ( -36.99835872953581628, 303.9880970021415578, -7.907733237980351326 ) ) ;
#30816=CARTESIAN_POINT ( 'NONE',  ( 20.09500326397664693, 304.8432866292113772, 8.935189372041850930 ) ) ;
#30817=CARTESIAN_POINT ( 'NONE',  ( 38.56577463025284658, 437.0885780681464325, 4.837144025084519683 ) ) ;
#30827=CARTESIAN_POINT ( 'NONE',  ( -34.80007552946424454, 439.6089305507155132, 24.02984928258333142 ) ) ;
#30829=CARTESIAN_POINT ( 'NONE',  ( -37.65940170220832783, 425.4627519512775393, 5.785112291392917605 ) ) ;
#30831=CARTESIAN_POINT ( 'NONE',  ( 41.51027627991900459, 460.7143023130748816, 2.893840913533772152 ) ) ;
#30837=B_SPLINE_CURVE_WITH_KNOTS ( 'NONE', 3,
 ( #58937, #100442, #100972, #17418 ),
 .UNSPECIFIED., .F., .F.,
 ( 4, 4 ),
 ( 0.000000000000000000, 0.002847824002212700611 ),
 .UNSPECIFIED. ) ;
#30849=ORIENTED_EDGE ( 'NONE', *, *, #35001, .F. ) ;
#30856=DIRECTION ( 'NONE',  ( 0.000000000000000000, 0.000000000000000000, -1.000000000000000000 ) ) ;
#30861=( BOUNDED_SURFACE ( )  B_SPLINE_SURFACE ( 3, 2, ( 
 ( #73190, #25786, #98020 ),
 ( #90463, #66726, #24172 ),
 ( #81286, #17123, #72676 ),
 ( #31717, #99065, #106094 ) ),
 .UNSPECIFIED., .F., .F., .F. ) 
 B_SPLINE_SURFACE_WITH_KNOTS ( ( 4, 4 ),
 ( 3, 3 ),
 ( -9.974659986866640793E-18, 0.002066227528073599946 ),
 ( 0.000000000000000000, 1.000000000000000000 ),
 .UNSPECIFIED. ) 
 GEOMETRIC_REPRESENTATION_ITEM ( )  RATIONAL_B_SPLINE_SURFACE ( (
 ( 1.000000000000000000, 0.7788880963805091540, 1.000000000000000000),
 ( 1.000000000000000000, 0.7743040464398368572, 1.000000000000000000),
 ( 1.000000000000000000, 0.7669333544817394932, 1.000000000000000000),
 ( 1.000000000000000000, 0.7583909709669780508, 1.000000000000000000) ) ) 
 REPRESENTATION_ITEM ( '' )  SURFACE ( )  );
#30896=CARTESIAN_POINT ( 'NONE',  ( 32.89392925376883170, 485.8745504892934832, 5.316642333858703218 ) ) ;
#30899=VERTEX_POINT ( 'NONE', #86240 ) ;
#30906=CARTESIAN_POINT ( 'NONE',  ( -32.82269234420702730, 485.2607240917816966, 5.823166218282519679 ) ) ;
#30915=CARTESIAN_POINT ( 'NONE',  ( -38.26360760319844445, 461.1057584915775465, 2.390039129069520207 ) ) ;
#30921=CARTESIAN_POINT ( 'NONE',  ( 34.88900972248876542, 464.6206820656010450, 18.69027339340470562 ) ) ;
#30923=ORIENTED_EDGE ( 'NONE', *, *, #40000, .T. ) ;
#30925=CARTESIAN_POINT ( 'NONE',  ( -27.97565635352651015, 315.9216507687758053, 12.64980990155120999 ) ) ;
#30927=CARTESIAN_POINT ( 'NONE',  ( -33.82591814952031939, 464.6968131430478479, 6.992934999028650900 ) ) ;
#30933=EDGE_CURVE ( 'NONE', #22245, #18315, #27600, .T. ) ;
#30946=CARTESIAN_POINT ( 'NONE',  ( 32.19467213680352558, 397.8364619396728585, 25.61660791817880067 ) ) ;
#30949=CARTESIAN_POINT ( 'NONE',  ( -44.15484044304455580, 485.1632656165609205, 0.5589787062256319494 ) ) ;
#30951=ADVANCED_FACE ( 'NONE', ( #103457 ), #11430, .F. ) ;
#30965=CARTESIAN_POINT ( 'NONE',  ( 20.15799098111282461, 294.7575367430327447, 1.916962552282521548 ) ) ;
#30974=CARTESIAN_POINT ( 'NONE',  ( -40.80890826771884861, 489.2901651173327764, 10.52137389376217058 ) ) ;
#31000=CARTESIAN_POINT ( 'NONE',  ( -43.00000000000000000, 436.5989882784185170, 19.94133085611150591 ) ) ;
#31005=CARTESIAN_POINT ( 'NONE',  ( 36.51687796781347828, 361.6932586242723460, 2.830374312397382575 ) ) ;
#31012=B_SPLINE_CURVE_WITH_KNOTS ( 'NONE', 3,
 ( #52316, #13442, #70639, #12384 ),
 .UNSPECIFIED., .F., .F.,
 ( 4, 4 ),
 ( 0.000000000000000000, 0.0005776816123925365568 ),
 .UNSPECIFIED. ) ;
#31013=CARTESIAN_POINT ( 'NONE',  ( 41.35127657993756856, 489.6199665183289653, 10.83744867395911982 ) ) ;
#31015=CARTESIAN_POINT ( 'NONE',  ( -32.85155332502864667, 463.8111683108725174, 7.359358840565846549 ) ) ;
#31021=CARTESIAN_POINT ( 'NONE',  ( -32.42656933073506309, 485.5064012031770631, 3.828740380151607781 ) ) ;
#31030=CARTESIAN_POINT ( 'NONE',  ( 36.17363157034238696, 304.2818952488495370, 0.1746411899071270979 ) ) ;
#31035=( LENGTH_UNIT ( ) NAMED_UNIT ( * ) SI_UNIT ( .MILLI., .METRE. ) );
#31039=CARTESIAN_POINT ( 'NONE',  ( 43.35553785602063215, 484.2706869240204810, -0.02741892261372324072 ) ) ;
#31042=CARTESIAN_POINT ( 'NONE',  ( -33.84761347220299399, 488.7471039746336032, 11.01988148152527103 ) ) ;
#31044=EDGE_CURVE ( 'NONE', #51980, #85207, #42828, .T. ) ;
#31045=B_SPLINE_CURVE_WITH_KNOTS ( 'NONE', 3,
 ( #46811, #45754, #87284, #53835 ),
 .UNSPECIFIED., .F., .F.,
 ( 4, 4 ),
 ( 0.000000000000000000, 0.001795780652499570293 ),
 .UNSPECIFIED. ) ;
#31053=EDGE_CURVE ( 'NONE', #62342, #17301, #71288, .T. ) ;
#31058=CARTESIAN_POINT ( 'NONE',  ( 43.71297783477844234, 485.1278128289774827, -1.116606130290200172 ) ) ;
#31061=CARTESIAN_POINT ( 'NONE',  ( -43.68737779332776228, 464.3703856682102469, 8.648249337457524888 ) ) ;
#31077=CARTESIAN_POINT ( 'NONE',  ( -34.82215666917964825, 439.1572798958988528, 24.08424788675419848 ) ) ;
#31078=CARTESIAN_POINT ( 'NONE',  ( 32.88833697125316746, 356.1062394740008017, 21.81815766810190027 ) ) ;
#31079=CARTESIAN_POINT ( 'NONE',  ( -44.17677142954600100, 334.0173847572560817, -0.5134196407643211169 ) ) ;
#31080=CARTESIAN_POINT ( 'NONE',  ( 32.39813942120852630, 439.6661968104010043, 24.00603005215503316 ) ) ;
#31081=CARTESIAN_POINT ( 'NONE',  ( -44.05377772243112844, 485.6975038926928505, 3.984329897971015111 ) ) ;
#31089=CARTESIAN_POINT ( 'NONE',  ( -38.47428897412150661, 485.7788508071988076, -4.770630528146577731 ) ) ;
#31110=CARTESIAN_POINT ( 'NONE',  ( 18.93091876528353623, 304.6959338034921529, 9.903868442296822394 ) ) ;
#31126=CARTESIAN_POINT ( 'NONE',  ( -30.00000000000000355, 461.9311049912134877, 11.83317730145777702 ) ) ;
#31130=ORIENTED_EDGE ( 'NONE', *, *, #80811, .F. ) ;
#31153=CARTESIAN_POINT ( 'NONE',  ( -30.19359820436435626, 332.6063179250270991, 15.69166344793225853 ) ) ;
#31181=CARTESIAN_POINT ( 'NONE',  ( 6.812123203431564633, 304.7372914378963173, -10.02434013685850012 ) ) ;
#31182=CARTESIAN_POINT ( 'NONE',  ( 31.00389226642222340, 485.8187364282109115, 14.27494812388583512 ) ) ;
#31187=CARTESIAN_POINT ( 'NONE',  ( 46.00000000000000711, 461.5044003753988591, 9.500280912739080819 ) ) ;
#31191=EDGE_CURVE ( 'NONE', #85207, #98535, #104718, .T. ) ;
#31193=ORIENTED_EDGE ( 'NONE', *, *, #95616, .T. ) ;
#31194=CIRCLE ( 'NONE', #12437, 1.000000000000000888 ) ;
#31196=ORIENTED_EDGE ( 'NONE', *, *, #84778, .F. ) ;
#31199=CARTESIAN_POINT ( 'NONE',  ( -46.00000000000000000, 461.6622277975411635, 10.18145404766348783 ) ) ;
#31209=CARTESIAN_POINT ( 'NONE',  ( 35.11261897330833648, 305.4840936023398967, 12.42931627445148379 ) ) ;
#31210=CARTESIAN_POINT ( 'NONE',  ( 42.18756898894605456, 484.4522853017719513, -2.425645685620597014 ) ) ;
#31211=ADVANCED_FACE ( 'NONE', ( #95783 ), #103124, .T. ) ;
#31212=CARTESIAN_POINT ( 'NONE',  ( -32.22503847990287795, 485.9064490506194716, 4.829857536089223302 ) ) ;
#31217=CARTESIAN_POINT ( 'NONE',  ( -35.44533458431160255, 462.1326274906116964, 4.365931901573204321 ) ) ;
#31221=CARTESIAN_POINT ( 'NONE',  ( -35.53880766297544369, 395.9677348675359667, 6.885462253420658207 ) ) ;
#31222=CARTESIAN_POINT ( 'NONE',  ( -25.74576498548020709, 305.2861965535228137, 10.48332055224852866 ) ) ;
#31247=CARTESIAN_POINT ( 'NONE',  ( 9.371250387798994552, 295.2890354897136262, -10.04040834969837448 ) ) ;
#31258=EDGE_CURVE ( 'NONE', #51023, #64324, #98216, .T. ) ;
#31288=CARTESIAN_POINT ( 'NONE',  ( -22.18906107735381283, 305.1406206946286943, -9.938500898754245583 ) ) ;
#31295=CARTESIAN_POINT ( 'NONE',  ( 43.31389755119118945, 487.3431498771903989, 8.040475431002054307 ) ) ;
#31299=ORIENTED_EDGE ( 'NONE', *, *, #84641, .F. ) ;
#31306=CARTESIAN_POINT ( 'NONE',  ( -2.477041358201104604, 294.8392925341222508, 1.934412764169636034 ) ) ;
#31312=CARTESIAN_POINT ( 'NONE',  ( 19.53022819233322949, 303.7299160955794264, -10.02590801686515043 ) ) ;
#31314=EDGE_CURVE ( 'NONE', #68586, #23322, #73765, .T. ) ;
#31319=ORIENTED_EDGE ( 'NONE', *, *, #47652, .T. ) ;
#31329=CARTESIAN_POINT ( 'NONE',  ( 30.00000000000000355, 464.1078291054766964, 11.04693782968297100 ) ) ;
#31333=CARTESIAN_POINT ( 'NONE',  ( -35.42573747137001305, 370.6060757378968447, 4.789908646769843514 ) ) ;
#31338=( BOUNDED_SURFACE ( )  B_SPLINE_SURFACE ( 3, 2, ( 
 ( #7503, #6983, #14008 ),
 ( #71711, #104625, #31306 ),
 ( #16141, #40421, #88981 ),
 ( #63661, #47442, #96549 ),
 ( #64191, #24273, #22683 ),
 ( #97060, #40957, #64704 ),
 ( #80335, #47964, #6448 ),
 ( #81926, #73301, #49029 ),
 ( #106197, #23206, #32361 ),
 ( #73848, #97576, #80874 ),
 ( #39902, #72775, #30230 ),
 ( #105681, #31820, #23742 ),
 ( #65233, #56593, #98125 ),
 ( #42542, #10174, #43090 ),
 ( #100250, #32891, #18301 ),
 ( #50614, #17233, #74372 ),
 ( #65766, #74897, #99723 ),
 ( #51696, #58750, #84613 ),
 ( #91646, #24796, #449 ),
 ( #33419, #66292, #9633 ) ),
 .UNSPECIFIED., .F., .F., .F. ) 
 B_SPLINE_SURFACE_WITH_KNOTS ( ( 4, 2, 2, 2, 2, 2, 2, 2, 2, 4 ),
 ( 3, 3 ),
 ( 0.02263415075989269262, 0.02743304099212479086, 0.02983248610824084171, 0.03103220866629886887, 0.03223193122435689256, 0.03703082145658899427, 0.03763068273561800958, 0.03823054401464701796, 0.03943026657270504165, 0.04182971168882109597 ),
 ( 0.000000000000000000, 1.000000000000000000 ),
 .UNSPECIFIED. ) 
 GEOMETRIC_REPRESENTATION_ITEM ( )  RATIONAL_B_SPLINE_SURFACE ( (
 ( 1.000000000000000000, 0.7071075261727414185, 1.000000000000000000),
 ( 1.000000000000000000, 0.7071101665684027537, 1.000000000000000000),
 ( 1.000000000000000000, 0.7071141823836638585, 1.000000000000000000),
 ( 1.000000000000000000, 0.7071130896034428792, 1.000000000000000000),
 ( 1.000000000000000000, 0.7071116449877591359, 1.000000000000000000),
 ( 1.000000000000000000, 0.7071091580431273504, 1.000000000000000000),
 ( 1.000000000000000000, 0.7071082982894895119, 1.000000000000000000),
 ( 1.000000000000000000, 0.7071070358518728449, 1.000000000000000000),
 ( 1.000000000000000000, 0.7071066027193460002, 1.000000000000000000),
 ( 1.000000000000000000, 0.7071078298307942323, 1.000000000000000000),
 ( 1.000000000000000000, 0.7071068905341975075, 1.000000000000000000),
 ( 1.000000000000000000, 0.7071067685343632725, 1.000000000000000000),
 ( 1.000000000000000000, 0.7071080607249466965, 1.000000000000000000),
 ( 1.000000000000000000, 0.7071121120183785358, 1.000000000000000000),
 ( 1.000000000000000000, 0.7071147527875665251, 1.000000000000000000),
 ( 1.000000000000000000, 0.7071223063742563264, 1.000000000000000000),
 ( 1.000000000000000000, 0.7071265710165801632, 1.000000000000000000),
 ( 1.000000000000000000, 0.7071280425582433526, 1.000000000000000000),
 ( 1.000000000000000000, 0.7071102348506560498, 1.000000000000000000),
 ( 1.000000000000000000, 0.7071067811865472397, 1.000000000000000000) ) ) 
 REPRESENTATION_ITEM ( '' )  SURFACE ( )  );
#31339=VERTEX_POINT ( 'NONE', #554 ) ;
#31342=CARTESIAN_POINT ( 'NONE',  ( -28.00030505598783037, 305.7606182409026019, -9.353795520816204245 ) ) ;
#31350=CARTESIAN_POINT ( 'NONE',  ( 31.36487079234788311, 435.2129478716335598, 22.89275833565512386 ) ) ;
#31366=CARTESIAN_POINT ( 'NONE',  ( 41.47568061452221144, 477.4151321979921363, -1.107586631990791437 ) ) ;
#31401=CARTESIAN_POINT ( 'NONE',  ( 30.87955015324946828, 351.7733141111877444, 20.67482462247657082 ) ) ;
#31402=CARTESIAN_POINT ( 'NONE',  ( -32.17646412119409405, 464.6980787822278671, 10.84896803612746474 ) ) ;
#31406=VERTEX_POINT ( 'NONE', #76078 ) ;
#31409=CARTESIAN_POINT ( 'NONE',  ( 33.49051768644739013, 464.3918346588610007, 8.532988796831755707 ) ) ;
#31437=CARTESIAN_POINT ( 'NONE',  ( 46.00000000000000000, 461.6622277975423003, 10.18145404766882933 ) ) ;
#31442=CARTESIAN_POINT ( 'NONE',  ( 31.90579019990244447, 311.1086333623303517, -8.069066494172007609 ) ) ;
#31449=CARTESIAN_POINT ( 'NONE',  ( 33.85195725564123848, 465.2464970902066739, 17.18122764674258462 ) ) ;
#31453=CARTESIAN_POINT ( 'NONE',  ( 29.07128654445882887, 296.9339959557834163, -9.548856946221640385 ) ) ;
#31455=CARTESIAN_POINT ( 'NONE',  ( -33.77559172535808329, 464.7834715296605737, 7.192701217093241617 ) ) ;
#31457=CARTESIAN_POINT ( 'NONE',  ( -38.55706197334059482, 437.0914394628632635, 4.833655886046459571 ) ) ;
#31469=ORIENTED_EDGE ( 'NONE', *, *, #3866, .F. ) ;
#31502=FACE_OUTER_BOUND ( 'NONE', #64024, .T. ) ;
#31512=CARTESIAN_POINT ( 'NONE',  ( -44.13343456913869289, 464.3829732007670259, 9.622105740874530966 ) ) ;
#31519=EDGE_CURVE ( 'NONE', #12676, #91673, #55795, .T. ) ;
#31520=CARTESIAN_POINT ( 'NONE',  ( 34.88900972249024335, 464.6206820656014429, 18.69027339340525629 ) ) ;
#31525=CARTESIAN_POINT ( 'NONE',  ( -32.35336999986095208, 300.6590557721156642, 11.25190399080426751 ) ) ;
#31526=DIRECTION ( 'NONE',  ( -0.1269898409407502204, 0.9919025243773941236, -0.001721171576547747550 ) ) ;
#31527=CARTESIAN_POINT ( 'NONE',  ( -45.17824257314219949, 354.4244853104167987, 3.762393652172960845 ) ) ;
#31531=CARTESIAN_POINT ( 'NONE',  ( 21.68456034400251653, 305.0468853612085240, -9.958482390678179641 ) ) ;
#31538=CARTESIAN_POINT ( 'NONE',  ( 42.99999999999992184, 487.9285348210859752, 8.903916466042419486 ) ) ;
#31552=CARTESIAN_POINT ( 'NONE',  ( 31.44871638334648267, 310.1705813142233978, -8.300853151410109376 ) ) ;
#31561=TOROIDAL_SURFACE ( 'NONE', #22938, 12.00000000000000711, 3.000000000000000000 ) ;
#31578=CARTESIAN_POINT ( 'NONE',  ( -44.29288495125481973, 463.9154455111743118, 8.171315969396212964 ) ) ;
#31590=ORIENTED_EDGE ( 'NONE', *, *, #53506, .T. ) ;
#31594=CARTESIAN_POINT ( 'NONE',  ( -40.31745201298756598, 437.2080480237208917, 22.20101732755830426 ) ) ;
#31595=CARTESIAN_POINT ( 'NONE',  ( 21.79648701958511836, 303.1339518336154697, 9.997617627940190488 ) ) ;
#31596=CARTESIAN_POINT ( 'NONE',  ( -43.46274389541398619, 361.0170833077261818, 12.68963403053921368 ) ) ;
#31606=CARTESIAN_POINT ( 'NONE',  ( -39.23335254075706047, 485.6839217479342778, -4.505383133713231736 ) ) ;
#31618=CARTESIAN_POINT ( 'NONE',  ( -37.49684268402597809, 491.2987049188604942, 12.22740886044745245 ) ) ;
#31633=B_SPLINE_CURVE_WITH_KNOTS ( 'NONE', 3,
 ( #17354, #105803, #23869, #56713, #64825, #32485, #31942, #80988, #49695, #41612, #50228, #89634 ),
 .UNSPECIFIED., .F., .F.,
 ( 4, 2, 2, 2, 2, 4 ),
 ( 9.300487239283920478E-15, 0.0007788392030127789254, 0.001557678406016257348, 0.001947098007517979049, 0.002336517609019700750, 0.003115356812023144586 ),
 .UNSPECIFIED. ) ;
#31641=CARTESIAN_POINT ( 'NONE',  ( -32.31275654990349722, 464.7713635351630046, 15.30476493091208212 ) ) ;
#31644=B_SPLINE_CURVE_WITH_KNOTS ( 'NONE', 3,
 ( #92535, #18139, #74214, #67217 ),
 .UNSPECIFIED., .F., .F.,
 ( 4, 4 ),
 ( 1.734723475976807094E-18, 0.001668351617186183012 ),
 .UNSPECIFIED. ) ;
#31657=CARTESIAN_POINT ( 'NONE',  ( -43.71273081481922418, 464.5191621324576658, 7.248379604737841930 ) ) ;
#31669=CARTESIAN_POINT ( 'NONE',  ( -33.54350669342006341, 484.9999455485477142, -0.3061812613743876144 ) ) ;
#31673=CARTESIAN_POINT ( 'NONE',  ( -27.67545152213132909, 310.9892636312667378, 11.64432264744174184 ) ) ;
#31676=CARTESIAN_POINT ( 'NONE',  ( 22.66207472693116642, 304.4407013690983490, 10.06416949456371768 ) ) ;
#31697=CARTESIAN_POINT ( 'NONE',  ( 34.06332199976886699, 330.0526646846329299, -3.810096259360388427 ) ) ;
#31704=FILL_AREA_STYLE ('',( #7390 ) ) ;
#31713=CARTESIAN_POINT ( 'NONE',  ( -33.86879232827779873, 484.1347737343850781, 1.564974661443849557 ) ) ;
#31717=CARTESIAN_POINT ( 'NONE',  ( 42.10086803841211633, 435.6552064019012960, 19.95582312411057302 ) ) ;
#31724=CARTESIAN_POINT ( 'NONE',  ( 38.42690270509001493, 318.8932286035306447, 15.80036497839117793 ) ) ;
#31727=EDGE_CURVE ( 'NONE', #22950, #52196, #41204, .T. ) ;
#31730=CARTESIAN_POINT ( 'NONE',  ( 42.77949383849493614, 391.0275278356816671, 19.62059687413802678 ) ) ;
#31731=CARTESIAN_POINT ( 'NONE',  ( 32.78741055188847042, 485.3331003366707819, 5.977022408747033388 ) ) ;
#31735=CARTESIAN_POINT ( 'NONE',  ( -42.55949806392435875, 435.1558328882642286, 18.91815692827004014 ) ) ;
#31737=CARTESIAN_POINT ( 'NONE',  ( -27.07835102769082525, 307.1390153984987705, 10.92803387578435625 ) ) ;
#31745=ORIENTED_EDGE ( 'NONE', *, *, #19418, .T. ) ;
#31757=DIRECTION ( 'NONE',  ( -1.000000000000000000, 0.000000000000000000, 0.000000000000000000 ) ) ;
#31773=CARTESIAN_POINT ( 'NONE',  ( 0.000000000000000000, 67.05096163904791240, -10.02537308446411402 ) ) ;
#31790=ORIENTED_EDGE ( 'NONE', *, *, #49238, .F. ) ;
#31813=CARTESIAN_POINT ( 'NONE',  ( -5.433201317752814674, 294.7714280552114587, -8.410911388488676366 ) ) ;
#31820=CARTESIAN_POINT ( 'NONE',  ( -15.65218212520301755, 294.5588111923345878, 9.874722130675968046 ) ) ;
#31824=CARTESIAN_POINT ( 'NONE',  ( 18.68302636746854262, 303.6623007926234550, -10.04032342916666920 ) ) ;
#31825=CARTESIAN_POINT ( 'NONE',  ( 36.90171438447441687, 490.9796882048100315, 12.46551445837898875 ) ) ;
#31828=ADVANCED_BREP_SHAPE_REPRESENTATION ( '', ( #19858, #87588, #10728 ), #60740 ) ;
#31829=B_SPLINE_CURVE_WITH_KNOTS ( 'NONE', 3,
 ( #92793, #69072, #101947, #17861 ),
 .UNSPECIFIED., .F., .F.,
 ( 4, 4 ),
 ( 8.835602482133882738E-17, 0.0007664883490338720738 ),
 .UNSPECIFIED. ) ;
#31843=CARTESIAN_POINT ( 'NONE',  ( -42.76758846428410976, 409.7905884173310369, 19.95987282388911765 ) ) ;
#31845=B_SPLINE_CURVE_WITH_KNOTS ( 'NONE', 3,
 ( #57582, #90505, #84009, #99656 ),
 .UNSPECIFIED., .F., .F.,
 ( 4, 4 ),
 ( 0.000000000000000000, 0.0004300933845558184399 ),
 .UNSPECIFIED. ) ;
#31847=CARTESIAN_POINT ( 'NONE',  ( -27.39853812899586671, 307.9048118753939320, -9.316184934693556130 ) ) ;
#31852=ORIENTED_EDGE ( 'NONE', *, *, #82812, .F. ) ;
#31855=CARTESIAN_POINT ( 'NONE',  ( -30.25140696341276580, 297.9349684876631272, -1.321983318591468670 ) ) ;
#31858=CARTESIAN_POINT ( 'NONE',  ( 51.01037695545453232, 450.0000000000002274, 18.20242257375371153 ) ) ;
#31871=CARTESIAN_POINT ( 'NONE',  ( 30.00000000000000355, 490.2060126478330631, 6.957942417092681353 ) ) ;
#31872=FACE_OUTER_BOUND ( 'NONE', #50886, .T. ) ;
#31878=DIRECTION ( 'NONE',  ( 0.000000000000000000, 0.000000000000000000, -1.000000000000000000 ) ) ;
#31892=AXIS2_PLACEMENT_3D ( 'NONE', #54161, #79518, #47671 ) ;
#31907=DIRECTION ( 'NONE',  ( 0.000000000000000000, 0.000000000000000000, -1.000000000000000000 ) ) ;
#31925=CARTESIAN_POINT ( 'NONE',  ( 32.95589646111153570, 464.8957215206403930, 10.75300444715520953 ) ) ;
#31942=CARTESIAN_POINT ( 'NONE',  ( 36.29583367650112535, 464.0085854085123174, 19.58118771088512489 ) ) ;
#31943=EDGE_LOOP ( 'NONE', ( #34493, #19963, #58391, #45988, #57215, #46872 ) ) ;
#31951=CARTESIAN_POINT ( 'NONE',  ( 33.54350669342029079, 484.9999455485476574, -0.3061812613748190470 ) ) ;
#31954=( NAMED_UNIT ( * ) PLANE_ANGLE_UNIT ( ) SI_UNIT ( $, .RADIAN. ) );
#31969=PLANE ( 'NONE',  #26274 ) ;
#31970=CARTESIAN_POINT ( 'NONE',  ( 32.16694665535142406, 298.7751107022914425, -9.134474995491629556 ) ) ;
#31975=CARTESIAN_POINT ( 'NONE',  ( -39.36202273480736835, 437.3280700035132895, 5.163426856676655241 ) ) ;
#31977=CARTESIAN_POINT ( 'NONE',  ( -30.63800635041225817, 340.2357850014829523, 17.36489564963465781 ) ) ;
#31990=FACE_OUTER_BOUND ( 'NONE', #10085, .T. ) ;
#32008=CIRCLE ( 'NONE', #13020, 1.000000000000000888 ) ;
#32020=CARTESIAN_POINT ( 'NONE',  ( -39.36786586063794147, 490.3672761926048906, 11.50922959349409247 ) ) ;
#32039=CARTESIAN_POINT ( 'NONE',  ( 35.04496600797013883, 464.5002996787647476, 18.88267410154261938 ) ) ;
#32047=CARTESIAN_POINT ( 'NONE',  ( -40.85254446136673323, 441.7500193615117610, 25.53625856138344474 ) ) ;
#32049=CARTESIAN_POINT ( 'NONE',  ( -39.13885763974980136, 324.4948203046521371, 17.18769520460729439 ) ) ;
#32052=CARTESIAN_POINT ( 'NONE',  ( 26.32888263779799587, 307.0379615089039476, -8.516298782527641720 ) ) ;
#32061=CIRCLE ( 'NONE', #45829, 15.00000000000000711 ) ;
#32063=CARTESIAN_POINT ( 'NONE',  ( -33.13158811977432094, 464.8683774689862958, 15.82274808388414478 ) ) ;
#32083=CARTESIAN_POINT ( 'NONE',  ( -43.71217423904474231, 435.6632154632216043, 9.092528312227496912 ) ) ;
#32092=ORIENTED_EDGE ( 'NONE', *, *, #69328, .F. ) ;
#32095=CARTESIAN_POINT ( 'NONE',  ( -16.36990510813551936, 294.5678840341198566, -2.060234697054666775 ) ) ;
#32111=CARTESIAN_POINT ( 'NONE',  ( -41.90771402882865715, 435.8631093490271269, 20.33118759140370102 ) ) ;
#32112=CARTESIAN_POINT ( 'NONE',  ( 33.16841335515274380, 391.5752490215859325, 25.61045263980480158 ) ) ;
#32113=CARTESIAN_POINT ( 'NONE',  ( -43.35589224434611566, 354.9930173192397547, 11.71192746841661148 ) ) ;
#32128=( BOUNDED_SURFACE ( )  B_SPLINE_SURFACE ( 3, 2, ( 
 ( #58786, #10211, #41522 ),
 ( #66330, #83049, #42052 ),
 ( #2109, #100812, #40995 ),
 ( #1022, #25929, #11261 ) ),
 .UNSPECIFIED., .F., .F., .F. ) 
 B_SPLINE_SURFACE_WITH_KNOTS ( ( 4, 4 ),
 ( 3, 3 ),
 ( 2.905661822261151883E-17, 0.0002890439564778435463 ),
 ( 0.000000000000000000, 1.000000000000000000 ),
 .UNSPECIFIED. ) 
 GEOMETRIC_REPRESENTATION_ITEM ( )  RATIONAL_B_SPLINE_SURFACE ( (
 ( 1.000000000000000000, 0.8001746426090936559, 1.000000000000000000),
 ( 1.000000000000000000, 0.7985501684305429393, 1.000000000000000000),
 ( 1.000000000000000000, 0.7968416491994178008, 1.000000000000000000),
 ( 1.000000000000000000, 0.7950530193019601510, 1.000000000000000000) ) ) 
 REPRESENTATION_ITEM ( '' )  SURFACE ( )  );
#32134=CIRCLE ( 'NONE', #35614, 3.000000000000012434 ) ;
#32138=FILL_AREA_STYLE ('',( #55832 ) ) ;
#32141=CARTESIAN_POINT ( 'NONE',  ( -37.00151214922456688, 491.8254423329677252, 12.57683263657885497 ) ) ;
#32148=CARTESIAN_POINT ( 'NONE',  ( 6.663820940124920433, 304.7444949031477677, 9.914190422159109062 ) ) ;
#32150=CARTESIAN_POINT ( 'NONE',  ( 43.55054245096676624, 486.2288135416363275, 8.070792277557991667 ) ) ;
#32159=CARTESIAN_POINT ( 'NONE',  ( -39.68467815576735802, 459.8383127612378303, 1.879537633271044728 ) ) ;
#32163=CARTESIAN_POINT ( 'NONE',  ( 34.16642289233210050, 463.8422268500519863, 18.98106911353328385 ) ) ;
#32178=CARTESIAN_POINT ( 'NONE',  ( 32.21125840474181956, 298.9095371842905138, -9.102426614015140416 ) ) ;
#32183=CARTESIAN_POINT ( 'NONE',  ( -32.54922218626916930, 319.8023524069591303, -6.363686095274232457 ) ) ;
#32190=EDGE_CURVE ( 'NONE', #103730, #2640, #8038, .T. ) ;
#32196=B_SPLINE_CURVE_WITH_KNOTS ( 'NONE', 3,
 ( #85058, #28442, #1990, #67807 ),
 .UNSPECIFIED., .F., .F.,
 ( 4, 4 ),
 ( 0.000000000000000000, 0.0004475792522134993041 ),
 .UNSPECIFIED. ) ;
#32199=CARTESIAN_POINT ( 'NONE',  ( -22.76293769579003623, 305.5621053821230930, 10.09118165409745593 ) ) ;
#32201=CARTESIAN_POINT ( 'NONE',  ( 33.88237199998279436, 485.0486819176492759, 1.241522336454514264 ) ) ;
#32202=CARTESIAN_POINT ( 'NONE',  ( 31.91891815526927445, 439.7370520509067546, 23.87859572923007434 ) ) ;
#32207=CARTESIAN_POINT ( 'NONE',  ( 44.29544435252744705, 435.1888869815376779, 13.53377863749212828 ) ) ;
#32222=CARTESIAN_POINT ( 'NONE',  ( 31.19792890532719198, 414.2215770364159084, 25.44228638033458623 ) ) ;
#32226=VERTEX_POINT ( 'NONE', #20721 ) ;
#32245=DIRECTION ( 'NONE',  ( -1.000000000000000000, 0.000000000000000000, 0.000000000000000000 ) ) ;
#32249=CARTESIAN_POINT ( 'NONE',  ( 40.04056949100335316, 318.9660535511408739, 7.801086534252953619 ) ) ;
#32255=( BOUNDED_SURFACE ( )  B_SPLINE_SURFACE ( 3, 2, ( 
 ( #20206, #12052, #79837 ),
 ( #43895, #105188, #55020 ),
 ( #22170, #22707, #14557 ),
 ( #30799, #14033, #23228 ) ),
 .UNSPECIFIED., .F., .F., .F. ) 
 B_SPLINE_SURFACE_WITH_KNOTS ( ( 4, 4 ),
 ( 3, 3 ),
 ( 8.673617379884035472E-19, 0.003511371752238591840 ),
 ( 0.000000000000000000, 1.000000000000000000 ),
 .UNSPECIFIED. ) 
 GEOMETRIC_REPRESENTATION_ITEM ( )  RATIONAL_B_SPLINE_SURFACE ( (
 ( 1.000000000000000000, 0.7409272757993143887, 1.000000000000000000),
 ( 1.000000000000000000, 0.7572402302192213774, 1.000000000000000000),
 ( 1.000000000000000000, 0.7731133056332801790, 1.000000000000000000),
 ( 1.000000000000000000, 0.7888522786295014688, 1.000000000000000000) ) ) 
 REPRESENTATION_ITEM ( '' )  SURFACE ( )  );
#32260=CARTESIAN_POINT ( 'NONE',  ( -42.43166099484149356, 436.1632441641000355, 19.16791492761042903 ) ) ;
#32262=CARTESIAN_POINT ( 'NONE',  ( -24.91217021099775764, 295.6308500594226985, 2.104243703054258674 ) ) ;
#32265=DIRECTION ( 'NONE',  ( 0.000000000000000000, 0.000000000000000000, 1.000000000000000000 ) ) ;
#32275=CARTESIAN_POINT ( 'NONE',  ( 6.615539890938310741, 303.7455199599310731, 9.914405304616634496 ) ) ;
#32279=CARTESIAN_POINT ( 'NONE',  ( 1.128238012697730275, 300.0000000000000000, 9.936150108905557943 ) ) ;
#32283=CARTESIAN_POINT ( 'NONE',  ( 36.57768354961403645, 437.5705742298895302, 4.260889744331655571 ) ) ;
#32296=CARTESIAN_POINT ( 'NONE',  ( -31.95313894478998051, 438.9705935198780935, 23.61757669276694571 ) ) ;
#32314=CARTESIAN_POINT ( 'NONE',  ( 42.19180677453717720, 462.2931784592651638, 3.389262873192018244 ) ) ;
#32315=EDGE_CURVE ( 'NONE', #76425, #85977, #25441, .T. ) ;
#32333=CARTESIAN_POINT ( 'NONE',  ( 31.19344562713908431, 380.6578681173627956, 24.42638549347173793 ) ) ;
#32351=ORIENTED_EDGE ( 'NONE', *, *, #1542, .F. ) ;
#32356=ORIENTED_EDGE ( 'NONE', *, *, #7586, .F. ) ;
#32361=CARTESIAN_POINT ( 'NONE',  ( -9.966015359215459668, 294.6437633021450893, 1.892774790111525496 ) ) ;
#32364=CARTESIAN_POINT ( 'NONE',  ( 36.52797673977651982, 490.9928046865358624, 12.47113835539106041 ) ) ;
#32371=CARTESIAN_POINT ( 'NONE',  ( -7.188580507048828672, 302.2771598081733941, -10.02656291412436751 ) ) ;
#32383=CARTESIAN_POINT ( 'NONE',  ( -31.67563778497622096, 439.7335944510184049, 23.71446993618755172 ) ) ;
#32385=CARTESIAN_POINT ( 'NONE',  ( -35.53731096081859420, 361.9375032173327327, 2.592946827012501121 ) ) ;
#32392=CARTESIAN_POINT ( 'NONE',  ( -22.09288372273234202, 303.0838735200828182, -9.950444626390048342 ) ) ;
#32399=CARTESIAN_POINT ( 'NONE',  ( 24.48998408367273427, 306.7567165393634809, 9.364080809398716454 ) ) ;
#32400=CARTESIAN_POINT ( 'NONE',  ( -39.97809621673793856, 463.9322724720692577, 18.76396717432225714 ) ) ;
#32409=DIRECTION ( 'NONE',  ( -0.4127509058099244066, 0.1524945595934079634, -0.8979878056229381178 ) ) ;
#32435=CARTESIAN_POINT ( 'NONE',  ( -46.00000000000000000, 450.0000000000002274, 13.20242257375370976 ) ) ;
#32447=AXIS2_PLACEMENT_3D ( 'NONE', #96024, #71715, #95482 ) ;
#32451=CARTESIAN_POINT ( 'NONE',  ( -6.953930663124324063, 304.7325910270068334, -10.02533923955978956 ) ) ;
#32465=CARTESIAN_POINT ( 'NONE',  ( 33.22740183697520422, 464.7219767738044425, 9.606361102772776661 ) ) ;
#32482=DIRECTION ( 'NONE',  ( 0.1270361284032164306, 0.9918980905719708696, 0.000000000000000000 ) ) ;
#32485=CARTESIAN_POINT ( 'NONE',  ( 36.16933211627106459, 464.0306822413344889, 19.55183272904454128 ) ) ;
#32486=ORIENTED_EDGE ( 'NONE', *, *, #44781, .F. ) ;
#32487=DIRECTION ( 'NONE',  ( -0.2277538186085105443, 0.3726643368266331913, 0.8995829534661088367 ) ) ;
#32492=CARTESIAN_POINT ( 'NONE',  ( 46.00000000000004263, 463.6789860417705995, 9.766835940523808546 ) ) ;
#32496=SURFACE_STYLE_FILL_AREA ( #23879 ) ;
#32498=CARTESIAN_POINT ( 'NONE',  ( -32.64609568143473695, 299.7802937897311040, -0.8989887599977948174 ) ) ;
#32506=CARTESIAN_POINT ( 'NONE',  ( 44.35819766388060259, 435.2221642642162465, 12.65712761108002837 ) ) ;
#32511=CARTESIAN_POINT ( 'NONE',  ( 40.17205142263708240, 310.2804317922712016, -6.358608209523628929 ) ) ;
#32513=CARTESIAN_POINT ( 'NONE',  ( -33.07276483573669168, 438.9325140356086195, 23.89537236861389147 ) ) ;
#32516=CARTESIAN_POINT ( 'NONE',  ( -38.90208975916836209, 437.7929390082023815, 4.481369775519661758 ) ) ;
#32523=ORIENTED_EDGE ( 'NONE', *, *, #106268, .T. ) ;
#32528=DIRECTION ( 'NONE',  ( -1.000000000000000000, 0.000000000000000000, 0.000000000000000000 ) ) ;
#32532=CARTESIAN_POINT ( 'NONE',  ( -32.94021323899823983, 485.0599191339510980, 5.361609822537303671 ) ) ;
#32545=CARTESIAN_POINT ( 'NONE',  ( -30.00000000000000000, 461.8887775513397855, 11.55279652844097171 ) ) ;
#32563=CARTESIAN_POINT ( 'NONE',  ( 38.54364474655984907, 439.2805328589141709, 23.69816338776510989 ) ) ;
#32568=CARTESIAN_POINT ( 'NONE',  ( -36.31162387720043228, 438.2523736922216244, 3.875403351156469167 ) ) ;
#32569=( BOUNDED_SURFACE ( )  B_SPLINE_SURFACE ( 3, 2, ( 
 ( #45433, #37363, #103130 ),
 ( #27688, #4964, #29279 ),
 ( #37895, #10899, #76711 ),
 ( #68653, #11976, #44360 ) ),
 .UNSPECIFIED., .F., .F., .F. ) 
 B_SPLINE_SURFACE_WITH_KNOTS ( ( 4, 4 ),
 ( 3, 3 ),
 ( 3.686287386450715076E-17, 0.002123809863745970954 ),
 ( 0.000000000000000000, 1.000000000000000000 ),
 .UNSPECIFIED. ) 
 GEOMETRIC_REPRESENTATION_ITEM ( )  RATIONAL_B_SPLINE_SURFACE ( (
 ( 1.000000000000000000, 0.8347624811021843172, 1.000000000000000000),
 ( 1.000000000000000000, 0.8202629603801117053, 1.000000000000000000),
 ( 1.000000000000000000, 0.8052718258174581534, 1.000000000000000000),
 ( 1.000000000000000000, 0.7904469216846389257, 1.000000000000000000) ) ) 
 REPRESENTATION_ITEM ( '' )  SURFACE ( )  );
#32574=ORIENTED_EDGE ( 'NONE', *, *, #74261, .T. ) ;
#32577=CARTESIAN_POINT ( 'NONE',  ( 36.32791536946660926, 464.0041716472645135, 19.58704090454613223 ) ) ;
#32584=FACE_OUTER_BOUND ( 'NONE', #24058, .T. ) ;
#32590=CARTESIAN_POINT ( 'NONE',  ( 26.59004530782534559, 307.2471289293887367, -8.468265503451595677 ) ) ;
#32598=CARTESIAN_POINT ( 'NONE',  ( -42.48722704179489540, 465.9004001135029398, 13.75636562493584414 ) ) ;
#32601=EDGE_CURVE ( 'NONE', #21098, #89053, #34230, .T. ) ;
#32605=CARTESIAN_POINT ( 'NONE',  ( -35.31443409317565596, 437.2805527638894318, 5.244185069633918950 ) ) ;
#32621=CARTESIAN_POINT ( 'NONE',  ( 44.19630675230467887, 485.6206890027685859, 3.558858865136342864 ) ) ;
#32625=CARTESIAN_POINT ( 'NONE',  ( 42.68684796707852769, 436.2654864220232867, 7.155924889999337957 ) ) ;
#32626=AXIS2_PLACEMENT_3D ( 'NONE', #26206, #42869, #99497 ) ;
#32631=CARTESIAN_POINT ( 'NONE',  ( 24.76885996170685544, 306.0690732980165194, -8.735186880116588171 ) ) ;
#32638=CARTESIAN_POINT ( 'NONE',  ( -20.21880305278369150, 304.8280059657581660, -9.005058168222323189 ) ) ;
#32643=CARTESIAN_POINT ( 'NONE',  ( -36.20419914068695988, 464.0241112302327906, 19.56059989341670757 ) ) ;
#32648=CARTESIAN_POINT ( 'NONE',  ( 30.00000000000000355, 461.8802764867031669, 14.89328939272364316 ) ) ;
#32656=CARTESIAN_POINT ( 'NONE',  ( 20.34579289372440059, 303.8361034413807147, -9.003336996645794343 ) ) ;
#32660=CARTESIAN_POINT ( 'NONE',  ( -44.11907783817835593, 333.2661371888331701, -0.6867057639839724281 ) ) ;
#32684=CARTESIAN_POINT ( 'NONE',  ( -35.96015918321902660, 491.7728760210378596, 12.54260821243620505 ) ) ;
#32689=CARTESIAN_POINT ( 'NONE',  ( 33.00540147335428287, 487.4196752801332195, 9.523982417622292473 ) ) ;
#32700=CARTESIAN_POINT ( 'NONE',  ( -40.42062918464028343, 485.1352466658498770, -4.233530644584298841 ) ) ;
#32719=EDGE_CURVE ( 'NONE', #57174, #68586, #20312, .T. ) ;
#32725=CARTESIAN_POINT ( 'NONE',  ( 34.89096242599858044, 301.3136321141124085, -8.544899998089542592 ) ) ;
#32726=ADVANCED_FACE ( 'NONE', ( #106743 ), #25989, .F. ) ;
#32727=CARTESIAN_POINT ( 'NONE',  ( 51.01037695545453232, 500.0000000000002274, 5.000000000000001776 ) ) ;
#32730=DIRECTION ( 'NONE',  ( -6.104959157215355576E-15, -0.3964176948853179727, -0.9180702648391412257 ) ) ;
#32738=CARTESIAN_POINT ( 'NONE',  ( 37.70204294583037807, 409.1425458642764852, 6.512462526010587283 ) ) ;
#32739=CARTESIAN_POINT ( 'NONE',  ( 43.36987996225059305, 463.6266071988662247, 5.362859980318074982 ) ) ;
#32741=CARTESIAN_POINT ( 'NONE',  ( -23.40846030801418820, 305.8699098592260270, 9.159741819081197889 ) ) ;
#32743=CARTESIAN_POINT ( 'NONE',  ( 37.69644952591121978, 484.8922498457696406, -3.621330182635625228 ) ) ;
#32760=CARTESIAN_POINT ( 'NONE',  ( 19.83463548332445825, 303.8035096162420245, 9.926734387303332241 ) ) ;
#32763=CARTESIAN_POINT ( 'NONE',  ( 1.224646799147353651E-15, 0.000000000000000000, 10.00000000000000355 ) ) ;
#32764=CARTESIAN_POINT ( 'NONE',  ( 31.02212611900126760, 360.5725590293961318, 22.12937154125974715 ) ) ;
#32767=CARTESIAN_POINT ( 'NONE',  ( 30.87955015324946828, 351.7733141111877444, 20.67482462247657082 ) ) ;
#32776=CARTESIAN_POINT ( 'NONE',  ( -46.00000000000000000, 500.0000000000002274, 5.000000000000001776 ) ) ;
#32783=CARTESIAN_POINT ( 'NONE',  ( 44.03654441205471670, 435.3114017552815085, 15.42721916007442751 ) ) ;
#32784=CARTESIAN_POINT ( 'NONE',  ( -39.21606699811488994, 464.6169417331591944, 18.47934099087227366 ) ) ;
#32789=CARTESIAN_POINT ( 'NONE',  ( 0.000000000000000000, 304.8518027762758038, 9.936999415352289589 ) ) ;
#32792=CARTESIAN_POINT ( 'NONE',  ( 37.78940342756484938, 315.0498657100115452, 14.83808658025191995 ) ) ;
#32793=DIRECTION ( 'NONE',  ( -0.2281669654643559142, 0.2206132685150330730, 0.9482982767177750016 ) ) ;
#32803=CARTESIAN_POINT ( 'NONE',  ( -25.12288893236338794, 295.6917592701588546, 2.117418662238229832 ) ) ;
#32808=ADVANCED_FACE ( 'NONE', ( #40303 ), #6866, .F. ) ;
#32813=B_SPLINE_CURVE_WITH_KNOTS ( 'NONE', 3,
 ( #4054, #6155, #38049, #78465 ),
 .UNSPECIFIED., .F., .F.,
 ( 4, 4 ),
 ( 0.0007620286332983192655, 0.02097007980334730098 ),
 .UNSPECIFIED. ) ;
#32830=CARTESIAN_POINT ( 'NONE',  ( -34.13947300040292276, 489.1610961117067404, 11.38003656226515581 ) ) ;
#32847=CARTESIAN_POINT ( 'NONE',  ( 41.94726657796896063, 461.2497493224228720, 3.266452559854905235 ) ) ;
#32863=CARTESIAN_POINT ( 'NONE',  ( 31.19215877409873627, 416.1752359029570130, 25.29151037147646974 ) ) ;
#32867=CARTESIAN_POINT ( 'NONE',  ( -42.61340452791774425, 486.8925439250689919, 7.464118458850297344 ) ) ;
#32878=CARTESIAN_POINT ( 'NONE',  ( -43.53995238963259595, 465.2530981678407898, 9.299505628812474001 ) ) ;
#32881=ORIENTED_EDGE ( 'NONE', *, *, #43057, .T. ) ;
#32883=CARTESIAN_POINT ( 'NONE',  ( -6.549255471957041941, 294.7416366638757381, -7.570647764150726822 ) ) ;
#32891=CARTESIAN_POINT ( 'NONE',  ( -16.52205554056997272, 294.5714208180984315, 9.877401598617169043 ) ) ;
#32902=CARTESIAN_POINT ( 'NONE',  ( -9.404050855906653794, 302.6623156739180445, -10.04027337526763120 ) ) ;
#32911=CARTESIAN_POINT ( 'NONE',  ( -30.99883150094105133, 438.8494022061962028, 22.05589272262757916 ) ) ;
#32913=CARTESIAN_POINT ( 'NONE',  ( -35.18713100599366328, 355.9408742645140364, 2.597692190029098125 ) ) ;
#32921=CARTESIAN_POINT ( 'NONE',  ( -21.51569398614849504, 294.9107018935608266, -9.987480606144570672 ) ) ;
#32928=CARTESIAN_POINT ( 'NONE',  ( -41.61767405872787862, 334.1594308673269325, 11.43720139602365293 ) ) ;
#32930=CARTESIAN_POINT ( 'NONE',  ( -42.72825394835516022, 464.8055660505491460, 15.62448665940029713 ) ) ;
#32941=FACE_OUTER_BOUND ( 'NONE', #85643, .T. ) ;
#32949=CARTESIAN_POINT ( 'NONE',  ( -44.17836536378457168, 435.2619773020560956, 14.65562696767996087 ) ) ;
#32979=CARTESIAN_POINT ( 'NONE',  ( -13.76424046522695122, 304.5457540960956067, -10.06505265514019243 ) ) ;
#32980=CARTESIAN_POINT ( 'NONE',  ( 27.97565635352651015, 315.9216507687758053, 12.64980990155120999 ) ) ;
#32981=CARTESIAN_POINT ( 'NONE',  ( -32.15961058743295808, 464.7082972388441817, 10.94058067631164022 ) ) ;
#32983=CARTESIAN_POINT ( 'NONE',  ( 29.99999999999051070, 486.8910789110960309, 5.528145857006796504 ) ) ;
#32989=CIRCLE ( 'NONE', #43287, 0.9999999999999980016 ) ;
#33002=CARTESIAN_POINT ( 'NONE',  ( -43.47770857297125957, 484.8227827122622102, 4.253339224813438513 ) ) ;
#33008=ORIENTED_EDGE ( 'NONE', *, *, #40000, .F. ) ;
#33018=ORIENTED_EDGE ( 'NONE', *, *, #8817, .F. ) ;
#33023=CARTESIAN_POINT ( 'NONE',  ( 46.00000000000580513, 462.9210814260900406, 7.766178785318980538 ) ) ;
#33038=CARTESIAN_POINT ( 'NONE',  ( 44.19123973042410825, 435.3640897803218763, 10.85603094146364533 ) ) ;
#33043=CARTESIAN_POINT ( 'NONE',  ( -43.51047069092275166, 435.7684321374283627, 8.546621873850019924 ) ) ;
#33047=CARTESIAN_POINT ( 'NONE',  ( 37.26669594562353893, 460.4728090823174966, 2.456107597708254708 ) ) ;
#33048=CARTESIAN_POINT ( 'NONE',  ( -38.22195112133888983, 437.6732586221718293, 4.643349236000520186 ) ) ;
#33053=CARTESIAN_POINT ( 'NONE',  ( -34.74668950323464145, 477.5735541584660382, -0.3049228838951520415 ) ) ;
#33061=CARTESIAN_POINT ( 'NONE',  ( 25.12563779285825305, 306.0698335614371217, 10.43520451652393355 ) ) ;
#33077=ADVANCED_FACE ( 'NONE', ( #61701 ), #29453, .F. ) ;
#33083=CARTESIAN_POINT ( 'NONE',  ( -32.13498246155330662, 335.5900755486186995, 17.83550542174494069 ) ) ;
#33084=B_SPLINE_CURVE_WITH_KNOTS ( 'NONE', 3,
 ( #24093, #8398, #67189, #26232, #100066, #81734, #798, #73656, #98986, #17577, #82286, #49377, #89335, #17042, #33768, #32163 ),
 .UNSPECIFIED., .F., .F.,
 ( 4, 2, 2, 2, 2, 2, 2, 4 ),
 ( 1.851527828850887154E-16, 0.0005159648664366578213, 0.001031929732873130461, 0.001547894599309602992, 0.002063859465746075740, 0.002579824332182548054, 0.003095789198619020802, 0.004127718931491971069 ),
 .UNSPECIFIED. ) ;
#33093=CARTESIAN_POINT ( 'NONE',  ( -40.22495779148586337, 489.7644056528380929, 10.97694427318330668 ) ) ;
#33095=FACE_OUTER_BOUND ( 'NONE', #73715, .T. ) ;
#33096=PRODUCT_CONTEXT ( 'NONE', #47261, 'mechanical' ) ;
#33105=FACE_OUTER_BOUND ( 'NONE', #60248, .T. ) ;
#33109=CARTESIAN_POINT ( 'NONE',  ( 36.55533968308436243, 463.5207292468175524, 19.71490071751826179 ) ) ;
#33116=CARTESIAN_POINT ( 'NONE',  ( -40.93435977689158989, 414.3154843149413296, 27.72243992809649527 ) ) ;
#33118=ORIENTED_EDGE ( 'NONE', *, *, #52769, .F. ) ;
#33119=CARTESIAN_POINT ( 'NONE',  ( 25.46344391298313781, 305.2723305331812185, -9.690526388420286352 ) ) ;
#33127=CARTESIAN_POINT ( 'NONE',  ( -43.00000000000000000, 500.0000000000002274, -12.00000000000000711 ) ) ;
#33144=SURFACE_SIDE_STYLE ('',( #25053 ) ) ;
#33147=CARTESIAN_POINT ( 'NONE',  ( 43.69219460922279552, 484.4832989965491947, 2.442496667976668867 ) ) ;
#33158=CARTESIAN_POINT ( 'NONE',  ( 35.50524833579024886, 381.4531880784116993, 5.944804199580530302 ) ) ;
#33163=CARTESIAN_POINT ( 'NONE',  ( 16.99873220396137796, 302.5765783365897619, -10.05837913125274952 ) ) ;
#33167=CARTESIAN_POINT ( 'NONE',  ( -36.69890166230307216, 463.9786769757894263, 19.62055820434390085 ) ) ;
#33171=CARTESIAN_POINT ( 'NONE',  ( 32.21352700826018634, 464.7514164808271175, 11.12064077799058559 ) ) ;
#33182=CARTESIAN_POINT ( 'NONE',  ( 30.83690085618862398, 321.2017700030009451, 14.45204011326535998 ) ) ;
#33185=CARTESIAN_POINT ( 'NONE',  ( -43.59476163150520733, 373.0867689854657669, 14.23677538628125561 ) ) ;
#33193=CARTESIAN_POINT ( 'NONE',  ( 11.93255308427328565, 294.5886021379643580, 9.881054392645332030 ) ) ;
#33206=CARTESIAN_POINT ( 'NONE',  ( -34.84618260875192419, 489.9833681528629654, 11.97975507378832738 ) ) ;
#33213=FACE_OUTER_BOUND ( 'NONE', #2478, .T. ) ;
#33230=CARTESIAN_POINT ( 'NONE',  ( -40.96815392870907857, 488.3809129049190574, 10.59964723858178992 ) ) ;
#33244=EDGE_LOOP ( 'NONE', ( #59175, #77767, #57504, #8477, #53504, #24754 ) ) ;
#33249=CARTESIAN_POINT ( 'NONE',  ( 30.86342090715118047, 298.3468162791613736, -1.228562068932849360 ) ) ;
#33253=CARTESIAN_POINT ( 'NONE',  ( -35.76482652855951017, 405.2378813769876729, 6.148826621638260548 ) ) ;
#33259=DIRECTION ( 'NONE',  ( -1.000000000000000000, -0.000000000000000000, -0.000000000000000000 ) ) ;
#33264=CARTESIAN_POINT ( 'NONE',  ( -22.15956248098668269, 304.2723657570961677, 10.02744636126657163 ) ) ;
#33266=CARTESIAN_POINT ( 'NONE',  ( 38.23234611763021462, 485.0120663942624333, -3.939776079184425406 ) ) ;
#33285=CARTESIAN_POINT ( 'NONE',  ( 27.97565635352651015, 315.9216507687758053, 12.64980990155120999 ) ) ;
#33289=CARTESIAN_POINT ( 'NONE',  ( -33.00000000000000000, 463.5362553048592531, 6.739467187734380360 ) ) ;
#33304=B_SPLINE_CURVE_WITH_KNOTS ( 'NONE', 3,
 ( #34716, #99935, #10909, #2289 ),
 .UNSPECIFIED., .F., .F.,
 ( 4, 4 ),
 ( 1.734723475976807094E-18, 0.001632242847434939390 ),
 .UNSPECIFIED. ) ;
#33310=CARTESIAN_POINT ( 'NONE',  ( -41.74718156901468546, 464.4924520314310712, 17.10319308832293572 ) ) ;
#33311=CARTESIAN_POINT ( 'NONE',  ( -31.35087655471889434, 439.7415908874936576, 22.35622233947958648 ) ) ;
#33319=CARTESIAN_POINT ( 'NONE',  ( 33.64205033492135044, 302.6176840280941178, 11.72452048251792078 ) ) ;
#33324=CARTESIAN_POINT ( 'NONE',  ( 42.71746488131647368, 428.6810652414584979, 19.02199747807395624 ) ) ;
#33332=CARTESIAN_POINT ( 'NONE',  ( -25.79311565262062089, 295.8993310619729868, 2.162649885535623540 ) ) ;
#33372=ORIENTED_EDGE ( 'NONE', *, *, #17580, .T. ) ;
#33385=CIRCLE ( 'NONE', #57445, 15.00000000000001421 ) ;
#33388=CARTESIAN_POINT ( 'NONE',  ( 31.21596591978341095, 336.6249549339077021, 17.82539080634884243 ) ) ;
#33393=ORIENTED_EDGE ( 'NONE', *, *, #47214, .F. ) ;
#33419=CARTESIAN_POINT ( 'NONE',  ( -19.96162532426518865, 302.8116070918645164, 9.928455558879852205 ) ) ;
#33423=CARTESIAN_POINT ( 'NONE',  ( 34.58748436418837002, 491.1940522429740668, 12.14470207312156269 ) ) ;
#33430=CARTESIAN_POINT ( 'NONE',  ( -1.954521441386776859, 298.2604977439763729, -10.00252169235627164 ) ) ;
#33441=CARTESIAN_POINT ( 'NONE',  ( -35.02151964022808528, 330.0018426590012837, -3.593274941009661827 ) ) ;
#33442=CIRCLE ( 'NONE', #74671, 3.000000000000023981 ) ;
#33447=ORIENTED_EDGE ( 'NONE', *, *, #103458, .T. ) ;
#33449=CARTESIAN_POINT ( 'NONE',  ( -26.51252764419330532, 296.0026311473873193, -9.752274705943550615 ) ) ;
#33454=CARTESIAN_POINT ( 'NONE',  ( -33.08824659830909809, 433.9163703247937747, 24.51824011208189447 ) ) ;
#33468=CARTESIAN_POINT ( 'NONE',  ( 42.52018344083600709, 435.0260445551345470, 8.239822296317143469 ) ) ;
#33482=ORIENTED_EDGE ( 'NONE', *, *, #28138, .T. ) ;
#33485=CARTESIAN_POINT ( 'NONE',  ( -40.97493796728242188, 465.3173804043414634, 16.74015881913296155 ) ) ;
#33494=DIRECTION ( 'NONE',  ( -1.000000000000000000, 0.000000000000000000, 0.000000000000000000 ) ) ;
#33503=CARTESIAN_POINT ( 'NONE',  ( 39.45202195020148395, 464.6983304258686758, 18.31344484327332367 ) ) ;
#33512=ORIENTED_EDGE ( 'NONE', *, *, #31314, .F. ) ;
#33524=CARTESIAN_POINT ( 'NONE',  ( -43.33498512661116564, 464.9732568094945577, 13.98542553804671407 ) ) ;
#33538=CARTESIAN_POINT ( 'NONE',  ( -46.00000000000000711, 488.1785408034348848, 2.468284771847338632 ) ) ;
#33543=CARTESIAN_POINT ( 'NONE',  ( 46.00000000000000000, 460.6862940191787175, 7.630022560110487184 ) ) ;
#33548=CARTESIAN_POINT ( 'NONE',  ( -30.00000000000000355, 464.1059074601055272, 11.21808947555541103 ) ) ;
#33558=CARTESIAN_POINT ( 'NONE',  ( 43.79821706557852679, 434.9662578767633363, 12.22743114679940035 ) ) ;
#33562=CARTESIAN_POINT ( 'NONE',  ( 40.61216075948964033, 351.1469683695276558, 22.89433108575548914 ) ) ;
#33565=CARTESIAN_POINT ( 'NONE',  ( -43.50250715914095423, 464.6389613228375879, 9.611700240010623730 ) ) ;
#33568=CARTESIAN_POINT ( 'NONE',  ( -31.18764089105624393, 357.3273780643992268, 20.56365793791859531 ) ) ;
#33572=CARTESIAN_POINT ( 'NONE',  ( -33.76223977132627141, 470.3516487496773948, 6.012963278766592978 ) ) ;
#33580=CARTESIAN_POINT ( 'NONE',  ( 31.36136185978966040, 339.5482298604329685, 18.45068369565698418 ) ) ;
#33585=ADVANCED_FACE ( 'NONE', ( #37305 ), #43271, .F. ) ;
#33594=ORIENTED_EDGE ( 'NONE', *, *, #94914, .F. ) ;
#33599=AXIS2_PLACEMENT_3D ( 'NONE', #59580, #75196, #19685 ) ;
#33601=CARTESIAN_POINT ( 'NONE',  ( -29.22284240011272161, 312.6584099927333682, 12.30496723460669273 ) ) ;
#33615=CARTESIAN_POINT ( 'NONE',  ( 37.10858375827000089, 439.7067619725109466, 24.11495004416381960 ) ) ;
#33628=CARTESIAN_POINT ( 'NONE',  ( 36.12805158198114697, 463.5537319797338682, 19.64593688561118157 ) ) ;
#33634=CARTESIAN_POINT ( 'NONE',  ( -22.91651842568168362, 295.0901107613288445, -9.949346074078583513 ) ) ;
#33638=CARTESIAN_POINT ( 'NONE',  ( 30.62685779490040261, 313.0583036694750945, -8.065315349801879918 ) ) ;
#33653=CARTESIAN_POINT ( 'NONE',  ( -35.94513182849163258, 437.3829582663586848, 4.385777999725225307 ) ) ;
#33654=EDGE_CURVE ( 'NONE', #26193, #80767, #67932, .T. ) ;
#33657=VERTEX_POINT ( 'NONE', #17255 ) ;
#33666=EDGE_CURVE ( 'NONE', #90700, #22313, #96221, .T. ) ;
#33672=DIRECTION ( 'NONE',  ( 1.000000000000000000, 0.000000000000000000, 0.000000000000000000 ) ) ;
#33686=CARTESIAN_POINT ( 'NONE',  ( 25.72383541997187706, 306.6074583397111155, -8.614371337684147534 ) ) ;
#33694=CARTESIAN_POINT ( 'NONE',  ( 20.21880305278369150, 304.8280059657581660, -9.005058168222337400 ) ) ;
#33696=CARTESIAN_POINT ( 'NONE',  ( -35.47699217159583185, 463.6829005663038288, 19.36631617875508127 ) ) ;
#33701=CARTESIAN_POINT ( 'NONE',  ( 20.24579557674103469, 304.8297271373346575, -10.00469232190998703 ) ) ;
#33709=CARTESIAN_POINT ( 'NONE',  ( 43.71297783477844234, 485.1278128289774827, -1.116606130290200172 ) ) ;
#33710=CARTESIAN_POINT ( 'NONE',  ( -33.00000000000000000, 461.8163627757383551, 11.11111419091028729 ) ) ;
#33711=DIRECTION ( 'NONE',  ( 0.3144882010765461811, 0.9492613820142679071, 0.000000000000000000 ) ) ;
#33713=CARTESIAN_POINT ( 'NONE',  ( -37.49627282300918552, 304.7695756402364395, -7.718605803013700140 ) ) ;
#33719=EDGE_LOOP ( 'NONE', ( #51880, #105634, #17124, #102575 ) ) ;
#33732=CARTESIAN_POINT ( 'NONE',  ( 37.50059943756144776, 490.7879993827856993, 12.38039871356534505 ) ) ;
#33741=CARTESIAN_POINT ( 'NONE',  ( 43.32918576489185369, 484.9664181796746334, 4.870614540792619351 ) ) ;
#33746=ADVANCED_FACE ( 'NONE', ( #102405 ), #54263, .T. ) ;
#33751=CARTESIAN_POINT ( 'NONE',  ( 43.00000000000000000, 488.3725375423206287, 3.127739281036224117 ) ) ;
#33753=AXIS2_PLACEMENT_3D ( 'NONE', #80530, #6647, #64376 ) ;
#33757=ORIENTED_EDGE ( 'NONE', *, *, #11952, .F. ) ;
#33766=B_SPLINE_CURVE_WITH_KNOTS ( 'NONE', 3,
 ( #25274, #32830, #90509, #16619 ),
 .UNSPECIFIED., .F., .F.,
 ( 4, 4 ),
 ( 0.000000000000000000, 0.001856568542221336254 ),
 .UNSPECIFIED. ) ;
#33768=CARTESIAN_POINT ( 'NONE',  ( 34.38981283644013587, 463.7396323591540295, 19.22682496774580940 ) ) ;
#33783=CARTESIAN_POINT ( 'NONE',  ( 33.32676612059159282, 300.4738025130130836, -0.7366437868951274393 ) ) ;
#33791=CARTESIAN_POINT ( 'NONE',  ( -33.00000000000000000, 450.0000000000002274, 13.20242257375370976 ) ) ;
#33793=CARTESIAN_POINT ( 'NONE',  ( 45.50299341493403205, 391.6058417003721388, 8.004974616321380410 ) ) ;
#33798=ADVANCED_FACE ( 'NONE', ( #18532 ), #65379, .T. ) ;
#33802=CARTESIAN_POINT ( 'NONE',  ( 31.70215989067338214, 439.7444121578560043, 23.75167943470401255 ) ) ;
#33804=AXIS2_PLACEMENT_3D ( 'NONE', #77492, #59723, #1442 ) ;
#33807=CARTESIAN_POINT ( 'NONE',  ( 46.00000000000003553, 436.0514809771110549, 12.15836796610173742 ) ) ;
#33816=DIRECTION ( 'NONE',  ( -1.000000000000000000, 0.000000000000000000, 0.000000000000000000 ) ) ;
#33823=CIRCLE ( 'NONE', #68217, 15.00000000000001243 ) ;
#33825=CARTESIAN_POINT ( 'NONE',  ( 30.87955015324946828, 351.7733141111877444, 20.67482462247657082 ) ) ;
#33841=( BOUNDED_SURFACE ( )  B_SPLINE_SURFACE ( 3, 2, ( 
 ( #56621, #15636, #48528 ),
 ( #25920, #106769, #41511 ),
 ( #74397, #17259, #17788 ),
 ( #50638, #83559, #81420 ),
 ( #101874, #60382, #36657 ),
 ( #77609, #51182, #94332 ),
 ( #93257, #69521, #102413 ),
 ( #28556, #61440, #19420 ),
 ( #86252, #20495, #11252 ),
 ( #68998, #12326, #59848 ),
 ( #52253, #45251, #53334 ),
 ( #93794, #78129, #92717 ) ),
 .UNSPECIFIED., .F., .F., .T. ) 
 B_SPLINE_SURFACE_WITH_KNOTS ( ( 4, 2, 2, 2, 2, 4 ),
 ( 3, 3 ),
 ( 1.517883041479706208E-18, 0.001471464792626227692, 0.002942929585252453649, 0.003678661981565566844, 0.004414394377878680040, 0.005885859170504905563 ),
 ( 0.000000000000000000, 1.000000000000000000 ),
 .UNSPECIFIED. ) 
 GEOMETRIC_REPRESENTATION_ITEM ( )  RATIONAL_B_SPLINE_SURFACE ( (
 ( 1.000000000000000000, 0.8274249441183813003, 1.000000000000000000),
 ( 1.000000000000000000, 0.8369779515087686361, 1.000000000000000000),
 ( 1.000000000000000000, 0.8428664650350916610, 1.000000000000000000),
 ( 1.000000000000000000, 0.8506961607560086236, 1.000000000000000000),
 ( 1.000000000000000000, 0.8526029425209923351, 1.000000000000000000),
 ( 1.000000000000000000, 0.8531612821182233963, 1.000000000000000000),
 ( 1.000000000000000000, 0.8529462785849180051, 1.000000000000000000),
 ( 1.000000000000000000, 0.8517601151911999846, 1.000000000000000000),
 ( 1.000000000000000000, 0.8507906177106665524, 1.000000000000000000),
 ( 1.000000000000000000, 0.8467143344643495162, 1.000000000000000000),
 ( 1.000000000000000000, 0.8424736042941722847, 1.000000000000000000),
 ( 1.000000000000000000, 0.8360809698953560742, 1.000000000000000000) ) ) 
 REPRESENTATION_ITEM ( '' )  SURFACE ( )  );
#33850=FACE_OUTER_BOUND ( 'NONE', #71290, .T. ) ;
#33859=CARTESIAN_POINT ( 'NONE',  ( 32.37165988990192744, 299.8773295831273344, 3.063193199593787330 ) ) ;
#33864=CARTESIAN_POINT ( 'NONE',  ( 42.69811214730273718, 434.9611672192513652, 18.34625614733210242 ) ) ;
#33873=CARTESIAN_POINT ( 'NONE',  ( 34.12349128637467999, 490.8027302422241860, 11.84948222508893068 ) ) ;
#33874=CARTESIAN_POINT ( 'NONE',  ( 3.945802338410542731, 299.4462438666951698, 9.201290498665041895 ) ) ;
#33875=CARTESIAN_POINT ( 'NONE',  ( 46.00000000000000000, 463.6369139993324211, 9.775485381103553806 ) ) ;
#33878=EDGE_CURVE ( 'NONE', #46568, #104224, #72221, .T. ) ;
#33880=CARTESIAN_POINT ( 'NONE',  ( 2.494577234427376227E-15, -18.92596047533412573, 20.36976895023282097 ) ) ;
#33881=VERTEX_POINT ( 'NONE', #75130 ) ;
#33886=EDGE_CURVE ( 'NONE', #13401, #90391, #105185, .T. ) ;
#33901=CARTESIAN_POINT ( 'NONE',  ( -43.03185303983481447, 485.3613526602391062, 6.073233449168579767 ) ) ;
#33905=VECTOR ( 'NONE', #89089, 1000.000000000000227 ) ;
#33915=CARTESIAN_POINT ( 'NONE',  ( 37.50843704408828216, 482.0135999900019215, 15.15320708953895057 ) ) ;
#33924=PRESENTATION_STYLE_ASSIGNMENT (( #2576 ) ) ;
#33933=EDGE_CURVE ( 'NONE', #27223, #28630, #103260, .T. ) ;
#33935=CARTESIAN_POINT ( 'NONE',  ( 32.16709058540200772, 380.6344658977095605, 24.65337216308995139 ) ) ;
#33937=CARTESIAN_POINT ( 'NONE',  ( -38.85446894546474539, 460.8903912184078422, 2.218456751110488678 ) ) ;
#33952=DIRECTION ( 'NONE',  ( -0.000000000000000000, -1.000000000000000000, -0.000000000000000000 ) ) ;
#33955=CARTESIAN_POINT ( 'NONE',  ( -4.913676358978594116, 296.1360674233372379, -10.01007018187696218 ) ) ;
#33965=CARTESIAN_POINT ( 'NONE',  ( 34.84618260875171103, 489.9833681528626244, 11.97975507378817994 ) ) ;
#33985=CARTESIAN_POINT ( 'NONE',  ( 32.66130572512987129, 465.7845731394320978, 12.51261058352552880 ) ) ;
#33986=CARTESIAN_POINT ( 'NONE',  ( -35.34007772701297512, 353.1885634555609954, 1.120430972263593672 ) ) ;
#33996=CARTESIAN_POINT ( 'NONE',  ( -23.61536189776495220, 303.4785653241179375, -9.865317176963937840 ) ) ;
#33997=EDGE_CURVE ( 'NONE', #32226, #105963, #47282, .T. ) ;
#34001=CARTESIAN_POINT ( 'NONE',  ( -40.94307380459559198, 409.3606216529898916, 27.70111150611745998 ) ) ;
#34011=CARTESIAN_POINT ( 'NONE',  ( -39.82817075493480274, 438.7291009509302171, 23.10551559802240718 ) ) ;
#34014=CARTESIAN_POINT ( 'NONE',  ( 42.89842744804999342, 435.5680593355373276, 8.824050052262007782 ) ) ;
#34030=CARTESIAN_POINT ( 'NONE',  ( 27.42790055916795566, 296.3899668198013160, -1.667331554639347013 ) ) ;
#34036=CARTESIAN_POINT ( 'NONE',  ( 0.000000000000000000, 70.00000000000000000, 0.000000000000000000 ) ) ;
#34043=CIRCLE ( 'NONE', #66746, 1.000000000000003331 ) ;
#34044=EDGE_LOOP ( 'NONE', ( #97639, #39035, #57099, #48398 ) ) ;
#34053=CARTESIAN_POINT ( 'NONE',  ( 20.24579557674108088, 304.8297271373347144, -10.00469232190996749 ) ) ;
#34060=ORIENTED_EDGE ( 'NONE', *, *, #43950, .T. ) ;
#34064=EDGE_CURVE ( 'NONE', #74993, #76425, #31845, .T. ) ;
#34072=CARTESIAN_POINT ( 'NONE',  ( 43.55333112596303380, 465.2342844084865874, 9.238213423009675296 ) ) ;
#34088=CIRCLE ( 'NONE', #30611, 12.00000000000000711 ) ;
#34100=CARTESIAN_POINT ( 'NONE',  ( -30.00000000000000355, 461.8423776372225689, 11.25810401088562607 ) ) ;
#34102=CARTESIAN_POINT ( 'NONE',  ( -31.44127085143751188, 298.7743126848183692, -1.130929553568158052 ) ) ;
#34110=CARTESIAN_POINT ( 'NONE',  ( 43.22728423987868496, 434.6919775797230727, 9.646941480579668493 ) ) ;
#34119=CARTESIAN_POINT ( 'NONE',  ( 34.05841483224278932, 462.4673622309109078, 4.856678830036404548 ) ) ;
#34123=AXIS2_PLACEMENT_3D ( 'NONE', #77367, #2932, #3483 ) ;
#34130=CARTESIAN_POINT ( 'NONE',  ( 27.95351751955323749, 311.8734759528393283, 11.86698417665069982 ) ) ;
#34141=VERTEX_POINT ( 'NONE', #83471 ) ;
#34145=CARTESIAN_POINT ( 'NONE',  ( -26.14413424799793262, 305.7334878758448440, 10.58890971036053941 ) ) ;
#34151=DIRECTION ( 'NONE',  ( 0.000000000000000000, 0.9900230405584208304, 0.1409055682485944594 ) ) ;
#34160=CARTESIAN_POINT ( 'NONE',  ( 41.97106272281727968, 437.4388437799331655, 21.41148611803419755 ) ) ;
#34162=EDGE_CURVE ( 'NONE', #64324, #61408, #55042, .T. ) ;
#34165=( BOUNDED_SURFACE ( )  B_SPLINE_SURFACE ( 3, 2, ( 
 ( #91160, #24832, #83563 ),
 ( #1020, #76007, #57686 ),
 ( #8617, #43122, #50139 ),
 ( #16718, #75477, #17266 ),
 ( #9665, #58784, #83047 ),
 ( #84109, #49607, #35057 ),
 ( #91679, #9139, #50645 ),
 ( #74407, #82514, #2107 ),
 ( #42050, #42578, #92185 ),
 ( #67925, #1571, #100284 ),
 ( #100810, #99211, #41520 ),
 ( #34534, #26446, #484 ) ),
 .UNSPECIFIED., .F., .F., .F. ) 
 B_SPLINE_SURFACE_WITH_KNOTS ( ( 4, 2, 2, 2, 2, 4 ),
 ( 3, 3 ),
 ( 1.840107927142398125E-15, 0.002111337082682424732, 0.003167005624022716827, 0.004222674165363008922, 0.006334011248043593112, 0.008445348330724177302 ),
 ( 0.000000000000000000, 1.000000000000000000 ),
 .UNSPECIFIED. ) 
 GEOMETRIC_REPRESENTATION_ITEM ( )  RATIONAL_B_SPLINE_SURFACE ( (
 ( 1.000000000000000000, 0.8812198548864098591, 1.000000000000000000),
 ( 1.000000000000000000, 0.8727984268039941096, 1.000000000000000000),
 ( 1.000000000000000000, 0.8622592014671073279, 1.000000000000000000),
 ( 1.000000000000000000, 0.8442704230973751001, 1.000000000000000000),
 ( 1.000000000000000000, 0.8379082757199421971, 1.000000000000000000),
 ( 1.000000000000000000, 0.8246032719432775382, 1.000000000000000000),
 ( 1.000000000000000000, 0.8177416415213525358, 1.000000000000000000),
 ( 1.000000000000000000, 0.7969800896719004824, 1.000000000000000000),
 ( 1.000000000000000000, 0.7828175013986581332, 1.000000000000000000),
 ( 1.000000000000000000, 0.7557468352507644704, 1.000000000000000000),
 ( 1.000000000000000000, 0.7431293883733521843, 1.000000000000000000),
 ( 1.000000000000000000, 0.7328671738315113426, 1.000000000000000000) ) ) 
 REPRESENTATION_ITEM ( '' )  SURFACE ( )  );
#34173=CARTESIAN_POINT ( 'NONE',  ( 33.92709525147887462, 435.0559456452658651, 11.89085117398059843 ) ) ;
#34177=CARTESIAN_POINT ( 'NONE',  ( 19.18290667320985676, 302.7118746156783686, 9.907256564758082362 ) ) ;
#34182=CARTESIAN_POINT ( 'NONE',  ( -45.29905483467455696, 497.0732240353902398, -8.041250874568902418 ) ) ;
#34202=CARTESIAN_POINT ( 'NONE',  ( -35.93056730070349403, 437.9188583894979274, 4.302256410573773948 ) ) ;
#34221=B_SPLINE_CURVE_WITH_KNOTS ( 'NONE', 3,
 ( #25815, #45673, #62393, #20389, #36554, #79089, #46203, #53751 ),
 .UNSPECIFIED., .F., .F.,
 ( 4, 2, 2, 4 ),
 ( 2.602085213965210642E-18, 0.002636210293396384820, 0.003954315440094607371, 0.005272420586792830356 ),
 .UNSPECIFIED. ) ;
#34227=CARTESIAN_POINT ( 'NONE',  ( -33.00540147334746166, 487.4196752801198613, 9.523982417603901851 ) ) ;
#34230=CIRCLE ( 'NONE', #106552, 8.000000000000014211 ) ;
#34239=CARTESIAN_POINT ( 'NONE',  ( 32.12756478244934044, 464.8250811501558246, 14.60600970018909095 ) ) ;
#34240=CARTESIAN_POINT ( 'NONE',  ( -36.94903695760827134, 463.9900885034068665, 19.60515700096717495 ) ) ;
#34244=CARTESIAN_POINT ( 'NONE',  ( 32.19135603494942188, 464.6890496749892350, 10.76801839735704469 ) ) ;
#34246=CARTESIAN_POINT ( 'NONE',  ( 3.269135563215229023, 294.8518027752268722, -10.00000000024436453 ) ) ;
#34251=ORIENTED_EDGE ( 'NONE', *, *, #73202, .F. ) ;
#34257=CARTESIAN_POINT ( 'NONE',  ( -30.88942347583406089, 309.2109866158478440, -8.534727214836138387 ) ) ;
#34258=CARTESIAN_POINT ( 'NONE',  ( -20.37278541768179707, 303.8378246129572062, -10.00297115033344042 ) ) ;
#34267=ORIENTED_EDGE ( 'NONE', *, *, #58597, .F. ) ;
#34279=ADVANCED_FACE ( 'NONE', ( #52166 ), #97064, .F. ) ;
#34288=CARTESIAN_POINT ( 'NONE',  ( 6.123233995736765296E-16, 0.000000000000000000, 4.999999999999999112 ) ) ;
#34308=CARTESIAN_POINT ( 'NONE',  ( -39.41275501335248777, 489.7121233615637834, 11.67778311875232333 ) ) ;
#34319=B_SPLINE_SURFACE_WITH_KNOTS ( 'NONE', 1, 3, ( 
 ( #35627, #19986, #34564, #77649, #67957, #44219, #3226, #60941, #101392, #43676, #75507, #36168, #27543, #36696, #85757, #69037, #93301, #76564, #93831, #52830, #59885, #28594, #43155, #61478, #60423, #94371, #50676, #83591 ),
 ( #10242, #67439, #100312, #59346, #18366, #2134, #35087, #100841, #27004, #92758, #18917, #51761, #84675, #2675, #54938, #88396, #86816, #46860, #78166, #79229, #5356, #53883, #13416, #64137, #78685, #96488, #70082, #63601 ) ),
 .UNSPECIFIED., .F., .F., .F.,
 ( 2, 2 ),
 ( 4, 2, 2, 2, 2, 2, 2, 2, 2, 2, 2, 2, 2, 4 ),
 ( 0.000000000000000000, 1.000000000000000000 ),
 ( 0.08901491201581737678, 0.1032490540155679704, 0.1174831960153185778, 0.1317173380150691853, 0.1459514800148197788, 0.1744197640143299588, 0.2028880480138401388, 0.2598246160128514504, 0.3167611840118632616, 0.4306343200098861623, 0.5445074560079088410, 0.6583805920059359051, 0.7722537280039543095, 1.000000000000000000 ),
 .UNSPECIFIED. ) ;
#34320=CARTESIAN_POINT ( 'NONE',  ( -34.40498866140573853, 302.2778906776350709, 3.632078850025649341 ) ) ;
#34328=CARTESIAN_POINT ( 'NONE',  ( 29.93558873341680027, 297.4490136268220795, -9.432928331562733248 ) ) ;
#34329=CARTESIAN_POINT ( 'NONE',  ( 26.27902093981875709, 306.9027577142574614, -9.548073367145329726 ) ) ;
#34330=CLOSED_SHELL ( 'NONE', ( #2839, #9074, #20124, #32808, #65014, #46538, #94210, #92228, #36977, #74535, #42217, #7243, #22479, #78075, #96383, #105486, #8624, #54681, #37267, #10612, #83747, #11618, #100517, #60180, #49635, #105264, #22744, #58655, #101535, #75146, #76635, #15584, #104263, #105736, #39830, #71923, #105296, #21684, #94022, #29087, #25773, #51756, #39482, #47171, #99679, #30166, #69992, #75024, #83313, #9458, #65743, #104834, #38253, #102196, #84160, #104122, #6463, #40032, #13170, #95413, #35226, #47630, #6081, #37457, #87605, #34279, #94518, #30781, #38564, #99646, #55361, #6558, #79239, #95825, #24340, #20246, #9483, #24477, #1917, #29714, #72273, #31211, #36513, #99496, #96501, #33746, #51420, #58167, #28583, #78550, #101798, #76174, #62987, #3520, #26768, #38641, #13157, #48801, #52408, #70682, #83657, #60244, #92245, #42684, #40209, #66950, #98434, #93154, #2712, #80319, #70334, #82689, #3742, #58476, #62519, #61216, #24083, #104065, #76848, #33798, #88957, #91028, #63899, #21188, #20436, #94148, #40168, #20115, #71620, #74001, #103142, #106673, #1129, #34634, #7411, #993, #58360, #49779, #38898, #13427, #54955, #34371, #30244, #463, #2878, #28487, #49388, #24079, #20080, #72685, #102510, #15848, #56138, #9201, #83719, #9876, #36590, #15807, #75778, #98582, #20687, #67051, #30951, #5331, #59696, #102047, #21447, #63584, #72589, #52293, #46108, #75644, #72019, #11265, #95645, #101609, #23057, #58609, #94832, #52638, #12894, #63375, #33585, #9512, #87855, #33077, #41334, #96246, #45338, #92329, #103474, #55001, #6935, #64303, #101351, #83151, #78309, #14547, #62693, #42146, #18855, #25012, #30261, #19676, #98839, #71426, #51330, #29275, #88584, #38594, #8658, #104337, #96537, #70804, #69728, #44462, #85344, #21481, #77055, #45772, #71128, #26919, #7319, #99206, #105986, #67570, #2995, #48385, #72309, #49885, #83605, #62180, #32726, #81705, #87051, #39233, #11133, #41254, #46837, #45229, #61133, #23822, #93555 ) ) ;
#34333=CARTESIAN_POINT ( 'NONE',  ( 32.10528697966009304, 486.1671898930079578, 5.449875171705039989 ) ) ;
#34342=CARTESIAN_POINT ( 'NONE',  ( 45.44493243946729422, 426.7325925718847657, 7.514341639838392872 ) ) ;
#34347=CARTESIAN_POINT ( 'NONE',  ( -21.40103372500290035, 305.0975791469744536, 9.989648404215305533 ) ) ;
#34349=CARTESIAN_POINT ( 'NONE',  ( 33.51155624906014197, 484.9914999643505666, -0.2834665992334333695 ) ) ;
#34351=CARTESIAN_POINT ( 'NONE',  ( 32.67430661331284369, 485.6291057174275352, 6.589190333399087329 ) ) ;
#34360=CARTESIAN_POINT ( 'NONE',  ( 34.40458878342295890, 463.9182705154310611, 5.552276315902680892 ) ) ;
#34366=ORIENTED_EDGE ( 'NONE', *, *, #33878, .T. ) ;
#34371=ADVANCED_FACE ( 'NONE', ( #105499 ), #105320, .F. ) ;
#34372=CARTESIAN_POINT ( 'NONE',  ( 18.61218452878530982, 304.6205044140078257, -10.04916398453198134 ) ) ;
#34373=CARTESIAN_POINT ( 'NONE',  ( -30.00000000000000355, 488.9470845376447414, 4.704489282118356819 ) ) ;
#34389=CARTESIAN_POINT ( 'NONE',  ( 42.77484754423761615, 436.8064166223269353, 20.35382343675431471 ) ) ;
#34390=CARTESIAN_POINT ( 'NONE',  ( -31.93160697752860955, 357.0395867317242846, 21.73737814537944502 ) ) ;
#34395=VERTEX_POINT ( 'NONE', #89327 ) ;
#34399=CARTESIAN_POINT ( 'NONE',  ( 25.74782367108087655, 305.2883975259064755, 10.48383779441362762 ) ) ;
#34412=CARTESIAN_POINT ( 'NONE',  ( -24.17732587070753780, 304.0407788276623933, 10.19688566026630561 ) ) ;
#34435=CARTESIAN_POINT ( 'NONE',  ( 42.08762648273149409, 487.0030674539048618, 9.106351919857861077 ) ) ;
#34449=ORIENTED_EDGE ( 'NONE', *, *, #7373, .F. ) ;
#34466=CARTESIAN_POINT ( 'NONE',  ( -7.718587331531163720, 294.7084858445363693, -6.364235840924446386 ) ) ;
#34474=CARTESIAN_POINT ( 'NONE',  ( 30.93388742938943636, 332.2947140929742886, 16.85568211106954095 ) ) ;
#34475=( BOUNDED_SURFACE ( )  B_SPLINE_SURFACE ( 3, 2, ( 
 ( #60280, #74813, #50536 ),
 ( #43539, #101247, #897 ),
 ( #93689, #75353, #83449 ),
 ( #33873, #10618, #75893 ) ),
 .UNSPECIFIED., .F., .F., .F. ) 
 B_SPLINE_SURFACE_WITH_KNOTS ( ( 4, 4 ),
 ( 3, 3 ),
 ( -1.617629641348372616E-16, 0.002038086101534472387 ),
 ( 0.000000000000000000, 1.000000000000000000 ),
 .UNSPECIFIED. ) 
 GEOMETRIC_REPRESENTATION_ITEM ( )  RATIONAL_B_SPLINE_SURFACE ( (
 ( 1.000000000000000000, 0.7927020107002088478, 1.000000000000000000),
 ( 1.000000000000000000, 0.8068894940779032243, 1.000000000000000000),
 ( 1.000000000000000000, 0.8212065780166589724, 1.000000000000000000),
 ( 1.000000000000000000, 0.8350736500407835994, 1.000000000000000000) ) ) 
 REPRESENTATION_ITEM ( '' )  SURFACE ( )  );
#34481=CARTESIAN_POINT ( 'NONE',  ( -42.51080986285575847, 487.1495428173020059, 7.889844863765286931 ) ) ;
#34482=CARTESIAN_POINT ( 'NONE',  ( -32.82691535583477105, 485.1045372766795367, 1.724905475514941999 ) ) ;
#34487=CARTESIAN_POINT ( 'NONE',  ( -35.44563196690202744, 355.0508310518326311, 1.542887188955126110 ) ) ;
#34493=ORIENTED_EDGE ( 'NONE', *, *, #67597, .T. ) ;
#34495=CARTESIAN_POINT ( 'NONE',  ( -9.581329576352811017, 294.6545431190999125, -2.865389023815151592 ) ) ;
#34509=DIRECTION ( 'NONE',  ( -0.000000000000000000, -1.000000000000000000, -0.000000000000000000 ) ) ;
#34516=ORIENTED_EDGE ( 'NONE', *, *, #255, .T. ) ;
#34524=CARTESIAN_POINT ( 'NONE',  ( -25.24358573813086437, 305.1635960858602630, -9.714717598486441119 ) ) ;
#34528=ORIENTED_EDGE ( 'NONE', *, *, #83070, .F. ) ;
#34534=CARTESIAN_POINT ( 'NONE',  ( -33.94783393359914214, 484.1261039197349305, 1.321740980884732686 ) ) ;
#34535=CARTESIAN_POINT ( 'NONE',  ( -40.92186998856096380, 418.6655855945966209, 27.42381574914823972 ) ) ;
#34550=CARTESIAN_POINT ( 'NONE',  ( 11.51753701180622613, 304.6035715647410598, 8.884240010328225523 ) ) ;
#34564=CARTESIAN_POINT ( 'NONE',  ( 24.37088254901632567, 295.3567874699774620, -9.892597027136796228 ) ) ;
#34567=ORIENTED_EDGE ( 'NONE', *, *, #36655, .F. ) ;
#34587=DIRECTION ( 'NONE',  ( -0.4157805170468990563, -0.4085867419963748470, -0.8125167296179206522 ) ) ;
#34589=CARTESIAN_POINT ( 'NONE',  ( 32.11411341898570981, 317.7919323371296514, -6.873671351699469412 ) ) ;
#34591=CARTESIAN_POINT ( 'NONE',  ( -34.24135949700323778, 434.2621254486631983, 10.63646157856311802 ) ) ;
#34597=CARTESIAN_POINT ( 'NONE',  ( -3.398604459340648809, 303.8518027749813086, -10.00000000027307223 ) ) ;
#34606=CIRCLE ( 'NONE', #98320, 1.000000000000004441 ) ;
#34631=CARTESIAN_POINT ( 'NONE',  ( -31.03867016165222026, 468.3124986733989772, 18.90871194958903345 ) ) ;
#34633=CARTESIAN_POINT ( 'NONE',  ( 29.01988888469873018, 321.8047804620298393, 14.12772110426748284 ) ) ;
#34634=ADVANCED_FACE ( 'NONE', ( #94658 ), #35097, .T. ) ;
#34639=CIRCLE ( 'NONE', #61, 5.000000000000000000 ) ;
#34641=CARTESIAN_POINT ( 'NONE',  ( -32.00986601473474735, 486.4616239121606895, 6.105527853528552207 ) ) ;
#34654=CARTESIAN_POINT ( 'NONE',  ( -24.09682408347498139, 306.3733087561651587, 9.274668387549985127 ) ) ;
#34664=CARTESIAN_POINT ( 'NONE',  ( 30.60303901177592323, 328.0989884029825703, 15.88304988518486915 ) ) ;
#34675=CARTESIAN_POINT ( 'NONE',  ( -46.00000000000000000, 462.4470051410875726, 6.587392890220048258 ) ) ;
#34684=DIRECTION ( 'NONE',  ( -0.1270361284032253957, -0.9918980905719697594, 0.000000000000000000 ) ) ;
#34709=CARTESIAN_POINT ( 'NONE',  ( 31.03678703375048187, 438.6650838204853926, 21.86890379897692327 ) ) ;
#34713=CARTESIAN_POINT ( 'NONE',  ( 12.12012043129136529, 302.5867796431402326, 9.880676409032833618 ) ) ;
#34716=CARTESIAN_POINT ( 'NONE',  ( -43.41290683822509067, 487.0833545439620593, 7.569976829064872348 ) ) ;
#34727=DIRECTION ( 'NONE',  ( 0.2776092459793209066, -0.06763270420234848701, 0.9583104527599972666 ) ) ;
#34764=CARTESIAN_POINT ( 'NONE',  ( 35.53880462860536937, 395.8745130103307019, 6.882435263909567169 ) ) ;
#34765=ORIENTED_EDGE ( 'NONE', *, *, #1653, .F. ) ;
#34771=CARTESIAN_POINT ( 'NONE',  ( -44.26720285007399269, 485.4142925135642486, 2.510465450176162960 ) ) ;
#34779=EDGE_CURVE ( 'NONE', #62342, #60518, #58608, .T. ) ;
#34784=ORIENTED_EDGE ( 'NONE', *, *, #82026, .T. ) ;
#34785=DIRECTION ( 'NONE',  ( -1.000000000000000000, -0.000000000000000000, -0.000000000000000000 ) ) ;
#34793=CARTESIAN_POINT ( 'NONE',  ( -37.61245331168856154, 304.9616315839961089, -7.671943079217724559 ) ) ;
#34812=ORIENTED_EDGE ( 'NONE', *, *, #97991, .F. ) ;
#34826=CARTESIAN_POINT ( 'NONE',  ( 30.00000000000000000, 450.0000000000002274, 13.20242257375370976 ) ) ;
#34839=DIRECTION ( 'NONE',  ( 0.8139476909583217568, 0.000000000000000000, 0.5809381691571112727 ) ) ;
#34842=CARTESIAN_POINT ( 'NONE',  ( -31.00196442608961789, 438.8341882283345967, 22.04045832193504850 ) ) ;
#34847=FACE_OUTER_BOUND ( 'NONE', #38382, .T. ) ;
#34851=CARTESIAN_POINT ( 'NONE',  ( -42.57401446191834538, 489.2306033394490896, 6.899174279275240629 ) ) ;
#34852=CARTESIAN_POINT ( 'NONE',  ( -21.58423181737243368, 294.9402007847133973, 1.955789080085255982 ) ) ;
#34855=CARTESIAN_POINT ( 'NONE',  ( -34.97110905785431356, 329.4978619204799770, -3.714909018897103454 ) ) ;
#34857=CYLINDRICAL_SURFACE ( 'NONE', #56844, 6.999999999999993783 ) ;
#34859=CARTESIAN_POINT ( 'NONE',  ( 22.52750012656957423, 295.0402877133163315, -9.959936289882007188 ) ) ;
#34860=CARTESIAN_POINT ( 'NONE',  ( 33.56345473223404241, 299.9083031499212666, -8.874823776836098688 ) ) ;
#34862=DIRECTION ( 'NONE',  ( 0.000000000000000000, 0.000000000000000000, 1.000000000000000000 ) ) ;
#34881=EDGE_CURVE ( 'NONE', #41735, #70272, #68932, .T. ) ;
#34889=CARTESIAN_POINT ( 'NONE',  ( 37.69154037552305425, 413.5868078396032388, 6.418144976575544725 ) ) ;
#34892=TOROIDAL_SURFACE ( 'NONE', #22790, 8.000000000000007105, 1.000000000000000888 ) ;
#34897=CARTESIAN_POINT ( 'NONE',  ( -43.79329400983250764, 434.3557490607461773, 12.18619556048586006 ) ) ;
#34901=CARTESIAN_POINT ( 'NONE',  ( -30.00000000000000355, 489.3008774416998108, 5.491695563541885150 ) ) ;
#34911=CARTESIAN_POINT ( 'NONE',  ( -26.51187371842186025, 308.1715024495429134, 10.94285474946573622 ) ) ;
#34914=EDGE_LOOP ( 'NONE', ( #21744, #61358, #41206, #47811, #52433 ) ) ;
#34918=CARTESIAN_POINT ( 'NONE',  ( 37.03121509147988633, 439.7235855775043660, 24.13066540521764836 ) ) ;
#34919=CARTESIAN_POINT ( 'NONE',  ( -31.43460449399193024, 410.2305464698810624, 24.47796294967516317 ) ) ;
#34926=CARTESIAN_POINT ( 'NONE',  ( 32.49403296435929889, 299.9991840122719964, 3.091681079173501434 ) ) ;
#34927=CIRCLE ( 'NONE', #29762, 3.000000000000009326 ) ;
#34932=CARTESIAN_POINT ( 'NONE',  ( 39.34669569945254608, 315.1114205638089629, 6.831757979675468384 ) ) ;
#34941=CARTESIAN_POINT ( 'NONE',  ( 6.426095497085385411, 294.7471186225963606, 9.914748094734409989 ) ) ;
#34956=EDGE_CURVE ( 'NONE', #17636, #47279, #2187, .T. ) ;
#34957=CIRCLE ( 'NONE', #2179, 1.000000000000001110 ) ;
#34967=FACE_OUTER_BOUND ( 'NONE', #98019, .T. ) ;
#34982=VERTEX_POINT ( 'NONE', #36584 ) ;
#34990=CARTESIAN_POINT ( 'NONE',  ( -46.00000000000000000, 488.9831568219305495, 4.757012338623842318 ) ) ;
#34992=ORIENTED_EDGE ( 'NONE', *, *, #22623, .T. ) ;
#34994=ORIENTED_EDGE ( 'NONE', *, *, #98299, .F. ) ;
#34997=CARTESIAN_POINT ( 'NONE',  ( 26.22660380935851521, 309.5493840096061149, 10.04179730271015103 ) ) ;
#35001=EDGE_CURVE ( 'NONE', #7582, #48477, #20231, .T. ) ;
#35014=EDGE_LOOP ( 'NONE', ( #95081, #28793, #64201 ) ) ;
#35019=CARTESIAN_POINT ( 'NONE',  ( -4.240736524251620843, 300.6921934601531348, -10.01075408398145861 ) ) ;
#35028=EDGE_CURVE ( 'NONE', #15128, #36676, #54918, .T. ) ;
#35033=DIRECTION ( 'NONE',  ( 1.000000000000000000, 0.000000000000000000, 0.000000000000000000 ) ) ;
#35057=CARTESIAN_POINT ( 'NONE',  ( -35.58611802053648177, 485.2911282079576267, -2.949779747020754517 ) ) ;
#35058=CARTESIAN_POINT ( 'NONE',  ( -40.74344824707514334, 359.9914281314131017, 24.28752742797811237 ) ) ;
#35066=ORIENTED_EDGE ( 'NONE', *, *, #75972, .T. ) ;
#35086=CARTESIAN_POINT ( 'NONE',  ( 8.890893604443357745, 294.6744728344714304, -4.583208782230876466 ) ) ;
#35087=CARTESIAN_POINT ( 'NONE',  ( 30.55228927099183522, 298.7536840786443690, 10.80461237140096209 ) ) ;
#35092=CARTESIAN_POINT ( 'NONE',  ( 30.00000000000000000, 500.0000000000002274, 12.00000000000000888 ) ) ;
#35094=AXIS2_PLACEMENT_3D ( 'NONE', #70990, #29514, #38134 ) ;
#35096=CARTESIAN_POINT ( 'NONE',  ( -39.21851180500383549, 464.6178194517503357, 18.47749881120159898 ) ) ;
#35097=( BOUNDED_SURFACE ( )  B_SPLINE_SURFACE ( 3, 2, ( 
 ( #76311, #19202, #20804 ),
 ( #11039, #44500, #52038 ),
 ( #102729, #52567, #53117 ),
 ( #76847, #93580, #2424 ) ),
 .UNSPECIFIED., .F., .F., .F. ) 
 B_SPLINE_SURFACE_WITH_KNOTS ( ( 4, 4 ),
 ( 3, 3 ),
 ( 0.01611645847898209721, 0.01831749139115259814 ),
 ( 0.1613811371914657955, 1.000000000000000000 ),
 .UNSPECIFIED. ) 
 GEOMETRIC_REPRESENTATION_ITEM ( )  RATIONAL_B_SPLINE_SURFACE ( (
 ( 0.9207212652179901369, 0.7543742219143241279, 1.000000000000000000),
 ( 0.9269995412618095010, 0.7738259253571211360, 1.000000000000000000),
 ( 0.9331146633523605960, 0.7927721361627118046, 1.000000000000000000),
 ( 0.9388524989238742346, 0.8105494169260341053, 1.000000000000000000) ) ) 
 REPRESENTATION_ITEM ( '' )  SURFACE ( )  );
#35104=CARTESIAN_POINT ( 'NONE',  ( 9.928454760406586033, 294.6449062848762992, 1.239352149953448334 ) ) ;
#35112=CARTESIAN_POINT ( 'NONE',  ( -43.00000000000004263, 435.7055874969797173, 20.39059140826869765 ) ) ;
#35114=CARTESIAN_POINT ( 'NONE',  ( 34.72474116627837759, 338.3618661353910966, -1.881472242819908436 ) ) ;
#35115=CARTESIAN_POINT ( 'NONE',  ( 39.26668904305612529, 460.2385666352532780, 2.228751329589347741 ) ) ;
#35120=VERTEX_POINT ( 'NONE', #21974 ) ;
#35130=CARTESIAN_POINT ( 'NONE',  ( 43.69363714723023406, 464.9777160013941852, 8.439175988291857777 ) ) ;
#35133=EDGE_CURVE ( 'NONE', #64798, #37996, #84558, .T. ) ;
#35148=CARTESIAN_POINT ( 'NONE',  ( 32.69883954133203474, 464.5926484747985796, 16.74362576150353021 ) ) ;
#35151=CARTESIAN_POINT ( 'NONE',  ( -20.52350613252515643, 304.8999024697870937, 9.947223320822450532 ) ) ;
#35166=CARTESIAN_POINT ( 'NONE',  ( -43.71217423904473520, 435.6632154632216043, 9.092528312227512899 ) ) ;
#35170=CARTESIAN_POINT ( 'NONE',  ( 36.12951349333496154, 461.0357385931042700, 3.035048805483111511 ) ) ;
#35176=TOROIDAL_SURFACE ( 'NONE', #48904, 7.025805963803935406, 3.000000000000000000 ) ;
#35185=DIRECTION ( 'NONE',  ( 1.000000000000000000, 0.000000000000000000, 0.000000000000000000 ) ) ;
#35190=CARTESIAN_POINT ( 'NONE',  ( -43.63899620156477965, 434.3182181978404515, 14.37213632273176422 ) ) ;
#35201=DIRECTION ( 'NONE',  ( -0.000000000000000000, -1.000000000000000000, -0.000000000000000000 ) ) ;
#35203=CARTESIAN_POINT ( 'NONE',  ( -23.88903980719504716, 303.8749885964456894, 10.15971976529453080 ) ) ;
#35215=CARTESIAN_POINT ( 'NONE',  ( -40.96842839773133704, 488.3806639627545110, 10.59944728061772956 ) ) ;
#35217=CARTESIAN_POINT ( 'NONE',  ( 32.81992448453895150, 465.7192846569213316, 11.17271167765130890 ) ) ;
#35219=CARTESIAN_POINT ( 'NONE',  ( 43.00000000000000000, 436.5989882784185738, 19.94133085611157341 ) ) ;
#35223=CARTESIAN_POINT ( 'NONE',  ( 39.30650688512051971, 485.8522658471749764, -4.984147873724974254 ) ) ;
#35226=ADVANCED_FACE ( 'NONE', ( #94674, #45580 ), #4581, .F. ) ;
#35229=DIRECTION ( 'NONE',  ( 0.000000000000000000, -1.000000000000000000, 0.000000000000000000 ) ) ;
#35232=CARTESIAN_POINT ( 'NONE',  ( 32.84237740334622657, 485.2251842821286800, 5.746442123025142124 ) ) ;
#35236=DIRECTION ( 'NONE',  ( 0.000000000000000000, 0.9952410070626042105, -0.09744402424476066027 ) ) ;
#35244=CARTESIAN_POINT ( 'NONE',  ( -1.128077836147719282, 302.8478239976500390, 9.936168295454388399 ) ) ;
#35250=CARTESIAN_POINT ( 'NONE',  ( -35.74363442581862671, 380.1068966271811860, 4.951945592532029927 ) ) ;
#35273=CARTESIAN_POINT ( 'NONE',  ( 32.74032929948388926, 316.4554875038838873, -6.969597370910324940 ) ) ;
#35279=AXIS2_PLACEMENT_3D ( 'NONE', #57521, #40819, #40293 ) ;
#35302=VERTEX_POINT ( 'NONE', #55230 ) ;
#35313=EDGE_LOOP ( 'NONE', ( #101211, #98537, #76746, #91092 ) ) ;
#35314=B_SPLINE_CURVE_WITH_KNOTS ( 'NONE', 3,
 ( #16566, #47848, #41368, #49449, #80754, #39792, #68857, #83419, #19803, #10063, #60245, #93113, #3036, #10587, #92575, #67776, #34911, #35441, #51039, #59697, #100134, #85572, #101209, #44576, #92044, #83954, #18728, #44032, #68313, #3580, #42973, #75864, #1958, #77467, #18178, #91529, #19285, #84497, #2493, #99594, #36516, #25771, #76925, #27900, #60767, #58631, #26823, #27365 ),
 .UNSPECIFIED., .F., .F.,
 ( 4, 2, 2, 2, 2, 2, 2, 2, 2, 2, 2, 2, 2, 2, 2, 2, 2, 2, 2, 2, 2, 2, 2, 4 ),
 ( -6.000000000621486066E-08, 0.001110492795678789599, 0.002221045591357585346, 0.003331598387036381094, 0.004442151182715176408, 0.005552703978393972589, 0.006663256774072767903, 0.007773809569751563217, 0.008884362365430359398, 0.01110546795678795176, 0.01332657354814554239, 0.01776878473086072538, 0.02221099591357591010, 0.02665320709629109136, 0.03109541827900627262, 0.03553762946172146081, 0.04442205182715165679, 0.05330647419258186664, 0.07107531892344241820, 0.08884416365430296281, 0.1066130083851635352, 0.1243818531160240798, 0.1332662754814543937, 0.1421506978468846660 ),
 .UNSPECIFIED. ) ;
#35321=CARTESIAN_POINT ( 'NONE',  ( -31.43882072741231681, 310.1515563548447858, -8.305534716118780025 ) ) ;
#35327=ORIENTED_EDGE ( 'NONE', *, *, #30789, .T. ) ;
#35335=EDGE_CURVE ( 'NONE', #101821, #78629, #18111, .T. ) ;
#35345=CARTESIAN_POINT ( 'NONE',  ( 32.74728942619678662, 438.8764684952982975, 23.82517967440744400 ) ) ;
#35371=STYLED_ITEM ( 'NONE', ( #50969 ), #87588 ) ;
#35376=( LENGTH_UNIT ( ) NAMED_UNIT ( * ) SI_UNIT ( .MILLI., .METRE. ) );
#35385=CARTESIAN_POINT ( 'NONE',  ( -35.64312564391374138, 304.2402637384089985, 4.107419002728130764 ) ) ;
#35389=CARTESIAN_POINT ( 'NONE',  ( -36.73034038993296235, 408.1380310545363272, 6.297704266999571310 ) ) ;
#35391=DIRECTION ( 'NONE',  ( -0.2271661929664648139, 0.3956501727912606903, 0.8898631701241311864 ) ) ;
#35392=CARTESIAN_POINT ( 'NONE',  ( 26.72825103767788235, 296.1707100295333817, -1.715122094987715062 ) ) ;
#35393=CARTESIAN_POINT ( 'NONE',  ( 45.33180403702434091, 464.4945808635454227, 2.178908857919817699 ) ) ;
#35395=DIRECTION ( 'NONE',  ( -0.2908996821237400665, 0.5336441332591916886, 0.7941040951779264612 ) ) ;
#35403=CARTESIAN_POINT ( 'NONE',  ( 34.79138225435746534, 321.1841114852068131, -5.534975474723330180 ) ) ;
#35407=CARTESIAN_POINT ( 'NONE',  ( -13.76424046522695122, 304.5457540960956067, -10.06505265514019065 ) ) ;
#35408=CARTESIAN_POINT ( 'NONE',  ( 31.34138169376840466, 438.6792511472767160, 22.89137509121641401 ) ) ;
#35421=CARTESIAN_POINT ( 'NONE',  ( 37.70493684217908026, 407.6483267487184321, 6.531453235178003247 ) ) ;
#35427=( NAMED_UNIT ( * ) PLANE_ANGLE_UNIT ( ) SI_UNIT ( $, .RADIAN. ) );
#35441=CARTESIAN_POINT ( 'NONE',  ( -26.98213138876943162, 309.1463827484340072, 11.18347436010351537 ) ) ;
#35451=CARTESIAN_POINT ( 'NONE',  ( 33.49732520203519215, 439.8560114000520116, 24.25307120326154475 ) ) ;
#35452=CARTESIAN_POINT ( 'NONE',  ( -30.85687531707146292, 345.5963099307835478, 18.44619323452473125 ) ) ;
#35460=CARTESIAN_POINT ( 'NONE',  ( 24.95205008382144030, 304.5524501393400669, 10.31272274050776439 ) ) ;
#35467=CARTESIAN_POINT ( 'NONE',  ( -44.11327388758650159, 464.4313852428384735, 9.822198357558047377 ) ) ;
#35478=CARTESIAN_POINT ( 'NONE',  ( 8.363851124833434625, 294.6905162191789600, 1.902776341390910453 ) ) ;
#35493=CARTESIAN_POINT ( 'NONE',  ( 6.953930663124324063, 304.7325910270068334, -10.02533923955978779 ) ) ;
#35511=AXIS2_PLACEMENT_3D ( 'NONE', #19831, #75883, #76404 ) ;
#35516=DIRECTION ( 'NONE',  ( 0.000000000000000000, 0.000000000000000000, 1.000000000000000000 ) ) ;
#35520=EDGE_LOOP ( 'NONE', ( #76691, #26222, #65185, #46815 ) ) ;
#35521=FACE_OUTER_BOUND ( 'NONE', #59762, .T. ) ;
#35533=CARTESIAN_POINT ( 'NONE',  ( 25.02429500009634822, 305.9718288055595963, 10.41235884080700203 ) ) ;
#35543=CARTESIAN_POINT ( 'NONE',  ( -30.95643954367146833, 313.8918926584737505, -7.857037206977866006 ) ) ;
#35547=CARTESIAN_POINT ( 'NONE',  ( -46.00000000000000000, 437.9690125970932968, 14.09127711025707796 ) ) ;
#35554=CARTESIAN_POINT ( 'NONE',  ( -9.740083726526439278, 294.6493269980080072, -10.04303756037268158 ) ) ;
#35567=EDGE_CURVE ( 'NONE', #104315, #71900, #72861, .T. ) ;
#35572=CARTESIAN_POINT ( 'NONE',  ( -43.71297783477830734, 485.1278128289774259, -1.116606130290624721 ) ) ;
#35580=CARTESIAN_POINT ( 'NONE',  ( 34.24300530784454111, 434.2296727341958444, 10.63337750349099764 ) ) ;
#35581=CARTESIAN_POINT ( 'NONE',  ( 43.00000000000000000, 450.0000000000002274, 13.20242257375370976 ) ) ;
#35590=B_SPLINE_CURVE_WITH_KNOTS ( 'NONE', 3,
 ( #52819, #26994, #93817, #34550, #18902, #60930, #28058, #19973, #10748, #101378 ),
 .UNSPECIFIED., .F., .F.,
 ( 4, 2, 2, 2, 4 ),
 ( 3.698327573679174046E-29, 0.009876477788552447123, 0.01481471668282867589, 0.01728383612996678420, 0.01975295557710489425 ),
 .UNSPECIFIED. ) ;
#35593=CARTESIAN_POINT ( 'NONE',  ( -35.10770204084435875, 352.9232395558267399, 2.060922233138942072 ) ) ;
#35594=CARTESIAN_POINT ( 'NONE',  ( -34.17726614582090150, 303.5588809801041634, 11.95427360728275445 ) ) ;
#35608=ORIENTED_EDGE ( 'NONE', *, *, #45450, .F. ) ;
#35614=AXIS2_PLACEMENT_3D ( 'NONE', #3380, #68103, #35236 ) ;
#35618=CIRCLE ( 'NONE', #95877, 15.00000000000001243 ) ;
#35626=CARTESIAN_POINT ( 'NONE',  ( 4.913676358839419223, 296.1360674232993802, -10.01007018187845077 ) ) ;
#35627=CARTESIAN_POINT ( 'NONE',  ( 21.51569398614858031, 294.9107018935607130, -9.987480606144490736 ) ) ;
#35638=CIRCLE ( 'NONE', #87276, 1.000000000000001110 ) ;
#35651=CARTESIAN_POINT ( 'NONE',  ( 40.97307933990123985, 465.3163409530395711, 16.72193089366239960 ) ) ;
#35661=CARTESIAN_POINT ( 'NONE',  ( -16.13870609129251221, 303.5610354609489150, -10.06180398438553247 ) ) ;
#35674=CARTESIAN_POINT ( 'NONE',  ( -43.00000000000000000, 464.8825480873695710, 15.07585856869432206 ) ) ;
#35698=CARTESIAN_POINT ( 'NONE',  ( 27.57151080649627417, 314.0751515626058676, 12.18133379269485239 ) ) ;
#35717=CARTESIAN_POINT ( 'NONE',  ( 32.04696785526762426, 435.9094004289368627, 19.86239142642784117 ) ) ;
#35723=CARTESIAN_POINT ( 'NONE',  ( 36.73887825314411515, 438.2333816059632454, 3.899276075025526644 ) ) ;
#35736=ORIENTED_EDGE ( 'NONE', *, *, #35753, .T. ) ;
#35738=B_SPLINE_CURVE_WITH_KNOTS ( 'NONE', 3,
 ( #103794, #61777, #29937, #12648, #23298, #80962, #56133, #87103, #89078, #4580, #70379, #103274, #102205, #29424, #7078, #64793 ),
 .UNSPECIFIED., .F., .F.,
 ( 4, 2, 2, 2, 2, 2, 2, 4 ),
 ( 1.366913666845653131E-16, 0.001031042176150235266, 0.001546563264225255321, 0.002062084352300275810, 0.002577605440375296299, 0.003093126528450315920, 0.003608647616525335975, 0.004124168704600356464 ),
 .UNSPECIFIED. ) ;
#35748=( BOUNDED_SURFACE ( )  B_SPLINE_SURFACE ( 3, 2, ( 
 ( #10980, #87951, #101610 ),
 ( #30256, #102128, #63145 ),
 ( #85426, #47465, #60639 ),
 ( #97085, #96042, #5943 ),
 ( #39406, #104647, #77333 ),
 ( #38870, #85980, #63686 ),
 ( #76786, #2890, #27765 ),
 ( #44982, #77866, #3445 ),
 ( #36907, #55545, #36389 ),
 ( #102669, #69257, #72284 ),
 ( #31333, #94045, #28284 ),
 ( #64215, #61158, #53061 ),
 ( #73870, #32385, #105704 ),
 ( #32913, #58220, #65790 ),
 ( #90595, #33986, #81416 ),
 ( #8072, #65256, #15103 ),
 ( #82503, #64729, #99746 ),
 ( #49594, #47990, #33441 ),
 ( #7527, #89009, #97603 ),
 ( #106765, #91147, #72799 ),
 ( #106223, #8604, #41506 ),
 ( #89540, #98667, #98147 ),
 ( #50127, #24819, #17256 ),
 ( #74919, #16705, #66856 ),
 ( #73325, #40981, #1003 ),
 ( #40445, #80898, #74394 ),
 ( #57672, #90061, #23769 ),
 ( #473, #16165, #56617 ),
 ( #24299, #49052, #57148 ),
 ( #9127, #25915, #66315 ),
 ( #83036, #81948, #99197 ),
 ( #25360, #42037, #7007 ),
 ( #39927, #31847, #15632 ),
 ( #48525, #28030, #68456 ),
 ( #101348, #85160, #1560 ),
 ( #51717, #11248, #43109 ),
 ( #17783, #84097, #27503 ),
 ( #92174, #10719, #60378 ),
 ( #43635, #67912, #34524 ),
 ( #44177, #59302, #93253 ),
 ( #59841, #92713, #26437 ),
 ( #50635, #100799, #18873 ),
 ( #84632, #75997, #67393 ),
 ( #42566, #36126, #60899 ) ),
 .UNSPECIFIED., .F., .F., .F. ) 
 B_SPLINE_SURFACE_WITH_KNOTS ( ( 4, 2, 2, 2, 2, 2, 2, 2, 2, 2, 2, 2, 2, 2, 2, 2, 2, 2, 2, 2, 2, 4 ),
 ( 3, 3 ),
 ( 0.05136275451448887863, 0.06919263422628305071, 0.08702251393807722279, 0.1048523936498713949, 0.1137673335057684809, 0.1226822733616655670, 0.1315972132175626530, 0.1405121530734597390, 0.1583420327852539111, 0.1672569726411509972, 0.1717144425690995402, 0.1761719124970480832, 0.1784006474610223547, 0.1806293824249966262, 0.1828581173889708977, 0.1850868523529451692, 0.1862012198349323189, 0.1873155873169194408, 0.1884299547989065626, 0.1895443222808937123, 0.1917730572448679838, 0.1940017922088422553 ),
 ( 0.000000000000000000, 1.000000000000000000 ),
 .UNSPECIFIED. ) 
 GEOMETRIC_REPRESENTATION_ITEM ( )  RATIONAL_B_SPLINE_SURFACE ( (
 ( 1.000000000000000000, 0.7071066982518089405, 1.000000000000000000),
 ( 1.000000000000000000, 0.7071066243399852791, 1.000000000000000000),
 ( 1.000000000000000000, 0.7071067817164773395, 1.000000000000000000),
 ( 1.000000000000000000, 0.7071067817164773395, 1.000000000000000000),
 ( 1.000000000000000000, 0.7071067820464573828, 1.000000000000000000),
 ( 1.000000000000000000, 0.7071067820464573828, 1.000000000000000000),
 ( 1.000000000000000000, 0.7071085455477897908, 1.000000000000000000),
 ( 1.000000000000000000, 0.7071090295291238004, 1.000000000000000000),
 ( 1.000000000000000000, 0.7071083385704458601, 1.000000000000000000),
 ( 1.000000000000000000, 0.7071068389492060069, 1.000000000000000000),
 ( 1.000000000000000000, 0.7071066205750288214, 1.000000000000000000),
 ( 1.000000000000000000, 0.7071083160947816415, 1.000000000000000000),
 ( 1.000000000000000000, 0.7071093954417188021, 1.000000000000000000),
 ( 1.000000000000000000, 0.7071094620417358589, 1.000000000000000000),
 ( 1.000000000000000000, 0.7071083849275382471, 1.000000000000000000),
 ( 1.000000000000000000, 0.7071056411300526978, 1.000000000000000000),
 ( 1.000000000000000000, 0.7070875072514104520, 1.000000000000000000),
 ( 1.000000000000000000, 0.7071202496626299849, 1.000000000000000000),
 ( 1.000000000000000000, 0.7071338852168149725, 1.000000000000000000),
 ( 1.000000000000000000, 0.7071095136704249606, 1.000000000000000000),
 ( 1.000000000000000000, 0.7071065123001155639, 1.000000000000000000),
 ( 1.000000000000000000, 0.7071128202845421429, 1.000000000000000000),
 ( 1.000000000000000000, 0.7071080869018205872, 1.000000000000000000),
 ( 1.000000000000000000, 0.7071063200084551914, 1.000000000000000000),
 ( 1.000000000000000000, 0.7071396742970895710, 1.000000000000000000),
 ( 1.000000000000000000, 0.7071960107269280593, 1.000000000000000000),
 ( 1.000000000000000000, 0.7072035974108880074, 1.000000000000000000),
 ( 1.000000000000000000, 0.7071532259081326766, 1.000000000000000000),
 ( 1.000000000000000000, 0.7071047821262952393, 1.000000000000000000),
 ( 1.000000000000000000, 0.7071096296259671288, 1.000000000000000000),
 ( 1.000000000000000000, 0.7071125913011165887, 1.000000000000000000),
 ( 1.000000000000000000, 0.7071062656804929514, 1.000000000000000000),
 ( 1.000000000000000000, 0.7071058024559618849, 1.000000000000000000),
 ( 1.000000000000000000, 0.7071001851375554592, 1.000000000000000000),
 ( 1.000000000000000000, 0.7070990685193431213, 1.000000000000000000),
 ( 1.000000000000000000, 0.7071030088798048174, 1.000000000000000000),
 ( 1.000000000000000000, 0.7071042265699299945, 1.000000000000000000),
 ( 1.000000000000000000, 0.7071104316389814626, 1.000000000000000000),
 ( 1.000000000000000000, 0.7071217845162482973, 1.000000000000000000),
 ( 1.000000000000000000, 0.7071252912931403900, 1.000000000000000000),
 ( 1.000000000000000000, 0.7071009329475237415, 1.000000000000000000),
 ( 1.000000000000000000, 0.7071402609100536640, 1.000000000000000000),
 ( 1.000000000000000000, 0.7071206810161836387, 1.000000000000000000),
 ( 1.000000000000000000, 0.7071067811865464625, 1.000000000000000000) ) ) 
 REPRESENTATION_ITEM ( '' )  SURFACE ( )  );
#35753=EDGE_CURVE ( 'NONE', #68586, #100942, #23430, .T. ) ;
#35764=CARTESIAN_POINT ( 'NONE',  ( -42.44022245594207732, 488.6041665467083135, 9.766690314390181982 ) ) ;
#35770=CARTESIAN_POINT ( 'NONE',  ( 40.81956795959206374, 485.7841149218990040, -4.786840289929677361 ) ) ;
#35779=FACE_OUTER_BOUND ( 'NONE', #92126, .T. ) ;
#35785=CARTESIAN_POINT ( 'NONE',  ( -45.29905483467455696, 497.0732240353902398, -8.041250874568902418 ) ) ;
#35818=CARTESIAN_POINT ( 'NONE',  ( 25.36273202697566020, 305.2221405902974425, -9.701703692503940601 ) ) ;
#35822=B_SPLINE_CURVE_WITH_KNOTS ( 'NONE', 3,
 ( #13212, #37549, #103313, #87666, #5667, #79028, #65889, #71454, #57779, #21358, #104353, #29460, #5147, #65364, #38080, #70936 ),
 .UNSPECIFIED., .F., .F.,
 ( 4, 2, 2, 2, 2, 2, 2, 4 ),
 ( 7.757919228897728493E-18, 0.001041806880168140350, 0.001562710320252229824, 0.002083613760336319298, 0.002604517200420408338, 0.003125420640504497811, 0.003646324080588587285, 0.004167227520672676759 ),
 .UNSPECIFIED. ) ;
#35833=ORIENTED_EDGE ( 'NONE', *, *, #17963, .F. ) ;
#35834=CARTESIAN_POINT ( 'NONE',  ( -42.79777464980524826, 484.2777864412636291, -1.379167304946371964 ) ) ;
#35839=CARTESIAN_POINT ( 'NONE',  ( -43.68138489372817901, 484.4283016034073057, 2.027755642628957578 ) ) ;
#35843=CARTESIAN_POINT ( 'NONE',  ( -35.52386467438594764, 464.2380653034055058, 19.26634992204778030 ) ) ;
#35845=EDGE_CURVE ( 'NONE', #15190, #62284, #44054, .T. ) ;
#35854=CIRCLE ( 'NONE', #96095, 5.000000000000000000 ) ;
#35856=ORIENTED_EDGE ( 'NONE', *, *, #29608, .F. ) ;
#35862=CARTESIAN_POINT ( 'NONE',  ( -33.58551248210795848, 315.8335180326819795, -6.885581302250129987 ) ) ;
#35863=CARTESIAN_POINT ( 'NONE',  ( -1.496989374907284246E-10, 304.8518027762757470, -10.00000000000000533 ) ) ;
#35867=CARTESIAN_POINT ( 'NONE',  ( -42.80674476975001852, 434.8200572689409000, 17.89667068453010046 ) ) ;
#35873=ORIENTED_EDGE ( 'NONE', *, *, #56279, .F. ) ;
#35895=CARTESIAN_POINT ( 'NONE',  ( -43.66729043033831914, 435.6676719292337907, 17.39374879622100423 ) ) ;
#35905=VERTEX_POINT ( 'NONE', #8151 ) ;
#35915=DIRECTION ( 'NONE',  ( -0.000000000000000000, -1.000000000000000000, -0.000000000000000000 ) ) ;
#35926=CARTESIAN_POINT ( 'NONE',  ( -30.32981733298740323, 298.1626997294918056, 2.667535392438074915 ) ) ;
#35931=CIRCLE ( 'NONE', #77234, 1.000000000000002220 ) ;
#35934=CARTESIAN_POINT ( 'NONE',  ( 25.99908587619278322, 295.9244531611905700, -1.769008014947292429 ) ) ;
#35935=CARTESIAN_POINT ( 'NONE',  ( 32.16694665535142406, 298.7751107022914425, -9.134474995493537364 ) ) ;
#35946=CARTESIAN_POINT ( 'NONE',  ( 44.90265637069953186, 347.4290076447818478, 2.367369570399655565 ) ) ;
#35951=CARTESIAN_POINT ( 'NONE',  ( 31.50721393268916870, 439.7147443804711315, 23.57029083728580687 ) ) ;
#35959=CARTESIAN_POINT ( 'NONE',  ( -30.00000000000000000, 450.0000000000002274, 8.202422573753707979 ) ) ;
#35973=CIRCLE ( 'NONE', #44321, 1.000000000000000666 ) ;
#36005=CARTESIAN_POINT ( 'NONE',  ( 24.95947819434403669, 295.7176545011159874, 10.12322481647160899 ) ) ;
#36010=CARTESIAN_POINT ( 'NONE',  ( 29.36753485554255505, 297.5156562771362587, 2.520813113073917755 ) ) ;
#36019=CARTESIAN_POINT ( 'NONE',  ( -32.85555225121258616, 465.7063523440040171, 11.00064571225268217 ) ) ;
#36022=DIRECTION ( 'NONE',  ( 0.9735618822052878318, 0.000000000000000000, 0.2284234259372218689 ) ) ;
#36042=CARTESIAN_POINT ( 'NONE',  ( -34.12349128637492157, 490.8027302422244134, 11.84948222508912252 ) ) ;
#36043=FACE_OUTER_BOUND ( 'NONE', #94861, .T. ) ;
#36050=CARTESIAN_POINT ( 'NONE',  ( 41.13328595189572923, 484.9084785457743578, -3.795084846869928974 ) ) ;
#36055=VERTEX_POINT ( 'NONE', #15180 ) ;
#36064=( NAMED_UNIT ( * ) SI_UNIT ( $, .STERADIAN. ) SOLID_ANGLE_UNIT ( ) );
#36066=CIRCLE ( 'NONE', #96335, 10.00000000000000178 ) ;
#36074=CARTESIAN_POINT ( 'NONE',  ( 22.89314219808496986, 305.6227281603157167, 10.10461317236653400 ) ) ;
#36083=CARTESIAN_POINT ( 'NONE',  ( 31.33351735136876570, 438.6532904498233165, 22.86609632551569149 ) ) ;
#36089=CARTESIAN_POINT ( 'NONE',  ( -43.50250715914157240, 464.6389613228374742, 9.611700240009312779 ) ) ;
#36096=DIRECTION ( 'NONE',  ( 0.000000000000000000, 0.000000000000000000, 1.000000000000000000 ) ) ;
#36111=ORIENTED_EDGE ( 'NONE', *, *, #93065, .F. ) ;
#36116=EDGE_CURVE ( 'NONE', #942, #22950, #10968, .T. ) ;
#36126=CARTESIAN_POINT ( 'NONE',  ( -20.24579557674104890, 304.8297271373346575, -10.00469232190997282 ) ) ;
#36139=CARTESIAN_POINT ( 'NONE',  ( -27.19575328468113184, 307.3469062500455493, 10.97895680454243283 ) ) ;
#36145=CARTESIAN_POINT ( 'NONE',  ( 43.00000000000000000, 436.0987441542287115, 7.567257455462724991 ) ) ;
#36153=CARTESIAN_POINT ( 'NONE',  ( 9.797174393178803964E-16, 273.9999999999999432, 7.999999999999983125 ) ) ;
#36167=CARTESIAN_POINT ( 'NONE',  ( 9.482342435883346354, 294.6573797848125196, -3.183473687089551252 ) ) ;
#36168=CARTESIAN_POINT ( 'NONE',  ( 41.58649125062324003, 315.0454808444952732, -5.157136739135766312 ) ) ;
#36173=CARTESIAN_POINT ( 'NONE',  ( -19.36103579130787367, 294.6347466944262692, -10.04613669444748503 ) ) ;
#36174=ORIENTED_EDGE ( 'NONE', *, *, #24389, .F. ) ;
#36183=DIRECTION ( 'NONE',  ( -0.000000000000000000, -1.000000000000000000, -0.000000000000000000 ) ) ;
#36192=FACE_OUTER_BOUND ( 'NONE', #224, .T. ) ;
#36193=CARTESIAN_POINT ( 'NONE',  ( 39.82070819425764086, 460.7076632888625909, 2.105638695484907785 ) ) ;
#36194=CARTESIAN_POINT ( 'NONE',  ( -34.17998405129007722, 435.1836295971070285, 10.78820992711269788 ) ) ;
#36199=CARTESIAN_POINT ( 'NONE',  ( -43.60092683753732246, 434.9832283443418532, 14.46740323056809352 ) ) ;
#36220=ORIENTED_EDGE ( 'NONE', *, *, #28199, .F. ) ;
#36229=LINE ( 'NONE', #13480, #4742 ) ;
#36231=CARTESIAN_POINT ( 'NONE',  ( -19.70764564238371719, 304.7954121406193622, 9.925013215726785631 ) ) ;
#36255=CARTESIAN_POINT ( 'NONE',  ( -23.67370564920981124, 306.0413591249409819, 9.198534280147706355 ) ) ;
#36262=CARTESIAN_POINT ( 'NONE',  ( 36.16847030042395517, 438.2414514106960723, 3.889105687734257799 ) ) ;
#36266=B_SPLINE_CURVE_WITH_KNOTS ( 'NONE', 3,
 ( #49759, #57837, #26599, #40607, #98317, #66476, #41673, #67557, #99904, #1176, #58933, #75628, #89701, #57306 ),
 .UNSPECIFIED., .F., .F.,
 ( 4, 2, 2, 2, 2, 2, 4 ),
 ( 0.000000000000000000, 0.003030522498881887093, 0.004545783748322844951, 0.006061044997763803677, 0.007576306247204760667, 0.009091567496645719393, 0.01212208999552772531 ),
 .UNSPECIFIED. ) ;
#36300=DIRECTION ( 'NONE',  ( 0.2244612941943401052, 0.4655631424235968097, 0.8560771506267808029 ) ) ;
#36303=CARTESIAN_POINT ( 'NONE',  ( 17.66137975014545347, 294.6000572424684378, -10.05351037453485574 ) ) ;
#36316=CARTESIAN_POINT ( 'NONE',  ( 31.63611612624782410, 436.4523533804024851, 18.85849934886137191 ) ) ;
#36352=CARTESIAN_POINT ( 'NONE',  ( 46.00000000000000000, 488.0336798547363628, -0.8984331811833941028 ) ) ;
#36354=CARTESIAN_POINT ( 'NONE',  ( 43.41290683822506935, 487.0833545439620593, 7.569976829064905210 ) ) ;
#36380=CARTESIAN_POINT ( 'NONE',  ( -19.70764564238371719, 304.7954121406193622, 9.925013215726785631 ) ) ;
#36382=CARTESIAN_POINT ( 'NONE',  ( -44.24061507096541845, 485.5299576667499082, 3.142227259638529446 ) ) ;
#36387=CARTESIAN_POINT ( 'NONE',  ( 33.68177706158841289, 464.5004658938951252, 17.05886715805537790 ) ) ;
#36389=CARTESIAN_POINT ( 'NONE',  ( -36.69704126099654218, 379.5140801041114287, 5.019973760696065490 ) ) ;
#36412=ORIENTED_EDGE ( 'NONE', *, *, #44112, .T. ) ;
#36430=CARTESIAN_POINT ( 'NONE',  ( -43.58525529925911002, 435.7810014872756028, 17.82021598409041729 ) ) ;
#36432=CARTESIAN_POINT ( 'NONE',  ( 33.95156263172585653, 464.5083255208626838, 6.608064661821390295 ) ) ;
#36433=ORIENTED_EDGE ( 'NONE', *, *, #11079, .F. ) ;
#36436=DIRECTION ( 'NONE',  ( 0.9736964118527576817, 0.000000000000000000, 0.2278492869092748896 ) ) ;
#36451=CARTESIAN_POINT ( 'NONE',  ( -31.05728869196802222, 439.4224417574423569, 22.81104631550758555 ) ) ;
#36452=EDGE_CURVE ( 'NONE', #73090, #73065, #31644, .T. ) ;
#36453=SURFACE_SIDE_STYLE ('',( #2430 ) ) ;
#36463=CARTESIAN_POINT ( 'NONE',  ( -36.54584131692897131, 364.1367592788530487, 3.156418272699054395 ) ) ;
#36468=CARTESIAN_POINT ( 'NONE',  ( 45.40507512465600115, 439.2794387026467575, 6.273370203490043373 ) ) ;
#36479=CARTESIAN_POINT ( 'NONE',  ( 42.63769942292682202, 336.9641833527253425, 8.128834346956653079 ) ) ;
#36480=CARTESIAN_POINT ( 'NONE',  ( 43.69307663853744117, 464.9794299858319278, 8.444152807414981865 ) ) ;
#36484=FACE_OUTER_BOUND ( 'NONE', #66706, .T. ) ;
#36499=EDGE_CURVE ( 'NONE', #21601, #4872, #50466, .T. ) ;
#36513=ADVANCED_FACE ( 'NONE', ( #8424 ), #1986, .T. ) ;
#36516=CARTESIAN_POINT ( 'NONE',  ( -32.19467125704959187, 397.8372596365960021, 25.61661318660594944 ) ) ;
#36535=CARTESIAN_POINT ( 'NONE',  ( 22.71368435182198553, 303.3994564710546342, 10.05503188144461291 ) ) ;
#36538=ORIENTED_EDGE ( 'NONE', *, *, #43704, .T. ) ;
#36542=CARTESIAN_POINT ( 'NONE',  ( -30.38238271166500937, 438.0643985706049648, 22.32817737084010190 ) ) ;
#36554=CARTESIAN_POINT ( 'NONE',  ( 44.30168388726523432, 463.8374982934681725, 7.948620458287060764 ) ) ;
#36561=CARTESIAN_POINT ( 'NONE',  ( 35.32911723019127237, 437.0667969981781198, 5.602639083905786244 ) ) ;
#36574=CARTESIAN_POINT ( 'NONE',  ( -43.71217423904474231, 435.6632154632216043, 9.092528312227496912 ) ) ;
#36581=CARTESIAN_POINT ( 'NONE',  ( 41.14690903223204543, 485.7356601713281066, -4.640470638256346980 ) ) ;
#36584=CARTESIAN_POINT ( 'NONE',  ( -33.00000000000000000, 500.0000000000002274, -15.00000000000000711 ) ) ;
#36590=ADVANCED_FACE ( 'NONE', ( #71970 ), #17134, .F. ) ;
#36594=CARTESIAN_POINT ( 'NONE',  ( 43.75010090114224681, 464.8337800386878484, 11.75004750934975029 ) ) ;
#36604=CARTESIAN_POINT ( 'NONE',  ( 25.26398632472819727, 307.7598616557737046, 9.603387314540041686 ) ) ;
#36626=VERTEX_POINT ( 'NONE', #64938 ) ;
#36636=CARTESIAN_POINT ( 'NONE',  ( -32.89533925684112603, 465.6911419323517975, 10.83014164272533542 ) ) ;
#36653=CARTESIAN_POINT ( 'NONE',  ( 39.77617528725443208, 332.6151105793712190, 19.06785702275038119 ) ) ;
#36655=EDGE_CURVE ( 'NONE', #91003, #55140, #37306, .T. ) ;
#36657=CARTESIAN_POINT ( 'NONE',  ( -43.69860345152756764, 434.4324800463848533, 11.31831452736303945 ) ) ;
#36659=ORIENTED_EDGE ( 'NONE', *, *, #17401, .T. ) ;
#36662=CARTESIAN_POINT ( 'NONE',  ( -32.17889379758944557, 439.3695696554026426, 23.63219374846805820 ) ) ;
#36664=CARTESIAN_POINT ( 'NONE',  ( -29.57788238113521828, 311.1740376248832831, -7.528724879610501297 ) ) ;
#36666=CARTESIAN_POINT ( 'NONE',  ( -37.63844833726898997, 314.2537075340847537, 14.63743747242352278 ) ) ;
#36674=CARTESIAN_POINT ( 'NONE',  ( 42.68083702883374997, 436.2686870323771018, 7.148029379848829912 ) ) ;
#36676=VERTEX_POINT ( 'NONE', #48207 ) ;
#36686=( BOUNDED_SURFACE ( )  B_SPLINE_SURFACE ( 3, 2, ( 
 ( #29159, #4300, #86308 ),
 ( #78185, #53901, #37235 ),
 ( #44778, #70096, #62033 ),
 ( #18932, #2151, #51773 ) ),
 .UNSPECIFIED., .F., .F., .F. ) 
 B_SPLINE_SURFACE_WITH_KNOTS ( ( 4, 4 ),
 ( 3, 3 ),
 ( 0.05563112469177167174, 0.08036552975359016748 ),
 ( 0.000000000000000000, 0.6299180559300312510 ),
 .UNSPECIFIED. ) 
 GEOMETRIC_REPRESENTATION_ITEM ( )  RATIONAL_B_SPLINE_SURFACE ( (
 ( 1.000000000000000000, 0.8155016482959264179, 0.8634409826473032901),
 ( 1.000000000000000000, 0.8155019398125198382, 0.8634411984173584464),
 ( 1.000000000000000000, 0.8155018685912485132, 0.8634411457019453007),
 ( 1.000000000000000000, 0.8155015759137222986, 0.8634409290726094977) ) ) 
 REPRESENTATION_ITEM ( '' )  SURFACE ( )  );
#36695=CARTESIAN_POINT ( 'NONE',  ( 3.610928089892441850, 295.9072949364349938, -10.00534087566975572 ) ) ;
#36696=CARTESIAN_POINT ( 'NONE',  ( 43.29658055318886767, 324.1952503670673877, -2.852919881210743913 ) ) ;
#36701=CARTESIAN_POINT ( 'NONE',  ( -20.97754405179127346, 294.8763868968453608, 9.942224931492237516 ) ) ;
#36705=CARTESIAN_POINT ( 'NONE',  ( 46.00000000000000711, 488.0081391511161542, -0.5582540307957969405 ) ) ;
#36712=CARTESIAN_POINT ( 'NONE',  ( 9.994386960703202760, 294.6428459689212787, -0.7381326186433831982 ) ) ;
#36714=AXIS2_PLACEMENT_3D ( 'NONE', #79965, #72413, #5035 ) ;
#36723=CARTESIAN_POINT ( 'NONE',  ( 11.71694229689447297, 294.5934945994754912, 1.882065127989447584 ) ) ;
#36724=CARTESIAN_POINT ( 'NONE',  ( 44.14911905790283697, 464.3766534542007207, 9.623404994951284763 ) ) ;
#36727=ORIENTED_EDGE ( 'NONE', *, *, #77843, .F. ) ;
#36749=ORIENTED_EDGE ( 'NONE', *, *, #53413, .T. ) ;
#36757=DIRECTION ( 'NONE',  ( -1.000000000000000000, 0.000000000000000000, 0.000000000000000000 ) ) ;
#36761=CARTESIAN_POINT ( 'NONE',  ( -31.14694070047868735, 432.3293837220155069, 24.29762062537629319 ) ) ;
#36762=CARTESIAN_POINT ( 'NONE',  ( 21.25502769577498796, 305.0480251235313176, 9.978840188629131802 ) ) ;
#36769=CARTESIAN_POINT ( 'NONE',  ( -32.80551872593229490, 486.0171861992463960, 5.671217483525994751 ) ) ;
#36781=CARTESIAN_POINT ( 'NONE',  ( 33.16759796689489548, 434.2047070568555114, 15.25549030506044801 ) ) ;
#36793=CARTESIAN_POINT ( 'NONE',  ( 39.21279148650069146, 436.8435004666158079, 5.150741822288956051 ) ) ;
#36801=CARTESIAN_POINT ( 'NONE',  ( -42.18756898894582719, 484.4522853017719513, -2.425645685620470449 ) ) ;
#36804=FACE_OUTER_BOUND ( 'NONE', #71072, .T. ) ;
#36827=CARTESIAN_POINT ( 'NONE',  ( 39.13466327773082298, 485.8437493838399632, -4.960055907050037405 ) ) ;
#36845=CARTESIAN_POINT ( 'NONE',  ( 16.01635194906463866, 304.5593466744471698, -9.062162209746613684 ) ) ;
#36900=CARTESIAN_POINT ( 'NONE',  ( -20.36049642833716078, 294.7627513888867838, -10.01892845649183350 ) ) ;
#36907=CARTESIAN_POINT ( 'NONE',  ( -35.49529570007158696, 379.4505083648772938, 5.762799703950255648 ) ) ;
#36927=EDGE_CURVE ( 'NONE', #26711, #31406, #6286, .T. ) ;
#36944=CARTESIAN_POINT ( 'NONE',  ( 20.37278541768183615, 303.8378246129572631, -10.00297115033342266 ) ) ;
#36948=DIRECTION ( 'NONE',  ( 0.000000000000000000, -0.9109553866900513830, 0.4125048890139109137 ) ) ;
#36975=CARTESIAN_POINT ( 'NONE',  ( 36.74066248129624057, 397.0785584018862551, 6.179803345696205596 ) ) ;
#36977=ADVANCED_FACE ( 'NONE', ( #6554 ), #90697, .T. ) ;
#36986=VERTEX_POINT ( 'NONE', #25454 ) ;
#36987=CARTESIAN_POINT ( 'NONE',  ( 25.56253568781137986, 295.7864503539771022, -1.799098680748292045 ) ) ;
#36990=CARTESIAN_POINT ( 'NONE',  ( -32.05241217996611169, 487.5077369493866399, 9.813907492591894766 ) ) ;
#36999=AXIS2_PLACEMENT_3D ( 'NONE', #83389, #18151, #10035 ) ;
#37000=CARTESIAN_POINT ( 'NONE',  ( 37.00921004089878608, 345.1628843254408139, 0.03558237527558635871 ) ) ;
#37005=CARTESIAN_POINT ( 'NONE',  ( 31.39297415328601915, 438.8543991500256993, 23.05892055662082996 ) ) ;
#37020=EDGE_CURVE ( 'NONE', #51812, #942, #23310, .T. ) ;
#37025=CARTESIAN_POINT ( 'NONE',  ( -43.69871659247020546, 464.4396234996537487, 7.060974336457711331 ) ) ;
#37049=ORIENTED_EDGE ( 'NONE', *, *, #70960, .F. ) ;
#37055=CARTESIAN_POINT ( 'NONE',  ( -32.82691535583477105, 485.1045372766795367, 1.724905475514941999 ) ) ;
#37056=CARTESIAN_POINT ( 'NONE',  ( 28.98483177930387811, 297.3119720135404123, 2.475370038500326331 ) ) ;
#37060=ORIENTED_EDGE ( 'NONE', *, *, #17966, .F. ) ;
#37074=CARTESIAN_POINT ( 'NONE',  ( 0.000000000000000000, -19.99999999999998934, 0.000000000000000000 ) ) ;
#37094=CARTESIAN_POINT ( 'NONE',  ( 20.24579557674103469, 304.8297271373346575, -10.00469232190998525 ) ) ;
#37096=CARTESIAN_POINT ( 'NONE',  ( 30.00000000000000000, 500.0000000000002274, 0.000000000000000000 ) ) ;
#37110=CARTESIAN_POINT ( 'NONE',  ( 40.05546360247942772, 485.1954875884470084, -4.343530646189435629 ) ) ;
#37119=DIRECTION ( 'NONE',  ( 1.000000000000000000, 0.000000000000000000, -1.224646799147353207E-16 ) ) ;
#37127=CARTESIAN_POINT ( 'NONE',  ( 24.51862614704669596, 305.4800964025654366, 10.29769302249151863 ) ) ;
#37142=ORIENTED_EDGE ( 'NONE', *, *, #84767, .F. ) ;
#37147=CARTESIAN_POINT ( 'NONE',  ( 38.83413156601710625, 459.9242647137448898, 1.954013010003052830 ) ) ;
#37164=ORIENTED_EDGE ( 'NONE', *, *, #51619, .F. ) ;
#37168=CARTESIAN_POINT ( 'NONE',  ( -46.00000000000001421, 460.3161862120084606, 7.035773190462103699 ) ) ;
#37178=CARTESIAN_POINT ( 'NONE',  ( 41.96737725787325957, 484.5368175928538221, -2.772775517607982465 ) ) ;
#37188=CARTESIAN_POINT ( 'NONE',  ( -30.72562631177394010, 313.8450617825646987, -6.865185343166496423 ) ) ;
#37189=CARTESIAN_POINT ( 'NONE',  ( -36.83858993814808969, 310.7308067699071330, 13.74755661074275004 ) ) ;
#37197=DIRECTION ( 'NONE',  ( -1.000000000000000000, 0.000000000000000000, 0.000000000000000000 ) ) ;
#37201=DIRECTION ( 'NONE',  ( 0.000000000000000000, 0.9900230405585784821, 0.1409055682474875948 ) ) ;
#37212=CARTESIAN_POINT ( 'NONE',  ( 6.618938675379662406, 296.2345938571221495, -10.01875627917898548 ) ) ;
#37215=CARTESIAN_POINT ( 'NONE',  ( -20.25105829892553899, 294.7694562253329877, 1.919496115618561261 ) ) ;
#37221=CARTESIAN_POINT ( 'NONE',  ( -46.00000000000000000, 461.9428920847520317, 12.03309428281920113 ) ) ;
#37235=CARTESIAN_POINT ( 'NONE',  ( -41.45706733914236253, 469.3213988105399608, 0.9913809832463575944 ) ) ;
#37259=DIRECTION ( 'NONE',  ( 5.178224577996835961E-15, 0.3241911592372989093, 0.9459915920727711702 ) ) ;
#37262=CARTESIAN_POINT ( 'NONE',  ( 44.12585837658421895, 464.4133740036029963, 9.756218680429697088 ) ) ;
#37267=ADVANCED_FACE ( 'NONE', ( #94420 ), #37799, .T. ) ;
#37271=VERTEX_POINT ( 'NONE', #54979 ) ;
#37281=CARTESIAN_POINT ( 'NONE',  ( 25.93947128054312756, 296.0094280503604978, 10.18659011856751384 ) ) ;
#37284=CARTESIAN_POINT ( 'NONE',  ( -35.76379064120181539, 307.0162303970107587, 12.81051142610679960 ) ) ;
#37305=FACE_OUTER_BOUND ( 'NONE', #19313, .T. ) ;
#37306=CIRCLE ( 'NONE', #90620, 2.999999999999999112 ) ;
#37311=( BOUNDED_SURFACE ( )  B_SPLINE_SURFACE ( 3, 2, ( 
 ( #9439, #42898, #791 ),
 ( #67185, #75792, #52041 ),
 ( #1887, #42358, #92501 ),
 ( #10519, #43435, #76315 ) ),
 .UNSPECIFIED., .F., .F., .F. ) 
 B_SPLINE_SURFACE_WITH_KNOTS ( ( 4, 4 ),
 ( 3, 3 ),
 ( -1.734723475976807094E-17, 0.002491432948283776611 ),
 ( 0.000000000000000000, 1.000000000000000000 ),
 .UNSPECIFIED. ) 
 GEOMETRIC_REPRESENTATION_ITEM ( )  RATIONAL_B_SPLINE_SURFACE ( (
 ( 1.000000000000000000, 0.7978714159193172062, 1.000000000000000000),
 ( 1.000000000000000000, 0.8097755972627500576, 1.000000000000000000),
 ( 1.000000000000000000, 0.8213938805860364623, 1.000000000000000000),
 ( 1.000000000000000000, 0.8328393170029456671, 1.000000000000000000) ) ) 
 REPRESENTATION_ITEM ( '' )  SURFACE ( )  );
#37329=CARTESIAN_POINT ( 'NONE',  ( -33.74362713068849473, 463.9326864247044000, 7.533159870298644201 ) ) ;
#37348=CARTESIAN_POINT ( 'NONE',  ( -43.00000000000000000, 450.0000000000002274, 13.20242257375370976 ) ) ;
#37356=CARTESIAN_POINT ( 'NONE',  ( -34.99298670164664316, 490.1714394129022594, 12.08179005326680056 ) ) ;
#37363=CARTESIAN_POINT ( 'NONE',  ( -34.68490551324229898, 463.9993046474211837, 18.60480341025478523 ) ) ;
#37364=CIRCLE ( 'NONE', #58018, 5.000000000000001776 ) ;
#37403=CARTESIAN_POINT ( 'NONE',  ( -33.95156263172587785, 464.5083255208627406, 6.608064661821428487 ) ) ;
#37412=CARTESIAN_POINT ( 'NONE',  ( -30.00000000000000000, 450.0000000000002274, 13.20242257375370976 ) ) ;
#37422=CARTESIAN_POINT ( 'NONE',  ( 33.00000000000000000, 500.0000000000002274, -12.00000000000000711 ) ) ;
#37428=CARTESIAN_POINT ( 'NONE',  ( -43.03265099499957813, 484.2747968070553384, -0.8099405866661226749 ) ) ;
#37446=CARTESIAN_POINT ( 'NONE',  ( 33.00000000000000000, 464.3970849722209095, 17.41240408234224191 ) ) ;
#37455=CARTESIAN_POINT ( 'NONE',  ( 0.000000000000000000, 304.8518027762758038, 8.936999415352287812 ) ) ;
#37457=ADVANCED_FACE ( 'NONE', ( #40936 ), #6643, .F. ) ;
#37472=AXIS2_PLACEMENT_3D ( 'NONE', #11590, #66792, #78463 ) ;
#37492=CARTESIAN_POINT ( 'NONE',  ( -40.60713025163710910, 436.1947416310474068, 6.060763751012204992 ) ) ;
#37513=CARTESIAN_POINT ( 'NONE',  ( 34.02514208821929032, 329.8602221817346276, -3.866232146452765139 ) ) ;
#37536=CARTESIAN_POINT ( 'NONE',  ( 44.33761176843466956, 336.2903648585140672, 0.003362554233744022205 ) ) ;
#37539=CARTESIAN_POINT ( 'NONE',  ( -6.953930663124324063, 304.7325910270068334, -10.02533923955978779 ) ) ;
#37549=CARTESIAN_POINT ( 'NONE',  ( -34.38981283644526599, 463.7396323591523242, 19.22682496774974226 ) ) ;
#37558=B_SPLINE_CURVE_WITH_KNOTS ( 'NONE', 3,
 ( #100428, #77762, #3875, #43790, #21677, #62133, #63175, #22734, #5971, #38902, #80391, #6500, #55573, #95023, #22200, #86928, #20645, #96069, #30287, #5461, #62647, #4397, #13535, #70195, #21160, #95531, #55051, #38384, #103103, #71245, #70727, #53987, #14586, #29252, #78804, #45403, #72312, #103621, #54511, #87981, #29769, #46966, #104143, #87455, #14061, #30829, #46452, #79864 ),
 .UNSPECIFIED., .F., .F.,
 ( 4, 2, 2, 2, 2, 2, 2, 2, 2, 2, 2, 2, 2, 2, 2, 2, 2, 2, 2, 2, 2, 2, 2, 4 ),
 ( -6.000000001300036219E-08, 0.001124634766771550340, 0.002249329533543113768, 0.003374024300314676979, 0.004498719067086241058, 0.006748108600629357939, 0.007872803367400916380, 0.008997498134172474821, 0.01124688766771547895, 0.01349627720125848480, 0.01799505626834449479, 0.02024444580188758044, 0.02249383533543066610, 0.02699261440251668129, 0.03149139346960269648, 0.03599017253668870819, 0.04498773067086057204, 0.05398528880503244282, 0.07198040507337616356, 0.08097796320754802046, 0.08997552134171989124, 0.1079706376100636189, 0.1259657538784073327, 0.1439608701467510743 ),
 .UNSPECIFIED. ) ;
#37567=ORIENTED_EDGE ( 'NONE', *, *, #80933, .T. ) ;
#37582=CARTESIAN_POINT ( 'NONE',  ( 9.797174393178809880E-16, 274.9999999999999432, 7.999999999999986677 ) ) ;
#37588=AXIS2_PLACEMENT_3D ( 'NONE', #66833, #25893, #25335 ) ;
#37591=VERTEX_POINT ( 'NONE', #61394 ) ;
#37595=CARTESIAN_POINT ( 'NONE',  ( 24.83179908432460081, 295.6082205264385721, 2.099364176556762995 ) ) ;
#37596=CARTESIAN_POINT ( 'NONE',  ( 8.844474929605143032, 302.6213362138051934, -10.03676381922342564 ) ) ;
#37598=CIRCLE ( 'NONE', #97813, 7.999999999999989342 ) ;
#37603=CARTESIAN_POINT ( 'NONE',  ( -38.38188837495462735, 437.9257690784074839, 4.300778830038868961 ) ) ;
#37608=CARTESIAN_POINT ( 'NONE',  ( 43.64531880380447149, 464.9151967207193366, 12.30391130301436142 ) ) ;
#37610=AXIS2_PLACEMENT_3D ( 'NONE', #83256, #91884, #92945 ) ;
#37612=CARTESIAN_POINT ( 'NONE',  ( -18.00000000000001421, -20.00000000000001776, 9.000000000000008882 ) ) ;
#37620=CARTESIAN_POINT ( 'NONE',  ( -43.03265099499981972, 484.2747968070553952, -0.8099405866661884001 ) ) ;
#37622=CARTESIAN_POINT ( 'NONE',  ( 34.99225395455989940, 435.2420463162160900, 7.288472211092408060 ) ) ;
#37630=EDGE_CURVE ( 'NONE', #69611, #75902, #71811, .T. ) ;
#37654=CARTESIAN_POINT ( 'NONE',  ( -35.96492786661492858, 302.4488314805894902, -8.278427239162008178 ) ) ;
#37655=ORIENTED_EDGE ( 'NONE', *, *, #40858, .T. ) ;
#37673=CARTESIAN_POINT ( 'NONE',  ( -20.37278541768183615, 303.8378246129572631, -10.00297115033342266 ) ) ;
#37700=EDGE_CURVE ( 'NONE', #48471, #2695, #98276, .T. ) ;
#37702=ORIENTED_EDGE ( 'NONE', *, *, #44672, .T. ) ;
#37718=CARTESIAN_POINT ( 'NONE',  ( -42.88690404150482038, 465.8389234274137607, 12.02232841050726897 ) ) ;
#37725=CARTESIAN_POINT ( 'NONE',  ( -38.26552733536168915, 461.1050587587353107, 2.389481650175799832 ) ) ;
#37727=B_SPLINE_CURVE_WITH_KNOTS ( 'NONE', 3,
 ( #48587, #11, #95191, #39990, #86582, #106288, #16227, #81475, #5110, #65849 ),
 .UNSPECIFIED., .F., .F.,
 ( 4, 2, 2, 2, 4 ),
 ( 5.679895013065603427E-17, 0.002488089381717967750, 0.003110111727147444292, 0.003732134072576921702, 0.004976178763435875653 ),
 .UNSPECIFIED. ) ;
#37731=CARTESIAN_POINT ( 'NONE',  ( -38.19214260828640306, 317.3320220044833491, 15.41122486417729931 ) ) ;
#37751=AXIS2_PLACEMENT_3D ( 'NONE', #60272, #25801, #52136 ) ;
#37752=CARTESIAN_POINT ( 'NONE',  ( 42.61862771095000824, 462.7773917227530092, 13.89716710540371736 ) ) ;
#37755=CARTESIAN_POINT ( 'NONE',  ( 42.01176354208753594, 328.3689192229740001, 6.166223753866878710 ) ) ;
#37784=ORIENTED_EDGE ( 'NONE', *, *, #27851, .F. ) ;
#37793=DIRECTION ( 'NONE',  ( 0.000000000000000000, -0.9459915920727718364, 0.3241911592372968554 ) ) ;
#37799=CYLINDRICAL_SURFACE ( 'NONE', #40791, 15.00000000000000711 ) ;
#37807=CARTESIAN_POINT ( 'NONE',  ( 43.87115969799069148, 464.7386531662421589, 11.09928998703298397 ) ) ;
#37818=CARTESIAN_POINT ( 'NONE',  ( 32.35336999986095208, 300.6590557721156642, 11.25190399080426751 ) ) ;
#37823=DIRECTION ( 'NONE',  ( 0.000000000000000000, -0.9405207353770878020, 0.3397362893859623423 ) ) ;
#37838=CARTESIAN_POINT ( 'NONE',  ( -33.51637563653506646, 434.0198191192274066, 13.77959778571810290 ) ) ;
#37839=CARTESIAN_POINT ( 'NONE',  ( -33.38504658724071561, 488.8572893497079122, 10.16177171491941422 ) ) ;
#37840=CARTESIAN_POINT ( 'NONE',  ( -32.21290004233181037, 485.9817488812122406, 5.040586218662800988 ) ) ;
#37846=CARTESIAN_POINT ( 'NONE',  ( -34.60124782188066206, 301.9306886739316838, -0.3923369183991654574 ) ) ;
#37854=CARTESIAN_POINT ( 'NONE',  ( 43.51084452654469459, 465.2903130129626561, 9.421687747985401984 ) ) ;
#37860=CARTESIAN_POINT ( 'NONE',  ( 30.00000000000000000, 461.8163627757383551, 11.11111419091032460 ) ) ;
#37863=ORIENTED_EDGE ( 'NONE', *, *, #98299, .T. ) ;
#37865=CARTESIAN_POINT ( 'NONE',  ( -44.27202126170846697, 463.8287145583149709, 7.882879088893235853 ) ) ;
#37866=CARTESIAN_POINT ( 'NONE',  ( -38.13233550252180493, 438.4599495265808855, 23.49086985287510743 ) ) ;
#37879=CARTESIAN_POINT ( 'NONE',  ( -43.50721599125494521, 484.7945671711814271, 4.126833950652403438 ) ) ;
#37884=CARTESIAN_POINT ( 'NONE',  ( -38.47428897411860760, 484.8307741943502833, -5.088672563356786860 ) ) ;
#37893=DIRECTION ( 'NONE',  ( -1.000000000000000000, 0.000000000000000000, 0.000000000000000000 ) ) ;
#37895=CARTESIAN_POINT ( 'NONE',  ( -34.15253942429701084, 465.0582672257402805, 17.72214182034827346 ) ) ;
#37896=ORIENTED_EDGE ( 'NONE', *, *, #41302, .F. ) ;
#37915=B_SPLINE_CURVE_WITH_KNOTS ( 'NONE', 3,
 ( #63290, #73470, #96190, #22320, #55165, #14174, #47078, #30946, #96713, #22849, #49738, #24964, #57819, #9799, #76667, #33580, #76137, #25510, #99887, #34664, #67004, #65931, #617, #1711, #58366, #92317, #91287, #34130, #26058, #17396, #67537, #90742, #16858, #82647, #59995, #10338, #33061, #75065, #58914, #42716, #91808, #19021, #66459, #1158, #17929, #75611, #50271, #50782, #99335, #100417 ),
 .UNSPECIFIED., .F., .F.,
 ( 4, 2, 2, 2, 2, 2, 2, 2, 2, 2, 2, 2, 2, 2, 2, 2, 2, 2, 2, 2, 2, 2, 2, 2, 4 ),
 ( 0.0002970904109619049312, 0.009133031734025364584, 0.01796897305708882245, 0.03564085570321574165, 0.05331273834934266431, 0.07098462099546958004, 0.08865650364159649577, 0.09749244496466002996, 0.1063283862877235642, 0.1107463569492554284, 0.1151643276107872926, 0.1195822982723191430, 0.1240002689338510072, 0.1284182395953828437, 0.1306272249261486995, 0.1328362102569145553, 0.1339407029222974832, 0.1350451955876804111, 0.1361496882530633390, 0.1372541809184462669, 0.1383586735838292225, 0.1394631662492121504, 0.1405676589145950783, 0.1411199052472865145, 0.1416721515799779785 ),
 .UNSPECIFIED. ) ;
#37916=CARTESIAN_POINT ( 'NONE',  ( 33.82591814952031939, 464.6968131430474500, 6.992934999028691756 ) ) ;
#37951=CARTESIAN_POINT ( 'NONE',  ( -43.63597198433378566, 421.7854419661105112, 15.67568856678759204 ) ) ;
#37952=CARTESIAN_POINT ( 'NONE',  ( 32.73643714039037889, 313.1396241591655212, -7.563205551003425064 ) ) ;
#37953=VECTOR ( 'NONE', #79352, 1000.000000000000114 ) ;
#37963=DIRECTION ( 'NONE',  ( 0.000000000000000000, 0.000000000000000000, -1.000000000000000000 ) ) ;
#37972=B_SPLINE_CURVE_WITH_KNOTS ( 'NONE', 3,
 ( #86021, #45549, #79489, #20785 ),
 .UNSPECIFIED., .F., .F.,
 ( 4, 4 ),
 ( 1.734723475976807094E-18, 0.001327912649060388655 ),
 .UNSPECIFIED. ) ;
#37974=DIRECTION ( 'NONE',  ( -0.000000000000000000, 1.000000000000000000, -0.000000000000000000 ) ) ;
#37986=AXIS2_PLACEMENT_3D ( 'NONE', #37884, #54527, #101521 ) ;
#37987=CARTESIAN_POINT ( 'NONE',  ( -44.24141271893151384, 485.5284546383997508, 3.135518353093314392 ) ) ;
#37996=VERTEX_POINT ( 'NONE', #101043 ) ;
#38009=AXIS2_PLACEMENT_3D ( 'NONE', #69055, #51235, #20008 ) ;
#38012=CARTESIAN_POINT ( 'NONE',  ( -46.00000000000000000, 488.9831568219306064, 4.757012338623855641 ) ) ;
#38025=ORIENTED_EDGE ( 'NONE', *, *, #46714, .F. ) ;
#38030=CARTESIAN_POINT ( 'NONE',  ( 32.93513049338658760, 465.6726574193327792, 10.66039033145146142 ) ) ;
#38035=CARTESIAN_POINT ( 'NONE',  ( -32.17608548772882671, 486.0066403424740997, 5.076835838891838648 ) ) ;
#38039=ORIENTED_EDGE ( 'NONE', *, *, #28328, .F. ) ;
#38040=CARTESIAN_POINT ( 'NONE',  ( 35.75530239586758796, 408.8884727095264111, 6.061804817591524674 ) ) ;
#38046=B_SPLINE_CURVE_WITH_KNOTS ( 'NONE', 3,
 ( #89961, #40344, #88900, #65685, #95536, #14998 ),
 .UNSPECIFIED., .F., .F.,
 ( 4, 1, 1, 4 ),
 ( 0.000000000000000000, 0.4213833399777465738, 0.5213833399777465516, 0.9843640123765010630 ),
 .UNSPECIFIED. ) ;
#38049=CARTESIAN_POINT ( 'NONE',  ( -43.49620567743568955, 471.8615734360724332, 7.936790638083616400 ) ) ;
#38056=CARTESIAN_POINT ( 'NONE',  ( -32.62734573167237073, 485.2399387473970478, 2.793905986283565568 ) ) ;
#38065=CARTESIAN_POINT ( 'NONE',  ( 37.66863543806578463, 305.0556223276453807, -7.649085916423524090 ) ) ;
#38070=CARTESIAN_POINT ( 'NONE',  ( 31.95183731899507862, 438.9709496923862844, 23.61699702108921528 ) ) ;
#38079=AXIS2_PLACEMENT_3D ( 'NONE', #77589, #34509, #43618 ) ;
#38080=CARTESIAN_POINT ( 'NONE',  ( -37.72536826884616090, 463.3861702155473381, 19.97111768659724973 ) ) ;
#38081=ORIENTED_EDGE ( 'NONE', *, *, #60495, .T. ) ;
#38098=CARTESIAN_POINT ( 'NONE',  ( 44.08840282922849241, 485.7747746244180007, 4.178803824087734320 ) ) ;
#38118=B_SPLINE_CURVE_WITH_KNOTS ( 'NONE', 3,
 ( #72548, #16438, #23501, #31077, #48787, #7802, #105453, #40710, #97886, #73059, #14836, #14301, #15375, #63956, #31594, #73598, #96842, #22971, #32111, #55295 ),
 .UNSPECIFIED., .F., .F.,
 ( 4, 2, 2, 2, 2, 2, 2, 2, 2, 4 ),
 ( 0.000000000000000000, 0.001397185393360531221, 0.002095778090040806806, 0.002794370786721082391, 0.004191556180081631826, 0.005588741573442182128, 0.006985926966802732431, 0.008383112360163280999, 0.009780297753523832169, 0.01117748314688438160 ),
 .UNSPECIFIED. ) ;
#38121=DIRECTION ( 'NONE',  ( 0.9077394194975960673, 0.1875825441113498915, -0.3752624887127422038 ) ) ;
#38126=CARTESIAN_POINT ( 'NONE',  ( 38.54943464502932926, 464.3877170423162397, 18.94545795437182178 ) ) ;
#38128=CARTESIAN_POINT ( 'NONE',  ( -39.84523985364283050, 437.5033382181499633, 4.901783744328629844 ) ) ;
#38129=DIRECTION ( 'NONE',  ( 0.1792365085106985001, 0.7133058216310638189, 0.6775463665640362176 ) ) ;
#38134=DIRECTION ( 'NONE',  ( 0.9738156377458878632, 0.000000000000000000, -0.2273391820201038915 ) ) ;
#38145=CARTESIAN_POINT ( 'NONE',  ( 19.02088688056375787, 303.6992897676895495, 9.904581773955044355 ) ) ;
#38162=CARTESIAN_POINT ( 'NONE',  ( 41.50869271557970563, 485.4378639541095595, -3.633045570236669519 ) ) ;
#38163=CARTESIAN_POINT ( 'NONE',  ( 33.21102376836596193, 438.9613914113129454, 23.92328486949907784 ) ) ;
#38178=CARTESIAN_POINT ( 'NONE',  ( -36.91281931599076671, 303.7809130842520631, -7.959270006439831846 ) ) ;
#38186=CARTESIAN_POINT ( 'NONE',  ( -26.26318723337799454, 307.7053845768774067, 10.82856312047318426 ) ) ;
#38189=CARTESIAN_POINT ( 'NONE',  ( -40.21603221112191306, 460.7694907478774553, 2.143794914364798743 ) ) ;
#38207=CARTESIAN_POINT ( 'NONE',  ( 36.56554981725791720, 437.5759650626826556, 4.257361216054158071 ) ) ;
#38209=ORIENTED_EDGE ( 'NONE', *, *, #7559, .T. ) ;
#38234=CARTESIAN_POINT ( 'NONE',  ( 42.75526354329229406, 382.2722604821533992, 18.98976758742777804 ) ) ;
#38239=FACE_OUTER_BOUND ( 'NONE', #35520, .T. ) ;
#38242=ORIENTED_EDGE ( 'NONE', *, *, #106429, .T. ) ;
#38244=CARTESIAN_POINT ( 'NONE',  ( -37.72254196851303476, 461.3702377715575835, 2.610691308934373289 ) ) ;
#38248=CARTESIAN_POINT ( 'NONE',  ( -35.22718675236506414, 303.5445495247209919, 3.938089295098547549 ) ) ;
#38249=CARTESIAN_POINT ( 'NONE',  ( 20.49977525862259142, 302.8459220885798686, -10.00124997875687427 ) ) ;
#38253=ADVANCED_FACE ( 'NONE', ( #83653 ), #7506, .F. ) ;
#38256=ORIENTED_EDGE ( 'NONE', *, *, #11495, .F. ) ;
#38258=EDGE_CURVE ( 'NONE', #21702, #85790, #94263, .T. ) ;
#38263=CARTESIAN_POINT ( 'NONE',  ( 42.59614121018028499, 472.7198067255873184, 11.67823714611269104 ) ) ;
#38268=AXIS2_PLACEMENT_3D ( 'NONE', #69081, #45855, #87388 ) ;
#38275=CARTESIAN_POINT ( 'NONE',  ( 42.51080986292980413, 487.1495428172316906, 7.889844863796903418 ) ) ;
#38277=CARTESIAN_POINT ( 'NONE',  ( 43.47475788941068942, 362.3245890593326521, 12.84241293556198649 ) ) ;
#38278=CARTESIAN_POINT ( 'NONE',  ( -17.41231411112303107, 294.5863894558068523, 1.881106854385071303 ) ) ;
#38279=DIRECTION ( 'NONE',  ( 0.000000000000000000, 0.000000000000000000, 1.000000000000000000 ) ) ;
#38287=ORIENTED_EDGE ( 'NONE', *, *, #29291, .F. ) ;
#38307=EDGE_LOOP ( 'NONE', ( #19353, #6998, #17946, #89506 ) ) ;
#38320=AXIS2_PLACEMENT_3D ( 'NONE', #80151, #48831, #7848 ) ;
#38332=CARTESIAN_POINT ( 'NONE',  ( -42.48192783572968523, 485.4100919824712719, -3.499593777785077631 ) ) ;
#38336=CARTESIAN_POINT ( 'NONE',  ( -40.73878143178837519, 486.4834083601638213, 16.46716573231486436 ) ) ;
#38347=CARTESIAN_POINT ( 'NONE',  ( 33.00000000000000000, 439.7597899781497972, 24.16317522621304192 ) ) ;
#38357=FACE_OUTER_BOUND ( 'NONE', #16112, .T. ) ;
#38363=CARTESIAN_POINT ( 'NONE',  ( -30.10228782825764426, 308.0113986215986870, -8.824383475263772425 ) ) ;
#38369=DIRECTION ( 'NONE',  ( 0.000000000000000000, 0.000000000000000000, 1.000000000000000000 ) ) ;
#38381=CARTESIAN_POINT ( 'NONE',  ( -41.50820411079202188, 461.5963371455320612, 2.703439750996428081 ) ) ;
#38382=EDGE_LOOP ( 'NONE', ( #53950, #76863, #12378, #21178 ) ) ;
#38384=CARTESIAN_POINT ( 'NONE',  ( -35.21460518038509235, 323.6916001596177352, -4.906611162513216051 ) ) ;
#38386=DIRECTION ( 'NONE',  ( -0.000000000000000000, -1.000000000000000000, -0.000000000000000000 ) ) ;
#38392=CARTESIAN_POINT ( 'NONE',  ( -6.342436232120165052, 297.2558017715909386, 7.735853733431446777 ) ) ;
#38399=CARTESIAN_POINT ( 'NONE',  ( 16.03995343662826656, 302.5635438422187917, -10.06125143394410237 ) ) ;
#38408=ORIENTED_EDGE ( 'NONE', *, *, #25287, .F. ) ;
#38414=EDGE_CURVE ( 'NONE', #90133, #15190, #96934, .T. ) ;
#38419=UNCERTAINTY_MEASURE_WITH_UNIT (LENGTH_MEASURE( 1.000000000000000082E-05 ), #31035, 'distance_accuracy_value', 'NONE');
#38423=CARTESIAN_POINT ( 'NONE',  ( 44.03570364123596192, 435.3116947630522873, 15.43179346459484513 ) ) ;
#38434=CARTESIAN_POINT ( 'NONE',  ( -3.339336928304093011, 304.8518027742523486, 9.936999414809044140 ) ) ;
#38447=CARTESIAN_POINT ( 'NONE',  ( 43.00000000000000000, 500.0000000000002274, 12.00000000000000711 ) ) ;
#38461=CARTESIAN_POINT ( 'NONE',  ( -34.12349128637492157, 490.8027302422244134, 11.84948222508912252 ) ) ;
#38462=CARTESIAN_POINT ( 'NONE',  ( -38.79167372577270356, 310.2940712511280026, 1.667255102746370454 ) ) ;
#38463=CARTESIAN_POINT ( 'NONE',  ( 26.21593877366845504, 304.5184713299540817, -9.636447512346801858 ) ) ;
#38472=VERTEX_POINT ( 'NONE', #50375 ) ;
#38474=CARTESIAN_POINT ( 'NONE',  ( 45.29905483860081716, 480.9466865490944656, -2.171671249451534003 ) ) ;
#38480=CARTESIAN_POINT ( 'NONE',  ( -44.00013453485239268, 465.7974093566494957, 11.65569858486088606 ) ) ;
#38496=CIRCLE ( 'NONE', #74635, 0.9999999999999742428 ) ;
#38498=DIRECTION ( 'NONE',  ( 0.8400944247696998657, 0.000000000000000000, 0.5424401879201679044 ) ) ;
#38500=VERTEX_POINT ( 'NONE', #18047 ) ;
#38504=EDGE_CURVE ( 'NONE', #68326, #17636, #45368, .T. ) ;
#38506=ORIENTED_EDGE ( 'NONE', *, *, #37020, .T. ) ;
#38512=CARTESIAN_POINT ( 'NONE',  ( 21.19348424345039206, 294.8901562694577478, 1.945151701991080673 ) ) ;
#38551=CARTESIAN_POINT ( 'NONE',  ( 32.65439066521594924, 316.1413580166883435, -7.048974138691598945 ) ) ;
#38556=CARTESIAN_POINT ( 'NONE',  ( -30.22241138358163326, 310.0030499099321446, -8.579635021166650333 ) ) ;
#38564=ADVANCED_FACE ( 'NONE', ( #84891 ), #50617, .F. ) ;
#38573=CARTESIAN_POINT ( 'NONE',  ( 31.81093863508777630, 310.9010134536062537, -8.120521125203326918 ) ) ;
#38577=CARTESIAN_POINT ( 'NONE',  ( 31.62259664290086647, 439.0130977130161227, 23.39453342550511294 ) ) ;
#38594=ADVANCED_FACE ( 'NONE', ( #69777 ), #32255, .F. ) ;
#38597=CARTESIAN_POINT ( 'NONE',  ( 51.01037695545453232, 450.0000000000002274, 13.20242257375370976 ) ) ;
#38602=DIRECTION ( 'NONE',  ( -0.1804394941703459376, -0.5071212677064720342, 0.8427749455123416666 ) ) ;
#38616=ORIENTED_EDGE ( 'NONE', *, *, #7117, .T. ) ;
#38622=CARTESIAN_POINT ( 'NONE',  ( -43.58191388046994774, 439.3921676197703050, 13.97026443796441875 ) ) ;
#38625=CARTESIAN_POINT ( 'NONE',  ( 43.63899620156487202, 434.3182181978403946, 14.37213632273145336 ) ) ;
#38631=CARTESIAN_POINT ( 'NONE',  ( -40.83852310120926887, 485.7816305618699175, -4.779469532615789440 ) ) ;
#38636=CARTESIAN_POINT ( 'NONE',  ( 38.21362991493155192, 463.7316259062602626, 19.26248154875775143 ) ) ;
#38638=CARTESIAN_POINT ( 'NONE',  ( 43.00000000000000000, 461.9428920847649920, 12.03309428281479576 ) ) ;
#38641=ADVANCED_FACE ( 'NONE', ( #80360 ), #35748, .T. ) ;
#38653=EDGE_CURVE ( 'NONE', #17301, #11843, #77136, .T. ) ;
#38677=CARTESIAN_POINT ( 'NONE',  ( -35.53540878342338516, 439.9360873049408838, 24.32554890336280806 ) ) ;
#38682=FACE_OUTER_BOUND ( 'NONE', #6115, .T. ) ;
#38686=CARTESIAN_POINT ( 'NONE',  ( -44.43774958859658142, 337.2802145563449017, 0.2445019049555710311 ) ) ;
#38693=CARTESIAN_POINT ( 'NONE',  ( -43.49286403356592956, 484.8086342565612767, 4.190194857772802095 ) ) ;
#38694=ORIENTED_EDGE ( 'NONE', *, *, #34779, .T. ) ;
#38697=CARTESIAN_POINT ( 'NONE',  ( -26.01452734666768762, 309.4082761259522840, 11.00913782773181104 ) ) ;
#38699=CARTESIAN_POINT ( 'NONE',  ( 20.19576726783346032, 303.8497611245961707, 9.936565449087714441 ) ) ;
#38707=CARTESIAN_POINT ( 'NONE',  ( 44.15550912980668841, 485.1924980653485591, 0.8858017399470232700 ) ) ;
#38709=CARTESIAN_POINT ( 'NONE',  ( 43.75401118688382951, 486.3173572309547694, 5.908089951475070656 ) ) ;
#38717=CARTESIAN_POINT ( 'NONE',  ( 42.00498316483407280, 460.5526920487831148, 2.538979661986996650 ) ) ;
#38718=B_SPLINE_CURVE_WITH_KNOTS ( 'NONE', 3,
 ( #52757, #85677, #51148, #11754, #74886, #972, #99713, #25884, #58742, #86747, #46270, #22012, #38207, #103957 ),
 .UNSPECIFIED., .F., .F.,
 ( 4, 2, 2, 2, 2, 2, 4 ),
 ( 3.758192634394940486E-15, 0.0005542516808482931797, 0.001108503361692828298, 0.001385629202115091357, 0.001662755042537354417, 0.001939880882959617477, 0.002217006723381880536 ),
 .UNSPECIFIED. ) ;
#38737=CARTESIAN_POINT ( 'NONE',  ( 19.36103579130787367, 294.6347466944262692, -10.04613669444748503 ) ) ;
#38748=CARTESIAN_POINT ( 'NONE',  ( 40.67681791045112760, 323.6015846532498585, 8.948094541999738638 ) ) ;
#38753=CARTESIAN_POINT ( 'NONE',  ( -40.21064024340174115, 459.8708642436288301, 1.907892319917269486 ) ) ;
#38761=CARTESIAN_POINT ( 'NONE',  ( -35.45036406932566564, 436.3203772529605544, 5.179456583033978490 ) ) ;
#38762=CARTESIAN_POINT ( 'NONE',  ( -31.50862643367105775, 299.7654595037400327, 11.04213083294634146 ) ) ;
#38776=CARTESIAN_POINT ( 'NONE',  ( 35.32911723019348926, 437.0667969981791430, 5.602639083904082717 ) ) ;
#38784=CARTESIAN_POINT ( 'NONE',  ( 42.58368960131090830, 480.4983903161937064, 9.551102386166812508 ) ) ;
#38830=CARTESIAN_POINT ( 'NONE',  ( -9.789044728060147804, 294.6486233851416614, -2.043184600577789833 ) ) ;
#38837=VERTEX_POINT ( 'NONE', #55311 ) ;
#38845=CARTESIAN_POINT ( 'NONE',  ( 6.123233995736771213E-16, 0.000000000000000000, 5.000000000000003553 ) ) ;
#38848=( BOUNDED_SURFACE ( )  B_SPLINE_SURFACE ( 3, 2, ( 
 ( #97501, #96478, #72192 ),
 ( #30701, #6913, #32283 ),
 ( #47893, #63589, #106127 ),
 ( #47372, #56517, #65153 ),
 ( #98053, #15003, #24201 ),
 ( #72709, #95948, #16071 ),
 ( #46846, #13935, #64633 ),
 ( #5851, #55975, #104015 ),
 ( #57048, #89446, #55452 ),
 ( #15536, #23134, #80263 ),
 ( #48953, #79746, #14460 ),
 ( #89965, #38776, #48430 ) ),
 .UNSPECIFIED., .F., .F., .F. ) 
 B_SPLINE_SURFACE_WITH_KNOTS ( ( 4, 2, 2, 2, 2, 4 ),
 ( 3, 3 ),
 ( 3.707971429900425164E-17, 0.0004396180695633393194, 0.0008792361391266415591, 0.001758472278253246038, 0.002637708417379850626, 0.003516944556506455214 ),
 ( 0.000000000000000000, 1.000000000000000000 ),
 .UNSPECIFIED. ) 
 GEOMETRIC_REPRESENTATION_ITEM ( )  RATIONAL_B_SPLINE_SURFACE ( (
 ( 1.000000000000000000, 0.9193453746270715543, 1.000000000000000000),
 ( 1.000000000000000000, 0.9231392589459156417, 1.000000000000000000),
 ( 1.000000000000000000, 0.9252300355209908123, 1.000000000000000000),
 ( 1.000000000000000000, 0.9257136340838321154, 1.000000000000000000),
 ( 1.000000000000000000, 0.9240662039545859407, 1.000000000000000000),
 ( 1.000000000000000000, 0.9140412217423881103, 1.000000000000000000),
 ( 1.000000000000000000, 0.9005671153087457803, 1.000000000000000000),
 ( 1.000000000000000000, 0.8672639112290936314, 1.000000000000000000),
 ( 1.000000000000000000, 0.8470036231256007353, 1.000000000000000000),
 ( 1.000000000000000000, 0.8036658034633893388, 1.000000000000000000),
 ( 1.000000000000000000, 0.7801896332604544293, 1.000000000000000000),
 ( 1.000000000000000000, 0.7557288854858671412, 1.000000000000000000) ) ) 
 REPRESENTATION_ITEM ( '' )  SURFACE ( )  );
#38850=CARTESIAN_POINT ( 'NONE',  ( 43.55333112596303380, 465.2342844084865874, 9.238213423009675296 ) ) ;
#38851=CARTESIAN_POINT ( 'NONE',  ( -37.04388863813380794, 311.3287000699716032, 13.89786840526617517 ) ) ;
#38854=CARTESIAN_POINT ( 'NONE',  ( -33.88237199998293647, 485.0486819176492759, 1.241522336454330411 ) ) ;
#38868=CARTESIAN_POINT ( 'NONE',  ( -31.29447218978298650, 439.6461559793971219, 23.31027018619894875 ) ) ;
#38869=CARTESIAN_POINT ( 'NONE',  ( -32.30941696154608422, 435.2301481353223949, 15.36959316898724737 ) ) ;
#38870=CARTESIAN_POINT ( 'NONE',  ( -35.53899189460923225, 397.1537505765458604, 6.928033022457113610 ) ) ;
#38871=CARTESIAN_POINT ( 'NONE',  ( -32.65592842490316627, 434.9896282828135554, 13.53682765909404040 ) ) ;
#38875=( BOUNDED_SURFACE ( )  B_SPLINE_SURFACE ( 3, 2, ( 
 ( #48059, #39473, #105255 ),
 ( #43179, #19480, #77137 ),
 ( #18942, #35115, #26503 ),
 ( #2704, #10265, #51785 ),
 ( #91214, #92782, #36193 ),
 ( #59374, #10782, #17852 ),
 ( #60451, #99808, #99258 ),
 ( #59915, #84698, #92236 ),
 ( #50705, #43701, #67461 ),
 ( #83617, #25434, #1628 ),
 ( #9721, #66928, #68530 ),
 ( #18390, #42637, #84170 ),
 ( #42102, #51243, #9191 ),
 ( #75534, #74986, #27031 ) ),
 .UNSPECIFIED., .F., .F., .F. ) 
 B_SPLINE_SURFACE_WITH_KNOTS ( ( 4, 2, 2, 2, 2, 2, 4 ),
 ( 3, 3 ),
 ( -1.457818241124009262E-15, 0.001036839948807126086, 0.001555259923211418146, 0.002073679897615710206, 0.002592099872020002266, 0.003110519846424294327, 0.004147359795232878447 ),
 ( 0.000000000000000000, 1.000000000000000000 ),
 .UNSPECIFIED. ) 
 GEOMETRIC_REPRESENTATION_ITEM ( )  RATIONAL_B_SPLINE_SURFACE ( (
 ( 1.000000000000000000, 0.8806660624989138819, 1.000000000000000000),
 ( 1.000000000000000000, 0.8881715692662220940, 1.000000000000000000),
 ( 1.000000000000000000, 0.8928479710807014635, 1.000000000000000000),
 ( 1.000000000000000000, 0.8947313045151512600, 1.000000000000000000),
 ( 1.000000000000000000, 0.8944961860243509921, 1.000000000000000000),
 ( 1.000000000000000000, 0.8923679545988014716, 1.000000000000000000),
 ( 1.000000000000000000, 0.8904472546607837824, 1.000000000000000000),
 ( 1.000000000000000000, 0.8850746651129741682, 1.000000000000000000),
 ( 1.000000000000000000, 0.8816555630472442395, 1.000000000000000000),
 ( 1.000000000000000000, 0.8735136825623661672, 1.000000000000000000),
 ( 1.000000000000000000, 0.8687495631818540343, 1.000000000000000000),
 ( 1.000000000000000000, 0.8530568296116498583, 1.000000000000000000),
 ( 1.000000000000000000, 0.8406856949812601121, 1.000000000000000000),
 ( 1.000000000000000000, 0.8270258197359576791, 1.000000000000000000) ) ) 
 REPRESENTATION_ITEM ( '' )  SURFACE ( )  );
#38878=CARTESIAN_POINT ( 'NONE',  ( -30.39554535350546161, 298.0292904638343998, -1.300630307310727707 ) ) ;
#38886=CARTESIAN_POINT ( 'NONE',  ( 26.53231809466943503, 310.2838222077303953, 10.22456148134894072 ) ) ;
#38898=ADVANCED_FACE ( 'NONE', ( #54239 ), #68148, .F. ) ;
#38900=CARTESIAN_POINT ( 'NONE',  ( -33.50393555050020922, 439.8572903566229684, 24.25426608324027455 ) ) ;
#38902=CARTESIAN_POINT ( 'NONE',  ( -25.55259955101245950, 304.1867599840693970, -9.710062353868671892 ) ) ;
#38905=CARTESIAN_POINT ( 'NONE',  ( 40.34377649348542860, 485.2488587072590462, -4.812891347181404100 ) ) ;
#38913=CARTESIAN_POINT ( 'NONE',  ( 43.03880698781976832, 435.3545807224048190, 16.83573131045122651 ) ) ;
#38938=CARTESIAN_POINT ( 'NONE',  ( 43.33498512661115143, 464.9732568094945577, 13.98542553804674426 ) ) ;
#38940=VERTEX_POINT ( 'NONE', #8889 ) ;
#38948=CARTESIAN_POINT ( 'NONE',  ( -13.26814552884363962, 304.5542534004749768, 8.873748344450744341 ) ) ;
#38967=EDGE_LOOP ( 'NONE', ( #80669, #69092, #20763, #57346 ) ) ;
#38973=CARTESIAN_POINT ( 'NONE',  ( 35.70257255451698342, 337.7971262439807560, -1.754882810684410321 ) ) ;
#38982=CARTESIAN_POINT ( 'NONE',  ( 33.43292762174942112, 315.2036803431912517, -7.045335761960068055 ) ) ;
#38985=CARTESIAN_POINT ( 'NONE',  ( -38.85446894546474539, 460.8903912184078422, 2.218456751110488678 ) ) ;
#38994=CARTESIAN_POINT ( 'NONE',  ( 45.33180403702434091, 464.4945808635454227, 2.178908857919817699 ) ) ;
#38996=CARTESIAN_POINT ( 'NONE',  ( -34.84618260875176787, 489.9833681528637044, 11.97975507378787619 ) ) ;
#39001=CIRCLE ( 'NONE', #18371, 12.00000000000000711 ) ;
#39023=EDGE_LOOP ( 'NONE', ( #70647, #8352, #22359, #23215, #44693 ) ) ;
#39033=CARTESIAN_POINT ( 'NONE',  ( 13.70960934686813637, 294.5458232874115083, 9.871961475911533057 ) ) ;
#39035=ORIENTED_EDGE ( 'NONE', *, *, #33997, .F. ) ;
#39044=CIRCLE ( 'NONE', #59682, 0.9999999999999911182 ) ;
#39050=CARTESIAN_POINT ( 'NONE',  ( -37.29743259733409388, 437.4067882691437603, 4.451017177258851376 ) ) ;
#39058=AXIS2_PLACEMENT_3D ( 'NONE', #73792, #71664, #23155 ) ;
#39060=CARTESIAN_POINT ( 'NONE',  ( -46.00000000004250467, 463.8885932306518498, 10.44912889367152786 ) ) ;
#39078=ORIENTED_EDGE ( 'NONE', *, *, #25478, .F. ) ;
#39079=CARTESIAN_POINT ( 'NONE',  ( 36.72895593185456420, 408.8932456075058894, 6.289864422344447092 ) ) ;
#39085=CARTESIAN_POINT ( 'NONE',  ( -31.21280335960756958, 312.0095200496609777, -8.085286564489109651 ) ) ;
#39093=CARTESIAN_POINT ( 'NONE',  ( -36.67995261982857613, 463.9785544991901247, 19.62073859179952606 ) ) ;
#39101=CARTESIAN_POINT ( 'NONE',  ( 38.87981064652338148, 307.2829811854333002, -7.103582886926979256 ) ) ;
#39120=CARTESIAN_POINT ( 'NONE',  ( 31.83945028356544071, 465.6738295161419501, 10.98138951113134709 ) ) ;
#39131=CARTESIAN_POINT ( 'NONE',  ( -44.22225178597525286, 464.2590902508154613, 9.202154635652870951 ) ) ;
#39133=CARTESIAN_POINT ( 'NONE',  ( -30.00000000000000355, 490.2058330551859626, 6.957713811045728391 ) ) ;
#39149=CARTESIAN_POINT ( 'NONE',  ( 32.64148745189749690, 347.3146175066438559, 20.23427429214728690 ) ) ;
#39157=CARTESIAN_POINT ( 'NONE',  ( 19.70764564238367100, 304.7954121406193053, 9.925013215726757210 ) ) ;
#39158=CARTESIAN_POINT ( 'NONE',  ( -40.49428179616828061, 485.6422782434504484, -4.370491944118827909 ) ) ;
#39170=( NAMED_UNIT ( * ) PLANE_ANGLE_UNIT ( ) SI_UNIT ( $, .RADIAN. ) );
#39185=( BOUNDED_SURFACE ( )  B_SPLINE_SURFACE ( 3, 2, ( 
 ( #100460, #75103, #31641 ),
 ( #23022, #26619, #72597 ),
 ( #59492, #67046, #6801 ),
 ( #17970, #50827, #92358 ),
 ( #105501, #18509, #51370 ),
 ( #39195, #72072, #104982 ),
 ( #31126, #66499, #64010 ),
 ( #64523, #96887, #55853 ) ),
 .UNSPECIFIED., .F., .F., .F. ) 
 B_SPLINE_SURFACE_WITH_KNOTS ( ( 4, 2, 2, 4 ),
 ( 3, 3 ),
 ( 0.006715319241923278261, 0.008391857906694557070, 0.009230127239080197776, 0.01006839657146583675 ),
 ( 0.000000000000000000, 0.8433639608880305616 ),
 .UNSPECIFIED. ) 
 GEOMETRIC_REPRESENTATION_ITEM ( )  RATIONAL_B_SPLINE_SURFACE ( (
 ( 1.000000000000000000, 0.7529844148637855339, 0.9226169142906758269),
 ( 1.000000000000000000, 0.7706979643850044859, 0.9281660747619107088),
 ( 1.000000000000000000, 0.7822228831078168465, 0.9317765100015680257),
 ( 1.000000000000000000, 0.7860222813518789042, 0.9329667553854859019),
 ( 1.000000000000000000, 0.7850393348246805791, 0.9326588256841275015),
 ( 1.000000000000000000, 0.7784080814446623364, 0.9305814391565394583),
 ( 1.000000000000000000, 0.7727688943794591703, 0.9288148393051297580),
 ( 1.000000000000000000, 0.7650504347444155862, 0.9263968614145721148) ) ) 
 REPRESENTATION_ITEM ( '' )  SURFACE ( )  );
#39195=CARTESIAN_POINT ( 'NONE',  ( -30.00000000000000355, 461.9652624853977159, 12.11314247086471596 ) ) ;
#39196=DIRECTION ( 'NONE',  ( -1.000000000000000000, 0.000000000000000000, 0.000000000000000000 ) ) ;
#39210=EDGE_CURVE ( 'NONE', #49781, #23997, #90233, .T. ) ;
#39220=CARTESIAN_POINT ( 'NONE',  ( -22.91651842568165165, 295.0901107613288445, -9.949346074078587066 ) ) ;
#39230=CARTESIAN_POINT ( 'NONE',  ( -23.65589420198908499, 306.0724382492799123, 10.20579241568104578 ) ) ;
#39233=ADVANCED_FACE ( 'NONE', ( #36804 ), #13639, .F. ) ;
#39252=EDGE_CURVE ( 'NONE', #21098, #51812, #86446, .T. ) ;
#39267=EDGE_LOOP ( 'NONE', ( #55869, #15411, #49359, #30849 ) ) ;
#39268=EDGE_LOOP ( 'NONE', ( #19409, #2231, #33594, #40717 ) ) ;
#39272=CARTESIAN_POINT ( 'NONE',  ( -43.64277943678018801, 435.6477504884530276, 9.088095002171668213 ) ) ;
#39274=CARTESIAN_POINT ( 'NONE',  ( 0.000000000000000000, 294.8518027762758038, -10.00000000000000178 ) ) ;
#39283=CARTESIAN_POINT ( 'NONE',  ( 36.84238428740148663, 310.7453882974721751, 13.75124073885965892 ) ) ;
#39291=CARTESIAN_POINT ( 'NONE',  ( -36.05619378504946582, 461.6897174690496968, 3.777659454257536353 ) ) ;
#39295=CARTESIAN_POINT ( 'NONE',  ( 32.17646412119353272, 464.6980787822281513, 10.84896803613063021 ) ) ;
#39296=CARTESIAN_POINT ( 'NONE',  ( -26.71365596510858964, 306.5311303962027978, 10.78021858148648349 ) ) ;
#39303=CARTESIAN_POINT ( 'NONE',  ( 19.83463548332445825, 303.8035096162420245, 9.926734387303332241 ) ) ;
#39304=ORIENTED_EDGE ( 'NONE', *, *, #36452, .F. ) ;
#39315=B_SPLINE_CURVE_WITH_KNOTS ( 'NONE', 3,
 ( #84213, #59419, #85828, #28139 ),
 .UNSPECIFIED., .F., .F.,
 ( 4, 4 ),
 ( 0.000000000000000000, 0.001019617110105362117 ),
 .UNSPECIFIED. ) ;
#39328=FACE_OUTER_BOUND ( 'NONE', #20166, .T. ) ;
#39334=CARTESIAN_POINT ( 'NONE',  ( 20.05074616892822448, 67.05096163904791240, -10.02537308446411402 ) ) ;
#39336=EDGE_CURVE ( 'NONE', #51812, #11400, #37558, .T. ) ;
#39357=CARTESIAN_POINT ( 'NONE',  ( 31.38691588366916818, 427.9687656044268920, 23.57225804472849617 ) ) ;
#39362=AXIS2_PLACEMENT_3D ( 'NONE', #9718, #51782, #84695 ) ;
#39376=CARTESIAN_POINT ( 'NONE',  ( 32.84237740334622657, 485.2251842821286800, 5.746442123025142124 ) ) ;
#39382=CARTESIAN_POINT ( 'NONE',  ( -38.51502786940007184, 460.0233756673457606, 2.043034587342192676 ) ) ;
#39406=CARTESIAN_POINT ( 'NONE',  ( -35.52712812490531746, 408.9705615248064419, 7.034401458122156114 ) ) ;
#39414=CARTESIAN_POINT ( 'NONE',  ( -34.29742002188510241, 300.7002447392828799, -8.688633338721277966 ) ) ;
#39421=CARTESIAN_POINT ( 'NONE',  ( -42.10086803841218739, 435.6552064019005002, 19.95582312411058368 ) ) ;
#39422=CARTESIAN_POINT ( 'NONE',  ( 29.91076667616410489, 328.9704351996689979, 14.85080938783550231 ) ) ;
#39435=CARTESIAN_POINT ( 'NONE',  ( -36.48988454258796565, 439.4722615773889629, 23.89747316622354845 ) ) ;
#39463=CARTESIAN_POINT ( 'NONE',  ( 44.18670859114681804, 435.3672560506858531, 10.83164355295159709 ) ) ;
#39465=ORIENTED_EDGE ( 'NONE', *, *, #33933, .F. ) ;
#39473=CARTESIAN_POINT ( 'NONE',  ( 38.73386039798916869, 460.3889633641978776, 2.371405894923816149 ) ) ;
#39480=VERTEX_POINT ( 'NONE', #56645 ) ;
#39481=DIRECTION ( 'NONE',  ( 0.000000000000000000, -0.9584033143583832182, 0.2854173908977277185 ) ) ;
#39482=ADVANCED_FACE ( 'NONE', ( #97112, #73353 ), #58246, .T. ) ;
#39511=CARTESIAN_POINT ( 'NONE',  ( 46.00000000000000000, 461.5066419892501131, 9.508543545646363171 ) ) ;
#39517=CARTESIAN_POINT ( 'NONE',  ( 36.89131349651913894, 342.5581385403770582, -0.5070065298284284205 ) ) ;
#39528=ORIENTED_EDGE ( 'NONE', *, *, #27784, .T. ) ;
#39530=CARTESIAN_POINT ( 'NONE',  ( -31.00389226249483698, 502.9289871839745842, 8.047326149841639520 ) ) ;
#39531=CARTESIAN_POINT ( 'NONE',  ( -32.99999999999999289, 439.7597899781498541, 24.16317522621304903 ) ) ;
#39533=DIRECTION ( 'NONE',  ( -1.000000000000000000, -0.000000000000000000, -0.000000000000000000 ) ) ;
#39536=FACE_OUTER_BOUND ( 'NONE', #82964, .T. ) ;
#39557=EDGE_CURVE ( 'NONE', #4842, #12476, #66340, .T. ) ;
#39571=CARTESIAN_POINT ( 'NONE',  ( 43.43869229197127169, 464.9661605157749591, 13.42065392471465834 ) ) ;
#39585=DIRECTION ( 'NONE',  ( -1.000000000000000000, 0.000000000000000000, 0.000000000000000000 ) ) ;
#39599=CARTESIAN_POINT ( 'NONE',  ( -43.71217423904474231, 435.6632154632216043, 9.092528312227496912 ) ) ;
#39602=CARTESIAN_POINT ( 'NONE',  ( 37.72498816021352752, 463.3860965757704093, 19.97126500438806218 ) ) ;
#39606=CARTESIAN_POINT ( 'NONE',  ( -40.93292669599463096, 378.0706848361106722, 26.55786848468904537 ) ) ;
#39610=CARTESIAN_POINT ( 'NONE',  ( 23.00643915961089903, 305.3757170294761067, -8.887520214983368305 ) ) ;
#39617=CARTESIAN_POINT ( 'NONE',  ( -42.64966854229462001, 465.0854819100622422, 13.23715615004960178 ) ) ;
#39635=CARTESIAN_POINT ( 'NONE',  ( 37.77771400876960683, 305.2406471639163215, -7.604042599900936672 ) ) ;
#39636=CIRCLE ( 'NONE', #26725, 1.000000000000019540 ) ;
#39638=ORIENTED_EDGE ( 'NONE', *, *, #47652, .F. ) ;
#39640=( NAMED_UNIT ( * ) SI_UNIT ( $, .STERADIAN. ) SOLID_ANGLE_UNIT ( ) );
#39654=CIRCLE ( 'NONE', #8592, 3.000000000000017764 ) ;
#39673=CARTESIAN_POINT ( 'NONE',  ( -33.00000000000000000, 464.3970849722209664, 17.41240408234212111 ) ) ;
#39675=CARTESIAN_POINT ( 'NONE',  ( 27.50975502829663100, 307.9109348731828959, 11.11733839782984745 ) ) ;
#39676=CARTESIAN_POINT ( 'NONE',  ( -37.60552182430246404, 371.2989764267708210, 4.344118227128259235 ) ) ;
#39686=CARTESIAN_POINT ( 'NONE',  ( 3.587928128302542596, 304.8518027750386636, 9.936999415048941131 ) ) ;
#39687=CARTESIAN_POINT ( 'NONE',  ( -39.78276460673632187, 485.2153259665885798, -4.379159006359595097 ) ) ;
#39692=CARTESIAN_POINT ( 'NONE',  ( 40.44044047303815859, 465.0924562876297159, 17.36401474854813287 ) ) ;
#39694=AXIS2_PLACEMENT_3D ( 'NONE', #7787, #40169, #66569 ) ;
#39708=CARTESIAN_POINT ( 'NONE',  ( 3.318391428298041124, 303.8518027738843443, 9.936999414637822881 ) ) ;
#39710=DIRECTION ( 'NONE',  ( -0.2244612941943540108, 0.4655631424236075233, 0.8560771506267712549 ) ) ;
#39718=CARTESIAN_POINT ( 'NONE',  ( 43.87189908087982104, 464.7380721632374048, 11.09531536897046422 ) ) ;
#39728=CARTESIAN_POINT ( 'NONE',  ( 37.75487775365388643, 438.6157932507177293, 23.62942516414488026 ) ) ;
#39739=ADVANCED_FACE ( 'NONE', ( #54252 ), #83260, .T. ) ;
#39746=CARTESIAN_POINT ( 'NONE',  ( -35.62292360717025019, 485.2979424254038463, -2.983350328822282904 ) ) ;
#39751=CARTESIAN_POINT ( 'NONE',  ( -29.34822610931458087, 317.9602820924653201, 13.40329343600991407 ) ) ;
#39752=EDGE_CURVE ( 'NONE', #59443, #34982, #84228, .T. ) ;
#39762=B_SPLINE_CURVE_WITH_KNOTS ( 'NONE', 3,
 ( #75878, #57547, #82373, #90467, #8480, #41385, #52127, #18747, #53731, #29502, #61308, #3597, #78528, #86659 ),
 .UNSPECIFIED., .F., .F.,
 ( 4, 2, 2, 2, 2, 2, 4 ),
 ( 5.204170427930421283E-18, 0.002831373411936749778, 0.004247060117905107970, 0.005662746823873466596, 0.007078433529841825222, 0.008494120235810182981, 0.01132549364774689329 ),
 .UNSPECIFIED. ) ;
#39766=CARTESIAN_POINT ( 'NONE',  ( 45.99999999999995026, 485.6428795626757164, -1.077934839663798439 ) ) ;
#39777=CARTESIAN_POINT ( 'NONE',  ( 42.19179521601841287, 485.4956273777429487, -3.824025998174274577 ) ) ;
#39784=CARTESIAN_POINT ( 'NONE',  ( 35.56416567029047116, 496.2909070316903239, -10.19064917708978335 ) ) ;
#39785=ORIENTED_EDGE ( 'NONE', *, *, #49602, .T. ) ;
#39792=CARTESIAN_POINT ( 'NONE',  ( -22.35502908346653328, 304.3280978137025272, 10.03953411925336248 ) ) ;
#39799=CARTESIAN_POINT ( 'NONE',  ( -38.21273700183271416, 463.7314486282535881, 19.26286508106272422 ) ) ;
#39809=CARTESIAN_POINT ( 'NONE',  ( 39.14633636556600038, 314.2407992262670291, 6.611805377155580032 ) ) ;
#39820=CARTESIAN_POINT ( 'NONE',  ( -29.83138824175510706, 298.2147009232574533, 10.68178215045177026 ) ) ;
#39830=ADVANCED_FACE ( 'NONE', ( #1602 ), #34319, .F. ) ;
#39861=ORIENTED_EDGE ( 'NONE', *, *, #19814, .T. ) ;
#39879=CARTESIAN_POINT ( 'NONE',  ( -32.84724476090489986, 479.6963199345864268, 7.498190490636539529 ) ) ;
#39883=CARTESIAN_POINT ( 'NONE',  ( -9.994350908930156763, 294.6428469334700253, -0.7388987851124564354 ) ) ;
#39884=CARTESIAN_POINT ( 'NONE',  ( -20.34819189090134017, 294.7750624004232805, -2.016311483866853660 ) ) ;
#39894=CARTESIAN_POINT ( 'NONE',  ( -3.001409217703660648, 294.8245242021811237, -9.555569693199137404 ) ) ;
#39902=CARTESIAN_POINT ( 'NONE',  ( -13.81794228156022974, 302.5467222371539719, 9.872154306231394116 ) ) ;
#39903=DIRECTION ( 'NONE',  ( -0.02876443886042204245, 0.9995862179207181120, 0.000000000000000000 ) ) ;
#39905=CARTESIAN_POINT ( 'NONE',  ( 3.398996499095806811, 303.8518027749813655, -10.00000000027310421 ) ) ;
#39910=ORIENTED_EDGE ( 'NONE', *, *, #57838, .F. ) ;
#39926=CARTESIAN_POINT ( 'NONE',  ( -32.05181932688683588, 439.7174019519748072, 23.91393675278271758 ) ) ;
#39927=CARTESIAN_POINT ( 'NONE',  ( -27.23735134814286951, 307.8362383646490343, -8.331602159243709949 ) ) ;
#39931=ORIENTED_EDGE ( 'NONE', *, *, #24443, .F. ) ;
#39933=CARTESIAN_POINT ( 'NONE',  ( -33.36333480850094446, 300.5116995142376481, -0.7277600820885061772 ) ) ;
#39942=CARTESIAN_POINT ( 'NONE',  ( 24.10451817204156910, 306.3800824377233880, 9.276234954072691608 ) ) ;
#39951=DIRECTION ( 'NONE',  ( -0.9086146812040659659, 0.000000000000000000, 0.4176354404267356157 ) ) ;
#39965=EDGE_CURVE ( 'NONE', #91921, #82451, #67137, .T. ) ;
#39981=CARTESIAN_POINT ( 'NONE',  ( 44.21332904831284338, 435.2494715644500616, 14.45449769377396976 ) ) ;
#39990=CARTESIAN_POINT ( 'NONE',  ( 43.66694997075330775, 484.4025358507092278, 1.806736142167242321 ) ) ;
#39996=ORIENTED_EDGE ( 'NONE', *, *, #21752, .T. ) ;
#40000=EDGE_CURVE ( 'NONE', #105135, #27903, #79899, .T. ) ;
#40001=CARTESIAN_POINT ( 'NONE',  ( 33.77559172535808329, 464.7834715296607442, 7.192701217093171451 ) ) ;
#40003=CARTESIAN_POINT ( 'NONE',  ( 0.000000000000000000, 273.9999999999999432, 0.000000000000000000 ) ) ;
#40012=ORIENTED_EDGE ( 'NONE', *, *, #51316, .T. ) ;
#40018=AXIS2_PLACEMENT_3D ( 'NONE', #16436, #56880, #73596 ) ;
#40028=CARTESIAN_POINT ( 'NONE',  ( 43.89455633144091706, 462.7155212543453331, 5.467842138882834213 ) ) ;
#40032=ADVANCED_FACE ( 'NONE', ( #34967 ), #67830, .T. ) ;
#40040=CARTESIAN_POINT ( 'NONE',  ( 32.99999999999998579, 464.3970849722209095, 17.41240408234205717 ) ) ;
#40043=FACE_OUTER_BOUND ( 'NONE', #10270, .T. ) ;
#40044=CARTESIAN_POINT ( 'NONE',  ( 35.96492786661492858, 302.4488314805894902, -8.278427239160079054 ) ) ;
#40049=CARTESIAN_POINT ( 'NONE',  ( -31.39112176491482842, 426.5443834901637956, 23.68269498481550173 ) ) ;
#40070=ORIENTED_EDGE ( 'NONE', *, *, #31191, .T. ) ;
#40094=CARTESIAN_POINT ( 'NONE',  ( -39.18961397227251098, 489.8685109512363738, 11.78848534766373746 ) ) ;
#40098=CARTESIAN_POINT ( 'NONE',  ( 33.21102376836596903, 438.9613914113129454, 23.92328486949907784 ) ) ;
#40103=EDGE_CURVE ( 'NONE', #104525, #61960, #24737, .T. ) ;
#40107=CARTESIAN_POINT ( 'NONE',  ( -8.400342417351219037E-11, 303.8518027762758038, 8.936999415352287812 ) ) ;
#40111=CARTESIAN_POINT ( 'NONE',  ( 35.02700494597931424, 463.8298975055690221, 19.03023931480278463 ) ) ;
#40116=CARTESIAN_POINT ( 'NONE',  ( -36.91281931599076671, 303.7809130842520631, -7.959270006439831846 ) ) ;
#40118=CARTESIAN_POINT ( 'NONE',  ( -40.95595929481465447, 405.2208686710653183, 27.85131585683114963 ) ) ;
#40121=CARTESIAN_POINT ( 'NONE',  ( 30.73677158032236889, 310.9900250146528151, -8.337346309561983304 ) ) ;
#40155=CARTESIAN_POINT ( 'NONE',  ( 43.32920196732025886, 484.9664025106548593, 4.870547201839677598 ) ) ;
#40160=ORIENTED_EDGE ( 'NONE', *, *, #68224, .F. ) ;
#40162=ORIENTED_EDGE ( 'NONE', *, *, #31044, .F. ) ;
#40163=FILL_AREA_STYLE_COLOUR ( '', #12354 ) ;
#40164=CARTESIAN_POINT ( 'NONE',  ( 38.26671806398906739, 461.1046247403738789, 2.389135870405684869 ) ) ;
#40166=CARTESIAN_POINT ( 'NONE',  ( -16.15504899495356028, 294.5642704844590298, -10.06111734223398635 ) ) ;
#40168=ADVANCED_FACE ( 'NONE', ( #658 ), #39185, .T. ) ;
#40169=DIRECTION ( 'NONE',  ( -0.3108677890940723665, -0.06041750367988984322, -0.9485309393756504726 ) ) ;
#40177=ORIENTED_EDGE ( 'NONE', *, *, #100725, .T. ) ;
#40182=CARTESIAN_POINT ( 'NONE',  ( 22.51458678521758827, 303.3309683193314186, 10.03994171628768406 ) ) ;
#40183=CARTESIAN_POINT ( 'NONE',  ( -37.67361056029813682, 380.0437454810148097, 5.298401756046660083 ) ) ;
#40185=CARTESIAN_POINT ( 'NONE',  ( -44.14731978900761789, 485.1890916993070277, 0.8858938469252318759 ) ) ;
#40187=ORIENTED_EDGE ( 'NONE', *, *, #104273, .T. ) ;
#40192=CARTESIAN_POINT ( 'NONE',  ( -40.02990647470183205, 485.1981161833896863, -4.348266463184057962 ) ) ;
#40193=VECTOR ( 'NONE', #20728, 1000.000000000000000 ) ;
#40196=B_SPLINE_CURVE_WITH_KNOTS ( 'NONE', 3,
 ( #96016, #38332, #29717, #22143 ),
 .UNSPECIFIED., .F., .F.,
 ( 4, 4 ),
 ( 4.336808689942017736E-18, 0.001327912649053314235 ),
 .UNSPECIFIED. ) ;
#40208=CARTESIAN_POINT ( 'NONE',  ( -35.62683129835190954, 491.6879615318166543, 12.48649695628544976 ) ) ;
#40209=ADVANCED_FACE ( 'NONE', ( #102595 ), #61231, .T. ) ;
#40219=CARTESIAN_POINT ( 'NONE',  ( 13.26813409727140680, 304.5542536273018186, 8.873748392553073572 ) ) ;
#40227=AXIS2_PLACEMENT_3D ( 'NONE', #98689, #37197, #52271 ) ;
#40245=CARTESIAN_POINT ( 'NONE',  ( 40.09057539293721106, 460.7411201710881414, 2.126307971703979671 ) ) ;
#40252=CARTESIAN_POINT ( 'NONE',  ( 33.10504549936585050, 299.5985994039988327, -8.944502871241384767 ) ) ;
#40254=EDGE_CURVE ( 'NONE', #34982, #74683, #63605, .T. ) ;
#40257=CARTESIAN_POINT ( 'NONE',  ( -35.59667163540026280, 463.9592197885497171, -0.04846191499040426731 ) ) ;
#40263=CARTESIAN_POINT ( 'NONE',  ( -36.14207491790881477, 485.3942915881596605, -3.424055767583114029 ) ) ;
#40268=CARTESIAN_POINT ( 'NONE',  ( -25.70012971588764117, 306.8024630045113099, 10.60968151228726519 ) ) ;
#40273=CARTESIAN_POINT ( 'NONE',  ( 31.02195986096099745, 439.2860129589981284, 22.60718686867361527 ) ) ;
#40278=CARTESIAN_POINT ( 'NONE',  ( 44.06229749045533595, 485.7005620094865321, 3.983350637705970865 ) ) ;
#40293=DIRECTION ( 'NONE',  ( 0.000000000000000000, 0.000000000000000000, -1.000000000000000000 ) ) ;
#40296=CARTESIAN_POINT ( 'NONE',  ( 35.74363442581862671, 380.1068966271811860, 4.951945592532029927 ) ) ;
#40299=ORIENTED_EDGE ( 'NONE', *, *, #77663, .T. ) ;
#40303=FACE_OUTER_BOUND ( 'NONE', #8013, .T. ) ;
#40306=DIRECTION ( 'NONE',  ( 0.000000000000000000, 0.000000000000000000, 1.000000000000000000 ) ) ;
#40322=CARTESIAN_POINT ( 'NONE',  ( 38.65571709296854408, 312.2086733158335505, 6.098135005489119465 ) ) ;
#40328=AXIS2_PLACEMENT_3D ( 'NONE', #65629, #99572, #74762 ) ;
#40331=CARTESIAN_POINT ( 'NONE',  ( -42.73089261237369385, 435.7309723475636360, 18.11242468272465089 ) ) ;
#40333=CARTESIAN_POINT ( 'NONE',  ( -30.76131805048738954, 299.0178075277323160, 10.86737662268762605 ) ) ;
#40344=CARTESIAN_POINT ( 'NONE',  ( 0.000000000000000000, -20.00000000000001776, -9.000000000000007105 ) ) ;
#40350=EDGE_CURVE ( 'NONE', #64595, #15159, #18029, .T. ) ;
#40373=ORIENTED_EDGE ( 'NONE', *, *, #50660, .F. ) ;
#40376=CARTESIAN_POINT ( 'NONE',  ( -42.08762648273019380, 487.0030674539066808, 9.106351919860241395 ) ) ;
#40408=CARTESIAN_POINT ( 'NONE',  ( 43.00000000000000000, 487.9285348210859752, 8.903916466042430145 ) ) ;
#40421=CARTESIAN_POINT ( 'NONE',  ( -4.061792834527171436, 294.8078979827683384, 9.927667182094811693 ) ) ;
#40427=CARTESIAN_POINT ( 'NONE',  ( 37.17693862423350737, 491.8028371848114944, 12.56217450279973846 ) ) ;
#40429=CARTESIAN_POINT ( 'NONE',  ( -34.04714008975742701, 484.1152113529151961, 1.016147467615854172 ) ) ;
#40441=CARTESIAN_POINT ( 'NONE',  ( 30.00000000000000355, 461.8163627757391509, 11.11111419091022512 ) ) ;
#40445=CARTESIAN_POINT ( 'NONE',  ( -30.50452656062791590, 313.2483899364063973, -7.014562113412794453 ) ) ;
#40453=CARTESIAN_POINT ( 'NONE',  ( -29.90770810728629669, 297.4343786746629235, -9.436196628746156279 ) ) ;
#40457=ORIENTED_EDGE ( 'NONE', *, *, #53996, .T. ) ;
#40460=CARTESIAN_POINT ( 'NONE',  ( 20.28383506696346572, 302.8321527159674815, -2.004176749255714540 ) ) ;
#40461=CARTESIAN_POINT ( 'NONE',  ( 26.77982661073470183, 310.9515876031056223, 10.39176322513353945 ) ) ;
#40482=EDGE_CURVE ( 'NONE', #41809, #79477, #25969, .T. ) ;
#40487=AXIS2_PLACEMENT_3D ( 'NONE', #59501, #26629, #44372 ) ;
#40489=CARTESIAN_POINT ( 'NONE',  ( 19.59433841236636553, 302.7299593794648445, -10.02589861385249215 ) ) ;
#40495=EDGE_LOOP ( 'NONE', ( #62996, #60030, #103941, #86870 ) ) ;
#40497=CARTESIAN_POINT ( 'NONE',  ( 43.95063711303827603, 484.1591904870578560, -1.189330446659109697 ) ) ;
#40508=DIRECTION ( 'NONE',  ( 1.000000000000000000, -0.000000000000000000, -0.000000000000000000 ) ) ;
#40515=CARTESIAN_POINT ( 'NONE',  ( 30.00000000000000355, 489.8675765671201248, 6.488452894205156696 ) ) ;
#40525=CARTESIAN_POINT ( 'NONE',  ( 32.64206520363632791, 464.2415374745278882, 8.403253426445765228 ) ) ;
#40535=CARTESIAN_POINT ( 'NONE',  ( -43.19279117978085480, 484.2727584554530154, -0.4218381927343575200 ) ) ;
#40550=CARTESIAN_POINT ( 'NONE',  ( 45.99999999999999289, 461.9217514388778341, 5.107711371735583761 ) ) ;
#40554=( NAMED_UNIT ( * ) SI_UNIT ( $, .STERADIAN. ) SOLID_ANGLE_UNIT ( ) );
#40564=EDGE_CURVE ( 'NONE', #44923, #24536, #86248, .T. ) ;
#40569=CARTESIAN_POINT ( 'NONE',  ( 39.24156521425334176, 307.7088117867400001, -7.003459073692002157 ) ) ;
#40571=CARTESIAN_POINT ( 'NONE',  ( -33.11888822396105780, 438.9412710830819151, 23.90522241289612992 ) ) ;
#40576=CARTESIAN_POINT ( 'NONE',  ( -39.41219261697557386, 436.7611714244557675, 5.258763975273992308 ) ) ;
#40583=EDGE_LOOP ( 'NONE', ( #37702, #15619, #93026, #21542 ) ) ;
#40589=DIRECTION ( 'NONE',  ( 0.000000000000000000, -0.000000000000000000, 1.000000000000000000 ) ) ;
#40607=CARTESIAN_POINT ( 'NONE',  ( -33.16948502134867027, 434.2034787425552622, 15.24753222728177882 ) ) ;
#40618=DIRECTION ( 'NONE',  ( 0.000000000000000000, -0.8568390274594218647, -0.5155840193628893342 ) ) ;
#40629=ORIENTED_EDGE ( 'NONE', *, *, #85737, .F. ) ;
#40642=LINE ( 'NONE', #91338, #18355 ) ;
#40644=EDGE_CURVE ( 'NONE', #13955, #98501, #36066, .T. ) ;
#40647=CARTESIAN_POINT ( 'NONE',  ( 26.73461998295247000, 307.3006012187427132, -9.456373384271907767 ) ) ;
#40654=CARTESIAN_POINT ( 'NONE',  ( -32.64200203778431586, 464.2416672416182450, 8.403568186820926655 ) ) ;
#40660=CARTESIAN_POINT ( 'NONE',  ( -35.72538317320573498, 438.1659592258367297, 3.984952432983437376 ) ) ;
#40668=DIRECTION ( 'NONE',  ( 0.000000000000000000, 0.000000000000000000, -1.000000000000000000 ) ) ;
#40674=CARTESIAN_POINT ( 'NONE',  ( 43.68959978692338098, 484.5138553196885596, 2.648407630515406286 ) ) ;
#40676=FILL_AREA_STYLE_COLOUR ( '', #79556 ) ;
#40684=CARTESIAN_POINT ( 'NONE',  ( 28.32487310513930012, 309.0837454060449545, -8.036865677558150622 ) ) ;
#40686=EDGE_CURVE ( 'NONE', #35905, #103542, #48944, .T. ) ;
#40689=CARTESIAN_POINT ( 'NONE',  ( 35.57182711849233669, 461.3662169729752804, 3.401134023656063654 ) ) ;
#40694=CARTESIAN_POINT ( 'NONE',  ( -36.32791536946549371, 464.0041716472547364, 19.58704090454801872 ) ) ;
#40708=DIRECTION ( 'NONE',  ( 0.9915366780650375356, 0.1269898409407626272, 0.02699252395738695881 ) ) ;
#40710=CARTESIAN_POINT ( 'NONE',  ( -36.44570453002955901, 439.0052206251579037, 23.96112351096716253 ) ) ;
#40711=CARTESIAN_POINT ( 'NONE',  ( 30.15981381208334611, 316.9131350538594916, 13.38073451593941243 ) ) ;
#40712=CARTESIAN_POINT ( 'NONE',  ( -37.40172753335533429, 356.7446856187958701, 2.250060923472283481 ) ) ;
#40715=ORIENTED_EDGE ( 'NONE', *, *, #30086, .F. ) ;
#40717=ORIENTED_EDGE ( 'NONE', *, *, #720, .F. ) ;
#40719=CARTESIAN_POINT ( 'NONE',  ( 0.000000000000000000, 304.8518027762758038, 9.936999415352289589 ) ) ;
#40723=COLOUR_RGB ( '', 0.08235294, 0.09019608, 0.10196078) ;
#40736=( NAMED_UNIT ( * ) SI_UNIT ( $, .STERADIAN. ) SOLID_ANGLE_UNIT ( ) );
#40739=CARTESIAN_POINT ( 'NONE',  ( -37.17693862423640638, 491.8028371848064353, 12.56217450279643089 ) ) ;
#40779=CARTESIAN_POINT ( 'NONE',  ( 28.02604061233149579, 305.7734989515280404, -9.350961192283897105 ) ) ;
#40791=AXIS2_PLACEMENT_3D ( 'NONE', #70660, #45335, #30215 ) ;
#40798=CARTESIAN_POINT ( 'NONE',  ( 32.90756164719129373, 485.1133553471450455, 5.490574211028886431 ) ) ;
#40819=DIRECTION ( 'NONE',  ( 1.000000000000000000, 0.000000000000000000, 0.000000000000000000 ) ) ;
#40821=CARTESIAN_POINT ( 'NONE',  ( 35.76482652855951017, 405.2378813769876729, 6.148826621638260548 ) ) ;
#40826=B_SPLINE_CURVE_WITH_KNOTS ( 'NONE', 3,
 ( #101248, #44074, #11680, #44615 ),
 .UNSPECIFIED., .F., .F.,
 ( 4, 4 ),
 ( 4.718958039861916012E-17, 0.001833966606955493919 ),
 .UNSPECIFIED. ) ;
#40835=FACE_OUTER_BOUND ( 'NONE', #76517, .T. ) ;
#40841=CARTESIAN_POINT ( 'NONE',  ( -39.85359070619685440, 464.8559547511466690, 17.95180902016827318 ) ) ;
#40849=CARTESIAN_POINT ( 'NONE',  ( 38.19547087256027851, 310.5571834646071920, 5.681190331431579033 ) ) ;
#40858=EDGE_CURVE ( 'NONE', #96476, #35120, #53116, .T. ) ;
#40871=EDGE_CURVE ( 'NONE', #12603, #75687, #14181, .T. ) ;
#40887=EDGE_CURVE ( 'NONE', #30899, #88227, #78899, .T. ) ;
#40897=DIRECTION ( 'NONE',  ( 1.000000000000000000, 0.000000000000000000, 0.000000000000000000 ) ) ;
#40918=CARTESIAN_POINT ( 'NONE',  ( -3.888269695933030512, 294.8076487912955486, -9.230909423689038107 ) ) ;
#40926=CARTESIAN_POINT ( 'NONE',  ( 31.42024293970219162, 416.1390842372517227, 24.31832173542546371 ) ) ;
#40936=FACE_OUTER_BOUND ( 'NONE', #31943, .T. ) ;
#40940=EDGE_CURVE ( 'NONE', #103542, #69385, #72074, .T. ) ;
#40950=CARTESIAN_POINT ( 'NONE',  ( -8.269522720489927536, 294.6925646268865080, -5.661848168111208501 ) ) ;
#40955=CARTESIAN_POINT ( 'NONE',  ( 43.59756234217316972, 434.3244621007173123, 14.55946156040339368 ) ) ;
#40957=CARTESIAN_POINT ( 'NONE',  ( -8.413883161774244002, 294.6898069128530437, 9.902566082097019162 ) ) ;
#40981=CARTESIAN_POINT ( 'NONE',  ( -31.20516925732897917, 314.7589119991607163, -7.638240531729924676 ) ) ;
#40987=CARTESIAN_POINT ( 'NONE',  ( -26.13808921511803618, 304.4947950084629156, -9.641429296246926128 ) ) ;
#40994=CARTESIAN_POINT ( 'NONE',  ( -41.79440637192924868, 337.1634255704665293, 12.10213894368624743 ) ) ;
#40995=CARTESIAN_POINT ( 'NONE',  ( -32.82274108734650753, 485.2606360904492817, 5.822976237827062640 ) ) ;
#41007=CARTESIAN_POINT ( 'NONE',  ( -42.21835935851001409, 436.4384481632507118, 19.62208033733219281 ) ) ;
#41011=CARTESIAN_POINT ( 'NONE',  ( -32.87547266101657328, 465.6993878536670195, 10.91512469976128585 ) ) ;
#41026=EDGE_CURVE ( 'NONE', #54099, #4842, #82365, .T. ) ;
#41027=EDGE_LOOP ( 'NONE', ( #90323, #8061, #93492, #22535 ) ) ;
#41028=EDGE_CURVE ( 'NONE', #4655, #69148, #65120, .T. ) ;
#41029=ORIENTED_EDGE ( 'NONE', *, *, #80392, .T. ) ;
#41033=DIRECTION ( 'NONE',  ( 0.000000000000000000, -0.9971933454386562312, -0.07486943176531225819 ) ) ;
#41034=DIRECTION ( 'NONE',  ( 0.000000000000000000, 1.000000000000000000, 0.000000000000000000 ) ) ;
#41040=VERTEX_POINT ( 'NONE', #53146 ) ;
#41042=DIRECTION ( 'NONE',  ( 0.000000000000000000, 0.000000000000000000, 1.000000000000000000 ) ) ;
#41047=DIRECTION ( 'NONE',  ( 0.000000000000000000, 0.000000000000000000, -1.000000000000000000 ) ) ;
#41050=CARTESIAN_POINT ( 'NONE',  ( 32.00777521468064890, 486.7707349829203736, 6.765100014220078783 ) ) ;
#41065=CARTESIAN_POINT ( 'NONE',  ( -44.08840282922865583, 485.7747746244177165, 4.178803824087112595 ) ) ;
#41071=ORIENTED_EDGE ( 'NONE', *, *, #43951, .T. ) ;
#41091=CARTESIAN_POINT ( 'NONE',  ( -32.15047201613565164, 464.7337454272254718, 11.12330847294773228 ) ) ;
#41108=CARTESIAN_POINT ( 'NONE',  ( 37.51854390953261742, 313.5286481325095451, 14.45587837336505999 ) ) ;
#41113=CARTESIAN_POINT ( 'NONE',  ( -39.99946440396828251, 437.0919103049818091, 5.547728658188754380 ) ) ;
#41120=AXIS2_PLACEMENT_3D ( 'NONE', #35112, #34587, #67458 ) ;
#41161=CIRCLE ( 'NONE', #25732, 2.999999999999975131 ) ;
#41166=CARTESIAN_POINT ( 'NONE',  ( 43.62593301837074478, 434.3202385713651097, 14.43474084663391288 ) ) ;
#41175=CARTESIAN_POINT ( 'NONE',  ( 34.38464471054295757, 463.7420058808928616, 19.22113941038953300 ) ) ;
#41180=CARTESIAN_POINT ( 'NONE',  ( -40.73878143178837519, 486.4834083601638213, 16.46716573231486436 ) ) ;
#41182=CARTESIAN_POINT ( 'NONE',  ( -36.91281931599076671, 303.7809130842520631, -7.959270006439831846 ) ) ;
#41186=CARTESIAN_POINT ( 'NONE',  ( 27.93171118006010545, 307.0302625388608249, -9.289381728957501139 ) ) ;
#41195=CARTESIAN_POINT ( 'NONE',  ( -36.35757485292756996, 437.5916776841835372, 4.247500867393831925 ) ) ;
#41204=CIRCLE ( 'NONE', #87727, 1.000000000000000888 ) ;
#41206=ORIENTED_EDGE ( 'NONE', *, *, #33654, .T. ) ;
#41218=CARTESIAN_POINT ( 'NONE',  ( 35.44660262691603947, 372.8063709863593544, 5.056757807262998838 ) ) ;
#41219=EDGE_CURVE ( 'NONE', #58935, #38837, #94065, .T. ) ;
#41222=AXIS2_PLACEMENT_3D ( 'NONE', #98896, #90835, #704 ) ;
#41227=CARTESIAN_POINT ( 'NONE',  ( -11.46347932110838919, 294.5997472607351142, -10.05357601397031786 ) ) ;
#41236=CARTESIAN_POINT ( 'NONE',  ( 0.000000000000000000, 304.8518027762758038, -10.00000000000000355 ) ) ;
#41238=ORIENTED_EDGE ( 'NONE', *, *, #47226, .F. ) ;
#41239=EDGE_CURVE ( 'NONE', #97550, #9120, #27373, .T. ) ;
#41247=CARTESIAN_POINT ( 'NONE',  ( -34.78631043426883451, 321.1559080357926632, -5.542067064983624114 ) ) ;
#41249=CARTESIAN_POINT ( 'NONE',  ( 36.87655955837855259, 438.2068510013161813, 3.933030107424693167 ) ) ;
#41254=ADVANCED_FACE ( 'NONE', ( #88689 ), #42617, .F. ) ;
#41262=ORIENTED_EDGE ( 'NONE', *, *, #8211, .T. ) ;
#41269=( LENGTH_UNIT ( ) NAMED_UNIT ( * ) SI_UNIT ( .MILLI., .METRE. ) );
#41271=CARTESIAN_POINT ( 'NONE',  ( -35.31256682049455975, 491.0612481437016754, 12.05460915451396176 ) ) ;
#41296=CARTESIAN_POINT ( 'NONE',  ( -46.00000000000000000, 436.1058985003094222, 16.82352493621296219 ) ) ;
#41302=EDGE_CURVE ( 'NONE', #22095, #84655, #17012, .T. ) ;
#41305=CARTESIAN_POINT ( 'NONE',  ( 0.000000000000000000, 304.8518027762758038, -9.000000000000005329 ) ) ;
#41314=CARTESIAN_POINT ( 'NONE',  ( 31.14007908953173853, 298.5476415064817388, -1.182771435588934938 ) ) ;
#41318=CARTESIAN_POINT ( 'NONE',  ( -45.43339346675878687, 430.7348383325900727, 7.234598910837349628 ) ) ;
#41325=CARTESIAN_POINT ( 'NONE',  ( 43.67962081600994395, 397.2354176719359771, 16.03058559300318464 ) ) ;
#41334=ADVANCED_FACE ( 'NONE', ( #58984 ), #76323, .F. ) ;
#41339=CARTESIAN_POINT ( 'NONE',  ( 45.99999999999999289, 436.0048661157462675, 13.49129311716465907 ) ) ;
#41352=CARTESIAN_POINT ( 'NONE',  ( 37.51854390953261742, 313.5286481325095451, 14.45587837336505999 ) ) ;
#41355=CARTESIAN_POINT ( 'NONE',  ( -32.16069320047662927, 487.8952013991981289, 8.686498104318150837 ) ) ;
#41356=ORIENTED_EDGE ( 'NONE', *, *, #86875, .T. ) ;
#41366=( BOUNDED_SURFACE ( )  B_SPLINE_SURFACE ( 3, 2, ( 
 ( #69953, #94777, #4689 ),
 ( #11690, #54262, #20924 ),
 ( #21422, #53238, #87205 ),
 ( #94230, #21952, #12227 ),
 ( #37622, #30040, #62929 ),
 ( #102850, #79094, #54803 ),
 ( #46209, #76967, #77514 ),
 ( #3627, #36561, #69429 ) ),
 .UNSPECIFIED., .F., .F., .F. ) 
 B_SPLINE_SURFACE_WITH_KNOTS ( ( 4, 2, 2, 4 ),
 ( 3, 3 ),
 ( -2.081668171172168513E-17, 0.003573135830214766578, 0.005359703745322160276, 0.007146271660429553974 ),
 ( 0.000000000000000000, 1.000000000000000000 ),
 .UNSPECIFIED. ) 
 GEOMETRIC_REPRESENTATION_ITEM ( )  RATIONAL_B_SPLINE_SURFACE ( (
 ( 1.000000000000000000, 0.7246213771201909237, 1.000000000000000000),
 ( 1.000000000000000000, 0.7303455725924656861, 1.000000000000000000),
 ( 1.000000000000000000, 0.7358045286937978657, 1.000000000000000000),
 ( 1.000000000000000000, 0.7436032658800217909, 1.000000000000000000),
 ( 1.000000000000000000, 0.7461375964764297430, 1.000000000000000000),
 ( 1.000000000000000000, 0.7510703106232340387, 1.000000000000000000),
 ( 1.000000000000000000, 0.7534558991517000814, 1.000000000000000000),
 ( 1.000000000000000000, 0.7557288854865493732, 1.000000000000000000) ) ) 
 REPRESENTATION_ITEM ( '' )  SURFACE ( )  );
#41368=CARTESIAN_POINT ( 'NONE',  ( -20.56738711532560160, 303.9076102621805262, 9.948868387141734715 ) ) ;
#41377=CARTESIAN_POINT ( 'NONE',  ( -30.95825898926416286, 357.0936102330114181, 21.51415573308821294 ) ) ;
#41385=CARTESIAN_POINT ( 'NONE',  ( 32.13362087237139519, 435.4431350903298039, 16.29023341600430541 ) ) ;
#41386=CARTESIAN_POINT ( 'NONE',  ( 30.93291330028446851, 298.5973685216983995, 2.766521101297645391 ) ) ;
#41390=CARTESIAN_POINT ( 'NONE',  ( -40.86877072095277441, 461.0519673121690403, 2.323807444223201291 ) ) ;
#41396=CARTESIAN_POINT ( 'NONE',  ( -25.24187064870846697, 295.8089182665369776, 10.14309838663142749 ) ) ;
#41401=CARTESIAN_POINT ( 'NONE',  ( 3.040263676388296421, 300.3110236163819877, 9.529558508250175919 ) ) ;
#41420=DIRECTION ( 'NONE',  ( 0.000000000000000000, 1.000000000000000000, 1.224646799147353207E-16 ) ) ;
#41454=CARTESIAN_POINT ( 'NONE',  ( 29.85853377316651347, 330.9760585468098952, 16.31649794843299262 ) ) ;
#41459=FACE_OUTER_BOUND ( 'NONE', #71143, .T. ) ;
#41466=CARTESIAN_POINT ( 'NONE',  ( 38.85446894546473828, 460.8903912184138676, 2.218456751109172398 ) ) ;
#41476=DIRECTION ( 'NONE',  ( 0.1957247465660570951, 0.4045265792282223827, 0.8933364821160978408 ) ) ;
#41478=ORIENTED_EDGE ( 'NONE', *, *, #94304, .F. ) ;
#41485=CARTESIAN_POINT ( 'NONE',  ( 34.34094660030152824, 491.0078558915772078, 12.00869558947917071 ) ) ;
#41489=AXIS2_PLACEMENT_3D ( 'NONE', #19402, #35033, #27486 ) ;
#41496=EDGE_CURVE ( 'NONE', #69309, #75237, #98980, .T. ) ;
#41506=CARTESIAN_POINT ( 'NONE',  ( -33.85467187920592380, 321.4589499777674177, -5.706254074088779049 ) ) ;
#41511=CARTESIAN_POINT ( 'NONE',  ( -43.22728423988735358, 434.6919775797696843, 9.646941480594554363 ) ) ;
#41515=CARTESIAN_POINT ( 'NONE',  ( -25.38862679093923802, 295.7342021531224532, -1.810452940856004167 ) ) ;
#41520=CARTESIAN_POINT ( 'NONE',  ( -33.22150838192236932, 484.9899766982439360, 0.3198735837378168800 ) ) ;
#41521=CARTESIAN_POINT ( 'NONE',  ( -40.87700745978003170, 434.1252800992320431, 26.33294680167561097 ) ) ;
#41522=CARTESIAN_POINT ( 'NONE',  ( -32.78741055188853437, 485.3331003366707250, 5.977022408746862858 ) ) ;
#41526=CARTESIAN_POINT ( 'NONE',  ( -43.00000000000000000, 438.4646224975039672, 9.895601460523741011 ) ) ;
#41529=CARTESIAN_POINT ( 'NONE',  ( 44.11330561868255273, 485.7407100969332419, 4.043737255555224230 ) ) ;
#41531=CARTESIAN_POINT ( 'NONE',  ( -39.08248342308210965, 438.6092072988694213, 22.97679020934365823 ) ) ;
#41560=CARTESIAN_POINT ( 'NONE',  ( -42.09158233638504498, 465.7816406625409513, 14.79318349170026892 ) ) ;
#41572=DIRECTION ( 'NONE',  ( 0.000000000000000000, -0.9238632370065121835, 0.3827227708248480686 ) ) ;
#41577=CARTESIAN_POINT ( 'NONE',  ( 30.00000000000000355, 490.5636507777060160, 7.413185101891562212 ) ) ;
#41596=CARTESIAN_POINT ( 'NONE',  ( -43.18011688719700913, 485.8502513091206083, 5.262111696809587791 ) ) ;
#41612=CARTESIAN_POINT ( 'NONE',  ( 37.06956559601371737, 463.9941799042751427, 19.59960652757460409 ) ) ;
#41622=CARTESIAN_POINT ( 'NONE',  ( 32.15969615473760257, 464.7082453577105525, 10.94011554326026037 ) ) ;
#41632=CARTESIAN_POINT ( 'NONE',  ( 43.28401190480957439, 435.3393147692861476, 9.722488360065341340 ) ) ;
#41637=CARTESIAN_POINT ( 'NONE',  ( 40.88293604215247967, 432.5779639752643675, 26.56799667982232549 ) ) ;
#41641=CARTESIAN_POINT ( 'NONE',  ( 37.87043015219848030, 460.2235823560122867, 2.222860475111648970 ) ) ;
#41644=DIRECTION ( 'NONE',  ( 0.9730146112118936985, 0.000000000000000000, -0.2307435077486851283 ) ) ;
#41653=CARTESIAN_POINT ( 'NONE',  ( 43.51233770555737124, 462.0554640178511931, 4.320559117861924037 ) ) ;
#41659=CARTESIAN_POINT ( 'NONE',  ( -41.49039443806330496, 469.1026463824607617, 1.097952796331059799 ) ) ;
#41662=CIRCLE ( 'NONE', #38009, 10.00000000000000178 ) ;
#41672=CARTESIAN_POINT ( 'NONE',  ( -32.28733632729606740, 338.4947552595653519, 18.46383803629149867 ) ) ;
#41673=CARTESIAN_POINT ( 'NONE',  ( -32.70896709465985452, 434.6719836098827159, 17.16937924263439541 ) ) ;
#41676=CARTESIAN_POINT ( 'NONE',  ( -1.128077836147719282, 302.8478239976500390, 9.936168295454388399 ) ) ;
#41679=EDGE_CURVE ( 'NONE', #104099, #72660, #85227, .T. ) ;
#41683=DIRECTION ( 'NONE',  ( 0.000000000000000000, 0.000000000000000000, -1.000000000000000000 ) ) ;
#41689=CARTESIAN_POINT ( 'NONE',  ( 43.59756234217316972, 434.3244621007173123, 14.55946156040339368 ) ) ;
#41692=DIRECTION ( 'NONE',  ( -8.400342417351198358E-11, -1.000000000000000000, 0.000000000000000000 ) ) ;
#41700=CARTESIAN_POINT ( 'NONE',  ( 46.00000000000000000, 450.0000000000002274, 18.20242257375371153 ) ) ;
#41703=CARTESIAN_POINT ( 'NONE',  ( 37.56086443614415060, 463.3607749238105384, 20.02088289192820625 ) ) ;
#41709=CARTESIAN_POINT ( 'NONE',  ( -45.43339346675878687, 430.7348383325900727, 7.234598910837349628 ) ) ;
#41711=CARTESIAN_POINT ( 'NONE',  ( -40.73878142687892279, 503.7113041876743864, 10.19672445236252045 ) ) ;
#41713=ORIENTED_EDGE ( 'NONE', *, *, #50693, .T. ) ;
#41714=CARTESIAN_POINT ( 'NONE',  ( 24.60261549097931422, 305.9904144327904874, -8.752652469573394711 ) ) ;
#41735=VERTEX_POINT ( 'NONE', #52611 ) ;
#41736=CIRCLE ( 'NONE', #354, 15.00000000000000711 ) ;
#41745=CARTESIAN_POINT ( 'NONE',  ( 42.37751841893198446, 435.9440627571722757, 7.948837343527291210 ) ) ;
#41750=CARTESIAN_POINT ( 'NONE',  ( 23.08346828195956135, 305.3972529807544447, -8.882845993008418262 ) ) ;
#41765=CARTESIAN_POINT ( 'NONE',  ( 30.00000000000000355, 461.9590195980686076, 14.34002891080987574 ) ) ;
#41766=CARTESIAN_POINT ( 'NONE',  ( 41.86260695335559490, 487.3392455165184742, 9.527470086610451361 ) ) ;
#41775=SURFACE_STYLE_FILL_AREA ( #91408 ) ;
#41779=TOROIDAL_SURFACE ( 'NONE', #89971, 12.00000000000001066, 3.000000000000000000 ) ;
#41780=CARTESIAN_POINT ( 'NONE',  ( -33.45340520273420282, 315.3731966014437944, -7.001726257038141554 ) ) ;
#41798=CARTESIAN_POINT ( 'NONE',  ( -35.91982565306560105, 490.8454349930416925, 12.40602332252255380 ) ) ;
#41806=CARTESIAN_POINT ( 'NONE',  ( -11.93255308427328565, 294.5886021379643580, 9.881054392645332030 ) ) ;
#41809=VERTEX_POINT ( 'NONE', #35959 ) ;
#41810=DIRECTION ( 'NONE',  ( 0.000000000000000000, -0.9523642049635228091, 0.3049629831704120941 ) ) ;
#41819=CIRCLE ( 'NONE', #78026, 1.000000000000001110 ) ;
#41843=CARTESIAN_POINT ( 'NONE',  ( 27.49230554713799535, 305.3620761542157425, -9.445234096144215385 ) ) ;
#41853=DIRECTION ( 'NONE',  ( 0.2246406655633822746, 0.2919586099461945472, 0.9296756108737748159 ) ) ;
#41855=( BOUNDED_SURFACE ( )  B_SPLINE_SURFACE ( 3, 2, ( 
 ( #61691, #61138, #33965 ),
 ( #41485, #72779, #16685 ),
 ( #33423, #90038, #65770 ),
 ( #985, #83016, #17238 ),
 ( #49576, #9109, #64710 ),
 ( #23749, #66836, #82485 ),
 ( #89519, #56050, #91128 ),
 ( #6987, #23212, #66296 ),
 ( #15084, #58202, #50108 ),
 ( #7507, #25339, #32364 ),
 ( #99178, #49033, #105686 ),
 ( #81931, #106745, #31825 ),
 ( #40427, #42017, #15613 ),
 ( #98650, #24800, #88985 ),
 ( #74901, #57654, #47969 ),
 ( #80878, #90575, #452 ) ),
 .UNSPECIFIED., .F., .F., .T. ) 
 B_SPLINE_SURFACE_WITH_KNOTS ( ( 4, 2, 2, 2, 2, 2, 2, 4 ),
 ( 3, 3 ),
 ( 2.545706700995964411E-16, 0.001044086800740991585, 0.001566130201111359983, 0.002088173601481728599, 0.002610217001852097214, 0.003132260402222465396, 0.003654303802592833578, 0.004176347202963202193 ),
 ( 0.000000000000000000, 1.000000000000000000 ),
 .UNSPECIFIED. ) 
 GEOMETRIC_REPRESENTATION_ITEM ( )  RATIONAL_B_SPLINE_SURFACE ( (
 ( 1.000000000000000000, 0.8350736500407900387, 1.000000000000000000),
 ( 1.000000000000000000, 0.8489954227499153516, 1.000000000000000000),
 ( 1.000000000000000000, 0.8615675893698659937, 1.000000000000000000),
 ( 1.000000000000000000, 0.8776574663914948893, 1.000000000000000000),
 ( 1.000000000000000000, 0.8825492266254932883, 1.000000000000000000),
 ( 1.000000000000000000, 0.8909252284681432599, 1.000000000000000000),
 ( 1.000000000000000000, 0.8944578560788611910, 1.000000000000000000),
 ( 1.000000000000000000, 0.9000429021731324308, 1.000000000000000000),
 ( 1.000000000000000000, 0.9020681612885971257, 1.000000000000000000),
 ( 1.000000000000000000, 0.9043430709035563675, 1.000000000000000000),
 ( 1.000000000000000000, 0.9046293304020973647, 1.000000000000000000),
 ( 1.000000000000000000, 0.9034445554302690251, 1.000000000000000000),
 ( 1.000000000000000000, 0.9019515008114564747, 1.000000000000000000),
 ( 1.000000000000000000, 0.8973842636250342064, 1.000000000000000000),
 ( 1.000000000000000000, 0.8943059481781064912, 1.000000000000000000),
 ( 1.000000000000000000, 0.8904848454315665851, 1.000000000000000000) ) ) 
 REPRESENTATION_ITEM ( '' )  SURFACE ( )  );
#41856=CARTESIAN_POINT ( 'NONE',  ( 45.46270652965668546, 379.8533979750452545, 7.113780170705016559 ) ) ;
#41873=CARTESIAN_POINT ( 'NONE',  ( 36.23910820157426826, 462.2855794318964513, 3.478784509830200822 ) ) ;
#41874=CARTESIAN_POINT ( 'NONE',  ( 37.62251730745840916, 437.3427388312647395, 4.535622330043188377 ) ) ;
#41902=CARTESIAN_POINT ( 'NONE',  ( 43.58619280597294221, 434.9882623928568819, 14.52865984557667112 ) ) ;
#41905=CARTESIAN_POINT ( 'NONE',  ( -38.54161147518751562, 464.3852313890828327, 18.95019507570325246 ) ) ;
#41906=CARTESIAN_POINT ( 'NONE',  ( -32.16711761884142362, 380.6411173872397740, 24.65392784832810946 ) ) ;
#41908=ORIENTED_EDGE ( 'NONE', *, *, #20735, .F. ) ;
#41914=CARTESIAN_POINT ( 'NONE',  ( 27.08164365510018357, 307.1447734948634434, 10.92944225879553244 ) ) ;
#41915=CARTESIAN_POINT ( 'NONE',  ( 46.00000000000000000, 450.0000000000002274, 8.202422573753707979 ) ) ;
#41918=CARTESIAN_POINT ( 'NONE',  ( -40.42601080768528732, 460.8348341399804440, 2.184598410783807676 ) ) ;
#41924=ORIENTED_EDGE ( 'NONE', *, *, #67566, .T. ) ;
#41933=CARTESIAN_POINT ( 'NONE',  ( 46.00000000000000000, 461.6622277975422435, 10.18145404766786655 ) ) ;
#41939=CARTESIAN_POINT ( 'NONE',  ( 0.000000000000000000, 274.9999999999999432, -10.00000000000000533 ) ) ;
#41967=ORIENTED_EDGE ( 'NONE', *, *, #40350, .T. ) ;
#41970=CARTESIAN_POINT ( 'NONE',  ( 42.36808196472505017, 461.6713445545161107, 3.771400599639998852 ) ) ;
#41971=CARTESIAN_POINT ( 'NONE',  ( 40.02102699515286588, 489.9193542772574688, 11.11924804287039947 ) ) ;
#41976=CARTESIAN_POINT ( 'NONE',  ( 2.255773162242571850, 294.8363355346813819, -9.758683423828378167 ) ) ;
#41983=CARTESIAN_POINT ( 'NONE',  ( 32.18022392672646959, 410.2513953074889628, 25.67977927016873352 ) ) ;
#42003=CARTESIAN_POINT ( 'NONE',  ( 0.000000000000000000, 69.00000000000000000, 0.000000000000000000 ) ) ;
#42006=CARTESIAN_POINT ( 'NONE',  ( -6.864655157840108046, 294.7328080983203336, -7.282300053873971279 ) ) ;
#42014=CARTESIAN_POINT ( 'NONE',  ( -41.92130353528092002, 485.3101580674256184, -3.082360575756684984 ) ) ;
#42017=CARTESIAN_POINT ( 'NONE',  ( 37.08530234602800135, 491.4084519804410434, 12.30481897466681218 ) ) ;
#42018=CARTESIAN_POINT ( 'NONE',  ( -35.96984888422242221, 491.2799073994592618, 12.80368214530777848 ) ) ;
#42036=CARTESIAN_POINT ( 'NONE',  ( 34.50120583711849775, 434.4753093497994314, 9.494494844945867484 ) ) ;
#42037=CARTESIAN_POINT ( 'NONE',  ( -27.64766936045855772, 308.1634638491052556, -9.255587232834342259 ) ) ;
#42041=CARTESIAN_POINT ( 'NONE',  ( -34.26493447578224760, 490.0907185571355740, 11.27927472376731544 ) ) ;
#42046=CARTESIAN_POINT ( 'NONE',  ( -25.53351597638959092, 295.7776190944981067, -1.801019599846679142 ) ) ;
#42050=CARTESIAN_POINT ( 'NONE',  ( -35.04037255257541972, 484.2364580523164932, -0.9782185570580150813 ) ) ;
#42051=CARTESIAN_POINT ( 'NONE',  ( -39.28811459529073602, 326.5013068576240585, 17.64810832725432022 ) ) ;
#42052=CARTESIAN_POINT ( 'NONE',  ( -32.80441372020654711, 485.2966253772736991, 5.899827864538937483 ) ) ;
#42059=CARTESIAN_POINT ( 'NONE',  ( 43.49287295680601773, 484.8086259266613069, 4.190157679464852514 ) ) ;
#42064=CARTESIAN_POINT ( 'NONE',  ( 42.20041562234358423, 435.2369744135583574, 7.788607701745476675 ) ) ;
#42078=CARTESIAN_POINT ( 'NONE',  ( 33.00000000000000000, 500.0000000000002274, 0.000000000000000000 ) ) ;
#42081=ORIENTED_EDGE ( 'NONE', *, *, #42575, .T. ) ;
#42084=CARTESIAN_POINT ( 'NONE',  ( -37.54559764570181812, 464.1143081516144662, 19.43664670202813838 ) ) ;
#42094=DIRECTION ( 'NONE',  ( -1.000000000000000000, -0.000000000000000000, -0.000000000000000000 ) ) ;
#42102=CARTESIAN_POINT ( 'NONE',  ( 42.00989057911306190, 460.5566595377485442, 2.543045191523135351 ) ) ;
#42104=CARTESIAN_POINT ( 'NONE',  ( 30.00000000000077094, 487.0612273928530840, 5.833475372789068025 ) ) ;
#42114=CARTESIAN_POINT ( 'NONE',  ( 31.95108112711128001, 486.7719899256358644, 6.757615638381732737 ) ) ;
#42143=FACE_OUTER_BOUND ( 'NONE', #6546, .T. ) ;
#42146=ADVANCED_FACE ( 'NONE', ( #10433 ), #72235, .F. ) ;
#42153=CARTESIAN_POINT ( 'NONE',  ( -32.84444940698905668, 439.0476299206102340, 24.86213004146479122 ) ) ;
#42156=CARTESIAN_POINT ( 'NONE',  ( 43.63899620156486492, 434.3182181978404515, 14.37213632273144448 ) ) ;
#42159=ORIENTED_EDGE ( 'NONE', *, *, #47226, .T. ) ;
#42175=VERTEX_POINT ( 'NONE', #84870 ) ;
#42187=EDGE_LOOP ( 'NONE', ( #62481, #5388 ) ) ;
#42198=CARTESIAN_POINT ( 'NONE',  ( -27.50149470030765286, 307.8944781523804863, 11.11325752724550497 ) ) ;
#42203=CARTESIAN_POINT ( 'NONE',  ( -1.700304210406924588, 301.6922864547469203, 9.856359514573828307 ) ) ;
#42209=CARTESIAN_POINT ( 'NONE',  ( 20.34580746390948747, 294.7747570175440615, -2.016376581567297155 ) ) ;
#42217=ADVANCED_FACE ( 'NONE', ( #72117 ), #48601, .T. ) ;
#42222=CARTESIAN_POINT ( 'NONE',  ( 33.97359119245065529, 434.1099241184708148, 11.80501937577158245 ) ) ;
#42230=CARTESIAN_POINT ( 'NONE',  ( -44.43774958859658142, 337.2802145563449017, 0.2445019049555710311 ) ) ;
#42241=CARTESIAN_POINT ( 'NONE',  ( 0.000000000000000000, 70.00000000000000000, 0.000000000000000000 ) ) ;
#42257=CARTESIAN_POINT ( 'NONE',  ( 0.000000000000000000, 0.000000000000000000, -5.000000000000003553 ) ) ;
#42261=DIRECTION ( 'NONE',  ( -0.000000000000000000, -1.000000000000000000, -0.000000000000000000 ) ) ;
#42263=CARTESIAN_POINT ( 'NONE',  ( 43.59536836154811823, 485.3411848763689704, 3.528079522877425322 ) ) ;
#42276=CARTESIAN_POINT ( 'NONE',  ( 35.30917598036950267, 361.3009821353402344, 3.520162773547422574 ) ) ;
#42280=EDGE_CURVE ( 'NONE', #27128, #87574, #74548, .T. ) ;
#42285=CARTESIAN_POINT ( 'NONE',  ( -19.13075804668806512, 294.6725005060797571, -2.037659674250595909 ) ) ;
#42291=CARTESIAN_POINT ( 'NONE',  ( 32.20627048526277036, 464.6794164287632611, 10.68709986547568391 ) ) ;
#42294=CARTESIAN_POINT ( 'NONE',  ( 3.493042281569127550, 304.8518027749427119, -10.00000000028269298 ) ) ;
#42300=ORIENTED_EDGE ( 'NONE', *, *, #67936, .F. ) ;
#42307=CARTESIAN_POINT ( 'NONE',  ( -41.98925252415875065, 316.9863883246551381, -4.665354603801200817 ) ) ;
#42314=CARTESIAN_POINT ( 'NONE',  ( 40.46237499442743513, 464.0765077733557860, 18.40249546253095758 ) ) ;
#42321=( BOUNDED_SURFACE ( )  B_SPLINE_SURFACE ( 3, 2, ( 
 ( #73505, #89717, #40098 ),
 ( #7183, #83203, #72973 ),
 ( #23406, #64904, #57850 ),
 ( #23952, #48697, #81584 ),
 ( #49228, #65960, #7709 ),
 ( #98840, #74573, #90239 ),
 ( #33615, #99368, #106404 ),
 ( #25547, #58406, #16343 ),
 ( #32563, #9300, #57321 ),
 ( #98329, #65435, #90779 ),
 ( #24485, #49774, #72457 ),
 ( #105365, #82133, #64386 ),
 ( #8248, #56249, #125 ),
 ( #82675, #2811, #91836 ),
 ( #34160, #58945, #77247 ),
 ( #11424, #59483, #26610 ),
 ( #60028, #100982, #27678 ),
 ( #35219, #9835, #3362 ) ),
 .UNSPECIFIED., .F., .F., .F. ) 
 B_SPLINE_SURFACE_WITH_KNOTS ( ( 4, 2, 2, 2, 2, 2, 2, 2, 4 ),
 ( 3, 3 ),
 ( -2.862293735361731706E-17, 0.001555391903720538442, 0.003110783807441105508, 0.004666175711161672790, 0.006221567614882239639, 0.007776959518602806487, 0.009332351422323373336, 0.01088774332604394018, 0.01244313522976450877 ),
 ( 0.000000000000000000, 1.000000000000000000 ),
 .UNSPECIFIED. ) 
 GEOMETRIC_REPRESENTATION_ITEM ( )  RATIONAL_B_SPLINE_SURFACE ( (
 ( 1.000000000000000000, 0.9028401456532985092, 1.000000000000000000),
 ( 1.000000000000000000, 0.9067516630662485477, 1.000000000000000000),
 ( 1.000000000000000000, 0.9091058375364423627, 1.000000000000000000),
 ( 1.000000000000000000, 0.9105595566477392433, 1.000000000000000000),
 ( 1.000000000000000000, 0.9096051370505221501, 1.000000000000000000),
 ( 1.000000000000000000, 0.9045241161555340748, 1.000000000000000000),
 ( 1.000000000000000000, 0.9004407328802259691, 1.000000000000000000),
 ( 1.000000000000000000, 0.8894899492097501081, 1.000000000000000000),
 ( 1.000000000000000000, 0.8827450154233547064, 1.000000000000000000),
 ( 1.000000000000000000, 0.8674022177617248808, 1.000000000000000000),
 ( 1.000000000000000000, 0.8587750089643293450, 1.000000000000000000),
 ( 1.000000000000000000, 0.8400002396215728862, 1.000000000000000000),
 ( 1.000000000000000000, 0.8300505958792420147, 1.000000000000000000),
 ( 1.000000000000000000, 0.8096117823345528874, 1.000000000000000000),
 ( 1.000000000000000000, 0.7991063331010617166, 1.000000000000000000),
 ( 1.000000000000000000, 0.7781243022290107447, 1.000000000000000000),
 ( 1.000000000000000000, 0.7679211400719462288, 1.000000000000000000),
 ( 1.000000000000000000, 0.7583909709667225885, 1.000000000000000000) ) ) 
 REPRESENTATION_ITEM ( '' )  SURFACE ( )  );
#42324=ORIENTED_EDGE ( 'NONE', *, *, #31191, .F. ) ;
#42332=AXIS2_PLACEMENT_3D ( 'NONE', #39120, #64965, #63928 ) ;
#42339=CARTESIAN_POINT ( 'NONE',  ( 31.90195216159137814, 465.6468698803305983, 10.69263942007829549 ) ) ;
#42341=CARTESIAN_POINT ( 'NONE',  ( -19.70764564238367100, 304.7954121406193053, 9.925013215726757210 ) ) ;
#42356=CARTESIAN_POINT ( 'NONE',  ( -38.51502786940007184, 460.0233756673457606, 2.043034587342192676 ) ) ;
#42358=CARTESIAN_POINT ( 'NONE',  ( -43.40156817618215968, 435.0518544017560316, 15.31415127474093651 ) ) ;
#42370=CARTESIAN_POINT ( 'NONE',  ( -35.25991156925849879, 303.5722148236554858, 3.944335390694383214 ) ) ;
#42375=CARTESIAN_POINT ( 'NONE',  ( 33.66264974566500712, 300.0834067526730564, -8.832479651548673871 ) ) ;
#42381=ORIENTED_EDGE ( 'NONE', *, *, #40350, .F. ) ;
#42390=CARTESIAN_POINT ( 'NONE',  ( -22.47298735892809418, 305.4392088308884468, 10.06407263457672663 ) ) ;
#42391=ORIENTED_EDGE ( 'NONE', *, *, #82481, .T. ) ;
#42392=CARTESIAN_POINT ( 'NONE',  ( 37.53110860859745657, 485.4504903723462235, -3.702833747837409373 ) ) ;
#42394=CARTESIAN_POINT ( 'NONE',  ( 32.80551872593247253, 486.0171861992463391, 5.671217483526194592 ) ) ;
#42398=CARTESIAN_POINT ( 'NONE',  ( 44.13152524673034094, 435.3762053705510766, 10.68396593870416567 ) ) ;
#42412=CYLINDRICAL_SURFACE ( 'NONE', #102950, 5.000000000000001776 ) ;
#42415=CARTESIAN_POINT ( 'NONE',  ( 22.91885868373643831, 305.6172567281201964, 10.10309701371861912 ) ) ;
#42418=CARTESIAN_POINT ( 'NONE',  ( -32.11957450231075484, 486.1307089099603331, 5.366351229208995655 ) ) ;
#42423=DIRECTION ( 'NONE',  ( 0.000000000000000000, 0.000000000000000000, -1.000000000000000000 ) ) ;
#42446=CARTESIAN_POINT ( 'NONE',  ( 33.40626526979832533, 300.9755454843282223, 3.321175472843470367 ) ) ;
#42450=AXIS2_PLACEMENT_3D ( 'NONE', #14655, #105285, #88051 ) ;
#42456=CARTESIAN_POINT ( 'NONE',  ( -26.05698008878660588, 296.0953443834534369, 10.20571257035117618 ) ) ;
#42458=CARTESIAN_POINT ( 'NONE',  ( 43.00000000000000000, 436.5989882784185738, 19.94133085611158407 ) ) ;
#42468=PLANE ( 'NONE',  #17725 ) ;
#42473=CIRCLE ( 'NONE', #74946, 6.000000000000001776 ) ;
#42479=CARTESIAN_POINT ( 'NONE',  ( 35.55347100935683358, 490.6492510279384760, 12.31610217058555534 ) ) ;
#42512=AXIS2_PLACEMENT_3D ( 'NONE', #176, #67084, #40668 ) ;
#42517=CARTESIAN_POINT ( 'NONE',  ( 29.19175403363693988, 323.8406402827946522, 14.62108096419524728 ) ) ;
#42526=CARTESIAN_POINT ( 'NONE',  ( -19.70764564238371719, 304.7954121406193622, 9.925013215726785631 ) ) ;
#42542=CARTESIAN_POINT ( 'NONE',  ( -16.16328599919005526, 302.5659913735702844, 9.876334255033473397 ) ) ;
#42543=CARTESIAN_POINT ( 'NONE',  ( -42.19179521602266902, 485.4956273777415277, -3.824025998169080953 ) ) ;
#42547=EDGE_CURVE ( 'NONE', #48471, #1725, #42745, .T. ) ;
#42549=ORIENTED_EDGE ( 'NONE', *, *, #106052, .T. ) ;
#42566=CARTESIAN_POINT ( 'NONE',  ( -20.21880305278368439, 304.8280059657581660, -9.005058168222323189 ) ) ;
#42575=EDGE_CURVE ( 'NONE', #49860, #67806, #89256, .T. ) ;
#42578=CARTESIAN_POINT ( 'NONE',  ( -34.88410131646318746, 485.0165076724375126, -0.9913809214317844676 ) ) ;
#42579=CARTESIAN_POINT ( 'NONE',  ( -32.95623456616201707, 360.3788937733320381, 22.49516265375592994 ) ) ;
#42593=CARTESIAN_POINT ( 'NONE',  ( 0.000000000000000000, -19.99999999999998934, 0.000000000000000000 ) ) ;
#42594=CARTESIAN_POINT ( 'NONE',  ( 43.71217423904101196, 435.6632154632235370, 9.092528312217412534 ) ) ;
#42595=CARTESIAN_POINT ( 'NONE',  ( -32.91772945487021929, 464.9199415683336838, 10.91424143556015736 ) ) ;
#42610=CARTESIAN_POINT ( 'NONE',  ( 46.00000000000000000, 450.0000000000002274, 13.20242257375370976 ) ) ;
#42617=( BOUNDED_SURFACE ( )  B_SPLINE_SURFACE ( 3, 2, ( 
 ( #80050, #71973, #23993 ),
 ( #79003, #5123, #38056 ),
 ( #104881, #55758, #31021 ),
 ( #29949, #62833, #63902 ) ),
 .UNSPECIFIED., .F., .F., .F. ) 
 B_SPLINE_SURFACE_WITH_KNOTS ( ( 4, 4 ),
 ( 3, 3 ),
 ( -1.994931997373328159E-17, 0.003511371752234733381 ),
 ( 0.000000000000000000, 1.000000000000000000 ),
 .UNSPECIFIED. ) 
 GEOMETRIC_REPRESENTATION_ITEM ( )  RATIONAL_B_SPLINE_SURFACE ( (
 ( 1.000000000000000000, 0.7409272757993310421, 1.000000000000000000),
 ( 1.000000000000000000, 0.7572402302192458023, 1.000000000000000000),
 ( 1.000000000000000000, 0.7731133056331223052, 1.000000000000000000),
 ( 1.000000000000000000, 0.7888522786294931421, 1.000000000000000000) ) ) 
 REPRESENTATION_ITEM ( '' )  SURFACE ( )  );
#42618=EDGE_CURVE ( 'NONE', #58946, #12676, #46216, .T. ) ;
#42625=CIRCLE ( 'NONE', #71969, 3.000000000000018208 ) ;
#42637=CARTESIAN_POINT ( 'NONE',  ( 41.35951450183790712, 460.7308729162546683, 2.709719765170301109 ) ) ;
#42638=CARTESIAN_POINT ( 'NONE',  ( -33.26776902584375506, 435.2199417381641524, 10.58436218359535985 ) ) ;
#42677=CIRCLE ( 'NONE', #58142, 2.999999999999999112 ) ;
#42678=CARTESIAN_POINT ( 'NONE',  ( 33.00000000000000000, 464.3970849722209095, 17.41240408234224191 ) ) ;
#42684=ADVANCED_FACE ( 'NONE', ( #105687 ), #46728, .T. ) ;
#42691=EDGE_LOOP ( 'NONE', ( #80619, #80324, #80549, #59596 ) ) ;
#42693=CARTESIAN_POINT ( 'NONE',  ( 43.71675722381548468, 435.0430370927871309, 11.37024750953607288 ) ) ;
#42703=CARTESIAN_POINT ( 'NONE',  ( -24.83963492381722915, 307.1563561209093223, 9.458452572052934215 ) ) ;
#42704=AXIS2_PLACEMENT_3D ( 'NONE', #59391, #99824, #100884 ) ;
#42711=EDGE_CURVE ( 'NONE', #59047, #6978, #3173, .T. ) ;
#42716=CARTESIAN_POINT ( 'NONE',  ( 23.71188932895429247, 304.9123084062130147, 10.16850580752430133 ) ) ;
#42734=CARTESIAN_POINT ( 'NONE',  ( 30.00000000000000355, 488.7105343895291298, 4.072475192012525724 ) ) ;
#42736=CARTESIAN_POINT ( 'NONE',  ( -33.14436125469611483, 382.5759126738042255, 24.99667975960740307 ) ) ;
#42745=CIRCLE ( 'NONE', #99637, 1.000000000000005329 ) ;
#42749=CARTESIAN_POINT ( 'NONE',  ( 33.00000000000000000, 450.0000000000002274, 13.20242257375370976 ) ) ;
#42754=EDGE_CURVE ( 'NONE', #79974, #69611, #51217, .T. ) ;
#42759=STYLED_ITEM ( 'NONE', ( #77332 ), #2839 ) ;
#42761=CARTESIAN_POINT ( 'NONE',  ( 32.10720520530002631, 436.4653991243506539, 19.53468662359128771 ) ) ;
#42765=CARTESIAN_POINT ( 'NONE',  ( -45.40507512465600115, 439.2794387026467575, 6.273370203490043373 ) ) ;
#42768=CARTESIAN_POINT ( 'NONE',  ( -45.40507512465600115, 439.2794387026467575, 6.273370203490043373 ) ) ;
#42779=CARTESIAN_POINT ( 'NONE',  ( -30.00000000000000000, 461.8423635046866025, 11.25802415799497247 ) ) ;
#42780=CARTESIAN_POINT ( 'NONE',  ( -43.00000000000000000, 500.0000000000002274, 0.000000000000000000 ) ) ;
#42787=CARTESIAN_POINT ( 'NONE',  ( -36.50546997061886856, 437.5879066196182521, 4.249723241245790817 ) ) ;
#42802=CARTESIAN_POINT ( 'NONE',  ( 31.90667051052400183, 313.6962960773610689, -7.665056271795368303 ) ) ;
#42808=CARTESIAN_POINT ( 'NONE',  ( -33.00000000000000000, 439.0771093100264011, 24.89389206971033630 ) ) ;
#42815=CARTESIAN_POINT ( 'NONE',  ( 35.49008156062310348, 378.5703878965198896, 5.677488699590466759 ) ) ;
#42821=ORIENTED_EDGE ( 'NONE', *, *, #14379, .F. ) ;
#42822=CARTESIAN_POINT ( 'NONE',  ( 0.000000000000000000, 70.00000000000000000, 0.000000000000000000 ) ) ;
#42824=CARTESIAN_POINT ( 'NONE',  ( -44.26028122668987663, 485.3157014729772527, 1.872110468834934371 ) ) ;
#42828=CIRCLE ( 'NONE', #97942, 15.00000000000000711 ) ;
#42832=CARTESIAN_POINT ( 'NONE',  ( 42.08762648273149409, 487.0030674539048618, 9.106351919857861077 ) ) ;
#42845=CARTESIAN_POINT ( 'NONE',  ( -40.50844031276214707, 311.4578814011395593, -6.061433927898559837 ) ) ;
#42846=CARTESIAN_POINT ( 'NONE',  ( -3.389927784054740378, 303.8518027742029517, -9.999999999492535707 ) ) ;
#42854=EDGE_CURVE ( 'NONE', #15159, #63037, #97445, .T. ) ;
#42869=DIRECTION ( 'NONE',  ( -1.000000000000000000, 0.000000000000000000, 0.000000000000000000 ) ) ;
#42876=B_SPLINE_CURVE_WITH_KNOTS ( 'NONE', 3,
 ( #84880, #78372, #10966, #93516 ),
 .UNSPECIFIED., .F., .F.,
 ( 4, 4 ),
 ( 1.110764993427085326E-17, 0.002190562081029153070 ),
 .UNSPECIFIED. ) ;
#42898=CARTESIAN_POINT ( 'NONE',  ( -43.03880698781986780, 435.3545807224046484, 16.83573131045131177 ) ) ;
#42910=CARTESIAN_POINT ( 'NONE',  ( -37.49021801792793696, 468.5024337580119891, 18.51843040749166036 ) ) ;
#42911=CARTESIAN_POINT ( 'NONE',  ( -42.77015032893616109, 384.6486852084936459, 19.22311796600492428 ) ) ;
#42914=CARTESIAN_POINT ( 'NONE',  ( -33.19749974117156910, 318.2248943830853705, -6.522189075947168568 ) ) ;
#42918=CARTESIAN_POINT ( 'NONE',  ( 24.04676408874582094, 303.6130512030635487, -9.836050131052919809 ) ) ;
#42919=CARTESIAN_POINT ( 'NONE',  ( 34.72474116627837759, 338.3618661353910966, -1.881472242819908436 ) ) ;
#42922=DIRECTION ( 'NONE',  ( -1.000000000000000000, 0.000000000000000000, 0.000000000000000000 ) ) ;
#42930=CARTESIAN_POINT ( 'NONE',  ( 45.39396809536891197, 371.0197163396430255, 6.150425833335645187 ) ) ;
#42960=DIRECTION ( 'NONE',  ( -1.000000000000000000, 0.000000000000000000, 0.000000000000000000 ) ) ;
#42962=CARTESIAN_POINT ( 'NONE',  ( -30.00000000000004263, 488.6881500922590931, 8.886576284446979557 ) ) ;
#42973=CARTESIAN_POINT ( 'NONE',  ( -30.93853997290534252, 332.3618051370746116, 16.87088913439686166 ) ) ;
#42977=ORIENTED_EDGE ( 'NONE', *, *, #59285, .T. ) ;
#42982=CARTESIAN_POINT ( 'NONE',  ( 41.93118512340635107, 437.4679042107824785, 21.45618714866054688 ) ) ;
#42983=CARTESIAN_POINT ( 'NONE',  ( -32.19453080399548384, 398.3975244587722386, 25.63225119969380472 ) ) ;
#42988=CARTESIAN_POINT ( 'NONE',  ( 33.00795325653179901, 439.3958174160654266, 23.82489859418954836 ) ) ;
#42991=CARTESIAN_POINT ( 'NONE',  ( 32.90571795128548871, 300.4295626401157620, 3.192642666177045285 ) ) ;
#43006=CARTESIAN_POINT ( 'NONE',  ( 0.9627154012949672435, 294.8487549602114086, 9.936351565176062550 ) ) ;
#43022=DIRECTION ( 'NONE',  ( 1.000000000000000000, 0.000000000000000000, 0.000000000000000000 ) ) ;
#43029=CARTESIAN_POINT ( 'NONE',  ( -35.48628994100880618, 491.6413678155955722, 12.45547902532470275 ) ) ;
#43034=B_SPLINE_CURVE_WITH_KNOTS ( 'NONE', 3,
 ( #98907, #69242, #29336, #44968, #94587, #102115, #77318, #2350, #3963, #61142, #94031, #95109 ),
 .UNSPECIFIED., .F., .F.,
 ( 4, 2, 2, 2, 2, 4 ),
 ( 0.000000000000000000, 0.0009583675032029950139, 0.001916735006405990028, 0.003833470012811976586, 0.005750205019217962711, 0.007666940025623949703 ),
 .UNSPECIFIED. ) ;
#43048=ORIENTED_EDGE ( 'NONE', *, *, #97623, .F. ) ;
#43054=CARTESIAN_POINT ( 'NONE',  ( 51.01037695545453232, 500.0000000000002274, 0.000000000000000000 ) ) ;
#43057=EDGE_CURVE ( 'NONE', #104952, #93305, #18768, .T. ) ;
#43062=ORIENTED_EDGE ( 'NONE', *, *, #86941, .F. ) ;
#43064=CARTESIAN_POINT ( 'NONE',  ( 30.47457020840358055, 336.9194354044551574, 16.65755050439408080 ) ) ;
#43073=CARTESIAN_POINT ( 'NONE',  ( -35.59667163540026280, 463.9592197885497171, -0.04846191499040426731 ) ) ;
#43082=CARTESIAN_POINT ( 'NONE',  ( -5.645355559288413261, 301.6283892719433197, -10.01771515669004309 ) ) ;
#43086=CARTESIAN_POINT ( 'NONE',  ( 44.11327388758692081, 464.4313852428372797, 9.822198357557351045 ) ) ;
#43090=CARTESIAN_POINT ( 'NONE',  ( -16.33234527380769663, 294.5674836605464293, 1.876698257015430027 ) ) ;
#43099=CARTESIAN_POINT ( 'NONE',  ( -46.00000000000000000, 437.8943772434384414, 13.39121328441609471 ) ) ;
#43109=CARTESIAN_POINT ( 'NONE',  ( -26.59921953414089657, 305.9461108162179244, -9.538870392573779000 ) ) ;
#43122=CARTESIAN_POINT ( 'NONE',  ( -37.53250272162412671, 485.4507222580152757, -3.703678762838515048 ) ) ;
#43123=CARTESIAN_POINT ( 'NONE',  ( -33.14071268597706421, 415.4777461792551208, 25.72715652696946620 ) ) ;
#43130=( BOUNDED_SURFACE ( )  B_SPLINE_SURFACE ( 3, 2, ( 
 ( #58930, #59468, #50804 ),
 ( #83708, #9817, #42734 ),
 ( #75625, #1728, #67553 ),
 ( #95534, #44880, #12472 ) ),
 .UNSPECIFIED., .F., .F., .F. ) 
 B_SPLINE_SURFACE_WITH_KNOTS ( ( 4, 4 ),
 ( 3, 3 ),
 ( 0.01376892490370373347, 0.01435419950459405729 ),
 ( 0.1691075354860943070, 1.000000000000000000 ),
 .UNSPECIFIED. ) 
 GEOMETRIC_REPRESENTATION_ITEM ( )  RATIONAL_B_SPLINE_SURFACE ( (
 ( 0.9176910440068992703, 0.7566372315801705994, 1.000000000000000000),
 ( 0.9194425871098819147, 0.7618160164815883650, 1.000000000000000000),
 ( 0.9211696495200940582, 0.7669224193549075697, 1.000000000000000000),
 ( 0.9228729927664841570, 0.7719586918116432273, 1.000000000000000000) ) ) 
 REPRESENTATION_ITEM ( '' )  SURFACE ( )  );
#43137=CARTESIAN_POINT ( 'NONE',  ( -18.00000000000001776, -20.00000000000001776, -9.000000000000003553 ) ) ;
#43155=CARTESIAN_POINT ( 'NONE',  ( 45.48126212248870814, 413.7349014071057240, 8.309231847991947362 ) ) ;
#43156=CARTESIAN_POINT ( 'NONE',  ( 25.18061011279516137, 295.6585344082096185, -1.827081243610339634 ) ) ;
#43178=CARTESIAN_POINT ( 'NONE',  ( 28.21644434148578640, 308.7733337496239301, -9.112255642778062992 ) ) ;
#43179=CARTESIAN_POINT ( 'NONE',  ( 38.83326880619124921, 459.9245326792457149, 1.954253696936976370 ) ) ;
#43180=CARTESIAN_POINT ( 'NONE',  ( -34.02564419663974604, 436.1159546367792359, 7.420618519801049473 ) ) ;
#43183=EDGE_LOOP ( 'NONE', ( #87454, #60009, #75230 ) ) ;
#43190=CARTESIAN_POINT ( 'NONE',  ( 32.28930913498017929, 488.2717154064768579, 9.213726894932253941 ) ) ;
#43207=EDGE_CURVE ( 'NONE', #85705, #11400, #64060, .T. ) ;
#43216=CARTESIAN_POINT ( 'NONE',  ( -46.00000000000000000, 461.9428920847514632, 12.03309428281624172 ) ) ;
#43234=ORIENTED_EDGE ( 'NONE', *, *, #16127, .T. ) ;
#43235=CARTESIAN_POINT ( 'NONE',  ( 42.35645304355708163, 435.3801053262068308, 19.45913382674007508 ) ) ;
#43241=CARTESIAN_POINT ( 'NONE',  ( 43.33388476020373048, 464.9733321035772065, 13.99141793829583236 ) ) ;
#43244=B_SPLINE_CURVE_WITH_KNOTS ( 'NONE', 3,
 ( #14795, #5651, #62848, #64436, #63912, #73018 ),
 .UNSPECIFIED., .F., .F.,
 ( 4, 2, 4 ),
 ( 0.000000000000000000, 0.001670251840629987045, 0.003340503681259974090 ),
 .UNSPECIFIED. ) ;
#43249=CARTESIAN_POINT ( 'NONE',  ( 34.89857526195121551, 437.7187790665914235, 4.586527422594350867 ) ) ;
#43271=( BOUNDED_SURFACE ( )  B_SPLINE_SURFACE ( 3, 2, ( 
 ( #20618, #93916, #11920 ),
 ( #28684, #95502, #20073 ),
 ( #37838, #12971, #86898 ),
 ( #28154, #29229, #94461 ),
 ( #62103, #21131, #38869 ),
 ( #61030, #45897, #62616 ),
 ( #46426, #86379, #12445 ),
 ( #63144, #70169, #102537 ),
 ( #85845, #22169, #45372 ),
 ( #21645, #5434, #78773 ),
 ( #52920, #54481, #70702 ),
 ( #87428, #96041, #13503 ),
 ( #46937, #94995, #103592 ),
 ( #79311, #44847, #77738 ) ),
 .UNSPECIFIED., .F., .F., .F. ) 
 B_SPLINE_SURFACE_WITH_KNOTS ( ( 4, 2, 2, 2, 2, 2, 4 ),
 ( 3, 3 ),
 ( -3.556183125752454544E-17, 0.003030258808122785353, 0.004545388212184195594, 0.006060517616245606268, 0.007575647020307016942, 0.009090776424368427616, 0.01212103523249124723 ),
 ( 0.000000000000000000, 1.000000000000000000 ),
 .UNSPECIFIED. ) 
 GEOMETRIC_REPRESENTATION_ITEM ( )  RATIONAL_B_SPLINE_SURFACE ( (
 ( 1.000000000000000000, 0.7246213771202291154, 1.000000000000000000),
 ( 1.000000000000000000, 0.7389031614989468588, 1.000000000000000000),
 ( 1.000000000000000000, 0.7528478292017520834, 1.000000000000000000),
 ( 1.000000000000000000, 0.7735487450444836766, 1.000000000000000000),
 ( 1.000000000000000000, 0.7804537612899002941, 1.000000000000000000),
 ( 1.000000000000000000, 0.7939987057269957127, 1.000000000000000000),
 ( 1.000000000000000000, 0.8006397256199081491, 1.000000000000000000),
 ( 1.000000000000000000, 0.8137168943989200320, 1.000000000000000000),
 ( 1.000000000000000000, 0.8201529051482028265, 1.000000000000000000),
 ( 1.000000000000000000, 0.8328685173623544546, 1.000000000000000000),
 ( 1.000000000000000000, 0.8391819167394514167, 1.000000000000000000),
 ( 1.000000000000000000, 0.8576788219182877038, 1.000000000000000000),
 ( 1.000000000000000000, 0.8693707786496762679, 1.000000000000000000),
 ( 1.000000000000000000, 0.8805984182416946027, 1.000000000000000000) ) ) 
 REPRESENTATION_ITEM ( '' )  SURFACE ( )  );
#43272=CARTESIAN_POINT ( 'NONE',  ( -33.10942428023948025, 427.0948870615109172, 25.12333264783021036 ) ) ;
#43280=CARTESIAN_POINT ( 'NONE',  ( 0.000000000000000000, 70.00000000000000000, 0.000000000000000000 ) ) ;
#43287=AXIS2_PLACEMENT_3D ( 'NONE', #47081, #63295, #38498 ) ;
#43293=CARTESIAN_POINT ( 'NONE',  ( 35.97769024725786124, 482.2773069761253169, 15.66015945297581169 ) ) ;
#43298=CARTESIAN_POINT ( 'NONE',  ( 33.16766815328914930, 434.2046602808906073, 15.25519444545857262 ) ) ;
#43311=CARTESIAN_POINT ( 'NONE',  ( -18.39955510352875834, 302.6496531622213979, 9.894388872991537909 ) ) ;
#43317=CARTESIAN_POINT ( 'NONE',  ( -20.24579557674108088, 304.8297271373347144, -10.00469232190996927 ) ) ;
#43342=CARTESIAN_POINT ( 'NONE',  ( 29.46624082845785253, 308.8359934246385592, -8.861758456725450372 ) ) ;
#43349=CARTESIAN_POINT ( 'NONE',  ( 42.20041562234358423, 435.2369744135583574, 7.788607701745473122 ) ) ;
#43362=CARTESIAN_POINT ( 'NONE',  ( -21.51569398614867623, 294.9107018935607698, -9.987480606144499617 ) ) ;
#43381=SURFACE_SIDE_STYLE ('',( #41775 ) ) ;
#43385=CARTESIAN_POINT ( 'NONE',  ( -34.36792678279851287, 318.9604217263056398, -6.095080103624761492 ) ) ;
#43387=CARTESIAN_POINT ( 'NONE',  ( -11.90233244705797766, 304.5915716174422982, -9.055312000094444258 ) ) ;
#43390=CARTESIAN_POINT ( 'NONE',  ( -42.69811214730274429, 434.9611672192513652, 18.34625614733215215 ) ) ;
#43394=DIRECTION ( 'NONE',  ( 0.2043693274454108089, 0.2793933298622084949, 0.9381751143725876041 ) ) ;
#43410=CARTESIAN_POINT ( 'NONE',  ( -32.86086508068097345, 472.2680268995223969, 9.428505756555059847 ) ) ;
#43432=EDGE_CURVE ( 'NONE', #2640, #56041, #93672, .T. ) ;
#43435=CARTESIAN_POINT ( 'NONE',  ( -43.58619280597272194, 434.9882623928570524, 14.52865984557737278 ) ) ;
#43437=CARTESIAN_POINT ( 'NONE',  ( -30.98778772510896218, 438.9961996591003413, 22.22074261274275386 ) ) ;
#43447=CARTESIAN_POINT ( 'NONE',  ( -23.14090638779910591, 295.2019495631942050, 2.012332626436514005 ) ) ;
#43454=CARTESIAN_POINT ( 'NONE',  ( 25.91107377119099198, 295.8152773742599493, -9.793025909729470513 ) ) ;
#43455=CARTESIAN_POINT ( 'NONE',  ( 35.56416567323501710, 480.2820146177156175, -4.363888856302766683 ) ) ;
#43457=VECTOR ( 'NONE', #14879, 1000.000000000000000 ) ;
#43467=CARTESIAN_POINT ( 'NONE',  ( 45.43264684998295877, 375.4384345595471473, 6.660155552370398802 ) ) ;
#43506=ORIENTED_EDGE ( 'NONE', *, *, #99905, .T. ) ;
#43523=CARTESIAN_POINT ( 'NONE',  ( 31.99770529497660831, 299.5165077758936718, 2.979034379301395141 ) ) ;
#43538=CARTESIAN_POINT ( 'NONE',  ( 42.74850648157743649, 465.8913842144178830, 12.61550125132738209 ) ) ;
#43539=CARTESIAN_POINT ( 'NONE',  ( 33.32781438368718341, 490.0012478077239280, 11.19551906499331828 ) ) ;
#43566=( BOUNDED_SURFACE ( )  B_SPLINE_SURFACE ( 3, 2, ( 
 ( #19791, #52625, #28951 ),
 ( #77980, #85556, #59684 ),
 ( #28402, #45101, #4097 ),
 ( #37025, #69893, #78500 ),
 ( #67763, #92562, #80614 ),
 ( #97332, #6194, #46153 ),
 ( #70949, #21899, #31578 ),
 ( #64460, #31061, #23486 ),
 ( #56327, #89261, #39131 ),
 ( #104364, #72009, #13757 ) ),
 .UNSPECIFIED., .F., .F., .T. ) 
 B_SPLINE_SURFACE_WITH_KNOTS ( ( 4, 2, 2, 2, 4 ),
 ( 3, 3 ),
 ( 2.960956133057912609E-15, 0.002844712610147792642, 0.003555890762684000509, 0.004267068915220208376, 0.005689425220292624111 ),
 ( 0.000000000000000000, 1.000000000000000000 ),
 .UNSPECIFIED. ) 
 GEOMETRIC_REPRESENTATION_ITEM ( )  RATIONAL_B_SPLINE_SURFACE ( (
 ( 1.000000000000000000, 0.8258027051675366215, 1.000000000000000000),
 ( 1.000000000000000000, 0.8423184768576185144, 1.000000000000000000),
 ( 1.000000000000000000, 0.8479189272866914928, 1.000000000000000000),
 ( 1.000000000000000000, 0.8482780919515218176, 1.000000000000000000),
 ( 1.000000000000000000, 0.8479712937353218738, 1.000000000000000000),
 ( 1.000000000000000000, 0.8466356411021724870, 1.000000000000000000),
 ( 1.000000000000000000, 0.8456087446167629418, 1.000000000000000000),
 ( 1.000000000000000000, 0.8414089630425088950, 1.000000000000000000),
 ( 1.000000000000000000, 0.8371477558872925107, 1.000000000000000000),
 ( 1.000000000000000000, 0.8308329163121775940, 1.000000000000000000) ) ) 
 REPRESENTATION_ITEM ( '' )  SURFACE ( )  );
#43567=CARTESIAN_POINT ( 'NONE',  ( -32.12958771267418712, 464.7275665249413805, 11.12424126545828784 ) ) ;
#43568=CARTESIAN_POINT ( 'NONE',  ( -38.45611865049527012, 439.3122198965025405, 23.73029221708416614 ) ) ;
#43570=CARTESIAN_POINT ( 'NONE',  ( -35.47320774096329643, 436.4618599381972217, 5.062587423523073227 ) ) ;
#43587=CARTESIAN_POINT ( 'NONE',  ( 28.80551732330762604, 315.1542978612143315, 12.69625289295432857 ) ) ;
#43596=CARTESIAN_POINT ( 'NONE',  ( -31.00389226249483698, 502.9289871839745842, 8.047326149841639520 ) ) ;
#43605=CARTESIAN_POINT ( 'NONE',  ( -9.766195837844021455, 294.6492712292731539, -2.152655282870724829 ) ) ;
#43618=DIRECTION ( 'NONE',  ( 0.000000000000000000, 0.000000000000000000, -1.000000000000000000 ) ) ;
#43635=CARTESIAN_POINT ( 'NONE',  ( -24.71530540495096417, 306.0434402448361766, -8.740882662338435694 ) ) ;
#43641=ORIENTED_EDGE ( 'NONE', *, *, #49947, .T. ) ;
#43646=CARTESIAN_POINT ( 'NONE',  ( -25.85485528147027168, 306.6938288622521895, -8.594803261285228757 ) ) ;
#43647=CARTESIAN_POINT ( 'NONE',  ( -36.42407664602379214, 305.7434830039975964, 4.478253505840557480 ) ) ;
#43653=TOROIDAL_SURFACE ( 'NONE', #69461, 12.00000000000001066, 3.000000000000000000 ) ;
#43658=ORIENTED_EDGE ( 'NONE', *, *, #29608, .T. ) ;
#43663=DIRECTION ( 'NONE',  ( 0.000000000000000000, 0.000000000000000000, 1.000000000000000000 ) ) ;
#43675=CARTESIAN_POINT ( 'NONE',  ( 1.249646147396492601, 294.8475419170831060, -9.939938411525382378 ) ) ;
#43676=CARTESIAN_POINT ( 'NONE',  ( 39.24156521425334176, 307.7088117867400001, -7.003459073692002157 ) ) ;
#43677=DIRECTION ( 'NONE',  ( 0.000000000000000000, 1.000000000000000000, 0.000000000000000000 ) ) ;
#43682=DIRECTION ( 'NONE',  ( 0.000000000000000000, 1.000000000000000000, 0.000000000000000000 ) ) ;
#43690=CARTESIAN_POINT ( 'NONE',  ( -44.21269619315447130, 463.3337519764560852, 6.736501381177894210 ) ) ;
#43693=ORIENTED_EDGE ( 'NONE', *, *, #42547, .F. ) ;
#43700=CARTESIAN_POINT ( 'NONE',  ( 39.86626972871174246, 464.8590688799406507, 17.95745982857005529 ) ) ;
#43701=CARTESIAN_POINT ( 'NONE',  ( 40.66084078640295729, 460.3808361429892102, 2.363412739912836180 ) ) ;
#43704=EDGE_CURVE ( 'NONE', #45269, #51428, #29429, .T. ) ;
#43725=B_SPLINE_CURVE_WITH_KNOTS ( 'NONE', 3,
 ( #7196, #63344, #72984, #39599 ),
 .UNSPECIFIED., .F., .F.,
 ( 4, 4 ),
 ( 4.336808689942017736E-18, 0.001738772145493835486 ),
 .UNSPECIFIED. ) ;
#43745=CARTESIAN_POINT ( 'NONE',  ( 19.70764564238371719, 304.7954121406193622, 9.925013215726785631 ) ) ;
#43747=UNCERTAINTY_MEASURE_WITH_UNIT (LENGTH_MEASURE( 1.000000000000000082E-05 ), #67761, 'distance_accuracy_value', 'NONE');
#43762=CARTESIAN_POINT ( 'NONE',  ( 42.31186848673542045, 465.8659795009741629, 14.28293630011768656 ) ) ;
#43790=CARTESIAN_POINT ( 'NONE',  ( -21.98328659339751212, 303.0786568297054373, -9.951468641084936451 ) ) ;
#43804=CARTESIAN_POINT ( 'NONE',  ( -41.86369521826392059, 487.3376196552076181, 9.525433426952293559 ) ) ;
#43811=ORIENTED_EDGE ( 'NONE', *, *, #84778, .T. ) ;
#43812=CARTESIAN_POINT ( 'NONE',  ( -35.88302647429859604, 490.8296403864111994, 12.39892816713287083 ) ) ;
#43817=EDGE_LOOP ( 'NONE', ( #48145, #47709, #30189, #8805 ) ) ;
#43820=CARTESIAN_POINT ( 'NONE',  ( 43.00000000000000000, 488.0336798547363628, -0.8984331811833908832 ) ) ;
#43831=AXIS2_PLACEMENT_3D ( 'NONE', #32150, #39710, #97924 ) ;
#43835=EDGE_CURVE ( 'NONE', #72660, #84500, #51257, .T. ) ;
#43879=ORIENTED_EDGE ( 'NONE', *, *, #2132, .F. ) ;
#43882=CYLINDRICAL_SURFACE ( 'NONE', #104309, 10.00000000000000178 ) ;
#43895=CARTESIAN_POINT ( 'NONE',  ( 32.62734573162120455, 485.2399387473994352, 2.793905986278862663 ) ) ;
#43897=( BOUNDED_SURFACE ( )  B_SPLINE_SURFACE ( 3, 2, ( 
 ( #58913, #17928, #19020 ),
 ( #91807, #8745, #41653 ),
 ( #10858, #25509, #67536 ),
 ( #50781, #75610, #74008 ) ),
 .UNSPECIFIED., .F., .F., .T. ) 
 B_SPLINE_SURFACE_WITH_KNOTS ( ( 4, 4 ),
 ( 3, 3 ),
 ( 3.469446951953614189E-18, 0.001998086366859867617 ),
 ( 0.000000000000000000, 1.000000000000000000 ),
 .UNSPECIFIED. ) 
 GEOMETRIC_REPRESENTATION_ITEM ( )  RATIONAL_B_SPLINE_SURFACE ( (
 ( 1.000000000000000000, 0.8258027051679468489, 1.000000000000000000),
 ( 1.000000000000000000, 0.8176579674346097226, 1.000000000000000000),
 ( 1.000000000000000000, 0.8085378326700221052, 1.000000000000000000),
 ( 1.000000000000000000, 0.7996726260853451729, 1.000000000000000000) ) ) 
 REPRESENTATION_ITEM ( '' )  SURFACE ( )  );
#43909=CARTESIAN_POINT ( 'NONE',  ( -31.79966957013667539, 310.8780264347615230, -8.126197538413364896 ) ) ;
#43910=FACE_OUTER_BOUND ( 'NONE', #6763, .T. ) ;
#43920=EDGE_LOOP ( 'NONE', ( #6352, #20955, #91857, #28227 ) ) ;
#43944=DIRECTION ( 'NONE',  ( -0.1957247465660222063, 0.4045265792283474493, 0.8933364821160492131 ) ) ;
#43950=EDGE_CURVE ( 'NONE', #23997, #93551, #84005, .T. ) ;
#43951=EDGE_CURVE ( 'NONE', #79477, #76499, #65058, .T. ) ;
#43956=AXIS2_PLACEMENT_3D ( 'NONE', #77193, #60504, #88347 ) ;
#43968=ORIENTED_EDGE ( 'NONE', *, *, #59880, .T. ) ;
#43973=CARTESIAN_POINT ( 'NONE',  ( -41.61991840646690832, 463.6613340606643305, 18.05819007330882187 ) ) ;
#43974=CARTESIAN_POINT ( 'NONE',  ( -42.62871025531358526, 365.8542140222418766, 17.21379826104702104 ) ) ;
#43977=CARTESIAN_POINT ( 'NONE',  ( -36.69279669379599795, 378.7816022980671846, 4.949611917198358135 ) ) ;
#43982=FACE_OUTER_BOUND ( 'NONE', #30645, .T. ) ;
#43992=CARTESIAN_POINT ( 'NONE',  ( 44.78819990628695535, 344.4780858062635502, 1.774547970702379684 ) ) ;
#43998=CARTESIAN_POINT ( 'NONE',  ( 31.32096926659178138, 438.4574200499464496, 22.73263893176079975 ) ) ;
#44001=LINE ( 'NONE', #10030, #63812 ) ;
#44018=CARTESIAN_POINT ( 'NONE',  ( -43.61075255792442107, 434.4875743724463746, 10.88293886035986446 ) ) ;
#44032=CARTESIAN_POINT ( 'NONE',  ( -30.47150538518798513, 326.6480560234095947, 15.53807219869773704 ) ) ;
#44039=CARTESIAN_POINT ( 'NONE',  ( -11.57605499558394513, 303.6016347804044244, 9.883825704079463037 ) ) ;
#44041=CARTESIAN_POINT ( 'NONE',  ( 39.33363774397094659, 438.9614164243666323, 23.36187085933288543 ) ) ;
#44052=CARTESIAN_POINT ( 'NONE',  ( 25.48181057333568944, 295.7987491915667420, 2.140656098138366659 ) ) ;
#44054=CIRCLE ( 'NONE', #14761, 12.00000000000001066 ) ;
#44061=CARTESIAN_POINT ( 'NONE',  ( 39.63516261196253510, 316.6154150605056543, 7.211374874840607241 ) ) ;
#44069=DIRECTION ( 'NONE',  ( -0.1270361284032274773, -0.9918980905719693153, 0.000000000000000000 ) ) ;
#44071=CARTESIAN_POINT ( 'NONE',  ( 4.024410228089478458, 294.8082131651069631, 1.927919447182780077 ) ) ;
#44074=CARTESIAN_POINT ( 'NONE',  ( 42.74851244753489254, 465.8913837062017365, 12.61547527226834653 ) ) ;
#44094=CARTESIAN_POINT ( 'NONE',  ( 40.43320803012314713, 490.2964122661032320, 11.44029694117896234 ) ) ;
#44100=ORIENTED_EDGE ( 'NONE', *, *, #67597, .F. ) ;
#44101=CARTESIAN_POINT ( 'NONE',  ( 41.66301127302162399, 485.3863426732068547, -3.409513628943111385 ) ) ;
#44105=CARTESIAN_POINT ( 'NONE',  ( 39.80046283020458731, 485.2148097320063584, -4.378247030186141586 ) ) ;
#44112=EDGE_CURVE ( 'NONE', #2708, #23052, #35854, .T. ) ;
#44117=DIRECTION ( 'NONE',  ( 0.000000000000000000, 0.000000000000000000, 1.000000000000000000 ) ) ;
#44130=CARTESIAN_POINT ( 'NONE',  ( 24.36322103432850739, 306.6249039800414948, 9.333189539698471648 ) ) ;
#44139=CARTESIAN_POINT ( 'NONE',  ( -30.87955015324946828, 351.7733141111877444, 20.67482462247657082 ) ) ;
#44159=CARTESIAN_POINT ( 'NONE',  ( 43.81051912592808151, 434.3294622498374906, 12.62549197245584764 ) ) ;
#44168=EDGE_CURVE ( 'NONE', #8963, #88625, #35931, .T. ) ;
#44176=CARTESIAN_POINT ( 'NONE',  ( 32.18156226254668439, 336.4576599714083613, 18.02643260092943933 ) ) ;
#44177=CARTESIAN_POINT ( 'NONE',  ( -23.74341347023494109, 305.6141507394339669, -8.835825535111036189 ) ) ;
#44190=CARTESIAN_POINT ( 'NONE',  ( -35.18278326935743650, 355.7732856895711961, 2.568028608958709658 ) ) ;
#44191=CARTESIAN_POINT ( 'NONE',  ( -40.67306599853077387, 323.5699801759080287, 8.940364875572813119 ) ) ;
#44216=CARTESIAN_POINT ( 'NONE',  ( 34.36770714279217032, 436.8600252229026069, 5.946269065013446209 ) ) ;
#44218=CARTESIAN_POINT ( 'NONE',  ( 8.233767125201939763, 295.9462895464749863, -10.03054565981218715 ) ) ;
#44219=CARTESIAN_POINT ( 'NONE',  ( 32.16694665535142406, 298.7751107022914425, -9.134474995491629556 ) ) ;
#44220=CARTESIAN_POINT ( 'NONE',  ( 41.10204028993562986, 320.7705685081051001, 4.305717556370822763 ) ) ;
#44224=AXIS2_PLACEMENT_3D ( 'NONE', #38447, #105281, #86995 ) ;
#44234=ORIENTED_EDGE ( 'NONE', *, *, #15609, .F. ) ;
#44235=CARTESIAN_POINT ( 'NONE',  ( 9.819056950928633398, 294.6481068335447731, 1.893705519456528208 ) ) ;
#44239=DIRECTION ( 'NONE',  ( 0.000000000000000000, 0.000000000000000000, -1.000000000000000000 ) ) ;
#44246=CARTESIAN_POINT ( 'NONE',  ( -33.65541652956997609, 435.5971107367176955, 8.976813231754876554 ) ) ;
#44249=CARTESIAN_POINT ( 'NONE',  ( -44.17836536378434431, 435.2619773020556408, 14.65562696767813833 ) ) ;
#44256=CARTESIAN_POINT ( 'NONE',  ( 42.51195073777421385, 462.6463319774611591, 3.762330311941330496 ) ) ;
#44262=CARTESIAN_POINT ( 'NONE',  ( 43.51084452654475143, 465.2903130129669762, 9.421687747984162087 ) ) ;
#44284=CARTESIAN_POINT ( 'NONE',  ( -30.87955015324946828, 351.7733141111877444, 20.67482462247657082 ) ) ;
#44304=CARTESIAN_POINT ( 'NONE',  ( 33.74587843296627199, 434.0087108331489958, 12.79530826050359060 ) ) ;
#44316=CARTESIAN_POINT ( 'NONE',  ( 45.99999999999998579, 437.8923892905293656, 12.67832064131795811 ) ) ;
#44321=AXIS2_PLACEMENT_3D ( 'NONE', #51676, #27459, #86209 ) ;
#44332=CARTESIAN_POINT ( 'NONE',  ( -32.22503847990277848, 485.9064490506194147, 4.829857536089201098 ) ) ;
#44344=CARTESIAN_POINT ( 'NONE',  ( -43.00000000000000000, 436.0987441542287115, 7.567257455462727656 ) ) ;
#44348=CIRCLE ( 'NONE', #23732, 15.00000000000000711 ) ;
#44355=CARTESIAN_POINT ( 'NONE',  ( 42.19179521601841287, 485.4956273777429487, -3.824025998174274577 ) ) ;
#44360=CARTESIAN_POINT ( 'NONE',  ( -32.99999999999997868, 464.3970849722209095, 17.41240408234209269 ) ) ;
#44362=CARTESIAN_POINT ( 'NONE',  ( 31.43208348565280374, 438.4707862388059993, 22.17802677910339781 ) ) ;
#44366=CARTESIAN_POINT ( 'NONE',  ( -34.15310232806815094, 465.0579147271379838, 17.72315479633533997 ) ) ;
#44372=DIRECTION ( 'NONE',  ( 0.000000000000000000, 0.000000000000000000, 1.000000000000000000 ) ) ;
#44404=ORIENTED_EDGE ( 'NONE', *, *, #29410, .T. ) ;
#44408=CARTESIAN_POINT ( 'NONE',  ( 28.80071264762327843, 307.9646382554784054, -9.069769307751089471 ) ) ;
#44429=CARTESIAN_POINT ( 'NONE',  ( -34.47678062873981020, 437.1474145881089157, 5.468662283310369077 ) ) ;
#44437=CARTESIAN_POINT ( 'NONE',  ( 33.85195725564124558, 465.2464970902059349, 17.18122764674278358 ) ) ;
#44454=ORIENTED_EDGE ( 'NONE', *, *, #78433, .F. ) ;
#44455=CARTESIAN_POINT ( 'NONE',  ( -42.91610777303993274, 434.7038292576191338, 17.44089724611687231 ) ) ;
#44462=ADVANCED_FACE ( 'NONE', ( #102867 ), #17761, .F. ) ;
#44500=CARTESIAN_POINT ( 'NONE',  ( 45.99999999995392130, 436.0345727780207881, 16.01583062800949264 ) ) ;
#44510=CARTESIAN_POINT ( 'NONE',  ( -42.23079339798735532, 460.7352525929354101, 2.726051457480703544 ) ) ;
#44517=CARTESIAN_POINT ( 'NONE',  ( -36.62035930702501929, 369.9849428499111923, 3.960109444795354872 ) ) ;
#44523=CARTESIAN_POINT ( 'NONE',  ( 25.41720494684658149, 295.7426751966382312, -1.808613394343576930 ) ) ;
#44525=CARTESIAN_POINT ( 'NONE',  ( 28.76346532419124458, 309.5219921958590135, -8.933260212751790164 ) ) ;
#44532=CARTESIAN_POINT ( 'NONE',  ( 42.63514723962018138, 485.0526260718772846, -1.920325882542133877 ) ) ;
#44536=CARTESIAN_POINT ( 'NONE',  ( 42.44170713277035389, 333.9443472539740014, 7.453073974849625749 ) ) ;
#44537=CARTESIAN_POINT ( 'NONE',  ( 33.74742301870519157, 478.7271368655381707, 3.791462368787906989 ) ) ;
#44544=( BOUNDED_SURFACE ( )  B_SPLINE_SURFACE ( 3, 2, ( 
 ( #64844, #71337, #30921 ),
 ( #47054, #63800, #96687 ),
 ( #7128, #88595, #23347 ),
 ( #40040, #14676, #31449 ) ),
 .UNSPECIFIED., .F., .F., .F. ) 
 B_SPLINE_SURFACE_WITH_KNOTS ( ( 4, 4 ),
 ( 3, 3 ),
 ( -5.212844045310305319E-16, 0.002123809863736959066 ),
 ( 0.000000000000000000, 1.000000000000000000 ),
 .UNSPECIFIED. ) 
 GEOMETRIC_REPRESENTATION_ITEM ( )  RATIONAL_B_SPLINE_SURFACE ( (
 ( 1.000000000000000000, 0.8347624811020261104, 1.000000000000000000),
 ( 1.000000000000000000, 0.8202629603800248859, 1.000000000000000000),
 ( 1.000000000000000000, 0.8052718258174417221, 1.000000000000000000),
 ( 1.000000000000000000, 0.7904469216846379265, 1.000000000000000000) ) ) 
 REPRESENTATION_ITEM ( '' )  SURFACE ( )  );
#44558=( GEOMETRIC_REPRESENTATION_CONTEXT ( 3 ) GLOBAL_UNCERTAINTY_ASSIGNED_CONTEXT ( ( #17901 ) ) GLOBAL_UNIT_ASSIGNED_CONTEXT ( ( #28830, #27764, #27225 ) ) REPRESENTATION_CONTEXT ( 'NONE', 'WORKASPACE' ) );
#44563=CARTESIAN_POINT ( 'NONE',  ( 34.21200799993543740, 462.3300391847291166, 4.640346717380173125 ) ) ;
#44570=EDGE_LOOP ( 'NONE', ( #7220, #96438 ) ) ;
#44576=CARTESIAN_POINT ( 'NONE',  ( -29.37670169769928208, 318.1281283369471566, 13.44543306026610097 ) ) ;
#44580=VERTEX_POINT ( 'NONE', #103658 ) ;
#44585=CARTESIAN_POINT ( 'NONE',  ( 33.00000000000000000, 439.7597899781497972, 24.16317522621304192 ) ) ;
#44586=CARTESIAN_POINT ( 'NONE',  ( -31.36093463545012838, 438.6317617946405676, 22.30207175520214591 ) ) ;
#44596=CARTESIAN_POINT ( 'NONE',  ( 28.52069848920484674, 297.0547176035682355, 2.417840208557171522 ) ) ;
#44612=CARTESIAN_POINT ( 'NONE',  ( 19.96162532426519221, 302.8116070918645164, 9.928455558879853982 ) ) ;
#44615=CARTESIAN_POINT ( 'NONE',  ( 43.02661387979727436, 465.7449615347604208, 11.43319743843670544 ) ) ;
#44626=CARTESIAN_POINT ( 'NONE',  ( 0.000000000000000000, 70.00000000000000000, 0.000000000000000000 ) ) ;
#44636=CARTESIAN_POINT ( 'NONE',  ( 41.32194754023684169, 489.6440166213181442, 10.86036015010091127 ) ) ;
#44649=CARTESIAN_POINT ( 'NONE',  ( 39.04686241056654694, 485.1639993256666799, -4.285741954104417495 ) ) ;
#44665=ORIENTED_EDGE ( 'NONE', *, *, #33666, .F. ) ;
#44668=CARTESIAN_POINT ( 'NONE',  ( 24.20115299029716383, 306.5553735938593150, 10.31754309208164422 ) ) ;
#44669=CARTESIAN_POINT ( 'NONE',  ( -39.71334445446657924, 460.7040462571920898, 2.103363390004036049 ) ) ;
#44671=ORIENTED_EDGE ( 'NONE', *, *, #33878, .F. ) ;
#44672=EDGE_CURVE ( 'NONE', #69309, #74993, #15244, .T. ) ;
#44693=ORIENTED_EDGE ( 'NONE', *, *, #69198, .F. ) ;
#44697=SURFACE_SIDE_STYLE ('',( #14816 ) ) ;
#44701=CYLINDRICAL_SURFACE ( 'NONE', #38079, 10.00000000000000178 ) ;
#44716=CARTESIAN_POINT ( 'NONE',  ( 42.74195034478192667, 379.2643428173500979, 18.73097918361189329 ) ) ;
#44728=ORIENTED_EDGE ( 'NONE', *, *, #42618, .T. ) ;
#44730=CARTESIAN_POINT ( 'NONE',  ( -33.86200970433443302, 330.3616465235857618, -2.745656544132137000 ) ) ;
#44731=CARTESIAN_POINT ( 'NONE',  ( -29.55140958588439659, 314.0474313513822722, 12.65717121493886133 ) ) ;
#44739=CARTESIAN_POINT ( 'NONE',  ( 37.85084083633365282, 438.0234350436313093, 4.171260309356235929 ) ) ;
#44756=CARTESIAN_POINT ( 'NONE',  ( 34.01847390526999959, 436.1371930933524368, 7.446563569466525756 ) ) ;
#44759=CARTESIAN_POINT ( 'NONE',  ( -1.435124379509183671E-09, 294.8518027762758038, -10.00000000000000178 ) ) ;
#44761=CARTESIAN_POINT ( 'NONE',  ( 43.09576643549013397, 346.8086250391238536, 10.18035955780312030 ) ) ;
#44777=CARTESIAN_POINT ( 'NONE',  ( 9.924872551452409652, 294.6447722021068216, -1.392423705979285442 ) ) ;
#44778=CARTESIAN_POINT ( 'NONE',  ( -43.48294191332882264, 479.1553598318504896, 6.034956245169025735 ) ) ;
#44781=EDGE_CURVE ( 'NONE', #97864, #8963, #20475, .T. ) ;
#44789=CARTESIAN_POINT ( 'NONE',  ( -46.00000000000000000, 500.0000000000002274, 0.000000000000000000 ) ) ;
#44795=VERTEX_POINT ( 'NONE', #10779 ) ;
#44828=CARTESIAN_POINT ( 'NONE',  ( -31.02212611900126760, 360.5725590293961318, 22.12937154125974715 ) ) ;
#44839=CARTESIAN_POINT ( 'NONE',  ( -32.68130198255966690, 486.6487900980505401, 8.407187415461715219 ) ) ;
#44847=CARTESIAN_POINT ( 'NONE',  ( -31.43208348565049093, 438.4707862388140711, 22.17802677911227960 ) ) ;
#44848=CARTESIAN_POINT ( 'NONE',  ( 42.38863085960136345, 465.0218298504000245, 14.26222171105679770 ) ) ;
#44852=( BOUNDED_SURFACE ( )  B_SPLINE_SURFACE ( 3, 2, ( 
 ( #71102, #70042, #72166 ),
 ( #103990, #30139, #102949 ),
 ( #105073, #64098, #29112 ),
 ( #54903, #61980, #79722 ),
 ( #87832, #94871, #21010 ),
 ( #53851, #13912, #38753 ),
 ( #91553, #72689, #58652 ),
 ( #41918, #73208, #48928 ),
 ( #15515, #65134, #887 ),
 ( #50009, #89941, #105587 ),
 ( #41390, #106645, #82913 ),
 ( #56494, #81825, #7949 ),
 ( #98030, #73747, #7413 ),
 ( #74803, #58097, #91029 ) ),
 .UNSPECIFIED., .F., .F., .F. ) 
 B_SPLINE_SURFACE_WITH_KNOTS ( ( 4, 2, 2, 2, 2, 2, 4 ),
 ( 3, 3 ),
 ( 1.066854937725736363E-16, 0.001036839948806552976, 0.001555259923209776230, 0.002073679897612999267, 0.002592099872016222738, 0.003110519846419445775, 0.004147359795225891849 ),
 ( 0.000000000000000000, 1.000000000000000000 ),
 .UNSPECIFIED. ) 
 GEOMETRIC_REPRESENTATION_ITEM ( )  RATIONAL_B_SPLINE_SURFACE ( (
 ( 1.000000000000000000, 0.8806660624990210184, 1.000000000000000000),
 ( 1.000000000000000000, 0.8881715692663398887, 1.000000000000000000),
 ( 1.000000000000000000, 0.8928479710807692982, 1.000000000000000000),
 ( 1.000000000000000000, 0.8947313045151574773, 1.000000000000000000),
 ( 1.000000000000000000, 0.8944961860243605400, 1.000000000000000000),
 ( 1.000000000000000000, 0.8923679545987566186, 1.000000000000000000),
 ( 1.000000000000000000, 0.8904472546607578032, 1.000000000000000000),
 ( 1.000000000000000000, 0.8850746651128988951, 1.000000000000000000),
 ( 1.000000000000000000, 0.8816555630482483252, 1.000000000000000000),
 ( 1.000000000000000000, 0.8735136825612432876, 1.000000000000000000),
 ( 1.000000000000000000, 0.8687495631807600205, 1.000000000000000000),
 ( 1.000000000000000000, 0.8530568296136552542, 1.000000000000000000),
 ( 1.000000000000000000, 0.8406856949796707168, 1.000000000000000000),
 ( 1.000000000000000000, 0.8270258197359637853, 1.000000000000000000) ) ) 
 REPRESENTATION_ITEM ( '' )  SURFACE ( )  );
#44864=EDGE_CURVE ( 'NONE', #15128, #47515, #101405, .T. ) ;
#44872=CARTESIAN_POINT ( 'NONE',  ( -46.00000000000000000, 460.3195313667367827, 7.040850765593992477 ) ) ;
#44880=CARTESIAN_POINT ( 'NONE',  ( 29.99999999999999645, 486.7667864837127354, 5.222266633581397421 ) ) ;
#44882=CARTESIAN_POINT ( 'NONE',  ( -42.57704743493907529, 486.1612337113410831, 7.852296464539637810 ) ) ;
#44886=CARTESIAN_POINT ( 'NONE',  ( -3.957035243681184866, 299.4356451597976161, 9.196738408810819720 ) ) ;
#44887=AXIS2_PLACEMENT_3D ( 'NONE', #74437, #58268, #1604 ) ;
#44897=DIRECTION ( 'NONE',  ( 0.000000000000000000, -0.9253863139535632998, 0.3790252893243894472 ) ) ;
#44905=CARTESIAN_POINT ( 'NONE',  ( 37.54639040359151636, 463.7818835076658388, 19.50744869160540773 ) ) ;
#44916=DIRECTION ( 'NONE',  ( 1.000000000000000000, 0.000000000000000000, 0.000000000000000000 ) ) ;
#44923=VERTEX_POINT ( 'NONE', #13969 ) ;
#44962=ORIENTED_EDGE ( 'NONE', *, *, #23819, .T. ) ;
#44968=CARTESIAN_POINT ( 'NONE',  ( 34.42195163688486303, 484.1350747783266684, 0.1342865971131924074 ) ) ;
#44973=CARTESIAN_POINT ( 'NONE',  ( -18.69764690323647116, 302.6592417714942940, -10.04078470653332822 ) ) ;
#44977=CARTESIAN_POINT ( 'NONE',  ( -34.38464471058380667, 463.7420058809016723, 19.22113941036815277 ) ) ;
#44982=CARTESIAN_POINT ( 'NONE',  ( -35.50958238476149376, 382.3993991366144201, 6.026798545227356918 ) ) ;
#45012=ORIENTED_EDGE ( 'NONE', *, *, #78405, .F. ) ;
#45028=VERTEX_POINT ( 'NONE', #95439 ) ;
#45057=CARTESIAN_POINT ( 'NONE',  ( -36.68474926415177606, 425.7828876856403895, 5.530442334352566824 ) ) ;
#45069=CARTESIAN_POINT ( 'NONE',  ( 42.36162206505706251, 485.1874691988858217, -2.398526663485936350 ) ) ;
#45073=CARTESIAN_POINT ( 'NONE',  ( 36.57040099523793941, 337.1877129126421551, -1.689591862844450620 ) ) ;
#45079=CARTESIAN_POINT ( 'NONE',  ( 31.50457389700596167, 439.3522922964306190, 23.21593941183056131 ) ) ;
#45099=CARTESIAN_POINT ( 'NONE',  ( 35.02909328022846580, 463.2801532500066628, 4.636725553699557523 ) ) ;
#45101=CARTESIAN_POINT ( 'NONE',  ( -43.61182701070574552, 463.4400368046242988, 6.347502766231601257 ) ) ;
#45116=EDGE_LOOP ( 'NONE', ( #37567, #96736, #37896, #25600 ) ) ;
#45117=ORIENTED_EDGE ( 'NONE', *, *, #6989, .T. ) ;
#45121=( GEOMETRIC_REPRESENTATION_CONTEXT ( 3 ) GLOBAL_UNCERTAINTY_ASSIGNED_CONTEXT ( ( #8583 ) ) GLOBAL_UNIT_ASSIGNED_CONTEXT ( ( #97329, #61412, #12300 ) ) REPRESENTATION_CONTEXT ( 'NONE', 'WORKASPACE' ) );
#45131=CARTESIAN_POINT ( 'NONE',  ( 32.87547266101556431, 465.6993878536748070, 10.91512469976365551 ) ) ;
#45133=CARTESIAN_POINT ( 'NONE',  ( 27.69667248624871903, 296.8482049418585120, 10.37257860731564385 ) ) ;
#45139=DIRECTION ( 'NONE',  ( 1.000000000000000000, 0.000000000000000000, 0.000000000000000000 ) ) ;
#45140=CARTESIAN_POINT ( 'NONE',  ( -43.00000000000000000, 436.0987441542287115, 7.567257455462727656 ) ) ;
#45142=DIRECTION ( 'NONE',  ( 0.8902151594054004136, 0.000000000000000000, 0.4555403055326912032 ) ) ;
#45168=DIRECTION ( 'NONE',  ( 0.000000000000000000, 0.000000000000000000, 1.000000000000000000 ) ) ;
#45169=CARTESIAN_POINT ( 'NONE',  ( -32.20627895475222857, 464.6794106235103641, 10.68705400064572686 ) ) ;
#45177=CARTESIAN_POINT ( 'NONE',  ( 40.17717846856370301, 485.8445156049149887, -4.962122411038198067 ) ) ;
#45193=ORIENTED_EDGE ( 'NONE', *, *, #26185, .T. ) ;
#45203=CARTESIAN_POINT ( 'NONE',  ( 25.37047581387864170, 306.3720789167446696, 10.50697067398095719 ) ) ;
#45221=ORIENTED_EDGE ( 'NONE', *, *, #106544, .F. ) ;
#45222=CARTESIAN_POINT ( 'NONE',  ( 39.85564080103976181, 459.8412824357643558, 1.882109076563826200 ) ) ;
#45226=ORIENTED_EDGE ( 'NONE', *, *, #46604, .T. ) ;
#45229=ADVANCED_FACE ( 'NONE', ( #35521 ), #60840, .F. ) ;
#45239=CARTESIAN_POINT ( 'NONE',  ( -46.00000000000000711, 461.1586514445786520, 8.541706603213405913 ) ) ;
#45247=CARTESIAN_POINT ( 'NONE',  ( 33.15578469393098260, 409.3745932105718452, 25.92517817600723617 ) ) ;
#45251=CARTESIAN_POINT ( 'NONE',  ( -43.71789550058824148, 434.9437403290502289, 13.92762231526895711 ) ) ;
#45255=EDGE_CURVE ( 'NONE', #46568, #59047, #101486, .T. ) ;
#45260=CARTESIAN_POINT ( 'NONE',  ( -27.53989814665412084, 308.1507782404630120, -8.257886362634577537 ) ) ;
#45261=CARTESIAN_POINT ( 'NONE',  ( -31.46913928081870182, 326.8580950721863019, 15.82560803904243407 ) ) ;
#45269=VERTEX_POINT ( 'NONE', #36594 ) ;
#45286=CARTESIAN_POINT ( 'NONE',  ( 7.697757149314820246, 296.0912719809091982, -10.02629731371293786 ) ) ;
#45289=CARTESIAN_POINT ( 'NONE',  ( 34.73151746388065675, 302.0917208187174197, -0.3540781040331686391 ) ) ;
#45290=DIRECTION ( 'NONE',  ( -0.6175266994148785882, 0.6213472858387578679, 0.4822741190345746221 ) ) ;
#45318=CARTESIAN_POINT ( 'NONE',  ( -40.66415791351455056, 490.1350948120810358, 11.30186264364090221 ) ) ;
#45335=DIRECTION ( 'NONE',  ( -1.000000000000000000, 0.000000000000000000, 0.000000000000000000 ) ) ;
#45338=ADVANCED_FACE ( 'NONE', ( #79655 ), #13005, .F. ) ;
#45341=ORIENTED_EDGE ( 'NONE', *, *, #85097, .T. ) ;
#45353=CARTESIAN_POINT ( 'NONE',  ( 22.20318009218133071, 295.0333587257888439, 9.975590323731541531 ) ) ;
#45368=B_SPLINE_CURVE_WITH_KNOTS ( 'NONE', 3,
 ( #42832, #41766, #91915, #91399, #57939, #2362, #50905, #76257, #83816, #27226, #75729, #92978 ),
 .UNSPECIFIED., .F., .F.,
 ( 4, 2, 2, 2, 2, 4 ),
 ( 0.000000000000000000, 0.001748721146019791700, 0.003497442292039583400, 0.004371802865049432413, 0.005246163438059279691, 0.006994884584079062717 ),
 .UNSPECIFIED. ) ;
#45372=CARTESIAN_POINT ( 'NONE',  ( -31.80090313571708904, 436.0476724931270951, 18.01393100247755541 ) ) ;
#45384=VERTEX_POINT ( 'NONE', #49401 ) ;
#45389=CARTESIAN_POINT ( 'NONE',  ( 38.11055680731727335, 437.2326489915187153, 4.664335030333705667 ) ) ;
#45395=CARTESIAN_POINT ( 'NONE',  ( -42.61140200160144786, 465.9030374194822457, 13.21253569360411895 ) ) ;
#45403=CARTESIAN_POINT ( 'NONE',  ( -37.34223837122399203, 354.2692148566569585, 1.818772290766931032 ) ) ;
#45408=DIRECTION ( 'NONE',  ( -0.000000000000000000, -1.000000000000000000, -0.000000000000000000 ) ) ;
#45409=CARTESIAN_POINT ( 'NONE',  ( -19.96162532426521352, 302.8116070918646301, 9.928455558879880627 ) ) ;
#45419=EDGE_CURVE ( 'NONE', #2695, #62559, #63980, .T. ) ;
#45433=CARTESIAN_POINT ( 'NONE',  ( -34.88900972249398080, 464.6206820655985439, 18.69027339340991034 ) ) ;
#45441=CARTESIAN_POINT ( 'NONE',  ( -37.83989825151947173, 491.6297408768480750, 12.44743998624971049 ) ) ;
#45443=CARTESIAN_POINT ( 'NONE',  ( 43.00000000000000000, 464.8825480873695710, 15.07585856869435936 ) ) ;
#45450=EDGE_CURVE ( 'NONE', #38500, #85705, #103878, .T. ) ;
#45475=ORIENTED_EDGE ( 'NONE', *, *, #42547, .T. ) ;
#45477=AXIS2_PLACEMENT_3D ( 'NONE', #17548, #100033, #26727 ) ;
#45480=CARTESIAN_POINT ( 'NONE',  ( 34.62633797947415104, 326.3522410840145653, -4.484366321573728165 ) ) ;
#45484=( BOUNDED_SURFACE ( )  B_SPLINE_SURFACE ( 3, 2, ( 
 ( #63348, #96248, #89736 ),
 ( #39602, #65972, #8262 ),
 ( #41703, #23968, #57332 ),
 ( #73518, #49786, #23423 ),
 ( #105892, #105380, #56264 ),
 ( #106419, #25563, #57866 ),
 ( #90794, #33109, #72987 ),
 ( #98852, #90255, #32577 ),
 ( #65452, #33628, #89201 ),
 ( #15300, #48187, #25013 ),
 ( #81090, #74586, #48712 ),
 ( #15829, #97275, #7202 ),
 ( #662, #74054, #16907 ),
 ( #6674, #40111, #82148 ),
 ( #41175, #98345, #32039 ),
 ( #82691, #24498, #31520 ) ),
 .UNSPECIFIED., .F., .F., .F. ) 
 B_SPLINE_SURFACE_WITH_KNOTS ( ( 4, 2, 2, 2, 2, 2, 2, 4 ),
 ( 3, 3 ),
 ( 4.542807102714263578E-16, 0.0005221599045761193174, 0.001044319809151784354, 0.001566479713727449499, 0.002088639618303114644, 0.002610799522878779790, 0.003132959427454444501, 0.004177279236605774791 ),
 ( 0.000000000000000000, 1.000000000000000000 ),
 .UNSPECIFIED. ) 
 GEOMETRIC_REPRESENTATION_ITEM ( )  RATIONAL_B_SPLINE_SURFACE ( (
 ( 1.000000000000000000, 0.8909749942925634381, 1.000000000000000000),
 ( 1.000000000000000000, 0.8947619310225533029, 1.000000000000000000),
 ( 1.000000000000000000, 0.8978044232700120864, 1.000000000000000000),
 ( 1.000000000000000000, 0.9023043032701206778, 1.000000000000000000),
 ( 1.000000000000000000, 0.9037672509123999554, 1.000000000000000000),
 ( 1.000000000000000000, 0.9049062503973974714, 1.000000000000000000),
 ( 1.000000000000000000, 0.9045936109753576204, 1.000000000000000000),
 ( 1.000000000000000000, 0.9022616022696634541, 1.000000000000000000),
 ( 1.000000000000000000, 0.9002067130753756974, 1.000000000000000000),
 ( 1.000000000000000000, 0.8945795303837162926, 1.000000000000000000),
 ( 1.000000000000000000, 0.8910211780061220166, 1.000000000000000000),
 ( 1.000000000000000000, 0.8825640046873736155, 1.000000000000000000),
 ( 1.000000000000000000, 0.8776492255282648536, 1.000000000000000000),
 ( 1.000000000000000000, 0.8615337984056086196, 1.000000000000000000),
 ( 1.000000000000000000, 0.8487841387201691123, 1.000000000000000000),
 ( 1.000000000000000000, 0.8347624811018451441, 1.000000000000000000) ) ) 
 REPRESENTATION_ITEM ( '' )  SURFACE ( )  );
#45489=CARTESIAN_POINT ( 'NONE',  ( -46.00000000000000000, 437.9690125970932968, 14.09127711025707796 ) ) ;
#45490=CARTESIAN_POINT ( 'NONE',  ( 39.86396139244071435, 437.4902212974453164, 4.924226175448357168 ) ) ;
#45491=CARTESIAN_POINT ( 'NONE',  ( 43.00000000000000000, 500.0000000000002274, 0.000000000000000000 ) ) ;
#45503=CARTESIAN_POINT ( 'NONE',  ( -28.21644434148578640, 308.7733337496239301, -9.112255642778062992 ) ) ;
#45512=CARTESIAN_POINT ( 'NONE',  ( 32.99999999999999289, 464.3970849722209095, 17.41240408234209980 ) ) ;
#45527=CARTESIAN_POINT ( 'NONE',  ( 34.88692455808023141, 481.7028197735354524, 14.61755684903771879 ) ) ;
#45534=B_SPLINE_CURVE_WITH_KNOTS ( 'NONE', 3,
 ( #92703, #77054, #3170, #35572 ),
 .UNSPECIFIED., .F., .F.,
 ( 4, 4 ),
 ( 2.442512830937285646E-17, 0.001829834443479524389 ),
 .UNSPECIFIED. ) ;
#45549=CARTESIAN_POINT ( 'NONE',  ( 42.75139825103809699, 485.3314578938637283, -3.157348782698981893 ) ) ;
#45555=FACE_OUTER_BOUND ( 'NONE', #63426, .T. ) ;
#45576=CARTESIAN_POINT ( 'NONE',  ( 36.40625082012290648, 355.8303869323650588, 1.860620477795003502 ) ) ;
#45577=CARTESIAN_POINT ( 'NONE',  ( -20.24579557674103469, 304.8297271373346575, -10.00469232190998703 ) ) ;
#45580=FACE_OUTER_BOUND ( 'NONE', #83168, .T. ) ;
#45602=CARTESIAN_POINT ( 'NONE',  ( 42.27457937377090502, 331.6756111660436659, 6.933568496604577192 ) ) ;
#45603=CARTESIAN_POINT ( 'NONE',  ( 38.89974058468706630, 460.7404207148335900, 2.234280701989461715 ) ) ;
#45610=CARTESIAN_POINT ( 'NONE',  ( 43.71297783477875498, 485.1278128289774259, -1.116606130291244892 ) ) ;
#45626=FACE_OUTER_BOUND ( 'NONE', #71623, .T. ) ;
#45642=CARTESIAN_POINT ( 'NONE',  ( -45.44494901784073448, 426.7272893100207511, 7.514821686672757295 ) ) ;
#45653=CARTESIAN_POINT ( 'NONE',  ( 25.14920469222126798, 295.6996425374044293, 2.119131604868921492 ) ) ;
#45667=CARTESIAN_POINT ( 'NONE',  ( 1.102182119232618897E-15, -20.00000000000001776, 9.000000000000007105 ) ) ;
#45673=CARTESIAN_POINT ( 'NONE',  ( 43.98364154369441792, 462.7566471324786335, 5.557736785945600388 ) ) ;
#45685=CARTESIAN_POINT ( 'NONE',  ( 0.000000000000000000, 304.8518027762758038, -10.00000000000000178 ) ) ;
#45692=CARTESIAN_POINT ( 'NONE',  ( 39.14057804814122221, 485.8491723118621053, -4.975388520153434690 ) ) ;
#45697=CARTESIAN_POINT ( 'NONE',  ( 38.81358894280276672, 485.1131561813238591, -4.191378885298274959 ) ) ;
#45699=VERTEX_POINT ( 'NONE', #50991 ) ;
#45700=CARTESIAN_POINT ( 'NONE',  ( 43.75401118688390767, 486.3173572309543715, 5.908089951475124835 ) ) ;
#45701=DIRECTION ( 'NONE',  ( -0.7663137714221263108, 0.000000000000000000, 0.6424665000829203887 ) ) ;
#45704=CARTESIAN_POINT ( 'NONE',  ( 32.63942548537020372, 439.6774874792970422, 24.06980402992034485 ) ) ;
#45735=CARTESIAN_POINT ( 'NONE',  ( 42.23079339798727716, 460.7352525929352964, 2.726051457480584972 ) ) ;
#45754=CARTESIAN_POINT ( 'NONE',  ( 43.27530345109022392, 461.7562057072080393, 3.870800370044423566 ) ) ;
#45755=FACE_OUTER_BOUND ( 'NONE', #14718, .T. ) ;
#45756=ORIENTED_EDGE ( 'NONE', *, *, #51266, .F. ) ;
#45759=ORIENTED_EDGE ( 'NONE', *, *, #42711, .T. ) ;
#45765=CARTESIAN_POINT ( 'NONE',  ( 40.85802308819273776, 440.2752458712913608, 25.57190656468647560 ) ) ;
#45772=ADVANCED_FACE ( 'NONE', ( #62314 ), #5466, .F. ) ;
#45775=CARTESIAN_POINT ( 'NONE',  ( -36.71055512278706345, 461.9588081675148601, 3.153288429120979508 ) ) ;
#45779=CARTESIAN_POINT ( 'NONE',  ( -36.51296643074312698, 309.5443268485549311, 13.44797477174485856 ) ) ;
#45794=CARTESIAN_POINT ( 'NONE',  ( -42.88690168185247842, 465.8389250139255751, 12.02233836084348262 ) ) ;
#45797=( BOUNDED_SURFACE ( )  B_SPLINE_SURFACE ( 3, 2, ( 
 ( #50976, #43973, #58572 ),
 ( #42910, #82832, #84438 ),
 ( #17586, #1896, #1357 ),
 ( #101678, #101143, #76861 ),
 ( #100604, #26240, #10528 ),
 ( #2968, #93054, #34851 ) ),
 .UNSPECIFIED., .F., .F., .F. ) 
 B_SPLINE_SURFACE_WITH_KNOTS ( ( 4, 2, 4 ),
 ( 3, 3 ),
 ( 0.1175780374352882046, 0.1311840582298423041, 0.1447900790243964175 ),
 ( 0.3700809061630451202, 1.000000000000000000 ),
 .UNSPECIFIED. ) 
 GEOMETRIC_REPRESENTATION_ITEM ( )  RATIONAL_B_SPLINE_SURFACE ( (
 ( 0.8634406101731282313, 0.8155006276293699230, 1.000000000000000000),
 ( 0.8634404976690126521, 0.8155004756300181512, 1.000000000000000000),
 ( 0.8634404321542359373, 0.8155003871158911233, 1.000000000000000000),
 ( 0.8634404611618202718, 0.8155004263067597847, 1.000000000000000000),
 ( 0.8634405542443903681, 0.8155005520665173924, 1.000000000000000000),
 ( 0.8634406634513454026, 0.8155006996112208473, 1.000000000000000000) ) ) 
 REPRESENTATION_ITEM ( '' )  SURFACE ( )  );
#45809=CARTESIAN_POINT ( 'NONE',  ( 0.9108375753702777633, 296.5938209094946956, -10.00058097679032265 ) ) ;
#45824=CARTESIAN_POINT ( 'NONE',  ( -42.50585811106670064, 460.9576338508424556, 2.953927975892561619 ) ) ;
#45827=CARTESIAN_POINT ( 'NONE',  ( -43.96303167068774087, 462.7533654737459301, 5.566168170703541307 ) ) ;
#45829=AXIS2_PLACEMENT_3D ( 'NONE', #49066, #80912, #64741 ) ;
#45849=CARTESIAN_POINT ( 'NONE',  ( -32.86204548368812084, 471.3237325390174419, 9.718390497932560379 ) ) ;
#45852=CARTESIAN_POINT ( 'NONE',  ( 43.52576059139532560, 465.2718218682666702, 9.360783428388922189 ) ) ;
#45855=DIRECTION ( 'NONE',  ( 0.000000000000000000, 0.3548932414479700759, 0.9349068334195407282 ) ) ;
#45864=CARTESIAN_POINT ( 'NONE',  ( 32.86086508068095213, 472.2680268995274560, 9.428505756553761330 ) ) ;
#45876=CARTESIAN_POINT ( 'NONE',  ( -33.74271564777244237, 484.1802673187709729, 2.058285076122319701 ) ) ;
#45897=CARTESIAN_POINT ( 'NONE',  ( -32.85046847605558185, 435.2650770123868256, 16.49042918348624553 ) ) ;
#45905=CARTESIAN_POINT ( 'NONE',  ( -26.62232737841250696, 304.7806955871358809, -9.577114476195255577 ) ) ;
#45923=B_SPLINE_CURVE_WITH_KNOTS ( 'NONE', 3,
 ( #28805, #87009, #88061, #14141 ),
 .UNSPECIFIED., .F., .F.,
 ( 4, 4 ),
 ( 0.000000000000000000, 0.0001235227585958290715 ),
 .UNSPECIFIED. ) ;
#45934=CARTESIAN_POINT ( 'NONE',  ( -9.756537947068297356, 294.6499343785214933, 2.217872953681543802 ) ) ;
#45946=DIRECTION ( 'NONE',  ( -0.8139476909583208686, 0.000000000000000000, 0.5809381691571124939 ) ) ;
#45957=( BOUNDED_SURFACE ( )  B_SPLINE_SURFACE ( 3, 2, ( 
 ( #51726, #104528, #47356 ),
 ( #103475, #22596, #80244 ),
 ( #95387, #6350, #5321 ),
 ( #79199, #88888, #95924 ),
 ( #4787, #105078, #22050 ),
 ( #30143, #78649, #14442 ),
 ( #63027, #31217, #13916 ),
 ( #71625, #39291, #72170 ),
 ( #45775, #71106, #64102 ),
 ( #38244, #14979, #54908 ),
 ( #37725, #96979, #87835 ),
 ( #23112, #63569, #30682 ) ),
 .UNSPECIFIED., .F., .F., .T. ) 
 B_SPLINE_SURFACE_WITH_KNOTS ( ( 4, 2, 2, 2, 2, 4 ),
 ( 3, 3 ),
 ( 0.0007440794992175734507, 0.002885623262178780343, 0.003956395143659383572, 0.005027167025139987235, 0.007168710788101193693, 0.009310254551062401018 ),
 ( 0.000000000000000000, 1.000000000000000000 ),
 .UNSPECIFIED. ) 
 GEOMETRIC_REPRESENTATION_ITEM ( )  RATIONAL_B_SPLINE_SURFACE ( (
 ( 1.000000000000000000, 0.7301269460246678777, 1.000000000000000000),
 ( 1.000000000000000000, 0.7402241639605217083, 1.000000000000000000),
 ( 1.000000000000000000, 0.7526921830315997930, 1.000000000000000000),
 ( 1.000000000000000000, 0.7732044076585372627, 1.000000000000000000),
 ( 1.000000000000000000, 0.7803010015268321276, 1.000000000000000000),
 ( 1.000000000000000000, 0.7944988828236099199, 1.000000000000000000),
 ( 1.000000000000000000, 0.8016356104975063124, 1.000000000000000000),
 ( 1.000000000000000000, 0.8228127629107910845, 1.000000000000000000),
 ( 1.000000000000000000, 0.8367252785235839152, 1.000000000000000000),
 ( 1.000000000000000000, 0.8612815991380949887, 1.000000000000000000),
 ( 1.000000000000000000, 0.8720645852075524784, 1.000000000000000000),
 ( 1.000000000000000000, 0.8806660624990084729, 1.000000000000000000) ) ) 
 REPRESENTATION_ITEM ( '' )  SURFACE ( )  );
#45968=CARTESIAN_POINT ( 'NONE',  ( 13.48661044872033266, 304.5494699462643666, -9.064266023533495087 ) ) ;
#45974=CARTESIAN_POINT ( 'NONE',  ( 44.53215874387051088, 465.2814620064199858, 9.437388644045839214 ) ) ;
#45975=EDGE_CURVE ( 'NONE', #37591, #72871, #20265, .T. ) ;
#45988=ORIENTED_EDGE ( 'NONE', *, *, #12477, .T. ) ;
#45994=CARTESIAN_POINT ( 'NONE',  ( 32.22503847990208925, 485.9064490506207221, 4.829857536092688974 ) ) ;
#46009=DIRECTION ( 'NONE',  ( 1.000000000000000000, -0.000000000000000000, -0.000000000000000000 ) ) ;
#46010=CARTESIAN_POINT ( 'NONE',  ( -42.49506089581998936, 334.4681969747575749, 7.580802331008121620 ) ) ;
#46012=CARTESIAN_POINT ( 'NONE',  ( 24.16352152586478752, 303.6474178691188968, -9.828590987157472370 ) ) ;
#46021=CARTESIAN_POINT ( 'NONE',  ( -34.72474116627837759, 338.3618661353910966, -1.881472242819908436 ) ) ;
#46033=CARTESIAN_POINT ( 'NONE',  ( -32.99999999999986500, 488.9035777786946255, 11.52689957822637901 ) ) ;
#46044=CARTESIAN_POINT ( 'NONE',  ( -44.26592756129811335, 485.3087896057427884, 1.848518878038618807 ) ) ;
#46045=CARTESIAN_POINT ( 'NONE',  ( -6.582107400625343274, 304.7470122113059574, 8.914715104312284311 ) ) ;
#46046=CARTESIAN_POINT ( 'NONE',  ( 31.86300348751240108, 472.3516342516534223, 13.84838610500362144 ) ) ;
#46051=ORIENTED_EDGE ( 'NONE', *, *, #100847, .F. ) ;
#46054=VERTEX_POINT ( 'NONE', #35547 ) ;
#46073=CIRCLE ( 'NONE', #63245, 8.000000000000005329 ) ;
#46075=CARTESIAN_POINT ( 'NONE',  ( -34.47678062873982441, 436.2905755606494722, 4.953078263947475968 ) ) ;
#46078=ORIENTED_EDGE ( 'NONE', *, *, #10917, .F. ) ;
#46082=CARTESIAN_POINT ( 'NONE',  ( -38.56577463025283947, 437.0885780681463757, 4.837144025084506360 ) ) ;
#46095=AXIS2_PLACEMENT_3D ( 'NONE', #73104, #29538, #21432 ) ;
#46102=CARTESIAN_POINT ( 'NONE',  ( 32.24532331159723952, 318.5265593782120845, -6.687297269301426539 ) ) ;
#46108=ADVANCED_FACE ( 'NONE', ( #19381 ), #68797, .F. ) ;
#46109=CARTESIAN_POINT ( 'NONE',  ( -26.47418998143891500, 305.8622656725908087, -9.557889300953828382 ) ) ;
#46126=CARTESIAN_POINT ( 'NONE',  ( 42.45506592911483068, 319.4331922859328756, -4.049034721733997699 ) ) ;
#46137=CARTESIAN_POINT ( 'NONE',  ( -44.36567622869332439, 435.2186464882956329, 12.63794204390610254 ) ) ;
#46144=CARTESIAN_POINT ( 'NONE',  ( 43.47770857297108904, 484.8227827122623808, 4.253339224814284059 ) ) ;
#46152=CARTESIAN_POINT ( 'NONE',  ( 33.21794938082042847, 463.2572442978370759, 6.155096106961184255 ) ) ;
#46153=CARTESIAN_POINT ( 'NONE',  ( -44.29460294111019891, 463.8401613562648436, 7.966579552388332708 ) ) ;
#46173=CARTESIAN_POINT ( 'NONE',  ( -33.00540147334746166, 487.4196752801198613, 9.523982417603901851 ) ) ;
#46178=CARTESIAN_POINT ( 'NONE',  ( -38.79307744976971861, 485.8212363931074265, -4.896981067614003535 ) ) ;
#46182=VECTOR ( 'NONE', #85885, 1000.000000000000000 ) ;
#46184=CARTESIAN_POINT ( 'NONE',  ( 40.05582037023106778, 464.2476455834488434, 17.93522255631042484 ) ) ;
#46187=DIRECTION ( 'NONE',  ( -0.4157805170469000555, 0.4085867419963847835, 0.8125167296179151011 ) ) ;
#46203=CARTESIAN_POINT ( 'NONE',  ( 44.22243490918458519, 464.2587958754115220, 9.201099836299508894 ) ) ;
#46206=CARTESIAN_POINT ( 'NONE',  ( 16.53875398580865053, 304.5679815164853608, 8.876634110831217228 ) ) ;
#46209=CARTESIAN_POINT ( 'NONE',  ( 35.34153741681340222, 436.0142057970623455, 5.687792605519862654 ) ) ;
#46216=CIRCLE ( 'NONE', #84090, 1.000000000000004885 ) ;
#46222=CIRCLE ( 'NONE', #68644, 7.999999999999973355 ) ;
#46225=ORIENTED_EDGE ( 'NONE', *, *, #26249, .T. ) ;
#46230=ORIENTED_EDGE ( 'NONE', *, *, #44112, .F. ) ;
#46234=CARTESIAN_POINT ( 'NONE',  ( 43.03185303983489263, 485.3613526602387083, 6.073233449168520259 ) ) ;
#46238=CARTESIAN_POINT ( 'NONE',  ( 8.572527594031457413E-16, 273.9999999999999432, 6.999999999999982236 ) ) ;
#46240=CARTESIAN_POINT ( 'NONE',  ( 32.39561178865213975, 439.6665705367017836, 24.00535790829840721 ) ) ;
#46241=CARTESIAN_POINT ( 'NONE',  ( -35.23236120362036417, 435.7070508914230231, 6.197761447607906149 ) ) ;
#46244=CARTESIAN_POINT ( 'NONE',  ( 0.000000000000000000, 303.8518027762758038, -10.00000000000000355 ) ) ;
#46245=ORIENTED_EDGE ( 'NONE', *, *, #24121, .T. ) ;
#46246=ORIENTED_EDGE ( 'NONE', *, *, #1841, .T. ) ;
#46247=CARTESIAN_POINT ( 'NONE',  ( -27.18383540787484520, 309.6430342986412256, 11.30725836788668204 ) ) ;
#46249=CARTESIAN_POINT ( 'NONE',  ( 21.85903006778882229, 305.2263394331082509, 10.01755384245877423 ) ) ;
#46257=CARTESIAN_POINT ( 'NONE',  ( 46.00000000000000000, 485.9062929993805255, 0.4531997891273246704 ) ) ;
#46260=CARTESIAN_POINT ( 'NONE',  ( -32.04737116498198901, 465.7264234052246934, 15.44069434688416464 ) ) ;
#46270=CARTESIAN_POINT ( 'NONE',  ( 36.28638774858024618, 437.5816761911047479, 4.254147741574738184 ) ) ;
#46273=EDGE_CURVE ( 'NONE', #69218, #50155, #96481, .T. ) ;
#46279=CARTESIAN_POINT ( 'NONE',  ( 0.000000000000000000, 67.05096163904791240, 0.000000000000000000 ) ) ;
#46287=CARTESIAN_POINT ( 'NONE',  ( -43.50377727019363761, 435.9167426301696651, 18.24083946424746117 ) ) ;
#46290=MECHANICAL_DESIGN_GEOMETRIC_PRESENTATION_REPRESENTATION('',(#97933),#99875);
#46291=VERTEX_POINT ( 'NONE', #81260 ) ;
#46301=CARTESIAN_POINT ( 'NONE',  ( 33.06938392854667086, 440.0271615209351239, 23.76204839300703853 ) ) ;
#46302=CARTESIAN_POINT ( 'NONE',  ( -43.64531880384350160, 464.9151967207102416, 12.30391130302176350 ) ) ;
#46312=CARTESIAN_POINT ( 'NONE',  ( -30.36635531035291535, 298.1745412196082157, 2.670034220700619354 ) ) ;
#46318=DIRECTION ( 'NONE',  ( -0.000000000000000000, 0.3049629831706211491, 0.9523642049634560847 ) ) ;
#46337=CARTESIAN_POINT ( 'NONE',  ( 41.60913933150737876, 468.1839071376891184, 17.09486578100470311 ) ) ;
#46339=CARTESIAN_POINT ( 'NONE',  ( 7.742691193538925987, 302.4167829614624452, -10.02995440365113744 ) ) ;
#46342=CARTESIAN_POINT ( 'NONE',  ( -11.71696977824031194, 294.5934938086913917, 1.882064959436767548 ) ) ;
#46347=CARTESIAN_POINT ( 'NONE',  ( -20.49977525862259142, 302.8459220885798686, -10.00124997875687427 ) ) ;
#46355=EDGE_LOOP ( 'NONE', ( #96919, #59698 ) ) ;
#46359=FACE_OUTER_BOUND ( 'NONE', #71863, .T. ) ;
#46361=EDGE_LOOP ( 'NONE', ( #9520, #44665, #5831, #46078 ) ) ;
#46380=CARTESIAN_POINT ( 'NONE',  ( -9.928372500597216543, 294.6449087092673835, 1.240117573296916298 ) ) ;
#46382=CARTESIAN_POINT ( 'NONE',  ( -19.38977043078304519, 294.6924723843361562, -2.033472732115015891 ) ) ;
#46391=CARTESIAN_POINT ( 'NONE',  ( 43.99225961071574176, 464.6045839418123364, 10.45666854317311589 ) ) ;
#46403=( BOUNDED_SURFACE ( )  B_SPLINE_SURFACE ( 3, 2, ( 
 ( #14553, #5431, #97598 ),
 ( #104108, #31329, #22166 ),
 ( #79834, #55541, #80355 ),
 ( #64211, #23765, #40441 ) ),
 .UNSPECIFIED., .F., .F., .F. ) 
 B_SPLINE_SURFACE_WITH_KNOTS ( ( 4, 4 ),
 ( 3, 3 ),
 ( 0.01401837328402455105, 0.01447126798403660167 ),
 ( 0.1702042094205807321, 1.000000000000000000 ),
 .UNSPECIFIED. ) 
 GEOMETRIC_REPRESENTATION_ITEM ( )  RATIONAL_B_SPLINE_SURFACE ( (
 ( 0.9213079014936687017, 0.7688303398187987803, 1.000000000000000000),
 ( 0.9199763408694713318, 0.7649186838476262906, 1.000000000000000000),
 ( 0.9186293857494203241, 0.7609618042715087238, 1.000000000000000000),
 ( 0.9172666068268391371, 0.7569584399386861673, 1.000000000000000000) ) ) 
 REPRESENTATION_ITEM ( '' )  SURFACE ( )  );
#46409=DIRECTION ( 'NONE',  ( -0.2284631855477322060, 0.3307511317731628431, 0.9156463627843199893 ) ) ;
#46416=AXIS2_PLACEMENT_3D ( 'NONE', #42339, #25124, #101112 ) ;
#46426=CARTESIAN_POINT ( 'NONE',  ( -32.70906958965466060, 434.6718458994130287, 17.16895555686161501 ) ) ;
#46432=CARTESIAN_POINT ( 'NONE',  ( -29.84307261967341063, 307.6666711317456020, -8.906761001086930918 ) ) ;
#46452=CARTESIAN_POINT ( 'NONE',  ( -37.64086492829254382, 431.4026006243604456, 5.263644812418108110 ) ) ;
#46458=B_SPLINE_SURFACE_WITH_KNOTS ( 'NONE', 1, 3, ( 
 ( #57208, #48057, #90127, #62299, #82014, #89604, #21322, #15698 ),
 ( #73388, #54158, #32451, #73929, #32979, #12646, #13176, #45577 ) ),
 .UNSPECIFIED., .F., .F., .F.,
 ( 2, 2 ),
 ( 4, 2, 2, 4 ),
 ( 0.000000000000000000, 1.000000000000000000 ),
 ( 0.000000000000000000, 0.04450745600790868145, 0.06676118401186306728, 0.08901491201581737678 ),
 .UNSPECIFIED. ) ;
#46460=ORIENTED_EDGE ( 'NONE', *, *, #7251, .T. ) ;
#46461=CARTESIAN_POINT ( 'NONE',  ( -9.145685108131942798, 294.9588331864474640, 4.056731813190911140 ) ) ;
#46465=CARTESIAN_POINT ( 'NONE',  ( -20.97754405179121662, 294.8763868968453608, 9.942224931492262385 ) ) ;
#46469=CARTESIAN_POINT ( 'NONE',  ( 15.43345822995523342, 294.5569497680363042, -10.06267294328710271 ) ) ;
#46482=AXIS2_PLACEMENT_3D ( 'NONE', #9418, #1322, #67159 ) ;
#46510=CARTESIAN_POINT ( 'NONE',  ( -33.82585650164656954, 464.6969192971417328, 6.993179704485911863 ) ) ;
#46513=CARTESIAN_POINT ( 'NONE',  ( 32.95646543402837381, 485.7809766657144905, 5.067016726498170698 ) ) ;
#46520=CARTESIAN_POINT ( 'NONE',  ( 36.74063307289657132, 396.2865697957464590, 6.153410032987091327 ) ) ;
#46530=CARTESIAN_POINT ( 'NONE',  ( 21.98474283332737045, 303.0789298805325416, -9.951410097099058660 ) ) ;
#46538=ADVANCED_FACE ( 'NONE', ( #92023 ), #87935, .T. ) ;
#46539=CARTESIAN_POINT ( 'NONE',  ( -43.18793366350591612, 465.6364658675350370, 10.75294125769769416 ) ) ;
#46543=CARTESIAN_POINT ( 'NONE',  ( 45.48126212248870814, 413.7349014071057240, 8.309231847991947362 ) ) ;
#46544=CARTESIAN_POINT ( 'NONE',  ( 6.123233995736766282E-16, 70.00000000000000000, -5.000000000000000000 ) ) ;
#46547=CYLINDRICAL_SURFACE ( 'NONE', #8638, 6.999999999999993783 ) ;
#46565=CARTESIAN_POINT ( 'NONE',  ( -43.71297783477830734, 485.1278128289774259, -1.116606130290624721 ) ) ;
#46568=VERTEX_POINT ( 'NONE', #70285 ) ;
#46578=CARTESIAN_POINT ( 'NONE',  ( 19.99629473115066958, 294.7507145989418404, 9.915512459802851453 ) ) ;
#46579=EDGE_CURVE ( 'NONE', #84500, #72783, #81059, .T. ) ;
#46580=ORIENTED_EDGE ( 'NONE', *, *, #95812, .F. ) ;
#46595=ORIENTED_EDGE ( 'NONE', *, *, #84212, .T. ) ;
#46604=EDGE_CURVE ( 'NONE', #66185, #81976, #54758, .T. ) ;
#46619=VERTEX_POINT ( 'NONE', #47047 ) ;
#46620=CARTESIAN_POINT ( 'NONE',  ( 32.84463799220507241, 316.8457873297845708, -6.870995899933766360 ) ) ;
#46623=CARTESIAN_POINT ( 'NONE',  ( -29.42328174557860265, 308.7510679269275897, -8.882624838725998728 ) ) ;
#46632=CARTESIAN_POINT ( 'NONE',  ( -36.93845425212112588, 463.9889438915046753, 19.60668832162587094 ) ) ;
#46640=CARTESIAN_POINT ( 'NONE',  ( 37.19305974667213377, 304.2850609022308959, -7.836023120251422114 ) ) ;
#46654=B_SPLINE_CURVE_WITH_KNOTS ( 'NONE', 3,
 ( #75364, #59740, #1465, #49497 ),
 .UNSPECIFIED., .F., .F.,
 ( 4, 4 ),
 ( 0.0007474059274884787369, 0.02468721214969757730 ),
 .UNSPECIFIED. ) ;
#46658=CARTESIAN_POINT ( 'NONE',  ( 43.18011688740498499, 485.8502513089949844, 5.262111696943175154 ) ) ;
#46681=ORIENTED_EDGE ( 'NONE', *, *, #55710, .T. ) ;
#46688=CARTESIAN_POINT ( 'NONE',  ( -37.70206801957033349, 409.1304537038757303, 6.512665395000928115 ) ) ;
#46700=CARTESIAN_POINT ( 'NONE',  ( 1.333692126671238043, 297.3239193841515089, -10.00118529339073525 ) ) ;
#46703=CARTESIAN_POINT ( 'NONE',  ( 38.71676723733723691, 463.8587156194949443, 18.97100414386192924 ) ) ;
#46708=ORIENTED_EDGE ( 'NONE', *, *, #84660, .F. ) ;
#46714=EDGE_CURVE ( 'NONE', #16979, #31406, #39315, .T. ) ;
#46723=CARTESIAN_POINT ( 'NONE',  ( 18.13823877062313272, 304.6380157655604535, 9.891557580208379719 ) ) ;
#46728=( BOUNDED_SURFACE ( )  B_SPLINE_SURFACE ( 3, 2, ( 
 ( #94978, #42018, #91129 ),
 ( #99728, #75449, #73307 ),
 ( #74376, #16686, #49577 ),
 ( #97581, #64711, #23750 ) ),
 .UNSPECIFIED., .F., .F., .F. ) 
 B_SPLINE_SURFACE_WITH_KNOTS ( ( 4, 4 ),
 ( 3, 3 ),
 ( 0.007402583550056900108, 0.03545809677458416909 ),
 ( 0.000000000000000000, 1.000000000000000000 ),
 .UNSPECIFIED. ) 
 GEOMETRIC_REPRESENTATION_ITEM ( )  RATIONAL_B_SPLINE_SURFACE ( (
 ( 1.000000000000000000, 0.8381405646299836532, 1.000000000000000000),
 ( 1.000000000000000000, 0.8381407646764915675, 1.000000000000000000),
 ( 1.000000000000000000, 0.8381408042060416452, 1.000000000000000000),
 ( 1.000000000000000000, 0.8381405998616443531, 1.000000000000000000) ) ) 
 REPRESENTATION_ITEM ( '' )  SURFACE ( )  );
#46740=CARTESIAN_POINT ( 'NONE',  ( 46.00000000000000000, 488.9831568219302653, 4.757012338623825443 ) ) ;
#46742=DIRECTION ( 'NONE',  ( -1.000000000000000000, -0.000000000000000000, -0.000000000000000000 ) ) ;
#46744=CIRCLE ( 'NONE', #81211, 1.000000000000000888 ) ;
#46751=CARTESIAN_POINT ( 'NONE',  ( -33.00000000000000000, 439.7597899781497972, 24.16317522621304192 ) ) ;
#46753=CARTESIAN_POINT ( 'NONE',  ( -43.64095197017179828, 465.1110681766505763, 8.836794732693006083 ) ) ;
#46769=CARTESIAN_POINT ( 'NONE',  ( -24.48174174843943973, 306.7381792433261580, 9.359562147283707390 ) ) ;
#46771=CARTESIAN_POINT ( 'NONE',  ( 20.05055460606549644, 304.8393297837531577, 9.934348198929242812 ) ) ;
#46781=CARTESIAN_POINT ( 'NONE',  ( 46.00000000000000000, 488.0336798547363628, -0.8984331811843099258 ) ) ;
#46785=AXIS2_PLACEMENT_3D ( 'NONE', #37412, #22277, #70276 ) ;
#46804=SURFACE_SIDE_STYLE ('',( #104502 ) ) ;
#46811=CARTESIAN_POINT ( 'NONE',  ( 43.00000000000000000, 461.4080316921935605, 3.462976341553817949 ) ) ;
#46813=ORIENTED_EDGE ( 'NONE', *, *, #84105, .F. ) ;
#46815=ORIENTED_EDGE ( 'NONE', *, *, #56668, .F. ) ;
#46821=CARTESIAN_POINT ( 'NONE',  ( 39.47876275252662737, 315.8379454371342945, 7.014882839542285531 ) ) ;
#46822=CARTESIAN_POINT ( 'NONE',  ( -43.43869229197126458, 464.9661605157749023, 13.42065392471464058 ) ) ;
#46832=CARTESIAN_POINT ( 'NONE',  ( -26.54090941152919214, 306.2719066919671036, 10.71778513407069688 ) ) ;
#46837=ADVANCED_FACE ( 'NONE', ( #104096 ), #50806, .F. ) ;
#46844=ORIENTED_EDGE ( 'NONE', *, *, #9730, .F. ) ;
#46846=CARTESIAN_POINT ( 'NONE',  ( 35.46984665180495711, 438.0686027085627074, 4.109636340053284265 ) ) ;
#46859=CARTESIAN_POINT ( 'NONE',  ( 9.407137736676965289, 302.6622268192648448, -10.04029227552669568 ) ) ;
#46860=CARTESIAN_POINT ( 'NONE',  ( 40.61216075948964033, 351.1469683695276558, 22.89433108575548914 ) ) ;
#46864=CYLINDRICAL_SURFACE ( 'NONE', #27915, 15.00000000000001421 ) ;
#46872=ORIENTED_EDGE ( 'NONE', *, *, #34064, .T. ) ;
#46882=EDGE_LOOP ( 'NONE', ( #15202, #6150, #16091, #50365 ) ) ;
#46885=ORIENTED_EDGE ( 'NONE', *, *, #25787, .F. ) ;
#46888=CARTESIAN_POINT ( 'NONE',  ( 43.71037717921923615, 462.3391554988761527, 4.824299547763561513 ) ) ;
#46892=CARTESIAN_POINT ( 'NONE',  ( -34.92245169924841974, 464.4743357356041429, 18.75701277737645611 ) ) ;
#46905=ORIENTED_EDGE ( 'NONE', *, *, #6813, .F. ) ;
#46915=FACE_OUTER_BOUND ( 'NONE', #9195, .T. ) ;
#46918=CARTESIAN_POINT ( 'NONE',  ( -39.13885763974980136, 324.4948203046521371, 17.18769520460729439 ) ) ;
#46921=CARTESIAN_POINT ( 'NONE',  ( 44.00534824917844645, 485.4287573672961003, 6.291782489092178743 ) ) ;
#46936=CARTESIAN_POINT ( 'NONE',  ( -32.10320572247816528, 439.3861412500730808, 23.61825846262832584 ) ) ;
#46937=CARTESIAN_POINT ( 'NONE',  ( -31.53901790643017478, 437.3649809074569816, 21.86268250587596995 ) ) ;
#46938=CARTESIAN_POINT ( 'NONE',  ( 21.51569398614863715, 294.9107018935607130, -9.987480606144508499 ) ) ;
#46939=CARTESIAN_POINT ( 'NONE',  ( -31.63473512700289092, 436.4561590364504013, 18.86554224087425879 ) ) ;
#46946=CARTESIAN_POINT ( 'NONE',  ( -35.61732482767578034, 303.3743595346010125, -0.04560823654630981328 ) ) ;
#46952=CARTESIAN_POINT ( 'NONE',  ( -20.34579289372443966, 303.8361034413807147, -9.003336996645776580 ) ) ;
#46962=CARTESIAN_POINT ( 'NONE',  ( -45.99999999998839684, 463.0730145254914873, 8.174293518655169066 ) ) ;
#46963=CARTESIAN_POINT ( 'NONE',  ( -36.60412653376215530, 439.8086773859736809, 24.20897003097096345 ) ) ;
#46964=ORIENTED_EDGE ( 'NONE', *, *, #40254, .T. ) ;
#46966=CARTESIAN_POINT ( 'NONE',  ( -37.71162116919980178, 389.8276394972959338, 6.083134903602375410 ) ) ;
#46973=EDGE_CURVE ( 'NONE', #45028, #103023, #61292, .T. ) ;
#46983=CARTESIAN_POINT ( 'NONE',  ( 20.35953037385061037, 294.7626276629184758, -10.01895475554768566 ) ) ;
#46991=EDGE_CURVE ( 'NONE', #94742, #48471, #69004, .T. ) ;
#47004=CARTESIAN_POINT ( 'NONE',  ( 30.35537264529554946, 338.7115663565144246, 18.05293407820170515 ) ) ;
#47047=CARTESIAN_POINT ( 'NONE',  ( 43.47770857297122404, 484.8227827122696567, 4.253339224811428565 ) ) ;
#47049=ORIENTED_EDGE ( 'NONE', *, *, #20378, .F. ) ;
#47054=CARTESIAN_POINT ( 'NONE',  ( 33.72687874471721869, 464.0440927329411238, 18.49751758896739418 ) ) ;
#47058=CARTESIAN_POINT ( 'NONE',  ( 36.91281931599076671, 303.7809130842520631, -7.959270006439831846 ) ) ;
#47069=CARTESIAN_POINT ( 'NONE',  ( -33.70225418956815133, 490.4053771886481172, 11.54106678942738462 ) ) ;
#47078=CARTESIAN_POINT ( 'NONE',  ( 32.18152564816683991, 409.5707777767445918, 25.68904866590993308 ) ) ;
#47081=CARTESIAN_POINT ( 'NONE',  ( -43.00000000000009237, 484.2804969086082565, -2.982821241663377254 ) ) ;
#47088=ORIENTED_EDGE ( 'NONE', *, *, #50693, .F. ) ;
#47091=ORIENTED_EDGE ( 'NONE', *, *, #44864, .F. ) ;
#47142=CARTESIAN_POINT ( 'NONE',  ( 35.49450300380783574, 379.3078207793571437, 5.749337263989718672 ) ) ;
#47145=CARTESIAN_POINT ( 'NONE',  ( -20.41854916970525835, 303.8436858046150633, -10.00172532726429075 ) ) ;
#47148=CARTESIAN_POINT ( 'NONE',  ( 40.03968747356719149, 489.2277061813577461, 11.31325917480963028 ) ) ;
#47150=CARTESIAN_POINT ( 'NONE',  ( 44.21332904831284338, 435.2494715644500616, 14.45449769377396976 ) ) ;
#47151=ORIENTED_EDGE ( 'NONE', *, *, #72357, .F. ) ;
#47161=CARTESIAN_POINT ( 'NONE',  ( 33.10170411573166405, 314.2231804304243497, -7.291332407212943956 ) ) ;
#47165=CARTESIAN_POINT ( 'NONE',  ( 31.35596682365711274, 438.0939828603570732, 22.55458131664589061 ) ) ;
#47171=ADVANCED_FACE ( 'NONE', ( #1544 ), #44701, .T. ) ;
#47209=CARTESIAN_POINT ( 'NONE',  ( -46.00000000000000000, 488.0504108836653359, 1.820875518055464770 ) ) ;
#47214=EDGE_CURVE ( 'NONE', #106028, #26488, #103673, .T. ) ;
#47217=CARTESIAN_POINT ( 'NONE',  ( -40.62309488084728315, 485.6251729596530140, -4.313937499028603462 ) ) ;
#47223=CARTESIAN_POINT ( 'NONE',  ( -38.88461863710598010, 437.7975295993174427, 4.475058894670826071 ) ) ;
#47226=EDGE_CURVE ( 'NONE', #10730, #25883, #13917, .T. ) ;
#47250=CARTESIAN_POINT ( 'NONE',  ( -38.81358894280271699, 485.1131561813180042, -4.191378885296423995 ) ) ;
#47261=APPLICATION_CONTEXT ( 'automotive_design' ) ;
#47266=ORIENTED_EDGE ( 'NONE', *, *, #62385, .T. ) ;
#47267=CARTESIAN_POINT ( 'NONE',  ( 41.18546553262711996, 436.5301601935307190, 21.34144970355281501 ) ) ;
#47274=CARTESIAN_POINT ( 'NONE',  ( 42.75202416080772139, 486.5826644063713502, 6.942705799351878149 ) ) ;
#47279=VERTEX_POINT ( 'NONE', #18856 ) ;
#47282=B_SPLINE_CURVE_WITH_KNOTS ( 'NONE', 3,
 ( #6386, #5353, #64640, #97511 ),
 .UNSPECIFIED., .F., .F.,
 ( 4, 4 ),
 ( 3.469446951953614189E-18, 0.0002123325198249128231 ),
 .UNSPECIFIED. ) ;
#47287=CARTESIAN_POINT ( 'NONE',  ( -26.96123873314553165, 312.0017479745702076, 11.65844439973563773 ) ) ;
#47289=CARTESIAN_POINT ( 'NONE',  ( 22.14525041823859297, 304.2680615509976860, 10.02651133272836681 ) ) ;
#47311=ORIENTED_EDGE ( 'NONE', *, *, #29619, .T. ) ;
#47332=CARTESIAN_POINT ( 'NONE',  ( -44.31081229532764354, 435.2284720930225603, 12.07948685322291382 ) ) ;
#47336=B_SPLINE_CURVE_WITH_KNOTS ( 'NONE', 3,
 ( #15657, #25385, #49076, #17277, #31871, #83059 ),
 .UNSPECIFIED., .F., .F.,
 ( 4, 2, 4 ),
 ( 0.000000000000000000, 0.001720102060488473651, 0.003440204120976947302 ),
 .UNSPECIFIED. ) ;
#47338=CARTESIAN_POINT ( 'NONE',  ( -42.19180677453720563, 462.2931784592652207, 3.389262873192004477 ) ) ;
#47345=CARTESIAN_POINT ( 'NONE',  ( 29.20990149186424745, 312.7062169680672241, 12.31820844411544869 ) ) ;
#47353=( BOUNDED_SURFACE ( )  B_SPLINE_SURFACE ( 3, 2, ( 
 ( #6342, #72162, #31210 ),
 ( #96971, #23106, #37178 ),
 ( #86251, #70039, #94868 ),
 ( #16582, #98548, #73744 ) ),
 .UNSPECIFIED., .F., .F., .F. ) 
 B_SPLINE_SURFACE_WITH_KNOTS ( ( 4, 4 ),
 ( 3, 3 ),
 ( -3.989863994746656317E-17, 0.001384307398017841327 ),
 ( 0.000000000000000000, 1.000000000000000000 ),
 .UNSPECIFIED. ) 
 GEOMETRIC_REPRESENTATION_ITEM ( )  RATIONAL_B_SPLINE_SURFACE ( (
 ( 1.000000000000000000, 0.7976994903569347706, 1.000000000000000000),
 ( 1.000000000000000000, 0.8073889694078232315, 1.000000000000000000),
 ( 1.000000000000000000, 0.8171087964277252702, 1.000000000000000000),
 ( 1.000000000000000000, 0.8266506655096979017, 1.000000000000000000) ) ) 
 REPRESENTATION_ITEM ( '' )  SURFACE ( )  );
#47356=CARTESIAN_POINT ( 'NONE',  ( -32.99999999999992184, 463.5362553048593099, 6.739467187734545561 ) ) ;
#47359=CARTESIAN_POINT ( 'NONE',  ( -35.30297382066545708, 361.4833082129059676, 3.507038767897731280 ) ) ;
#47360=CARTESIAN_POINT ( 'NONE',  ( -33.63754935668455914, 302.6102131421956756, 11.72270476798247962 ) ) ;
#47372=CARTESIAN_POINT ( 'NONE',  ( 36.29541806397946146, 438.2518625957742984, 3.876047449288812174 ) ) ;
#47384=CARTESIAN_POINT ( 'NONE',  ( 42.61340452791766609, 486.8925439250689351, 7.464118458850313331 ) ) ;
#47395=ORIENTED_EDGE ( 'NONE', *, *, #97914, .F. ) ;
#47416=CARTESIAN_POINT ( 'NONE',  ( 31.14080955122648220, 433.9629369115588702, 24.00288416902248656 ) ) ;
#47436=CARTESIAN_POINT ( 'NONE',  ( 32.87547266101556431, 465.6993878536748070, 10.91512469976365551 ) ) ;
#47442=CARTESIAN_POINT ( 'NONE',  ( -6.426132457094225536, 294.7471176151092891, 9.914747880764233301 ) ) ;
#47444=CARTESIAN_POINT ( 'NONE',  ( -42.15357157759102336, 485.2432036427136381, -2.744622672921036788 ) ) ;
#47448=DIRECTION ( 'NONE',  ( -0.1792365085138481196, 0.7133058216316990885, 0.6775463665625343079 ) ) ;
#47449=CARTESIAN_POINT ( 'NONE',  ( -35.04348997864995852, 484.2371297655225817, -0.9829126381465729256 ) ) ;
#47456=EDGE_CURVE ( 'NONE', #7582, #15655, #5322, .T. ) ;
#47465=CARTESIAN_POINT ( 'NONE',  ( -35.70850055078799556, 426.6386616601230912, 5.234124974471177083 ) ) ;
#47474=CARTESIAN_POINT ( 'NONE',  ( -28.98077275437907474, 306.6777056724459385, -9.140503625966282186 ) ) ;
#47481=CARTESIAN_POINT ( 'NONE',  ( 31.44900225665126570, 397.6393522637353044, 24.40758882435354948 ) ) ;
#47515=VERTEX_POINT ( 'NONE', #66173 ) ;
#47517=EDGE_CURVE ( 'NONE', #10424, #55309, #64004, .T. ) ;
#47526=CARTESIAN_POINT ( 'NONE',  ( -33.00000000000000000, 489.5971041675261404, 10.80646835458718868 ) ) ;
#47531=B_SPLINE_CURVE_WITH_KNOTS ( 'NONE', 3,
 ( #36801, #93944, #53482, #51869 ),
 .UNSPECIFIED., .F., .F.,
 ( 4, 4 ),
 ( 0.000000000000000000, 0.001257843226828573311 ),
 .UNSPECIFIED. ) ;
#47540=EDGE_LOOP ( 'NONE', ( #21238, #78076, #17859, #4141, #13694 ) ) ;
#47558=ORIENTED_EDGE ( 'NONE', *, *, #54679, .T. ) ;
#47564=VERTEX_POINT ( 'NONE', #32776 ) ;
#47571=CARTESIAN_POINT ( 'NONE',  ( 46.00000000000000000, 460.1242873147357386, 6.750975842511372171 ) ) ;
#47587=FACE_OUTER_BOUND ( 'NONE', #55814, .T. ) ;
#47623=CARTESIAN_POINT ( 'NONE',  ( 13.68615037905027876, 294.5456273187321017, 1.871922570298397703 ) ) ;
#47630=ADVANCED_FACE ( 'NONE', ( #64594, #40835 ), #16028, .T. ) ;
#47634=CARTESIAN_POINT ( 'NONE',  ( 0.000000000000000000, 0.000000000000000000, 5.000000000000000000 ) ) ;
#47652=EDGE_CURVE ( 'NONE', #73295, #103730, #35314, .T. ) ;
#47660=CARTESIAN_POINT ( 'NONE',  ( 34.47211195129249717, 489.5752767497880882, 11.69752549375474437 ) ) ;
#47664=LINE ( 'NONE', #28896, #14919 ) ;
#47669=CARTESIAN_POINT ( 'NONE',  ( 35.68999143317073219, 432.5319086955427679, 4.688598029357957664 ) ) ;
#47670=ORIENTED_EDGE ( 'NONE', *, *, #20735, .T. ) ;
#47671=DIRECTION ( 'NONE',  ( 0.8714291948010992606, 0.000000000000000000, -0.4905213129399249583 ) ) ;
#47672=CARTESIAN_POINT ( 'NONE',  ( -31.49856340160977908, 312.6924388527738756, -7.915384035900890680 ) ) ;
#47673=CARTESIAN_POINT ( 'NONE',  ( 41.99899754399194052, 488.0172855231593303, 9.044990669317995113 ) ) ;
#47674=CARTESIAN_POINT ( 'NONE',  ( 43.00000000000000000, 437.9690125970931831, 14.09127711025711349 ) ) ;
#47689=CARTESIAN_POINT ( 'NONE',  ( 36.14035709840733546, 304.2251051115202927, 0.1608020814845102231 ) ) ;
#47691=ORIENTED_EDGE ( 'NONE', *, *, #93065, .T. ) ;
#47703=ORIENTED_EDGE ( 'NONE', *, *, #94511, .T. ) ;
#47709=ORIENTED_EDGE ( 'NONE', *, *, #85036, .F. ) ;
#47711=AXIS2_PLACEMENT_3D ( 'NONE', #92868, #92334, #101504 ) ;
#47712=SURFACE_STYLE_USAGE ( .BOTH. , #44697 ) ;
#47733=CARTESIAN_POINT ( 'NONE',  ( 33.09106007554123607, 433.0116111952169717, 24.60471978344146393 ) ) ;
#47734=CARTESIAN_POINT ( 'NONE',  ( -44.28506098230518262, 335.5159265879102009, -0.1714402822340226062 ) ) ;
#47750=CARTESIAN_POINT ( 'NONE',  ( 41.75487894852329163, 464.7989896699401129, 15.72965077414808732 ) ) ;
#47753=ORIENTED_EDGE ( 'NONE', *, *, #2015, .F. ) ;
#47756=CARTESIAN_POINT ( 'NONE',  ( 0.000000000000000000, 67.00000000000002842, 0.000000000000000000 ) ) ;
#47761=UNCERTAINTY_MEASURE_WITH_UNIT (LENGTH_MEASURE( 1.000000000000000082E-05 ), #41269, 'distance_accuracy_value', 'NONE');
#47763=DIRECTION ( 'NONE',  ( 0.000000000000000000, -0.8273160954975392611, 0.5617366626193331935 ) ) ;
#47765=ORIENTED_EDGE ( 'NONE', *, *, #73923, .F. ) ;
#47769=EDGE_CURVE ( 'NONE', #66563, #46054, #50181, .T. ) ;
#47771=CARTESIAN_POINT ( 'NONE',  ( -39.29284405225726573, 485.1982890239684707, -4.348287318897845921 ) ) ;
#47804=CARTESIAN_POINT ( 'NONE',  ( -35.45036406932566564, 436.3203772529605544, 5.179456583033978490 ) ) ;
#47810=CARTESIAN_POINT ( 'NONE',  ( -24.31407123536968840, 306.6633020399330576, 10.34267655207518644 ) ) ;
#47811=ORIENTED_EDGE ( 'NONE', *, *, #61911, .T. ) ;
#47812=CARTESIAN_POINT ( 'NONE',  ( 21.05814741031886328, 305.0197153841863269, 9.972911420270587968 ) ) ;
#47829=AXIS2_PLACEMENT_3D ( 'NONE', #78622, #77585, #87275 ) ;
#47836=CARTESIAN_POINT ( 'NONE',  ( 11.89663243729389386, 304.5916485594502205, -10.05529748560153358 ) ) ;
#47843=CARTESIAN_POINT ( 'NONE',  ( 46.00000000000000711, 461.2856817983021074, 8.847499008863380254 ) ) ;
#47848=CARTESIAN_POINT ( 'NONE',  ( -20.20168668923396993, 303.8505198094663911, 9.936726593992792900 ) ) ;
#47850=B_SPLINE_CURVE_WITH_KNOTS ( 'NONE', 3,
 ( #46565, #14176, #30949, #46044, #13117, #37987, #21270, #78928 ),
 .UNSPECIFIED., .F., .F.,
 ( 4, 2, 2, 4 ),
 ( 2.359479019930958006E-17, 0.002589981853911959252, 0.003884972780867916760, 0.005179963707823875135 ),
 .UNSPECIFIED. ) ;
#47853=CARTESIAN_POINT ( 'NONE',  ( -32.94994279514429536, 464.9549361168403721, 15.12478419439328547 ) ) ;
#47856=CARTESIAN_POINT ( 'NONE',  ( -37.88504238421005965, 463.4171042825123550, 19.90923349044086166 ) ) ;
#47867=CARTESIAN_POINT ( 'NONE',  ( 39.29144825744032943, 326.5384315043369838, 17.65690345107428172 ) ) ;
#47876=EDGE_LOOP ( 'NONE', ( #103209, #16521, #15499, #54244 ) ) ;
#47877=CARTESIAN_POINT ( 'NONE',  ( -42.69811214730273718, 434.9611672192514220, 18.34625614733213439 ) ) ;
#47878=DIRECTION ( 'NONE',  ( 1.000000000000000000, 0.000000000000000000, 0.000000000000000000 ) ) ;
#47879=CARTESIAN_POINT ( 'NONE',  ( -25.54576300332514904, 305.0804997338725002, 10.43511780733714289 ) ) ;
#47893=CARTESIAN_POINT ( 'NONE',  ( 36.59119455513890529, 438.2489652597744225, 3.879698295689091747 ) ) ;
#47906=CARTESIAN_POINT ( 'NONE',  ( 9.497389752372439986, 295.1492747691102636, -10.04143169208125208 ) ) ;
#47928=DIRECTION ( 'NONE',  ( 0.000000000000000000, 0.000000000000000000, -1.000000000000000000 ) ) ;
#47935=EDGE_LOOP ( 'NONE', ( #32486, #50843, #53688, #49579, #13780 ) ) ;
#47949=CARTESIAN_POINT ( 'NONE',  ( -36.87655955837857391, 437.4206410680704948, 3.315070609669444224 ) ) ;
#47958=CARTESIAN_POINT ( 'NONE',  ( -1.959911964389828398, 298.2559866373201203, -10.00257402834333931 ) ) ;
#47964=CARTESIAN_POINT ( 'NONE',  ( -8.813378757748752790, 294.6780630559476890, 9.900069857271436291 ) ) ;
#47968=CARTESIAN_POINT ( 'NONE',  ( 11.89108997990703109, 303.5914306638122753, -10.05534273549331559 ) ) ;
#47969=CARTESIAN_POINT ( 'NONE',  ( 37.38602481900366570, 490.8442832704907914, 12.40593855171325899 ) ) ;
#47990=CARTESIAN_POINT ( 'NONE',  ( -34.05318764567596190, 330.1458591810355188, -3.797486262497478116 ) ) ;
#47999=CARTESIAN_POINT ( 'NONE',  ( -31.22333652669472670, 298.2284108743594970, -9.257293644257531540 ) ) ;
#48005=DIRECTION ( 'NONE',  ( 0.1270361284032155702, -0.9918980905719708696, 0.000000000000000000 ) ) ;
#48012=ORIENTED_EDGE ( 'NONE', *, *, #23065, .T. ) ;
#48015=CARTESIAN_POINT ( 'NONE',  ( -35.04511767293112712, 439.6082740367514248, 24.02922479211273910 ) ) ;
#48030=CARTESIAN_POINT ( 'NONE',  ( 43.02621584241281028, 434.6128289108257832, 16.97888786058996047 ) ) ;
#48057=CARTESIAN_POINT ( 'NONE',  ( -3.269135563215229023, 294.8518027752268722, -10.00000000024436453 ) ) ;
#48059=CARTESIAN_POINT ( 'NONE',  ( 38.51502786939607859, 460.0233756673479206, 2.043034587344076947 ) ) ;
#48060=B_SPLINE_CURVE_WITH_KNOTS ( 'NONE', 3,
 ( #77910, #60680, #11556, #9974 ),
 .UNSPECIFIED., .F., .F.,
 ( 4, 4 ),
 ( 2.442512830937285646E-17, 0.0004064560158402741601 ),
 .UNSPECIFIED. ) ;
#48069=CARTESIAN_POINT ( 'NONE',  ( 32.22120753352782430, 464.6691781026583499, 10.60621122532595884 ) ) ;
#48096=CARTESIAN_POINT ( 'NONE',  ( 34.25540317603680762, 485.0620278916508141, -1.482526247038510991 ) ) ;
#48110=CARTESIAN_POINT ( 'NONE',  ( -43.34934355818133866, 465.4850867214047980, 10.08239944467068661 ) ) ;
#48114=ORIENTED_EDGE ( 'NONE', *, *, #17917, .F. ) ;
#48116=CARTESIAN_POINT ( 'NONE',  ( -31.00389226642222340, 485.8187364282109115, 14.27494812388583512 ) ) ;
#48117=FACE_OUTER_BOUND ( 'NONE', #82685, .T. ) ;
#48129=LINE ( 'NONE', #55156, #16371 ) ;
#48131=ORIENTED_EDGE ( 'NONE', *, *, #9820, .T. ) ;
#48145=ORIENTED_EDGE ( 'NONE', *, *, #14904, .T. ) ;
#48155=CARTESIAN_POINT ( 'NONE',  ( 11.99465477046492623, 294.5867369860492886, 1.880684200158333930 ) ) ;
#48167=CARTESIAN_POINT ( 'NONE',  ( -38.50844621391336631, 490.3070771754929638, 12.08756601353534421 ) ) ;
#48168=AXIS2_PLACEMENT_3D ( 'NONE', #16177, #97096, #105714 ) ;
#48171=DIRECTION ( 'NONE',  ( 0.1804394941736726932, -0.5071212677061492924, 0.8427749455118236366 ) ) ;
#48187=CARTESIAN_POINT ( 'NONE',  ( 35.85615118283584479, 463.5955582468889133, 19.55698106745834153 ) ) ;
#48191=CARTESIAN_POINT ( 'NONE',  ( -45.17824257314219949, 354.4244853104167987, 3.762393652172960845 ) ) ;
#48198=CARTESIAN_POINT ( 'NONE',  ( 31.10268009770144104, 314.3950341270036120, -7.730101311383788421 ) ) ;
#48207=CARTESIAN_POINT ( 'NONE',  ( -33.00000000000000000, 439.7597899781497972, 24.16317522621304192 ) ) ;
#48219=CARTESIAN_POINT ( 'NONE',  ( 40.85601670693966980, 312.5844051700327100, -5.777679661402379985 ) ) ;
#48233=CARTESIAN_POINT ( 'NONE',  ( 43.18057774162367934, 485.1460640375465800, 5.477159825588830522 ) ) ;
#48240=ORIENTED_EDGE ( 'NONE', *, *, #923, .F. ) ;
#48242=CARTESIAN_POINT ( 'NONE',  ( 36.05499942621670328, 461.6905473683075911, 3.778726173785988074 ) ) ;
#48243=DIRECTION ( 'NONE',  ( -0.000000000000000000, -1.000000000000000000, -0.000000000000000000 ) ) ;
#48246=CARTESIAN_POINT ( 'NONE',  ( -30.00000000000000000, 489.8687857340703431, 6.490256706953523747 ) ) ;
#48258=ORIENTED_EDGE ( 'NONE', *, *, #24443, .T. ) ;
#48259=ORIENTED_EDGE ( 'NONE', *, *, #47456, .F. ) ;
#48263=CARTESIAN_POINT ( 'NONE',  ( 29.57346108177781474, 314.0826370294551566, 12.66639719735920444 ) ) ;
#48264=CARTESIAN_POINT ( 'NONE',  ( -41.11855258730697926, 320.9326643076389018, 4.345040179154948667 ) ) ;
#48270=B_SPLINE_CURVE_WITH_KNOTS ( 'NONE', 3,
 ( #84439, #34852, #10529, #52582, #43447, #60710, #68798, #76862, #18667, #35926, #85506, #101679, #2436, #68252, #27838, #19745, #50977, #34320, #9456, #42370, #35385, #92512, #26241, #101144, #50447, #27305, #67196, #2969, #83358, #10004, #93055, #75802, #11051, #67720, #51521, #19221, #1897, #52051, #75256, #59104, #43974, #84966, #18122, #42911, #26766, #59638, #31843, #72796, #6470, #56613, #21642, #72280 ),
 .UNSPECIFIED., .F., .F.,
 ( 4, 2, 2, 2, 2, 2, 2, 2, 2, 2, 2, 2, 2, 2, 2, 2, 2, 2, 2, 2, 2, 2, 2, 2, 2, 4 ),
 ( -6.000000002246681564E-08, 0.001182188478371536859, 0.002364436956743095914, 0.004728933913486179329, 0.009457927826972347893, 0.01064017630534381913, 0.01182242478371529383, 0.01418692174045836640, 0.01536917021882990876, 0.01655141869720145112, 0.01891591565394454277, 0.02128041261068763790, 0.02364490956743073996, 0.02837390348091693021, 0.03310289739440312046, 0.03783189130788931070, 0.04728987913486153855, 0.05674786696183375945, 0.06620585478880598729, 0.07566384261577820125, 0.08512183044275041521, 0.09457981826972264305, 0.1134957939236672514, 0.1324117695776118597, 0.1418697574045841570, 0.1513277452315564819 ),
 .UNSPECIFIED. ) ;
#48279=CARTESIAN_POINT ( 'NONE',  ( 39.44782958596293554, 464.6967695243274079, 18.31680536522812730 ) ) ;
#48287=CARTESIAN_POINT ( 'NONE',  ( -36.65199127662805978, 490.9971735395452015, 12.47305305857717350 ) ) ;
#48303=EDGE_CURVE ( 'NONE', #89572, #69385, #65004, .T. ) ;
#48325=CARTESIAN_POINT ( 'NONE',  ( -33.49722639937191104, 439.8559922839228307, 24.25305334379669731 ) ) ;
#48332=CARTESIAN_POINT ( 'NONE',  ( 33.81879868294056735, 301.0020191845601971, -0.6124722288186084107 ) ) ;
#48336=CARTESIAN_POINT ( 'NONE',  ( -28.76346532419124458, 309.5219921958590135, -8.933260212751790164 ) ) ;
#48338=CARTESIAN_POINT ( 'NONE',  ( -42.20041562234357002, 435.2369744135583574, 7.788607701745487333 ) ) ;
#48341=CARTESIAN_POINT ( 'NONE',  ( -32.28930913497458022, 488.2717154064632723, 9.213726894912692700 ) ) ;
#48347=CARTESIAN_POINT ( 'NONE',  ( -25.61096549847395565, 308.3358331228886300, 9.743382623630527206 ) ) ;
#48354=EDGE_LOOP ( 'NONE', ( #76384, #98086, #75451, #91383 ) ) ;
#48376=CARTESIAN_POINT ( 'NONE',  ( 35.66932529116966322, 438.9565575286536045, 4.011496722538590909 ) ) ;
#48378=ORIENTED_EDGE ( 'NONE', *, *, #55041, .T. ) ;
#48385=ADVANCED_FACE ( 'NONE', ( #64347 ), #97738, .F. ) ;
#48398=ORIENTED_EDGE ( 'NONE', *, *, #33886, .F. ) ;
#48403=CARTESIAN_POINT ( 'NONE',  ( 38.99788563095989247, 323.4896271503449725, 16.92816184090444409 ) ) ;
#48407=CARTESIAN_POINT ( 'NONE',  ( 42.77863378085803703, 403.5742920147162067, 19.98408815037751651 ) ) ;
#48408=CARTESIAN_POINT ( 'NONE',  ( -36.87655955837857391, 438.2068510013161244, 3.933030107424709598 ) ) ;
#48412=B_SPLINE_CURVE_WITH_KNOTS ( 'NONE', 3,
 ( #67994, #59927, #44256, #74996 ),
 .UNSPECIFIED., .F., .F.,
 ( 4, 4 ),
 ( 0.000000000000000000, 0.001800036990446803433 ),
 .UNSPECIFIED. ) ;
#48413=CARTESIAN_POINT ( 'NONE',  ( -33.30691720919135435, 302.0691436612021334, 11.59134413587671908 ) ) ;
#48414=DIRECTION ( 'NONE',  ( 0.9738156377458858648, 0.000000000000000000, 0.2273391820201123570 ) ) ;
#48430=CARTESIAN_POINT ( 'NONE',  ( 35.45036406932484141, 436.3203772529680009, 5.179456583036507133 ) ) ;
#48446=CARTESIAN_POINT ( 'NONE',  ( 33.80014854764886678, 484.1533675814796425, 1.810747741435669189 ) ) ;
#48464=VERTEX_POINT ( 'NONE', #105839 ) ;
#48471=VERTEX_POINT ( 'NONE', #71885 ) ;
#48473=ORIENTED_EDGE ( 'NONE', *, *, #23065, .F. ) ;
#48474=CARTESIAN_POINT ( 'NONE',  ( 34.49859336298668921, 464.8458904554861988, 18.22488476267798774 ) ) ;
#48477=VERTEX_POINT ( 'NONE', #105322 ) ;
#48505=CARTESIAN_POINT ( 'NONE',  ( 43.00000000000000000, 488.9831568219304927, 4.757012338623754388 ) ) ;
#48506=B_SPLINE_CURVE_WITH_KNOTS ( 'NONE', 3,
 ( #105166, #11492, #68710, #51958 ),
 .UNSPECIFIED., .F., .F.,
 ( 4, 4 ),
 ( 3.469446951953614189E-18, 0.001900242520396456082 ),
 .UNSPECIFIED. ) ;
#48507=ORIENTED_EDGE ( 'NONE', *, *, #72986, .F. ) ;
#48523=CARTESIAN_POINT ( 'NONE',  ( -32.02876608638647582, 439.3983902163913626, 23.59623870271461854 ) ) ;
#48525=CARTESIAN_POINT ( 'NONE',  ( -26.72816845841281719, 307.3634948383742085, -8.441436268651763442 ) ) ;
#48528=CARTESIAN_POINT ( 'NONE',  ( -43.04469050570866528, 434.7734435962897805, 9.248231035232430841 ) ) ;
#48534=AXIS2_PLACEMENT_3D ( 'NONE', #47949, #106181, #98109 ) ;
#48540=CARTESIAN_POINT ( 'NONE',  ( 23.21665375867825531, 305.7593017747301474, 9.134900160712305706 ) ) ;
#48544=DIRECTION ( 'NONE',  ( 0.000000000000000000, 1.000000000000000000, 0.000000000000000000 ) ) ;
#48553=DIRECTION ( 'NONE',  ( 0.02699252395738975518, 0.001721171576548164101, -0.9996341536876447442 ) ) ;
#48566=CARTESIAN_POINT ( 'NONE',  ( 19.24564409877616811, 294.6757776630491321, -10.03741501079465515 ) ) ;
#48568=B_SPLINE_CURVE_WITH_KNOTS ( 'NONE', 3,
 ( #79421, #5536, #102646, #21757, #103181, #87530, #94576, #45489 ),
 .UNSPECIFIED., .F., .F.,
 ( 4, 2, 2, 4 ),
 ( 0.000000000000000000, 0.002114848577942575209, 0.003172272866913863031, 0.004229697155885150418 ),
 .UNSPECIFIED. ) ;
#48574=CARTESIAN_POINT ( 'NONE',  ( -33.00540147334746166, 487.4196752801198613, 9.523982417603901851 ) ) ;
#48576=CARTESIAN_POINT ( 'NONE',  ( 0.000000000000000000, 70.00000000000000000, 0.000000000000000000 ) ) ;
#48587=CARTESIAN_POINT ( 'NONE',  ( 43.03265099500004709, 484.2747968070555089, -0.8099405866658345721 ) ) ;
#48601=TOROIDAL_SURFACE ( 'NONE', #91677, 12.00000000000000711, 3.000000000000000000 ) ;
#48602=CARTESIAN_POINT ( 'NONE',  ( -2.153051538919529300E-10, 304.8518027762758607, 9.936999415352289589 ) ) ;
#48603=TOROIDAL_SURFACE ( 'NONE', #67582, 12.00000000000001066, 3.000000000000000000 ) ;
#48625=CARTESIAN_POINT ( 'NONE',  ( 43.64647135119551535, 462.3514304094902627, 4.815965046162477670 ) ) ;
#48629=FACE_OUTER_BOUND ( 'NONE', #10065, .T. ) ;
#48639=CARTESIAN_POINT ( 'NONE',  ( 44.26374899284098063, 435.3115877955005431, 11.30001004033899648 ) ) ;
#48643=CARTESIAN_POINT ( 'NONE',  ( -25.95507789760542039, 309.1386286255022924, 10.94030088463808070 ) ) ;
#48683=CARTESIAN_POINT ( 'NONE',  ( -20.28383506696344085, 302.8321527159674815, -2.004176749255730083 ) ) ;
#48694=CARTESIAN_POINT ( 'NONE',  ( -37.50059943756536995, 490.7879993827801286, 12.38039871356563992 ) ) ;
#48697=CARTESIAN_POINT ( 'NONE',  ( 35.04441504084191905, 439.6183875618604020, 24.03893527320687085 ) ) ;
#48712=CARTESIAN_POINT ( 'NONE',  ( 35.85186990248600125, 464.1122956640385269, 19.44147592471152208 ) ) ;
#48718=CARTESIAN_POINT ( 'NONE',  ( -40.95595929481465447, 405.2208686710653183, 27.85131585683114963 ) ) ;
#48719=CARTESIAN_POINT ( 'NONE',  ( -30.55228927099183522, 298.7536840786443690, 10.80461237140096209 ) ) ;
#48722=CARTESIAN_POINT ( 'NONE',  ( 29.69961346318338258, 311.1410465299570660, -8.538517479574506908 ) ) ;
#48723=EDGE_CURVE ( 'NONE', #26330, #93114, #84414, .T. ) ;
#48761=CARTESIAN_POINT ( 'NONE',  ( 30.63716938955784386, 313.5010800886507241, -6.952601511637969800 ) ) ;
#48768=CARTESIAN_POINT ( 'NONE',  ( 37.55537146824799066, 460.8431059341384639, 2.817977571237513690 ) ) ;
#48770=CARTESIAN_POINT ( 'NONE',  ( -15.60207464173859648, 302.5584671467747739, -10.06235099409590283 ) ) ;
#48772=( BOUNDED_SURFACE ( )  B_SPLINE_SURFACE ( 3, 2, ( 
 ( #11611, #68823, #18688 ),
 ( #67744, #20314, #4074 ),
 ( #69872, #93620, #43998 ),
 ( #61256, #76347, #35408 ),
 ( #52603, #59659, #53160 ),
 ( #100629, #68276, #37005 ),
 ( #102766, #76884, #69352 ),
 ( #51546, #94142, #60212 ),
 ( #19248, #45079, #101172 ),
 ( #84460, #61804, #86077 ),
 ( #35951, #20845, #12674 ),
 ( #27333, #12148, #93078 ),
 ( #77959, #101703, #3000 ),
 ( #3545, #53676, #52075 ) ),
 .UNSPECIFIED., .F., .F., .F. ) 
 B_SPLINE_SURFACE_WITH_KNOTS ( ( 4, 2, 2, 2, 2, 2, 4 ),
 ( 3, 3 ),
 ( -6.682588510331655129E-15, 0.0008334212029357339607, 0.001250131804406942344, 0.001666842405878150510, 0.002083553007349358676, 0.002500263608820566842, 0.003333684811762983608 ),
 ( 0.000000000000000000, 1.000000000000000000 ),
 .UNSPECIFIED. ) 
 GEOMETRIC_REPRESENTATION_ITEM ( )  RATIONAL_B_SPLINE_SURFACE ( (
 ( 1.000000000000000000, 0.8805984182408446159, 1.000000000000000000),
 ( 1.000000000000000000, 0.8998845875341654477, 1.000000000000000000),
 ( 1.000000000000000000, 0.9147006518920367535, 1.000000000000000000),
 ( 1.000000000000000000, 0.9294517919825534547, 1.000000000000000000),
 ( 1.000000000000000000, 0.9330010648506072979, 1.000000000000000000),
 ( 1.000000000000000000, 0.9375969056690098835, 1.000000000000000000),
 ( 1.000000000000000000, 0.9385966513831063285, 1.000000000000000000),
 ( 1.000000000000000000, 0.9384391173341486425, 1.000000000000000000),
 ( 1.000000000000000000, 0.9372974232555458807, 1.000000000000000000),
 ( 1.000000000000000000, 0.9336465948887834321, 1.000000000000000000),
 ( 1.000000000000000000, 0.9311806706621335028, 1.000000000000000000),
 ( 1.000000000000000000, 0.9227779475329482839, 1.000000000000000000),
 ( 1.000000000000000000, 0.9161682460698783448, 1.000000000000000000),
 ( 1.000000000000000000, 0.9103180234519290259, 1.000000000000000000) ) ) 
 REPRESENTATION_ITEM ( '' )  SURFACE ( )  );
#48783=VERTEX_POINT ( 'NONE', #54870 ) ;
#48787=CARTESIAN_POINT ( 'NONE',  ( -35.05824969151932891, 439.1559171757481863, 24.08323619564622931 ) ) ;
#48789=CARTESIAN_POINT ( 'NONE',  ( -37.63230006911589953, 374.2148764567931494, 4.687993092313281984 ) ) ;
#48791=CARTESIAN_POINT ( 'NONE',  ( -46.00000000000000000, 488.0078051104092651, -0.5538049991128992655 ) ) ;
#48801=ADVANCED_FACE ( 'NONE', ( #14402 ), #27554, .T. ) ;
#48811=( NAMED_UNIT ( * ) PLANE_ANGLE_UNIT ( ) SI_UNIT ( $, .RADIAN. ) );
#48813=CARTESIAN_POINT ( 'NONE',  ( -37.67950550370962048, 491.6872717898309020, 12.48612654748556494 ) ) ;
#48823=DIRECTION ( 'NONE',  ( 0.000000000000000000, 0.000000000000000000, 1.000000000000000000 ) ) ;
#48831=DIRECTION ( 'NONE',  ( -0.000000000000000000, -1.000000000000000000, -0.000000000000000000 ) ) ;
#48850=CARTESIAN_POINT ( 'NONE',  ( 33.00000000000000000, 500.0000000000002274, -15.00000000000000711 ) ) ;
#48857=CARTESIAN_POINT ( 'NONE',  ( 28.95612569419542126, 306.6521615867090418, -9.146490758560222645 ) ) ;
#48862=CARTESIAN_POINT ( 'NONE',  ( -35.69739812508499455, 430.4862580793411553, 4.964222856391316441 ) ) ;
#48871=CARTESIAN_POINT ( 'NONE',  ( 43.99367409911575777, 462.7719748078419002, 5.584664003622480166 ) ) ;
#48874=CARTESIAN_POINT ( 'NONE',  ( -22.55365577865696736, 305.4547471613416292, 9.067395197859438483 ) ) ;
#48897=CARTESIAN_POINT ( 'NONE',  ( 18.67440746815751851, 303.6203069488627193, -10.04920595787936755 ) ) ;
#48898=CARTESIAN_POINT ( 'NONE',  ( 30.35537264529554946, 338.7115663565144246, 18.05293407820170515 ) ) ;
#48904=AXIS2_PLACEMENT_3D ( 'NONE', #17284, #15139, #31878 ) ;
#48908=( BOUNDED_SURFACE ( )  B_SPLINE_SURFACE ( 3, 2, ( 
 ( #76599, #2709, #91221 ),
 ( #101425, #60455, #93330 ),
 ( #52321, #36199, #85234 ),
 ( #44249, #77141, #99263 ) ),
 .UNSPECIFIED., .F., .F., .F. ) 
 B_SPLINE_SURFACE_WITH_KNOTS ( ( 4, 4 ),
 ( 3, 3 ),
 ( 2.632442874794804766E-16, 0.0002132038012140852017 ),
 ( 0.000000000000000000, 1.000000000000000000 ),
 .UNSPECIFIED. ) 
 GEOMETRIC_REPRESENTATION_ITEM ( )  RATIONAL_B_SPLINE_SURFACE ( (
 ( 1.000000000000000000, 0.8360809698953636238, 1.000000000000000000),
 ( 1.000000000000000000, 0.8350457441348965171, 1.000000000000000000),
 ( 1.000000000000000000, 0.8339645259288112067, 1.000000000000000000),
 ( 1.000000000000000000, 0.8328393170034699144, 1.000000000000000000) ) ) 
 REPRESENTATION_ITEM ( '' )  SURFACE ( )  );
#48916=CARTESIAN_POINT ( 'NONE',  ( -39.61570363597765976, 464.1137630033862820, 18.30708429227111367 ) ) ;
#48923=CARTESIAN_POINT ( 'NONE',  ( 38.31672866701944002, 310.9721894403955389, 5.785870559332880525 ) ) ;
#48928=CARTESIAN_POINT ( 'NONE',  ( -40.71513924616806435, 459.9692486989940789, 1.994549889840158130 ) ) ;
#48937=CARTESIAN_POINT ( 'NONE',  ( -22.88986873834216595, 295.1619009228529649, 10.00292581962222549 ) ) ;
#48942=CARTESIAN_POINT ( 'NONE',  ( 1.175710136697877717, 302.5234377367743264, 9.930896799880603254 ) ) ;
#48944=B_SPLINE_CURVE_WITH_KNOTS ( 'NONE', 3,
 ( #59899, #92770, #10771, #43690, #95972, #45827, #70095, #86831 ),
 .UNSPECIFIED., .F., .F.,
 ( 4, 2, 2, 4 ),
 ( 5.204170427930421283E-18, 0.002631563437787210521, 0.003947345156680811228, 0.005263126875574411501 ),
 .UNSPECIFIED. ) ;
#48953=CARTESIAN_POINT ( 'NONE',  ( 34.53029562236230277, 437.2884171348799782, 5.234332900499188312 ) ) ;
#48962=CARTESIAN_POINT ( 'NONE',  ( -31.33350209457356428, 438.6527987165884497, 22.86578116056119825 ) ) ;
#48994=ORIENTED_EDGE ( 'NONE', *, *, #52769, .T. ) ;
#48997=CARTESIAN_POINT ( 'NONE',  ( 31.44885746337475751, 398.4224732248688383, 24.43061767113179883 ) ) ;
#49003=CARTESIAN_POINT ( 'NONE',  ( -42.36735105583831995, 487.4262793961416946, 8.281278960744069551 ) ) ;
#49021=CARTESIAN_POINT ( 'NONE',  ( -2.435618412542380096, 294.8338784867304412, -9.717600221842332076 ) ) ;
#49029=CARTESIAN_POINT ( 'NONE',  ( -9.565054828409994769, 294.6554042961246864, 1.895259989615173168 ) ) ;
#49033=CARTESIAN_POINT ( 'NONE',  ( 36.65209206386361274, 491.4469928998128694, 12.33162904370259128 ) ) ;
#49035=CARTESIAN_POINT ( 'NONE',  ( -32.03361802173512274, 464.8552804869456168, 13.91311180126945857 ) ) ;
#49044=ORIENTED_EDGE ( 'NONE', *, *, #74834, .T. ) ;
#49052=CARTESIAN_POINT ( 'NONE',  ( -29.51136820535556282, 310.7658785638236623, -8.630889702403234054 ) ) ;
#49058=ORIENTED_EDGE ( 'NONE', *, *, #99417, .F. ) ;
#49060=EDGE_CURVE ( 'NONE', #13955, #38472, #456, .T. ) ;
#49061=CARTESIAN_POINT ( 'NONE',  ( -24.94621240166074472, 303.9363870782586332, -9.765254933829170980 ) ) ;
#49066=CARTESIAN_POINT ( 'NONE',  ( 43.00000000000000000, 500.0000000000002274, 0.000000000000000000 ) ) ;
#49067=CARTESIAN_POINT ( 'NONE',  ( -33.16823963622213967, 390.8948510558434464, 25.58094942542993877 ) ) ;
#49073=CARTESIAN_POINT ( 'NONE',  ( 32.84237740334622657, 485.2251842821286800, 5.746442123025142124 ) ) ;
#49076=CARTESIAN_POINT ( 'NONE',  ( 30.00000000000000000, 489.2891479521253473, 5.498062499254755764 ) ) ;
#49077=CARTESIAN_POINT ( 'NONE',  ( -40.97825696304336418, 438.0977617246737168, 22.33876858701082213 ) ) ;
#49109=EDGE_CURVE ( 'NONE', #63343, #100372, #27488, .T. ) ;
#49115=CARTESIAN_POINT ( 'NONE',  ( 24.93816302196866275, 307.4233949143036284, 10.52291764336465008 ) ) ;
#49116=CARTESIAN_POINT ( 'NONE',  ( -32.14399312865362646, 464.7181097252859558, 11.03234060977934483 ) ) ;
#49118=CARTESIAN_POINT ( 'NONE',  ( 30.00000000001042721, 488.0736639502548542, 7.689181908884415328 ) ) ;
#49130=B_SPLINE_CURVE_WITH_KNOTS ( 'NONE', 3,
 ( #59021, #76780, #90854, #49846 ),
 .UNSPECIFIED., .F., .F.,
 ( 4, 4 ),
 ( 0.0009723127763595034020, 0.02104041089405187664 ),
 .UNSPECIFIED. ) ;
#49133=CARTESIAN_POINT ( 'NONE',  ( 30.00000000000000000, 461.8802764867031669, 14.89328939272360053 ) ) ;
#49135=CARTESIAN_POINT ( 'NONE',  ( -43.32251133971205093, 485.6545735287840557, 4.688172406475217713 ) ) ;
#49141=CARTESIAN_POINT ( 'NONE',  ( -43.32509445547438531, 484.2781405677309863, -0.02261530909676546380 ) ) ;
#49149=ORIENTED_EDGE ( 'NONE', *, *, #13613, .F. ) ;
#49159=CARTESIAN_POINT ( 'NONE',  ( 32.89862776688912049, 464.9311084009901833, 10.99515925127326810 ) ) ;
#49174=CARTESIAN_POINT ( 'NONE',  ( 25.93947128054312756, 296.0094280503604978, 10.18659011856751384 ) ) ;
#49183=CARTESIAN_POINT ( 'NONE',  ( -31.35596682365705945, 438.0939828603719093, 22.55458131664414267 ) ) ;
#49186=AXIS2_PLACEMENT_3D ( 'NONE', #91524, #58069, #82353 ) ;
#49195=CARTESIAN_POINT ( 'NONE',  ( 46.00000000000000000, 500.0000000000002274, 0.000000000000000000 ) ) ;
#49209=DIRECTION ( 'NONE',  ( -1.000000000000000000, 0.000000000000000000, 0.000000000000000000 ) ) ;
#49228=CARTESIAN_POINT ( 'NONE',  ( 35.58576704944795210, 439.9331698772741106, 24.32295159899808468 ) ) ;
#49233=CARTESIAN_POINT ( 'NONE',  ( -34.53191791165069446, 437.2926915873502480, 5.227229271294363322 ) ) ;
#49238=EDGE_CURVE ( 'NONE', #103023, #2439, #29397, .T. ) ;
#49239=ORIENTED_EDGE ( 'NONE', *, *, #105370, .F. ) ;
#49257=CARTESIAN_POINT ( 'NONE',  ( 29.49339759867818600, 311.0110510053014536, -7.568740214377905673 ) ) ;
#49269=CARTESIAN_POINT ( 'NONE',  ( -36.87655955837859523, 438.2068510013161813, 3.933030107424713595 ) ) ;
#49278=DIRECTION ( 'NONE',  ( 0.000000000000000000, -1.000000000000000000, -0.000000000000000000 ) ) ;
#49279=ORIENTED_EDGE ( 'NONE', *, *, #78838, .F. ) ;
#49282=DIRECTION ( 'NONE',  ( -1.000000000000000000, -0.000000000000000000, -0.000000000000000000 ) ) ;
#49305=ORIENTED_EDGE ( 'NONE', *, *, #95223, .T. ) ;
#49323=CARTESIAN_POINT ( 'NONE',  ( -40.74567133769577509, 318.5959897825344456, 3.761255434899160033 ) ) ;
#49347=SURFACE_SIDE_STYLE ('',( #65016 ) ) ;
#49349=CARTESIAN_POINT ( 'NONE',  ( -36.94051212422546371, 491.4300504572172485, 12.31983948577911647 ) ) ;
#49357=CARTESIAN_POINT ( 'NONE',  ( -18.41162169223098033, 304.6294254666754568, 9.889731659030220001 ) ) ;
#49359=ORIENTED_EDGE ( 'NONE', *, *, #26249, .F. ) ;
#49365=CARTESIAN_POINT ( 'NONE',  ( -38.92806086102961416, 485.1409375601101601, -4.243407870181493458 ) ) ;
#49377=CARTESIAN_POINT ( 'NONE',  ( 35.22245897681152371, 463.4774333389169101, 19.78759537333438345 ) ) ;
#49388=ADVANCED_FACE ( 'NONE', ( #18039 ), #101851, .F. ) ;
#49393=CARTESIAN_POINT ( 'NONE',  ( 26.74014876403748175, 304.8529031102725639, -9.560831669777455133 ) ) ;
#49399=CARTESIAN_POINT ( 'NONE',  ( -45.33180403702434091, 464.4945808635454227, 2.178908857919817699 ) ) ;
#49401=CARTESIAN_POINT ( 'NONE',  ( 30.00000000000000000, 450.0000000000002274, 18.20242257375371153 ) ) ;
#49407=CARTESIAN_POINT ( 'NONE',  ( -35.37498230280494482, 485.2520700389512740, -2.749549059026963338 ) ) ;
#49414=CARTESIAN_POINT ( 'NONE',  ( -22.33139259354657469, 304.3259814047488589, 10.03910396366137192 ) ) ;
#49419=CARTESIAN_POINT ( 'NONE',  ( 32.94539137534165718, 488.0149952105424518, 9.145905951749512042 ) ) ;
#49435=CARTESIAN_POINT ( 'NONE',  ( 31.03867016165222026, 468.3124986733989772, 18.90871194958903345 ) ) ;
#49445=CARTESIAN_POINT ( 'NONE',  ( 33.00000000000000000, 450.0000000000002274, -1.797577426246301568 ) ) ;
#49449=CARTESIAN_POINT ( 'NONE',  ( -21.29078873992701659, 304.0464254837385170, 9.978592173037190705 ) ) ;
#49452=VERTEX_POINT ( 'NONE', #83808 ) ;
#49453=ORIENTED_EDGE ( 'NONE', *, *, #61367, .F. ) ;
#49457=CARTESIAN_POINT ( 'NONE',  ( -31.39122502990187513, 374.8582828950688963, 22.89686894917594273 ) ) ;
#49467=CARTESIAN_POINT ( 'NONE',  ( 32.67437147574466394, 300.1844539814272821, 3.135089118897082638 ) ) ;
#49479=CARTESIAN_POINT ( 'NONE',  ( -24.18257333278238264, 295.4930867534158665, 10.07449787404065233 ) ) ;
#49493=CARTESIAN_POINT ( 'NONE',  ( 1.128077836147720614, 302.8478239976497548, 9.936168295454386623 ) ) ;
#49497=CARTESIAN_POINT ( 'NONE',  ( 41.46910480218704009, 484.7338956289814860, -3.418960549715446717 ) ) ;
#49512=DIRECTION ( 'NONE',  ( 0.6181567188933647650, -0.3028222199719650121, 0.7253833289911206794 ) ) ;
#49514=CARTESIAN_POINT ( 'NONE',  ( 33.75766768374546700, 485.0582975308568621, 1.699565690043864707 ) ) ;
#49519=CARTESIAN_POINT ( 'NONE',  ( 43.02661387979727436, 465.7449615347604208, 11.43319743843670544 ) ) ;
#49524=ORIENTED_EDGE ( 'NONE', *, *, #41679, .F. ) ;
#49533=CARTESIAN_POINT ( 'NONE',  ( -6.752503985042242363, 294.7360527384791453, -7.398079589859515970 ) ) ;
#49542=CARTESIAN_POINT ( 'NONE',  ( 29.85428238372634269, 328.3168341217437387, 14.69675115712503910 ) ) ;
#49543=( BOUNDED_SURFACE ( )  B_SPLINE_SURFACE ( 3, 2, ( 
 ( #85846, #18454, #91796 ),
 ( #43762, #44848, #84231 ),
 ( #11379, #28155, #43241 ),
 ( #20075, #100935, #2223 ) ),
 .UNSPECIFIED., .F., .F., .F. ) 
 B_SPLINE_SURFACE_WITH_KNOTS ( ( 4, 4 ),
 ( 3, 3 ),
 ( -2.775557561562891351E-17, 0.001861785345366372352 ),
 ( 0.000000000000000000, 1.000000000000000000 ),
 .UNSPECIFIED. ) 
 GEOMETRIC_REPRESENTATION_ITEM ( )  RATIONAL_B_SPLINE_SURFACE ( (
 ( 1.000000000000000000, 0.7560596356357111025, 1.000000000000000000),
 ( 1.000000000000000000, 0.7634190799318307796, 1.000000000000000000),
 ( 1.000000000000000000, 0.7696912645870118697, 1.000000000000000000),
 ( 1.000000000000000000, 0.7737149417968429699, 1.000000000000000000) ) ) 
 REPRESENTATION_ITEM ( '' )  SURFACE ( )  );
#49547=CARTESIAN_POINT ( 'NONE',  ( 30.00000000000000000, 450.0000000000002274, 25.20242257375371864 ) ) ;
#49565=DIRECTION ( 'NONE',  ( 0.000000000000000000, -0.9109553866901075603, 0.4125048890137871238 ) ) ;
#49576=CARTESIAN_POINT ( 'NONE',  ( 35.15824258293613980, 491.5080798214766560, 12.36499586377719062 ) ) ;
#49577=CARTESIAN_POINT ( 'NONE',  ( -34.86930528710281862, 472.8495416016138506, 16.94467871989038343 ) ) ;
#49579=ORIENTED_EDGE ( 'NONE', *, *, #14168, .F. ) ;
#49594=CARTESIAN_POINT ( 'NONE',  ( -33.82200258925038838, 329.9395885283731218, -2.846730487787179520 ) ) ;
#49602=EDGE_CURVE ( 'NONE', #89572, #13768, #80488, .T. ) ;
#49603=CARTESIAN_POINT ( 'NONE',  ( -25.97041880520462698, 295.9150275961153511, -1.771067803760172366 ) ) ;
#49607=CARTESIAN_POINT ( 'NONE',  ( -36.06936872001291761, 485.1953429453741364, -2.471779398547188311 ) ) ;
#49608=CARTESIAN_POINT ( 'NONE',  ( -40.35637509736679363, 344.7269692263602110, 21.61016027867152900 ) ) ;
#49610=CARTESIAN_POINT ( 'NONE',  ( -37.88504238421052861, 463.4171042825119002, 19.90923349044181379 ) ) ;
#49618=CARTESIAN_POINT ( 'NONE',  ( 43.47770857297100378, 484.8227827122626081, 4.253339224814538078 ) ) ;
#49629=MECHANICAL_DESIGN_GEOMETRIC_PRESENTATION_REPRESENTATION('',(#85862),#80658);
#49630=AXIS2_PLACEMENT_3D ( 'NONE', #36990, #35395, #94127 ) ;
#49635=ADVANCED_FACE ( 'NONE', ( #22305 ), #46547, .T. ) ;
#49637=CARTESIAN_POINT ( 'NONE',  ( 22.86660670453057165, 295.1252011229040590, -1.941278114811820110 ) ) ;
#49643=CARTESIAN_POINT ( 'NONE',  ( -38.54489124932221955, 464.3862832426350451, 18.94817373525692261 ) ) ;
#49647=ORIENTED_EDGE ( 'NONE', *, *, #82026, .F. ) ;
#49659=CARTESIAN_POINT ( 'NONE',  ( 35.74363442581862671, 380.1068966271811860, 4.951945592532029927 ) ) ;
#49661=FACE_OUTER_BOUND ( 'NONE', #59464, .T. ) ;
#49665=ORIENTED_EDGE ( 'NONE', *, *, #40254, .F. ) ;
#49687=ORIENTED_EDGE ( 'NONE', *, *, #56945, .T. ) ;
#49695=CARTESIAN_POINT ( 'NONE',  ( 36.67849848893011000, 463.9785128198733446, 19.62079535019029564 ) ) ;
#49702=CARTESIAN_POINT ( 'NONE',  ( 44.22093662635627709, 464.1457359768089077, 8.759819298992027825 ) ) ;
#49715=FACE_OUTER_BOUND ( 'NONE', #61863, .T. ) ;
#49719=CARTESIAN_POINT ( 'NONE',  ( 39.84233570596349949, 333.3323931548420660, 19.23895789620553032 ) ) ;
#49726=CARTESIAN_POINT ( 'NONE',  ( -31.44899729243502051, 391.8699891364225891, 24.19055939260229238 ) ) ;
#49731=CARTESIAN_POINT ( 'NONE',  ( -34.78087296571919751, 461.0374007115530617, 3.662433066614679156 ) ) ;
#49732=ORIENTED_EDGE ( 'NONE', *, *, #85097, .F. ) ;
#49738=CARTESIAN_POINT ( 'NONE',  ( 32.13416664219985108, 374.4073344487368331, 24.05703695877565096 ) ) ;
#49759=CARTESIAN_POINT ( 'NONE',  ( -33.97359119245066239, 434.1099241184709285, 11.80501937577158778 ) ) ;
#49760=ORIENTED_EDGE ( 'NONE', *, *, #14359, .T. ) ;
#49768=EDGE_CURVE ( 'NONE', #89019, #78525, #105744, .T. ) ;
#49771=CARTESIAN_POINT ( 'NONE',  ( -38.42841492633962730, 491.4186471570457115, 12.30549038569188269 ) ) ;
#49774=CARTESIAN_POINT ( 'NONE',  ( 39.46660235664349159, 438.4151231452425463, 22.74768781139262330 ) ) ;
#49777=CARTESIAN_POINT ( 'NONE',  ( -36.16847030042355016, 438.2414514106959018, 3.889105687734305317 ) ) ;
#49779=ADVANCED_FACE ( 'NONE', ( #92303 ), #49543, .F. ) ;
#49780=DIRECTION ( 'NONE',  ( -0.6175266994149452016, -0.6213472858387197872, -0.4822741190345386508 ) ) ;
#49781=VERTEX_POINT ( 'NONE', #19542 ) ;
#49783=CARTESIAN_POINT ( 'NONE',  ( -43.03357534758841041, 463.2291678140047679, 4.675918524149428990 ) ) ;
#49786=CARTESIAN_POINT ( 'NONE',  ( 37.13212445136079509, 463.5388707510517747, 19.67708231430621879 ) ) ;
#49797=CARTESIAN_POINT ( 'NONE',  ( 28.20173342337447409, 307.2982505937521864, -9.226824045861857115 ) ) ;
#49812=CARTESIAN_POINT ( 'NONE',  ( -36.74148664940361186, 437.9559008978175143, 4.252305828303462043 ) ) ;
#49837=CARTESIAN_POINT ( 'NONE',  ( 20.21880305278369150, 304.8280059657581660, -9.005058168222337400 ) ) ;
#49845=CARTESIAN_POINT ( 'NONE',  ( -16.26028350797723832, 302.5670365178829684, -10.06049214740963293 ) ) ;
#49846=CARTESIAN_POINT ( 'NONE',  ( -33.74271564777242816, 484.1802673187708592, 2.058285076122308155 ) ) ;
#49848=CARTESIAN_POINT ( 'NONE',  ( -35.51382444471699529, 463.4141161792284720, 19.91564417027156253 ) ) ;
#49853=CARTESIAN_POINT ( 'NONE',  ( 30.00000000000000355, 461.9652624853973748, 12.11314247086045803 ) ) ;
#49860=VERTEX_POINT ( 'NONE', #85289 ) ;
#49866=CARTESIAN_POINT ( 'NONE',  ( -42.43985862560405309, 333.9176701535965890, 7.447030561597399512 ) ) ;
#49885=ADVANCED_FACE ( 'NONE', ( #14034 ), #6086, .F. ) ;
#49887=CARTESIAN_POINT ( 'NONE',  ( -37.50843646915485152, 482.0142436422872834, 15.15300368821568000 ) ) ;
#49889=CARTESIAN_POINT ( 'NONE',  ( -37.38602481899999219, 490.8442832704672014, 12.40593855172241611 ) ) ;
#49893=CARTESIAN_POINT ( 'NONE',  ( 33.21459943997680853, 487.8270262909274493, 10.08789160141814278 ) ) ;
#49896=CARTESIAN_POINT ( 'NONE',  ( -16.96954359408614366, 304.5683848806726814, 9.876757081930351845 ) ) ;
#49916=AXIS2_PLACEMENT_3D ( 'NONE', #1363, #93061, #67725 ) ;
#49919=ORIENTED_EDGE ( 'NONE', *, *, #29410, .F. ) ;
#49933=CARTESIAN_POINT ( 'NONE',  ( 35.18962234169666203, 301.6382339994959239, -8.468528340524796860 ) ) ;
#49944=CARTESIAN_POINT ( 'NONE',  ( 43.58191376438443143, 439.3922052527890401, 13.97025970319826982 ) ) ;
#49947=EDGE_CURVE ( 'NONE', #39480, #56970, #70989, .T. ) ;
#49948=CARTESIAN_POINT ( 'NONE',  ( -23.65461719027016230, 304.8910927077299107, 10.16394219231294294 ) ) ;
#49950=CARTESIAN_POINT ( 'NONE',  ( 34.40251038080555190, 484.1263118519839850, 0.1376245346420501836 ) ) ;
#49952=CARTESIAN_POINT ( 'NONE',  ( 32.62376965138175677, 486.1221409277114276, 7.511474791660580408 ) ) ;
#49958=CARTESIAN_POINT ( 'NONE',  ( 46.00000000000000000, 438.3644743593593489, 10.24495404210296989 ) ) ;
#49973=CARTESIAN_POINT ( 'NONE',  ( 16.94034599462699830, 304.5648770741773887, -9.060986067200369476 ) ) ;
#49974=CARTESIAN_POINT ( 'NONE',  ( -32.13503062639005492, 486.0946171966414795, 5.282847667695663496 ) ) ;
#49985=DIRECTION ( 'NONE',  ( 1.000000000000000000, -0.000000000000000000, -0.000000000000000000 ) ) ;
#49994=CARTESIAN_POINT ( 'NONE',  ( -42.09158233638503788, 465.7816406625424861, 14.79318349169994562 ) ) ;
#49996=CARTESIAN_POINT ( 'NONE',  ( -31.44885420705449164, 398.4269215821768171, 24.43068901296845752 ) ) ;
#50005=CARTESIAN_POINT ( 'NONE',  ( 33.84761347220318584, 488.7471039746334895, 11.01988148152525504 ) ) ;
#50006=CARTESIAN_POINT ( 'NONE',  ( 35.50538377702518744, 304.0193673134525056, 4.053817158089760397 ) ) ;
#50009=CARTESIAN_POINT ( 'NONE',  ( -40.76154164607882535, 460.9888869747143758, 2.282783108351643886 ) ) ;
#50010=CARTESIAN_POINT ( 'NONE',  ( 42.59003199992548616, 362.8236097783378682, 16.78898391992328243 ) ) ;
#50015=CARTESIAN_POINT ( 'NONE',  ( -21.31378532129378556, 303.0151486721171636, 9.972274757840462911 ) ) ;
#50021=AXIS2_PLACEMENT_3D ( 'NONE', #30125, #77059, #3175 ) ;
#50028=FACE_OUTER_BOUND ( 'NONE', #23315, .T. ) ;
#50037=DIRECTION ( 'NONE',  ( 0.000000000000000000, -0.9887960631535436251, 0.1492727218618769280 ) ) ;
#50040=CARTESIAN_POINT ( 'NONE',  ( -32.02495471002953309, 438.9490378437291156, 23.64594461092559996 ) ) ;
#50044=CARTESIAN_POINT ( 'NONE',  ( 33.74271564777237842, 484.1802673187710297, 2.058285076122392532 ) ) ;
#50053=CARTESIAN_POINT ( 'NONE',  ( 37.50059943756144776, 490.7879993827856993, 12.38039871356534505 ) ) ;
#50061=CARTESIAN_POINT ( 'NONE',  ( 38.17475322892877898, 491.0341113493716421, 12.03733759146246740 ) ) ;
#50066=DIRECTION ( 'NONE',  ( -1.000000000000000000, -0.000000000000000000, -0.000000000000000000 ) ) ;
#50069=CARTESIAN_POINT ( 'NONE',  ( 4.404194502973587610, 294.7962568506322327, -8.995744148930016948 ) ) ;
#50076=CARTESIAN_POINT ( 'NONE',  ( 31.16745676550236510, 425.0786795845950792, 24.76594861758827193 ) ) ;
#50080=CARTESIAN_POINT ( 'NONE',  ( -42.08762648273147988, 487.0030674539048618, 9.106351919857871735 ) ) ;
#50081=CARTESIAN_POINT ( 'NONE',  ( -32.42646496125482969, 485.5066083816486753, 3.829258843079225816 ) ) ;
#50098=CARTESIAN_POINT ( 'NONE',  ( -4.055648887808908754, 294.8040761930253666, -9.158006418688662720 ) ) ;
#50108=CARTESIAN_POINT ( 'NONE',  ( 36.28158941437224883, 490.9587137816808422, 12.45622313965986905 ) ) ;
#50109=CARTESIAN_POINT ( 'NONE',  ( -32.02016918911336774, 464.7988659274551537, 11.81876822792606774 ) ) ;
#50116=CARTESIAN_POINT ( 'NONE',  ( -33.33990657616918440, 464.2315420232590100, 17.97851960990337972 ) ) ;
#50119=ORIENTED_EDGE ( 'NONE', *, *, #29783, .F. ) ;
#50127=CARTESIAN_POINT ( 'NONE',  ( -31.78833566326770566, 317.3161387333121297, -5.990659203738045058 ) ) ;
#50134=CARTESIAN_POINT ( 'NONE',  ( -22.25540596620007605, 295.0193264978564684, -1.964391734705814629 ) ) ;
#50139=CARTESIAN_POINT ( 'NONE',  ( -37.21896735870636519, 485.5897823164965530, -4.183926505970648080 ) ) ;
#50140=CARTESIAN_POINT ( 'NONE',  ( -42.74137506439731737, 379.1533860022373119, 18.72083839136980643 ) ) ;
#50153=CARTESIAN_POINT ( 'NONE',  ( 43.94956565205495735, 434.7294131184629009, 8.824837262785111491 ) ) ;
#50155=VERTEX_POINT ( 'NONE', #10597 ) ;
#50181=CIRCLE ( 'NONE', #13986, 2.999999999999988010 ) ;
#50194=CARTESIAN_POINT ( 'NONE',  ( -44.03570364123616798, 435.3116947630537084, 15.43179346459665524 ) ) ;
#50196=CARTESIAN_POINT ( 'NONE',  ( -34.10808184343350291, 434.1697022380918156, 11.22013956023728909 ) ) ;
#50212=CARTESIAN_POINT ( 'NONE',  ( 43.03357534759661718, 463.2291678140137492, 4.675918524166122303 ) ) ;
#50214=CARTESIAN_POINT ( 'NONE',  ( 43.66729043033832625, 435.6676719292337907, 17.39374879622096159 ) ) ;
#50227=DIRECTION ( 'NONE',  ( 0.9915366780650388678, -0.1269898409407509698, -0.02699252395738872823 ) ) ;
#50228=CARTESIAN_POINT ( 'NONE',  ( 37.31633518135760141, 464.0415485246131198, 19.53686901080153149 ) ) ;
#50238=CARTESIAN_POINT ( 'NONE',  ( 32.87816783969756784, 464.9425048721737994, 11.07737551929927022 ) ) ;
#50249=CARTESIAN_POINT ( 'NONE',  ( 43.37695759419762709, 434.6160983767974813, 10.05510951421143595 ) ) ;
#50257=CARTESIAN_POINT ( 'NONE',  ( -43.34642793437723185, 464.8022470470604048, 10.25621957592192857 ) ) ;
#50260=CARTESIAN_POINT ( 'NONE',  ( -29.78543059554420225, 327.5436091316801139, 14.51305068536635012 ) ) ;
#50271=CARTESIAN_POINT ( 'NONE',  ( 20.56658349655994300, 303.9107536853347824, 9.949562365852784751 ) ) ;
#50287=CARTESIAN_POINT ( 'NONE',  ( -30.15464468665757991, 316.8850315688116552, 13.37365732414975206 ) ) ;
#50291=CIRCLE ( 'NONE', #19333, 10.00000000000000533 ) ;
#50298=CARTESIAN_POINT ( 'NONE',  ( -41.74100955526786549, 489.2843990805219505, 10.50852780968136813 ) ) ;
#50301=ORIENTED_EDGE ( 'NONE', *, *, #13090, .T. ) ;
#50303=CARTESIAN_POINT ( 'NONE',  ( -33.11890921805862575, 438.9412750689605787, 23.90522689637586140 ) ) ;
#50307=ORIENTED_EDGE ( 'NONE', *, *, #47517, .T. ) ;
#50319=CARTESIAN_POINT ( 'NONE',  ( -35.96492786661492858, 302.4488314805894902, -8.278427239160079054 ) ) ;
#50322=CARTESIAN_POINT ( 'NONE',  ( 24.06928029728074492, 304.6542708667294619, -9.827242677062491438 ) ) ;
#50330=CARTESIAN_POINT ( 'NONE',  ( 21.88049162136248071, 294.9920307902382319, 9.966805799653187137 ) ) ;
#50340=ORIENTED_EDGE ( 'NONE', *, *, #32601, .T. ) ;
#50348=CARTESIAN_POINT ( 'NONE',  ( 44.12472801210888917, 485.7238370326480208, 3.975897585123575606 ) ) ;
#50360=CARTESIAN_POINT ( 'NONE',  ( 35.48551685587499804, 424.7621062603631685, 6.304300610002332661 ) ) ;
#50361=VERTEX_POINT ( 'NONE', #38625 ) ;
#50364=EDGE_CURVE ( 'NONE', #69148, #27394, #23445, .T. ) ;
#50365=ORIENTED_EDGE ( 'NONE', *, *, #51014, .F. ) ;
#50367=CARTESIAN_POINT ( 'NONE',  ( 43.67170302692484540, 434.9885551707870945, 18.57290719901132547 ) ) ;
#50369=CARTESIAN_POINT ( 'NONE',  ( -15.65658065573060931, 294.5586797367948861, -2.062307047882345312 ) ) ;
#50371=CARTESIAN_POINT ( 'NONE',  ( -37.40828998626499668, 463.5731143434641695, 19.60478905907894287 ) ) ;
#50374=CARTESIAN_POINT ( 'NONE',  ( 32.89862776688910628, 464.9311084009901833, 10.99515925127345461 ) ) ;
#50375=CARTESIAN_POINT ( 'NONE',  ( 0.000000000000000000, 300.0000000000000000, 9.936999415352289589 ) ) ;
#50388=CARTESIAN_POINT ( 'NONE',  ( -40.84209758864429318, 312.5378719886987255, -5.789410655104530790 ) ) ;
#50389=CARTESIAN_POINT ( 'NONE',  ( -16.94581198861071769, 304.5649023924335097, -10.06098255995172508 ) ) ;
#50438=CARTESIAN_POINT ( 'NONE',  ( -31.71529466845016998, 439.7354232657903594, 23.74396842416312836 ) ) ;
#50447=CARTESIAN_POINT ( 'NONE',  ( -37.51894975547678968, 308.4495690710303961, 5.152636288847776136 ) ) ;
#50455=CARTESIAN_POINT ( 'NONE',  ( 34.83065384313196944, 301.2489324959578880, -8.560106014107077499 ) ) ;
#50462=ORIENTED_EDGE ( 'NONE', *, *, #69210, .T. ) ;
#50466=LINE ( 'NONE', #59655, #75116 ) ;
#50470=CARTESIAN_POINT ( 'NONE',  ( -20.08590916391416314, 304.8421219133190903, 8.934941684170844667 ) ) ;
#50488=ORIENTED_EDGE ( 'NONE', *, *, #4535, .F. ) ;
#50491=CARTESIAN_POINT ( 'NONE',  ( 39.84233570596349949, 333.3323931548420660, 19.23895789620553032 ) ) ;
#50501=UNCERTAINTY_MEASURE_WITH_UNIT (LENGTH_MEASURE( 1.000000000000000082E-05 ), #65367, 'distance_accuracy_value', 'NONE');
#50511=CARTESIAN_POINT ( 'NONE',  ( -31.99602169361977388, 464.8336097802194331, 12.51960734453166957 ) ) ;
#50515=CARTESIAN_POINT ( 'NONE',  ( -31.13164573599167184, 436.9142555170884066, 23.68610392534201736 ) ) ;
#50520=CARTESIAN_POINT ( 'NONE',  ( 33.21583695390473423, 487.8294359878499336, 10.09122741357699304 ) ) ;
#50521=CARTESIAN_POINT ( 'NONE',  ( 27.27586408842989130, 307.4943522527414075, 11.01523124013777100 ) ) ;
#50533=CARTESIAN_POINT ( 'NONE',  ( -24.05303310288100604, 295.4586947108799109, 10.06705650746367375 ) ) ;
#50536=CARTESIAN_POINT ( 'NONE',  ( 33.84761347220244687, 488.7471039746337738, 11.01988148152553748 ) ) ;
#50538=CARTESIAN_POINT ( 'NONE',  ( 1.917245519677769350, 301.4538546725594870, 9.817117674984364939 ) ) ;
#50558=DIRECTION ( 'NONE',  ( 0.9230641662213218135, 0.000000000000000000, 0.3846459996388055247 ) ) ;
#50562=ORIENTED_EDGE ( 'NONE', *, *, #87114, .T. ) ;
#50568=CARTESIAN_POINT ( 'NONE',  ( -43.00000000000000000, 500.0000000000002274, 0.000000000000000000 ) ) ;
#50587=CARTESIAN_POINT ( 'NONE',  ( 31.36030843854360128, 339.5225620909950521, 18.44549848323119434 ) ) ;
#50600=CARTESIAN_POINT ( 'NONE',  ( -31.19652432992544888, 378.3327707670021027, 24.28948218791313707 ) ) ;
#50604=DIRECTION ( 'NONE',  ( 0.000000000000000000, 0.000000000000000000, -1.000000000000000000 ) ) ;
#50607=CARTESIAN_POINT ( 'NONE',  ( -8.849035312365487016, 302.6218124189194896, -10.03679229143247476 ) ) ;
#50610=CARTESIAN_POINT ( 'NONE',  ( 44.14911905790283697, 464.3766534542007207, 9.623404994951284763 ) ) ;
#50614=CARTESIAN_POINT ( 'NONE',  ( -16.93833563167039458, 302.5835715773326910, 9.880235389495441112 ) ) ;
#50617=B_SPLINE_SURFACE_WITH_KNOTS ( 'NONE', 1, 3, ( 
 ( #41236, #42294, #66045, #98922, #737, #25081, #90861, #33701 ),
 ( #99459, #34246, #58496, #1280, #88481, #19672, #6474, #46938 ) ),
 .UNSPECIFIED., .F., .F., .F.,
 ( 2, 2 ),
 ( 4, 2, 2, 4 ),
 ( 0.000000000000000000, 1.000000000000000000 ),
 ( 0.000000000000000000, 0.04450745600790868145, 0.06676118401186306728, 0.08901491201581737678 ),
 .UNSPECIFIED. ) ;
#50635=CARTESIAN_POINT ( 'NONE',  ( -21.67644693109840048, 305.0488537841421248, -8.958167403557810715 ) ) ;
#50638=CARTESIAN_POINT ( 'NONE',  ( -44.19123973042153608, 435.3640897803193184, 10.85603094147129788 ) ) ;
#50645=CARTESIAN_POINT ( 'NONE',  ( -35.33914081917379946, 485.2455454566305093, -2.714404708513355580 ) ) ;
#50646=CARTESIAN_POINT ( 'NONE',  ( -33.15386418467154073, 409.3216133033088227, 25.87705685211801310 ) ) ;
#50656=CARTESIAN_POINT ( 'NONE',  ( -42.10086803841213765, 435.6552064019005570, 19.95582312411059789 ) ) ;
#50657=EDGE_LOOP ( 'NONE', ( #43506, #56733, #87360, #87814 ) ) ;
#50658=CARTESIAN_POINT ( 'NONE',  ( -21.04247164025376193, 37.86482112153537116, -10.52123582012687564 ) ) ;
#50660=EDGE_CURVE ( 'NONE', #8292, #32226, #47850, .T. ) ;
#50676=CARTESIAN_POINT ( 'NONE',  ( 45.29905483860081716, 480.9466865490944656, -2.171671249451534003 ) ) ;
#50684=CARTESIAN_POINT ( 'NONE',  ( -38.06522774901652184, 464.2393341908695561, 19.21804507436417353 ) ) ;
#50693=EDGE_CURVE ( 'NONE', #3187, #66199, #32989, .T. ) ;
#50703=CARTESIAN_POINT ( 'NONE',  ( 31.19792890532719198, 414.2215770364159084, 25.44228638033458623 ) ) ;
#50705=CARTESIAN_POINT ( 'NONE',  ( 40.87544524660111733, 460.0150911311816344, 2.035358705196582463 ) ) ;
#50713=EDGE_LOOP ( 'NONE', ( #101531, #81544, #22298, #59834 ) ) ;
#50716=ORIENTED_EDGE ( 'NONE', *, *, #31519, .T. ) ;
#50717=EDGE_CURVE ( 'NONE', #91205, #81976, #103740, .T. ) ;
#50730=CARTESIAN_POINT ( 'NONE',  ( -0.3760805828550403684, 300.0000000000000000, 9.936999415321508877 ) ) ;
#50740=CARTESIAN_POINT ( 'NONE',  ( -45.99999999999998579, 488.0052860040137830, 1.469193544622068526 ) ) ;
#50749=CARTESIAN_POINT ( 'NONE',  ( 23.96375140441108442, 306.3052962357393199, 10.25885168886986243 ) ) ;
#50758=ORIENTED_EDGE ( 'NONE', *, *, #80243, .T. ) ;
#50759=CARTESIAN_POINT ( 'NONE',  ( 43.77364510076557735, 434.9303853138975455, 13.50475697610904824 ) ) ;
#50769=CARTESIAN_POINT ( 'NONE',  ( -23.52494306516553380, 305.9412313528462164, 9.175829795430782809 ) ) ;
#50773=CARTESIAN_POINT ( 'NONE',  ( -34.76127857255404052, 469.3282716276013389, 1.881874431123442548 ) ) ;
#50781=CARTESIAN_POINT ( 'NONE',  ( 42.19180677453719142, 462.2931784592651070, 3.389262873192026682 ) ) ;
#50782=CARTESIAN_POINT ( 'NONE',  ( 20.20152979676450400, 303.8530952710909787, 9.937276093638269359 ) ) ;
#50789=AXIS2_PLACEMENT_3D ( 'NONE', #19790, #11632, #85555 ) ;
#50804=CARTESIAN_POINT ( 'NONE',  ( 30.00000000000000355, 488.6481008951276408, 3.890293910849272230 ) ) ;
#50806=( BOUNDED_SURFACE ( )  B_SPLINE_SURFACE ( 3, 2, ( 
 ( #79295, #86882, #45876 ),
 ( #97068, #63668, #80342 ),
 ( #103058, #70685, #71718 ),
 ( #94979, #38854, #103576 ) ),
 .UNSPECIFIED., .F., .F., .F. ) 
 B_SPLINE_SURFACE_WITH_KNOTS ( ( 4, 4 ),
 ( 3, 3 ),
 ( -4.770489558936219510E-18, 0.0008582108274411621215 ),
 ( 0.000000000000000000, 1.000000000000000000 ),
 .UNSPECIFIED. ) 
 GEOMETRIC_REPRESENTATION_ITEM ( )  RATIONAL_B_SPLINE_SURFACE ( (
 ( 1.000000000000000000, 0.7409272757993125014, 1.000000000000000000),
 ( 1.000000000000000000, 0.7386644886093398643, 1.000000000000000000),
 ( 1.000000000000000000, 0.7359402037277221753, 1.000000000000000000),
 ( 1.000000000000000000, 0.7328671738315111206, 1.000000000000000000) ) ) 
 REPRESENTATION_ITEM ( '' )  SURFACE ( )  );
#50807=CARTESIAN_POINT ( 'NONE',  ( -28.58275984112454537, 310.5877163737961837, 11.78456586285337870 ) ) ;
#50816=CARTESIAN_POINT ( 'NONE',  ( -30.00000000000000000, 500.0000000000002274, 5.000000000000001776 ) ) ;
#50827=CARTESIAN_POINT ( 'NONE',  ( -29.99999999998877698, 464.1630077738784621, 12.90488033688509795 ) ) ;
#50832=CARTESIAN_POINT ( 'NONE',  ( 31.53900113926844639, 437.3650476817602453, 21.86274588273925090 ) ) ;
#50843=ORIENTED_EDGE ( 'NONE', *, *, #63845, .T. ) ;
#50845=EDGE_LOOP ( 'NONE', ( #7825, #34251, #29127, #62386 ) ) ;
#50854=CARTESIAN_POINT ( 'NONE',  ( 21.19348424345033521, 294.8901562694577478, 1.945151701991103321 ) ) ;
#50859=CARTESIAN_POINT ( 'NONE',  ( -35.32911723019367400, 437.0667969981783472, 5.602639083905333273 ) ) ;
#50867=CIRCLE ( 'NONE', #69836, 12.00000000000001066 ) ;
#50877=CARTESIAN_POINT ( 'NONE',  ( 30.43016653122454329, 310.3809086888959996, -8.487237336552468037 ) ) ;
#50886=EDGE_LOOP ( 'NONE', ( #8407, #90888, #94426, #74270 ) ) ;
#50897=CARTESIAN_POINT ( 'NONE',  ( -43.65008909229012346, 485.2536725492916503, 3.136905111446141259 ) ) ;
#50899=CARTESIAN_POINT ( 'NONE',  ( 32.72541600403675233, 465.0324911293816967, 11.87889517178029841 ) ) ;
#50900=CARTESIAN_POINT ( 'NONE',  ( -37.88504238421005965, 463.4171042825123550, 19.90923349044087942 ) ) ;
#50904=CARTESIAN_POINT ( 'NONE',  ( 29.99999999999957723, 464.1603955069842300, 12.55952670045058284 ) ) ;
#50905=CARTESIAN_POINT ( 'NONE',  ( 39.83572194810514588, 489.3931820501625793, 11.44122026685077564 ) ) ;
#50917=CARTESIAN_POINT ( 'NONE',  ( -40.60927779514467773, 317.8171704805693025, 3.565600996951467927 ) ) ;
#50925=CARTESIAN_POINT ( 'NONE',  ( 37.88504238421471371, 463.4171042825133213, 19.90923349043903556 ) ) ;
#50929=CIRCLE ( 'NONE', #23407, 12.00000000000001066 ) ;
#50942=AXIS2_PLACEMENT_3D ( 'NONE', #98277, #7134, #13628 ) ;
#50957=ORIENTED_EDGE ( 'NONE', *, *, #58917, .F. ) ;
#50966=CARTESIAN_POINT ( 'NONE',  ( -39.19378338566357911, 489.8656698032278882, 11.78649807965604346 ) ) ;
#50969=PRESENTATION_STYLE_ASSIGNMENT (( #4039 ) ) ;
#50976=CARTESIAN_POINT ( 'NONE',  ( -37.50105686171508523, 463.9558322285216150, 19.48687368954042398 ) ) ;
#50977=CARTESIAN_POINT ( 'NONE',  ( -33.94524946120131403, 301.6549615082749369, 3.482976818372956362 ) ) ;
#50985=CARTESIAN_POINT ( 'NONE',  ( 24.80105969489321893, 306.0237540681346218, -9.745911707962003234 ) ) ;
#50986=CARTESIAN_POINT ( 'NONE',  ( -32.93513049338658760, 465.6726574193328361, 10.66039033145138326 ) ) ;
#50987=DIRECTION ( 'NONE',  ( 0.000000000000000000, 0.9180702648391416698, -0.3964176948853171401 ) ) ;
#50991=CARTESIAN_POINT ( 'NONE',  ( 32.78741055188847042, 485.3331003366707819, 5.977022408747033388 ) ) ;
#50995=CARTESIAN_POINT ( 'NONE',  ( 37.68709909070376796, 382.9750476856748378, 5.555079075619126172 ) ) ;
#51004=CARTESIAN_POINT ( 'NONE',  ( 32.62920465536820558, 486.5749440413383127, 6.880070463956039717 ) ) ;
#51014=EDGE_CURVE ( 'NONE', #27128, #87652, #83757, .T. ) ;
#51017=DIRECTION ( 'NONE',  ( 0.000000000000000000, 0.3241911592375312789, 0.9459915920726916783 ) ) ;
#51023=VERTEX_POINT ( 'NONE', #92321 ) ;
#51025=SURFACE_STYLE_USAGE ( .BOTH. , #91514 ) ;
#51027=CARTESIAN_POINT ( 'NONE',  ( 23.96375140441108442, 306.3052962357393199, 10.25885168886986243 ) ) ;
#51029=CARTESIAN_POINT ( 'NONE',  ( -33.22299792462370505, 463.2507813292579044, 6.141559824023456571 ) ) ;
#51036=CARTESIAN_POINT ( 'NONE',  ( -41.50820411079202188, 461.5963371455320612, 2.703439750996428081 ) ) ;
#51039=CARTESIAN_POINT ( 'NONE',  ( -27.25085409960445659, 309.8132056794035520, 11.34972795043210247 ) ) ;
#51046=CARTESIAN_POINT ( 'NONE',  ( -31.27232363897158152, 363.0966317728114063, 21.44374338523576640 ) ) ;
#51054=CARTESIAN_POINT ( 'NONE',  ( 25.39130259153011693, 304.9315442971644643, 10.40036917033271635 ) ) ;
#51090=EDGE_CURVE ( 'NONE', #5652, #74471, #70930, .T. ) ;
#51114=CARTESIAN_POINT ( 'NONE',  ( -35.68341320044621057, 437.0253618188252744, 4.635368180647969183 ) ) ;
#51117=CARTESIAN_POINT ( 'NONE',  ( -43.75401118688380819, 486.3173572309548263, 5.908089951475163915 ) ) ;
#51119=( LENGTH_UNIT ( ) NAMED_UNIT ( * ) SI_UNIT ( .MILLI., .METRE. ) );
#51122=CARTESIAN_POINT ( 'NONE',  ( 9.659821686343899927, 294.6522965669146856, -2.601680433888549970 ) ) ;
#51130=CARTESIAN_POINT ( 'NONE',  ( 32.19453407377343979, 398.3930569349155917, 25.63217955030058803 ) ) ;
#51132=CARTESIAN_POINT ( 'NONE',  ( -39.08699041849552458, 460.7998460666116216, 2.161775044689049796 ) ) ;
#51136=CARTESIAN_POINT ( 'NONE',  ( -32.62730128615267944, 485.2399689022751659, 2.794144060392764750 ) ) ;
#51137=CARTESIAN_POINT ( 'NONE',  ( -32.70807617001331380, 465.7746982375695666, 13.85399747859611885 ) ) ;
#51140=CARTESIAN_POINT ( 'NONE',  ( -24.93816302196866275, 307.4233949143036284, 10.52291764336465008 ) ) ;
#51144=CARTESIAN_POINT ( 'NONE',  ( -44.12590681760964628, 464.4133046726178691, 9.755964702276591183 ) ) ;
#51148=CARTESIAN_POINT ( 'NONE',  ( 35.51071014494291234, 436.6042799465416238, 4.950281864158008638 ) ) ;
#51150=CARTESIAN_POINT ( 'NONE',  ( -9.675290556387215801, 294.8809879903923843, -10.04271151416090291 ) ) ;
#51159=CARTESIAN_POINT ( 'NONE',  ( 43.77569424703103351, 434.3726356145342606, 11.96512969950840244 ) ) ;
#51176=CARTESIAN_POINT ( 'NONE',  ( 32.81882165182034328, 465.7334778289837800, 14.51165368401601441 ) ) ;
#51182=CARTESIAN_POINT ( 'NONE',  ( -43.78405977007513883, 434.9821340022087384, 12.01170688374028828 ) ) ;
#51191=CARTESIAN_POINT ( 'NONE',  ( -42.77250796224285523, 406.2445966473596854, 19.93629092197699748 ) ) ;
#51205=CARTESIAN_POINT ( 'NONE',  ( 34.12349128637390550, 490.8027302422246407, 11.84948222508928062 ) ) ;
#51217=B_SPLINE_CURVE_WITH_KNOTS ( 'NONE', 3,
 ( #90577, #50109, #16147, #49035, #81932, #8050 ),
 .UNSPECIFIED., .F., .F.,
 ( 4, 2, 4 ),
 ( 0.000000000000000000, 0.002094584110640377531, 0.004189168221280755063 ),
 .UNSPECIFIED. ) ;
#51235=DIRECTION ( 'NONE',  ( -0.000000000000000000, -1.000000000000000000, -0.000000000000000000 ) ) ;
#51242=CARTESIAN_POINT ( 'NONE',  ( 30.95643954367146833, 313.8918926584737505, -7.857037206977866006 ) ) ;
#51243=CARTESIAN_POINT ( 'NONE',  ( 41.54789589621260859, 460.8787123354391611, 2.862784844377739724 ) ) ;
#51257=CIRCLE ( 'NONE', #30685, 12.00000000000000711 ) ;
#51266=EDGE_CURVE ( 'NONE', #13401, #105963, #69176, .T. ) ;
#51277=CARTESIAN_POINT ( 'NONE',  ( -43.58492305596168137, 465.9553058690736407, 13.43507729846633758 ) ) ;
#51295=B_SPLINE_CURVE_WITH_KNOTS ( 'NONE', 3,
 ( #63475, #71013, #103904, #78565 ),
 .UNSPECIFIED., .F., .F.,
 ( 4, 4 ),
 ( 0.0005621349429477124748, 0.02562325005156303875 ),
 .UNSPECIFIED. ) ;
#51298=CARTESIAN_POINT ( 'NONE',  ( -32.73605680493314196, 486.1418706179324545, 5.972480793507408237 ) ) ;
#51308=CARTESIAN_POINT ( 'NONE',  ( -25.05029448812380721, 307.4428306656531618, 9.526979722917090498 ) ) ;
#51316=EDGE_CURVE ( 'NONE', #51548, #106028, #9060, .T. ) ;
#51327=AXIS2_PLACEMENT_3D ( 'NONE', #26252, #42922, #34862 ) ;
#51328=CARTESIAN_POINT ( 'NONE',  ( -43.62593301837079451, 434.3202385713651097, 14.43474084663357893 ) ) ;
#51330=ADVANCED_FACE ( 'NONE', ( #27932 ), #34475, .F. ) ;
#51345=LINE ( 'NONE', #74558, #69255 ) ;
#51347=CARTESIAN_POINT ( 'NONE',  ( -26.36618118159100632, 306.0239721618610815, 10.65825050287647358 ) ) ;
#51361=EDGE_CURVE ( 'NONE', #97120, #80103, #357, .T. ) ;
#51367=DIRECTION ( 'NONE',  ( 0.7092840680488031735, -0.7049227693954428497, 0.000000000000000000 ) ) ;
#51368=ORIENTED_EDGE ( 'NONE', *, *, #59875, .T. ) ;
#51369=CIRCLE ( 'NONE', #20504, 15.00000000000000711 ) ;
#51370=CARTESIAN_POINT ( 'NONE',  ( -32.03536204142076826, 464.8478167070323934, 12.52449229590025048 ) ) ;
#51372=CIRCLE ( 'NONE', #65162, 0.9999999999999930056 ) ;
#51375=CARTESIAN_POINT ( 'NONE',  ( 7.409683256360576564, 302.7200035818300421, 9.908966834550497538 ) ) ;
#51378=CARTESIAN_POINT ( 'NONE',  ( 46.00000000000000000, 500.0000000000002274, -12.00000000000000711 ) ) ;
#51393=CARTESIAN_POINT ( 'NONE',  ( 22.88508939410625942, 295.1610940167444710, 10.00275451425645734 ) ) ;
#51420=ADVANCED_FACE ( 'NONE', ( #83987 ), #4828, .T. ) ;
#51428=VERTEX_POINT ( 'NONE', #39571 ) ;
#51440=CARTESIAN_POINT ( 'NONE',  ( -46.00000000000000000, 450.0000000000002274, 13.20242257375370976 ) ) ;
#51441=CARTESIAN_POINT ( 'NONE',  ( -43.60560354499889257, 484.6927786829147067, 3.665222855601379504 ) ) ;
#51443=CARTESIAN_POINT ( 'NONE',  ( 31.99602169361446258, 464.8336097802171594, 12.51960734452490875 ) ) ;
#51444=CARTESIAN_POINT ( 'NONE',  ( -36.55533968308493797, 463.5207292468226115, 19.71490071751487605 ) ) ;
#51456=CARTESIAN_POINT ( 'NONE',  ( 46.00000000000000000, 438.4646224975062978, 9.895601460515761616 ) ) ;
#51461=CARTESIAN_POINT ( 'NONE',  ( -33.20442555830484110, 314.5462679929517549, -7.210101933046130007 ) ) ;
#51465=ORIENTED_EDGE ( 'NONE', *, *, #54274, .F. ) ;
#51466=CARTESIAN_POINT ( 'NONE',  ( -43.03880698781976832, 435.3545807224047053, 16.83573131045124427 ) ) ;
#51480=ORIENTED_EDGE ( 'NONE', *, *, #11529, .T. ) ;
#51496=ORIENTED_EDGE ( 'NONE', *, *, #22484, .F. ) ;
#51498=CARTESIAN_POINT ( 'NONE',  ( -30.00000000000000000, 450.0000000000002274, 13.20242257375370976 ) ) ;
#51511=DIRECTION ( 'NONE',  ( 0.000000000000000000, -0.2521971900443084613, -0.9676758637755490389 ) ) ;
#51514=CARTESIAN_POINT ( 'NONE',  ( -31.03678703374875880, 438.6650838204938054, 21.86890379898545334 ) ) ;
#51521=CARTESIAN_POINT ( 'NONE',  ( -41.83706036796058925, 337.9408106068874531, 12.27123674261958897 ) ) ;
#51529=CARTESIAN_POINT ( 'NONE',  ( 32.54922218626916930, 319.8023524069591303, -6.363686095274232457 ) ) ;
#51542=CARTESIAN_POINT ( 'NONE',  ( 45.47726348208502145, 415.0353453662364700, 8.193293366016010992 ) ) ;
#51546=CARTESIAN_POINT ( 'NONE',  ( 31.23310005892718166, 439.6097802320569485, 23.20956534902767743 ) ) ;
#51548=VERTEX_POINT ( 'NONE', #91305 ) ;
#51592=EDGE_CURVE ( 'NONE', #51812, #87574, #52049, .T. ) ;
#51594=FACE_OUTER_BOUND ( 'NONE', #71338, .T. ) ;
#51596=CARTESIAN_POINT ( 'NONE',  ( -32.87517070013019094, 485.0717976019059847, 1.466424316699820096 ) ) ;
#51597=CARTESIAN_POINT ( 'NONE',  ( 25.77264063226874313, 305.3150788826293933, 10.49011161150212068 ) ) ;
#51599=CARTESIAN_POINT ( 'NONE',  ( -43.00000000000000000, 485.2629658518202405, -2.796394914059407100 ) ) ;
#51600=ORIENTED_EDGE ( 'NONE', *, *, #79954, .F. ) ;
#51603=CARTESIAN_POINT ( 'NONE',  ( 32.97364094493251940, 300.4786680927070392, 3.203698462821897408 ) ) ;
#51613=CARTESIAN_POINT ( 'NONE',  ( 7.218596499961003055, 294.7245713411965085, 9.909955490001918221 ) ) ;
#51619=EDGE_CURVE ( 'NONE', #53610, #89019, #36266, .T. ) ;
#51637=CARTESIAN_POINT ( 'NONE',  ( -34.34679764914316991, 491.0133751866271723, 12.01297952733263763 ) ) ;
#51639=CARTESIAN_POINT ( 'NONE',  ( 44.48219350064427147, 478.0060774381361739, 1.937535957203245562 ) ) ;
#51651=CARTESIAN_POINT ( 'NONE',  ( -35.98161575412628821, 437.4062335063961200, 4.370829238943763073 ) ) ;
#51657=FILL_AREA_STYLE ('',( #18263 ) ) ;
#51658=CARTESIAN_POINT ( 'NONE',  ( -9.659790634495982076, 294.6522974485824875, -2.601814601459285115 ) ) ;
#51660=CARTESIAN_POINT ( 'NONE',  ( 7.160273590795869225, 294.7244959282127184, -7.003631132636504830 ) ) ;
#51666=CARTESIAN_POINT ( 'NONE',  ( 25.06945282685627774, 307.6499839075243017, 10.57814702769852389 ) ) ;
#51669=CARTESIAN_POINT ( 'NONE',  ( -39.45725925859406402, 460.7192990590703516, 2.112476274834657719 ) ) ;
#51671=ORIENTED_EDGE ( 'NONE', *, *, #35001, .T. ) ;
#51676=CARTESIAN_POINT ( 'NONE',  ( -42.23079339798739795, 461.4509360991310700, 2.027626716395849904 ) ) ;
#51677=CARTESIAN_POINT ( 'NONE',  ( -35.74483125092430669, 413.6409941285803598, 6.029078300230034770 ) ) ;
#51681=CARTESIAN_POINT ( 'NONE',  ( -44.13785234221902698, 464.3950528659657948, 9.689702101754715358 ) ) ;
#51688=CARTESIAN_POINT ( 'NONE',  ( -9.497389752370075655, 295.1492747691260092, -10.04143169208946240 ) ) ;
#51689=TOROIDAL_SURFACE ( 'NONE', #101606, 12.00000000000000711, 3.000000000000000000 ) ;
#51696=CARTESIAN_POINT ( 'NONE',  ( -18.46964424310625930, 302.6549491133945935, 9.895499654730381067 ) ) ;
#51699=CARTESIAN_POINT ( 'NONE',  ( 43.79329400983225185, 434.3557490607465184, 12.18619556048155239 ) ) ;
#51704=CARTESIAN_POINT ( 'NONE',  ( -44.32853450521363925, 435.2015765068597375, 12.56845903945290388 ) ) ;
#51717=CARTESIAN_POINT ( 'NONE',  ( -25.91098795542547961, 306.7335490000789946, -8.585778581918489749 ) ) ;
#51726=CARTESIAN_POINT ( 'NONE',  ( -33.95156263172580680, 464.5083255208629680, 6.608064661821540398 ) ) ;
#51730=CARTESIAN_POINT ( 'NONE',  ( -32.98783370188532160, 323.4213243428150690, -4.452354598022544074 ) ) ;
#51731=CARTESIAN_POINT ( 'NONE',  ( -37.81576683240294301, 309.3149194722910806, 5.368762553532455684 ) ) ;
#51746=DIRECTION ( 'NONE',  ( 1.000000000000000000, 0.000000000000000000, -1.224646799147353207E-16 ) ) ;
#51748=( BOUNDED_SURFACE ( )  B_SPLINE_SURFACE ( 3, 2, ( 
 ( #2807, #68638, #101516 ),
 ( #77239, #27674, #3355 ),
 ( #69166, #96611, #13011 ),
 ( #103632, #38913, #48030 ) ),
 .UNSPECIFIED., .F., .F., .T. ) 
 B_SPLINE_SURFACE_WITH_KNOTS ( ( 4, 4 ),
 ( 3, 3 ),
 ( 4.336808689942017736E-18, 0.001448708294673802226 ),
 ( 0.000000000000000000, 1.000000000000000000 ),
 .UNSPECIFIED. ) 
 GEOMETRIC_REPRESENTATION_ITEM ( )  RATIONAL_B_SPLINE_SURFACE ( (
 ( 1.000000000000000000, 0.7788880963805111524, 1.000000000000000000),
 ( 1.000000000000000000, 0.7852432470598105230, 1.000000000000000000),
 ( 1.000000000000000000, 0.7915643316727953849, 1.000000000000000000),
 ( 1.000000000000000000, 0.7978714159192913380, 1.000000000000000000) ) ) 
 REPRESENTATION_ITEM ( '' )  SURFACE ( )  );
#51756=ADVANCED_FACE ( 'NONE', ( #105629 ), #60791, .F. ) ;
#51760=CARTESIAN_POINT ( 'NONE',  ( 6.930002047096925466, 302.1778385079933855, -10.02505617572796659 ) ) ;
#51761=CARTESIAN_POINT ( 'NONE',  ( 37.04388863813380794, 311.3287000699716032, 13.89786840526617517 ) ) ;
#51773=CARTESIAN_POINT ( 'NONE',  ( -41.43589798206021158, 484.8608140988944797, -3.494610779850012339 ) ) ;
#51782=DIRECTION ( 'NONE',  ( -1.000000000000000000, -0.000000000000000000, -0.000000000000000000 ) ) ;
#51784=CARTESIAN_POINT ( 'NONE',  ( 35.56416567029047116, 496.2909070316903239, -10.19064917708978335 ) ) ;
#51785=CARTESIAN_POINT ( 'NONE',  ( 39.69724611604618048, 460.7042697230090766, 2.103486822546470680 ) ) ;
#51812=VERTEX_POINT ( 'NONE', #46347 ) ;
#51835=CARTESIAN_POINT ( 'NONE',  ( -32.62137895416891098, 486.7356100976077187, 7.182248123790627048 ) ) ;
#51849=CARTESIAN_POINT ( 'NONE',  ( -25.63293091691854286, 308.3345217834615823, 9.742415824227602883 ) ) ;
#51858=ORIENTED_EDGE ( 'NONE', *, *, #31044, .T. ) ;
#51866=CARTESIAN_POINT ( 'NONE',  ( -40.36578697173862196, 468.8173651557589210, -0.04324207066571782859 ) ) ;
#51869=CARTESIAN_POINT ( 'NONE',  ( -41.46910480218704009, 484.7338956289818270, -3.418960549715579500 ) ) ;
#51880=ORIENTED_EDGE ( 'NONE', *, *, #61911, .F. ) ;
#51881=AXIS2_PLACEMENT_3D ( 'NONE', #73723, #88865, #65650 ) ;
#51903=CARTESIAN_POINT ( 'NONE',  ( 37.50030914627209455, 491.1170837247063332, 12.27619315344390039 ) ) ;
#51921=CIRCLE ( 'NONE', #48534, 1.000000000000000666 ) ;
#51925=CARTESIAN_POINT ( 'NONE',  ( 22.15188447042185160, 295.0129022001648309, 1.971242154165463223 ) ) ;
#51956=ORIENTED_EDGE ( 'NONE', *, *, #75469, .F. ) ;
#51958=CARTESIAN_POINT ( 'NONE',  ( 43.50377727019363050, 435.9167426301696082, 18.24083946424737590 ) ) ;
#51967=CARTESIAN_POINT ( 'NONE',  ( -43.52075891743670866, 484.7805561108188499, 4.063293749114545328 ) ) ;
#51969=CARTESIAN_POINT ( 'NONE',  ( 31.99294114632900232, 464.8457910465707528, 12.87241426108012732 ) ) ;
#51970=CARTESIAN_POINT ( 'NONE',  ( 33.00000000000000000, 435.0774731480752280, 11.67986145722084501 ) ) ;
#51980=VERTEX_POINT ( 'NONE', #27963 ) ;
#51989=CARTESIAN_POINT ( 'NONE',  ( -41.03101037122678463, 313.1827267563339774, -5.626772567029049377 ) ) ;
#51993=CARTESIAN_POINT ( 'NONE',  ( -19.73463816634111012, 304.7971333121958537, 8.925379062039116462 ) ) ;
#52026=CARTESIAN_POINT ( 'NONE',  ( 33.89250494191496443, 463.6575930728430990, 6.993601543837892898 ) ) ;
#52038=CARTESIAN_POINT ( 'NONE',  ( 46.00000000000000000, 438.2055348970465616, 15.52909715622263676 ) ) ;
#52040=DIRECTION ( 'NONE',  ( 0.000000000000000000, 0.9676758637755492609, -0.2521971900443079062 ) ) ;
#52041=CARTESIAN_POINT ( 'NONE',  ( -43.89370568756214652, 435.4157859805903286, 16.19551141317008813 ) ) ;
#52046=CARTESIAN_POINT ( 'NONE',  ( 36.66358481845913531, 432.5585790697741686, 4.915382580107980459 ) ) ;
#52049=CIRCLE ( 'NONE', #28012, 8.000000000000014211 ) ;
#52051=CARTESIAN_POINT ( 'NONE',  ( -42.41055444770296390, 353.4000580228727131, 15.28812778342764034 ) ) ;
#52054=CARTESIAN_POINT ( 'NONE',  ( -36.70797521953156206, 381.7145783656985714, 5.219800535707618039 ) ) ;
#52055=CARTESIAN_POINT ( 'NONE',  ( 40.22681104634839500, 489.7629721959603444, 10.97561085253236968 ) ) ;
#52059=CARTESIAN_POINT ( 'NONE',  ( 21.29975379448945816, 294.8969325209483827, -1.990407376643369641 ) ) ;
#52060=CARTESIAN_POINT ( 'NONE',  ( 35.69739812508499455, 430.4862580793411553, 4.964222856391316441 ) ) ;
#52061=EDGE_CURVE ( 'NONE', #22313, #78629, #55289, .T. ) ;
#52062=EDGE_CURVE ( 'NONE', #1547, #60518, #24380, .T. ) ;
#52071=CARTESIAN_POINT ( 'NONE',  ( 36.41659902574616581, 335.0122255936540228, -2.184171530108547810 ) ) ;
#52072=CARTESIAN_POINT ( 'NONE',  ( 44.29288495124914249, 463.9154455111800530, 8.171315969404531643 ) ) ;
#52073=ORIENTED_EDGE ( 'NONE', *, *, #97820, .T. ) ;
#52075=CARTESIAN_POINT ( 'NONE',  ( 32.09911992168216699, 438.9232547152093957, 23.66653216045977359 ) ) ;
#52097=ORIENTED_EDGE ( 'NONE', *, *, #94904, .T. ) ;
#52098=CARTESIAN_POINT ( 'NONE',  ( 0.000000000000000000, 70.00000000000000000, -5.999999999999998224 ) ) ;
#52115=CARTESIAN_POINT ( 'NONE',  ( -32.12756478236646984, 464.8250811501316093, 14.60600970021982725 ) ) ;
#52117=CARTESIAN_POINT ( 'NONE',  ( -16.53810334270205828, 303.5675058441541978, 9.876558506355554101 ) ) ;
#52124=ORIENTED_EDGE ( 'NONE', *, *, #94914, .T. ) ;
#52127=CARTESIAN_POINT ( 'NONE',  ( 32.04846564072990134, 435.5722017075208896, 16.73368519115310704 ) ) ;
#52128=CARTESIAN_POINT ( 'NONE',  ( 24.04521816055709138, 295.4566507460422145, 10.06661448227953493 ) ) ;
#52134=AXIS2_PLACEMENT_3D ( 'NONE', #13957, #23689, #80821 ) ;
#52135=CARTESIAN_POINT ( 'NONE',  ( 36.70900294270256126, 306.3085992329407645, 4.617960540507793255 ) ) ;
#52136=DIRECTION ( 'NONE',  ( 0.9788760387920678596, 0.000000000000000000, -0.2044546421061400610 ) ) ;
#52140=DIRECTION ( 'NONE',  ( 0.9746329792208491272, 0.000000000000000000, 0.2238091951084492937 ) ) ;
#52143=CARTESIAN_POINT ( 'NONE',  ( 42.77633007798412024, 465.0956601428450767, 12.68100826444438667 ) ) ;
#52166=FACE_OUTER_BOUND ( 'NONE', #67104, .T. ) ;
#52169=CARTESIAN_POINT ( 'NONE',  ( -36.49104508226669452, 491.8392457932882849, 12.58580469730132201 ) ) ;
#52196=VERTEX_POINT ( 'NONE', #41305 ) ;
#52199=CARTESIAN_POINT ( 'NONE',  ( 23.63920041808693995, 304.8825889122297212, 10.16203760377671017 ) ) ;
#52202=CARTESIAN_POINT ( 'NONE',  ( 37.85084083633367413, 437.2249973798734572, 3.569182825063074382 ) ) ;
#52204=CARTESIAN_POINT ( 'NONE',  ( 32.94021323899734455, 485.0599191339525191, 5.361609822540892800 ) ) ;
#52209=CARTESIAN_POINT ( 'NONE',  ( -35.57955382936916067, 363.3973965622570859, 2.919629247011395368 ) ) ;
#52236=ORIENTED_EDGE ( 'NONE', *, *, #51090, .T. ) ;
#52250=DIRECTION ( 'NONE',  ( 0.000000000000000000, 0.000000000000000000, 1.000000000000000000 ) ) ;
#52253=CARTESIAN_POINT ( 'NONE',  ( -44.28914958155538528, 435.2230000814720938, 14.00302124382356261 ) ) ;
#52258=DIRECTION ( 'NONE',  ( 0.2282686145788442589, 0.2753452451894767283, 0.9338513990725731961 ) ) ;
#52261=CARTESIAN_POINT ( 'NONE',  ( -35.69538431007205759, 304.3564473186642658, 4.136361301185305095 ) ) ;
#52271=DIRECTION ( 'NONE',  ( 0.000000000000000000, 0.000000000000000000, -1.000000000000000000 ) ) ;
#52273=CIRCLE ( 'NONE', #95402, 6.999999999999982236 ) ;
#52277=CARTESIAN_POINT ( 'NONE',  ( 32.22120753352783140, 464.6691781026584636, 10.60621122532586291 ) ) ;
#52288=CARTESIAN_POINT ( 'NONE',  ( 34.47678062874019389, 437.1474145881098821, 5.468662283308706407 ) ) ;
#52290=CARTESIAN_POINT ( 'NONE',  ( 0.2504595177176738297, 295.3551702420456309, -10.00003484568028611 ) ) ;
#52292=CARTESIAN_POINT ( 'NONE',  ( 43.61018511057424973, 374.8234295527117865, 14.44054883524410826 ) ) ;
#52293=ADVANCED_FACE ( 'NONE', ( #34847 ), #11730, .F. ) ;
#52307=CARTESIAN_POINT ( 'NONE',  ( 10.00232142752224362, 294.6427048180378847, 0.2484324481109706217 ) ) ;
#52316=CARTESIAN_POINT ( 'NONE',  ( 30.00000000000000000, 488.6481008951278113, 3.890293910850189274 ) ) ;
#52318=CARTESIAN_POINT ( 'NONE',  ( -34.62900545891979220, 434.6649403350424450, 8.921687928929188161 ) ) ;
#52321=CARTESIAN_POINT ( 'NONE',  ( -44.19062745116208646, 435.2577039776292054, 14.58891375936595836 ) ) ;
#52322=ORIENTED_EDGE ( 'NONE', *, *, #103994, .F. ) ;
#52357=CARTESIAN_POINT ( 'NONE',  ( -30.12932728364529922, 334.4140447340107585, 17.11298374841474867 ) ) ;
#52358=CARTESIAN_POINT ( 'NONE',  ( 23.61963550967466574, 306.0340374937824777, 10.19690224617928287 ) ) ;
#52367=CARTESIAN_POINT ( 'NONE',  ( -32.62920465536350889, 486.5749440413351294, 6.880070463950354487 ) ) ;
#52378=CARTESIAN_POINT ( 'NONE',  ( -24.48540210594370947, 306.7517469399879246, 9.362912201731168338 ) ) ;
#52402=CARTESIAN_POINT ( 'NONE',  ( 43.03265099500004709, 484.2747968070555089, -0.8099405866658345721 ) ) ;
#52408=ADVANCED_FACE ( 'NONE', ( #101676 ), #92377, .T. ) ;
#52416=CARTESIAN_POINT ( 'NONE',  ( -43.52075891743682234, 484.7805561108189636, 4.063293749114582631 ) ) ;
#52419=DIRECTION ( 'NONE',  ( -0.000000000000000000, -1.000000000000000000, -0.000000000000000000 ) ) ;
#52422=CARTESIAN_POINT ( 'NONE',  ( 32.15310320217080431, 439.7024266304582056, 23.94087012106557211 ) ) ;
#52426=CARTESIAN_POINT ( 'NONE',  ( -35.55307928090937963, 490.6489906963894327, 12.31598007740004519 ) ) ;
#52428=CARTESIAN_POINT ( 'NONE',  ( 9.184850993605161750E-16, 81.00000000000000000, 7.000000000000006217 ) ) ;
#52433=ORIENTED_EDGE ( 'NONE', *, *, #39557, .F. ) ;
#52440=CARTESIAN_POINT ( 'NONE',  ( -45.50145573691759182, 405.2496736015978627, 8.430338687477670234 ) ) ;
#52448=CARTESIAN_POINT ( 'NONE',  ( -7.409678256911004901, 302.7200037710339871, 9.908966876114519096 ) ) ;
#52476=B_SPLINE_CURVE_WITH_KNOTS ( 'NONE', 3,
 ( #51117, #28488, #68934, #11719 ),
 .UNSPECIFIED., .F., .F.,
 ( 4, 4 ),
 ( 8.673617379884035472E-18, 0.001861443540404362270 ),
 .UNSPECIFIED. ) ;
#52486=CARTESIAN_POINT ( 'NONE',  ( 41.61741820144892756, 435.6127172585838707, 7.033059668060364089 ) ) ;
#52497=CARTESIAN_POINT ( 'NONE',  ( -35.59667163540026280, 463.9592197885497171, -0.04846191499040426731 ) ) ;
#52499=CARTESIAN_POINT ( 'NONE',  ( -21.29975379448952211, 294.8969325209483259, -1.990407376643348103 ) ) ;
#52504=CARTESIAN_POINT ( 'NONE',  ( 32.07495350393109135, 464.7631673202251932, 11.47102835346950656 ) ) ;
#52505=CARTESIAN_POINT ( 'NONE',  ( -35.04496600798486128, 464.5002996787812322, 18.88267410155424031 ) ) ;
#52509=CARTESIAN_POINT ( 'NONE',  ( 33.38752816062147133, 464.7252609254567801, 16.46839106254713414 ) ) ;
#52523=CARTESIAN_POINT ( 'NONE',  ( -38.37349848668355179, 306.2639072012707402, -7.354698554755767503 ) ) ;
#52539=VERTEX_POINT ( 'NONE', #24372 ) ;
#52550=FACE_OUTER_BOUND ( 'NONE', #4484, .T. ) ;
#52567=CARTESIAN_POINT ( 'NONE',  ( 46.00000000000000711, 436.0044609852890289, 15.17967024743226645 ) ) ;
#52582=CARTESIAN_POINT ( 'NONE',  ( -22.75399275862038095, 295.1281901880543046, 1.996464526093286507 ) ) ;
#52588=DIRECTION ( 'NONE',  ( -0.000000000000000000, -1.000000000000000000, -0.000000000000000000 ) ) ;
#52589=CARTESIAN_POINT ( 'NONE',  ( 21.51569398614867623, 294.9107018935608266, -9.987480606144547579 ) ) ;
#52590=CARTESIAN_POINT ( 'NONE',  ( 26.97491686565329161, 307.4599153070161606, -9.420584459367200125 ) ) ;
#52599=CARTESIAN_POINT ( 'NONE',  ( 39.30001941745848626, 312.0126453433533698, 2.100405576424947629 ) ) ;
#52602=CARTESIAN_POINT ( 'NONE',  ( -16.96954359408614366, 304.5683848806726814, 9.876757081930351845 ) ) ;
#52603=CARTESIAN_POINT ( 'NONE',  ( 31.03517274901688694, 439.3343806745134543, 22.67962720703587820 ) ) ;
#52606=AXIS2_PLACEMENT_3D ( 'NONE', #43280, #52419, #41683 ) ;
#52609=EDGE_CURVE ( 'NONE', #90391, #32226, #71223, .T. ) ;
#52611=CARTESIAN_POINT ( 'NONE',  ( -43.00000000000000000, 500.0000000000002274, 15.00000000000000711 ) ) ;
#52612=B_SPLINE_CURVE_WITH_KNOTS ( 'NONE', 3,
 ( #60477, #50730, #83640, #9745 ),
 .UNSPECIFIED., .F., .F.,
 ( 4, 4 ),
 ( 0.000000000000000000, 0.001128230833659103153 ),
 .UNSPECIFIED. ) ;
#52625=CARTESIAN_POINT ( 'NONE',  ( -43.10371592039292921, 462.6168321841616375, 4.970041475408518927 ) ) ;
#52638=ADVANCED_FACE ( 'NONE', ( #10787 ), #48908, .F. ) ;
#52646=CARTESIAN_POINT ( 'NONE',  ( -15.71086122448608613, 303.5558210301048803, 9.874087016084169832 ) ) ;
#52647=VECTOR ( 'NONE', #100122, 1000.000000000000000 ) ;
#52650=CARTESIAN_POINT ( 'NONE',  ( -31.39343312534550989, 438.8553142255844364, 23.06001087143945227 ) ) ;
#52658=CIRCLE ( 'NONE', #42332, 1.000000000000000222 ) ;
#52659=CARTESIAN_POINT ( 'NONE',  ( 24.90251836858309886, 295.6281153014862753, 2.103653583787406856 ) ) ;
#52682=EDGE_LOOP ( 'NONE', ( #46225, #22457, #49732, #2972 ) ) ;
#52693=CARTESIAN_POINT ( 'NONE',  ( 37.38584400634713489, 490.8443720919671023, 12.40597885709908077 ) ) ;
#52695=EDGE_CURVE ( 'NONE', #70272, #105135, #92548, .T. ) ;
#52698=DIRECTION ( 'NONE',  ( 1.000000000000000000, 0.000000000000000000, 0.000000000000000000 ) ) ;
#52709=( BOUNDED_SURFACE ( )  B_SPLINE_SURFACE ( 3, 2, ( 
 ( #53925, #78213, #29702 ),
 ( #4327, #86856, #12932 ),
 ( #37262, #60468, #45852 ),
 ( #61524, #93873, #44262 ) ),
 .UNSPECIFIED., .F., .F., .F. ) 
 B_SPLINE_SURFACE_WITH_KNOTS ( ( 4, 4 ),
 ( 3, 3 ),
 ( 4.163336342344337027E-17, 0.0002182426145221272784 ),
 ( 0.000000000000000000, 1.000000000000000000 ),
 .UNSPECIFIED. ) 
 GEOMETRIC_REPRESENTATION_ITEM ( )  RATIONAL_B_SPLINE_SURFACE ( (
 ( 1.000000000000000000, 0.8308329163121006555, 1.000000000000000000),
 ( 1.000000000000000000, 0.8297634434905108991, 1.000000000000000000),
 ( 1.000000000000000000, 0.8286461416559528503, 1.000000000000000000),
 ( 1.000000000000000000, 0.8274831119537282564, 1.000000000000000000) ) ) 
 REPRESENTATION_ITEM ( '' )  SURFACE ( )  );
#52711=CARTESIAN_POINT ( 'NONE',  ( -39.33352494920633546, 438.9614613858099119, 23.36191803517838395 ) ) ;
#52722=CARTESIAN_POINT ( 'NONE',  ( 33.07276483573660641, 438.9325140356084489, 23.89537236861389502 ) ) ;
#52731=AXIS2_PLACEMENT_3D ( 'NONE', #103111, #29262, #29782 ) ;
#52735=CARTESIAN_POINT ( 'NONE',  ( 23.77937657248197922, 306.1093036377834551, 9.213915351946365462 ) ) ;
#52736=CARTESIAN_POINT ( 'NONE',  ( -40.45545246860710620, 460.8457769820571457, 2.191470225627486723 ) ) ;
#52757=CARTESIAN_POINT ( 'NONE',  ( 35.45036406932566564, 436.3203772529585649, 5.179456583034234285 ) ) ;
#52766=FACE_OUTER_BOUND ( 'NONE', #81212, .T. ) ;
#52769=EDGE_CURVE ( 'NONE', #13768, #56970, #86723, .T. ) ;
#52787=CARTESIAN_POINT ( 'NONE',  ( 40.91702039389569023, 378.5672949884566378, 26.48911381135054555 ) ) ;
#52797=DIRECTION ( 'NONE',  ( 0.000000000000000000, 1.000000000000000000, -1.224646799147353207E-16 ) ) ;
#52800=CARTESIAN_POINT ( 'NONE',  ( -33.57932678495680534, 327.5754790332646280, -3.422513633634138408 ) ) ;
#52801=CARTESIAN_POINT ( 'NONE',  ( -37.52685452098302932, 308.4526037119397870, 5.153401396366573906 ) ) ;
#52819=CARTESIAN_POINT ( 'NONE',  ( 0.000000000000000000, 304.8518027762758038, 8.936999415352287812 ) ) ;
#52829=CARTESIAN_POINT ( 'NONE',  ( 5.833922283576983503, 294.7609306416175059, -8.134666899186667521 ) ) ;
#52830=CARTESIAN_POINT ( 'NONE',  ( 45.48003679188781234, 379.8448106960472614, 7.220331889307936457 ) ) ;
#52833=ORIENTED_EDGE ( 'NONE', *, *, #52062, .T. ) ;
#52846=ORIENTED_EDGE ( 'NONE', *, *, #97623, .T. ) ;
#52860=CARTESIAN_POINT ( 'NONE',  ( 37.83989825151499531, 491.0717236019729057, 13.27726931866749460 ) ) ;
#52888=ORIENTED_EDGE ( 'NONE', *, *, #68759, .T. ) ;
#52904=CARTESIAN_POINT ( 'NONE',  ( 43.00000000000000000, 485.2629658518202405, -2.796394914059364911 ) ) ;
#52920=CARTESIAN_POINT ( 'NONE',  ( -32.04928241692800839, 435.9036815552922803, 19.85315484758348248 ) ) ;
#52922=CARTESIAN_POINT ( 'NONE',  ( 32.70838245875363270, 434.6727645417001327, 17.17179653056833644 ) ) ;
#52928=CARTESIAN_POINT ( 'NONE',  ( 35.49824309011672341, 438.0806692989502835, 4.093885194487875800 ) ) ;
#52951=CARTESIAN_POINT ( 'NONE',  ( 33.00540147335379260, 487.4196752801331627, 9.523982417622169905 ) ) ;
#52963=CIRCLE ( 'NONE', #6436, 1.000000000000013989 ) ;
#52970=CARTESIAN_POINT ( 'NONE',  ( 0.000000000000000000, 67.05096163904791240, -10.02537308446410691 ) ) ;
#53016=CARTESIAN_POINT ( 'NONE',  ( -33.88461414431147745, 464.6055380068506224, 6.798187872896692241 ) ) ;
#53036=CARTESIAN_POINT ( 'NONE',  ( 37.71459991402554124, 437.7716825518408541, 4.505118785440091145 ) ) ;
#53049=CARTESIAN_POINT ( 'NONE',  ( -30.95643954367146833, 313.8918926584737505, -7.857037206977866006 ) ) ;
#53052=CARTESIAN_POINT ( 'NONE',  ( -43.66784424860031066, 484.4037905981319909, 1.818048676808925013 ) ) ;
#53060=CARTESIAN_POINT ( 'NONE',  ( 32.45893998680863746, 464.7013998967805719, 16.05169235330116706 ) ) ;
#53061=CARTESIAN_POINT ( 'NONE',  ( -36.55581286090212956, 364.8155619110331713, 3.255690858065809934 ) ) ;
#53069=CARTESIAN_POINT ( 'NONE',  ( 33.07276483573664905, 438.9325140356084489, 23.89537236861388081 ) ) ;
#53088=EDGE_CURVE ( 'NONE', #15159, #10424, #34927, .T. ) ;
#53092=MECHANICAL_DESIGN_GEOMETRIC_PRESENTATION_REPRESENTATION('',(#42759),#44558);
#53100=FACE_OUTER_BOUND ( 'NONE', #47540, .T. ) ;
#53103=ORIENTED_EDGE ( 'NONE', *, *, #35845, .F. ) ;
#53116=CIRCLE ( 'NONE', #51327, 5.000000000000001776 ) ;
#53117=CARTESIAN_POINT ( 'NONE',  ( 46.00000000000000000, 438.0646818832677809, 14.80758164884668560 ) ) ;
#53119=CIRCLE ( 'NONE', #48168, 3.000000000000000000 ) ;
#53142=CARTESIAN_POINT ( 'NONE',  ( 36.91281931599076671, 303.7809130842520631, -7.959270006439831846 ) ) ;
#53146=CARTESIAN_POINT ( 'NONE',  ( -34.84618260875176787, 489.9833681528637044, 11.97975507378787619 ) ) ;
#53155=CARTESIAN_POINT ( 'NONE',  ( 45.29236137015085006, 362.1850291255836396, 4.988315089120307633 ) ) ;
#53157=CARTESIAN_POINT ( 'NONE',  ( 43.71999369284589676, 463.9422086738373991, 7.488562083390279511 ) ) ;
#53160=CARTESIAN_POINT ( 'NONE',  ( 31.35397047751884614, 438.7442028766091653, 22.94603175516938265 ) ) ;
#53179=CARTESIAN_POINT ( 'NONE',  ( 34.40200853651277413, 463.9211969149139918, 5.556884403146712614 ) ) ;
#53183=CARTESIAN_POINT ( 'NONE',  ( -33.49615637169856086, 465.2403011571850584, 8.307633084691179448 ) ) ;
#53204=ORIENTED_EDGE ( 'NONE', *, *, #35567, .T. ) ;
#53208=CARTESIAN_POINT ( 'NONE',  ( 37.88504238421471371, 464.3115779013475048, 20.35635421821805480 ) ) ;
#53210=CARTESIAN_POINT ( 'NONE',  ( 29.45187729973999069, 297.5878244927288279, 2.537403480031316771 ) ) ;
#53212=CARTESIAN_POINT ( 'NONE',  ( 7.188569307834695721, 302.2771564544925695, -10.02656284648950624 ) ) ;
#53218=CARTESIAN_POINT ( 'NONE',  ( 43.00000000000000000, 435.7055874969797742, 20.39059140826877226 ) ) ;
#53221=COLOUR_RGB ( '', 0.66274510, 0.83137255, 0.94901961) ;
#53225=AXIS2_PLACEMENT_3D ( 'NONE', #91056, #43022, #17164 ) ;
#53232=CARTESIAN_POINT ( 'NONE',  ( 32.81992448453895150, 465.7192846569213316, 11.17271167765130890 ) ) ;
#53238=CARTESIAN_POINT ( 'NONE',  ( 34.42490260133396873, 435.3680287947617558, 9.712724143469429805 ) ) ;
#53252=CARTESIAN_POINT ( 'NONE',  ( 45.99999999999999289, 486.8231468695055923, 5.689692765235318639 ) ) ;
#53279=CARTESIAN_POINT ( 'NONE',  ( 26.01244650717567453, 309.4037012981271459, 11.00800451746652975 ) ) ;
#53282=ORIENTED_EDGE ( 'NONE', *, *, #90654, .T. ) ;
#53288=DIRECTION ( 'NONE',  ( 0.000000000000000000, 1.000000000000000000, 0.000000000000000000 ) ) ;
#53294=EDGE_CURVE ( 'NONE', #90391, #30344, #86085, .T. ) ;
#53318=ORIENTED_EDGE ( 'NONE', *, *, #57290, .F. ) ;
#53320=CARTESIAN_POINT ( 'NONE',  ( 43.74985542820358830, 435.5770091380369990, 16.96136490515564077 ) ) ;
#53331=CARTESIAN_POINT ( 'NONE',  ( 42.76923532591476373, 409.3122222668040990, 19.95929303662902754 ) ) ;
#53334=CARTESIAN_POINT ( 'NONE',  ( -43.72886361455299919, 434.3043191535924734, 13.94145212282985469 ) ) ;
#53339=CARTESIAN_POINT ( 'NONE',  ( 51.01037695545453232, 500.0000000000002274, -5.000000000000001776 ) ) ;
#53340=ORIENTED_EDGE ( 'NONE', *, *, #82481, .F. ) ;
#53341=CARTESIAN_POINT ( 'NONE',  ( -29.89885390591881276, 311.8322808163144373, -7.366452359367730018 ) ) ;
#53342=CARTESIAN_POINT ( 'NONE',  ( -38.65178583513453248, 312.1935651169637822, 6.094317023448435400 ) ) ;
#53362=AXIS2_PLACEMENT_3D ( 'NONE', #6788, #30566, #47763 ) ;
#53371=CARTESIAN_POINT ( 'NONE',  ( 4.055648887448357165, 294.8040761930213307, -9.158006418842486340 ) ) ;
#53373=CARTESIAN_POINT ( 'NONE',  ( 31.76566490452815117, 299.0319430614179055, -1.071778121186186317 ) ) ;
#53377=CARTESIAN_POINT ( 'NONE',  ( 0.000000000000000000, 70.00000000000000000, -7.025805963803935406 ) ) ;
#53386=ORIENTED_EDGE ( 'NONE', *, *, #105099, .F. ) ;
#53413=EDGE_CURVE ( 'NONE', #38472, #23399, #52612, .T. ) ;
#53434=DIRECTION ( 'NONE',  ( 0.000000000000000000, 0.000000000000000000, 1.000000000000000000 ) ) ;
#53439=CARTESIAN_POINT ( 'NONE',  ( 31.21759734847655210, 387.2566916973277671, 24.99345285570965913 ) ) ;
#53448=FACE_OUTER_BOUND ( 'NONE', #48354, .T. ) ;
#53451=B_SPLINE_CURVE_WITH_KNOTS ( 'NONE', 3,
 ( #83891, #93593, #91984, #100606 ),
 .UNSPECIFIED., .F., .F.,
 ( 4, 4 ),
 ( 0.0009672625908194888017, 0.02103544345022531625 ),
 .UNSPECIFIED. ) ;
#53459=CARTESIAN_POINT ( 'NONE',  ( -33.13096700376747350, 488.4252353400770517, 9.689492806026361649 ) ) ;
#53473=CARTESIAN_POINT ( 'NONE',  ( 40.96169049688617037, 435.9986040634733513, 6.367590718067603461 ) ) ;
#53482=CARTESIAN_POINT ( 'NONE',  ( -41.72774289522170221, 484.6318496107492138, -3.104024719548849731 ) ) ;
#53495=EDGE_CURVE ( 'NONE', #15460, #81556, #29996, .T. ) ;
#53500=CARTESIAN_POINT ( 'NONE',  ( 15.67124661040751299, 294.5587369836088101, -10.06229308860519467 ) ) ;
#53504=ORIENTED_EDGE ( 'NONE', *, *, #58597, .T. ) ;
#53505=CARTESIAN_POINT ( 'NONE',  ( -36.89244916174478561, 490.9813517997146164, 12.46623585235509601 ) ) ;
#53506=EDGE_CURVE ( 'NONE', #20836, #68326, #66763, .T. ) ;
#53514=( BOUNDED_SURFACE ( )  B_SPLINE_SURFACE ( 3, 2, ( 
 ( #99226, #18900, #91178 ),
 ( #82532, #91697, #90629 ),
 ( #8635, #42595, #500 ),
 ( #92744, #8100, #41011 ) ),
 .UNSPECIFIED., .F., .F., .F. ) 
 B_SPLINE_SURFACE_WITH_KNOTS ( ( 4, 4 ),
 ( 3, 3 ),
 ( -1.569924745759010420E-16, 0.0002622513198881918023 ),
 ( 0.000000000000000000, 1.000000000000000000 ),
 .UNSPECIFIED. ) 
 GEOMETRIC_REPRESENTATION_ITEM ( )  RATIONAL_B_SPLINE_SURFACE ( (
 ( 1.000000000000000000, 0.7874655377939425716, 1.000000000000000000),
 ( 1.000000000000000000, 0.7887353030063650738, 1.000000000000000000),
 ( 1.000000000000000000, 0.7900011776560427190, 1.000000000000000000),
 ( 1.000000000000000000, 0.7912633096139881639, 1.000000000000000000) ) ) 
 REPRESENTATION_ITEM ( '' )  SURFACE ( )  );
#53529=CARTESIAN_POINT ( 'NONE',  ( -12.12010901803227192, 302.5867799420356619, 9.880676471810863504 ) ) ;
#53535=DIRECTION ( 'NONE',  ( -0.9488877907218322694, 0.1950364375161481589, -0.2481385674578820699 ) ) ;
#53539=EDGE_CURVE ( 'NONE', #100925, #45269, #17864, .T. ) ;
#53554=CARTESIAN_POINT ( 'NONE',  ( -41.71039089156239044, 485.6269440496943730, -4.295528331867323857 ) ) ;
#53556=CARTESIAN_POINT ( 'NONE',  ( 36.61859841430800344, 369.8167902991359028, 3.938666744591956981 ) ) ;
#53558=CARTESIAN_POINT ( 'NONE',  ( 32.84237740334679501, 485.2251842821274295, 5.746442123022993620 ) ) ;
#53575=CARTESIAN_POINT ( 'NONE',  ( -26.97491686565329161, 307.4599153070161606, -9.420584459367196573 ) ) ;
#53577=CARTESIAN_POINT ( 'NONE',  ( -43.75010090113831751, 464.8337800386757408, 11.75004750935459263 ) ) ;
#53578=CARTESIAN_POINT ( 'NONE',  ( -41.15811204217362018, 436.5847606186492840, 6.466625614335570482 ) ) ;
#53581=CARTESIAN_POINT ( 'NONE',  ( -34.88900972249390975, 464.6206820655984302, 18.69027339340992455 ) ) ;
#53586=CYLINDRICAL_SURFACE ( 'NONE', #104823, 5.000000000000000888 ) ;
#53598=CARTESIAN_POINT ( 'NONE',  ( 32.84724555423649406, 479.6954591023948637, 7.498461155472820217 ) ) ;
#53601=CARTESIAN_POINT ( 'NONE',  ( -44.21332904831282917, 435.2494715644501184, 14.45449769377396976 ) ) ;
#53610=VERTEX_POINT ( 'NONE', #64181 ) ;
#53613=CARTESIAN_POINT ( 'NONE',  ( 0.000000000000000000, 274.9999999999999432, -7.999999999999986677 ) ) ;
#53616=DIRECTION ( 'NONE',  ( 0.000000000000000000, 0.000000000000000000, -1.000000000000000000 ) ) ;
#53620=CARTESIAN_POINT ( 'NONE',  ( -43.97892253343325564, 485.8746234537493365, 4.637105959633198715 ) ) ;
#53624=CARTESIAN_POINT ( 'NONE',  ( 33.74362713068861552, 463.9326864247046274, 7.533159870298661076 ) ) ;
#53626=CARTESIAN_POINT ( 'NONE',  ( 41.50820411079202898, 461.5963371455317770, 2.703439750996501800 ) ) ;
#53649=ORIENTED_EDGE ( 'NONE', *, *, #42711, .F. ) ;
#53650=CARTESIAN_POINT ( 'NONE',  ( 35.42407507202594275, 370.4409409265608133, 4.769248333007578999 ) ) ;
#53657=DIRECTION ( 'NONE',  ( -1.000000000000000000, 0.000000000000000000, 0.000000000000000000 ) ) ;
#53660=ORIENTED_EDGE ( 'NONE', *, *, #75133, .T. ) ;
#53666=ORIENTED_EDGE ( 'NONE', *, *, #89658, .F. ) ;
#53671=CARTESIAN_POINT ( 'NONE',  ( 37.40222091011669647, 356.7670940962378836, 2.253866884981312602 ) ) ;
#53672=CARTESIAN_POINT ( 'NONE',  ( 38.85838656119408085, 485.2519550107940063, -4.251882965831066841 ) ) ;
#53676=CARTESIAN_POINT ( 'NONE',  ( 32.17889379758944557, 439.3695696554026995, 23.63219374846804044 ) ) ;
#53679=CARTESIAN_POINT ( 'NONE',  ( 43.68138489372805822, 484.4283016034004277, 2.027755642628115140 ) ) ;
#53688=ORIENTED_EDGE ( 'NONE', *, *, #46273, .F. ) ;
#53696=UNCERTAINTY_MEASURE_WITH_UNIT (LENGTH_MEASURE( 1.000000000000000082E-05 ), #57945, 'distance_accuracy_value', 'NONE');
#53710=EDGE_CURVE ( 'NONE', #82451, #57189, #7541, .T. ) ;
#53731=CARTESIAN_POINT ( 'NONE',  ( 31.79718767439307925, 436.0559061093508149, 18.03304884062774249 ) ) ;
#53732=CARTESIAN_POINT ( 'NONE',  ( 28.10695518871528265, 297.0756177938578730, 10.42354765638709502 ) ) ;
#53733=CARTESIAN_POINT ( 'NONE',  ( 9.970195021754669540, 302.6460196488382053, -10.04373974541433689 ) ) ;
#53751=CARTESIAN_POINT ( 'NONE',  ( 44.14911905790283697, 464.3766534542007207, 9.623404994951284763 ) ) ;
#53767=CARTESIAN_POINT ( 'NONE',  ( -32.19136361712720884, 464.6890450778107038, 10.76797718186653974 ) ) ;
#53781=CARTESIAN_POINT ( 'NONE',  ( 42.72730916065222573, 485.8496625309479668, 7.279181987626980543 ) ) ;
#53788=CARTESIAN_POINT ( 'NONE',  ( 32.74748809522914428, 438.8765027064216042, 23.82522251964440585 ) ) ;
#53797=CARTESIAN_POINT ( 'NONE',  ( 26.97263248440125238, 311.5055359114008979, 10.53075476637147823 ) ) ;
#53798=CARTESIAN_POINT ( 'NONE',  ( -40.09057539293822714, 460.7411201710883688, 2.126307971704060495 ) ) ;
#53813=ORIENTED_EDGE ( 'NONE', *, *, #93690, .T. ) ;
#53820=ORIENTED_EDGE ( 'NONE', *, *, #82191, .T. ) ;
#53833=EDGE_LOOP ( 'NONE', ( #12375, #100619, #103437, #28676 ) ) ;
#53835=CARTESIAN_POINT ( 'NONE',  ( 43.71037717921923615, 462.3391554988761527, 4.824299547763561513 ) ) ;
#53848=CARTESIAN_POINT ( 'NONE',  ( 40.95803508205418808, 397.0725699660951591, 27.65389706927792446 ) ) ;
#53851=CARTESIAN_POINT ( 'NONE',  ( -40.06570913992068483, 460.7366702961384703, 2.123561850759500214 ) ) ;
#53861=CARTESIAN_POINT ( 'NONE',  ( -29.99619012559378461, 316.1192097185598300, 13.18038979099694252 ) ) ;
#53866=CARTESIAN_POINT ( 'NONE',  ( 39.84523985364286602, 437.5033382181499064, 4.901783744328642278 ) ) ;
#53882=CARTESIAN_POINT ( 'NONE',  ( 8.823089264674861099, 295.7038567688685475, -10.03557449693187564 ) ) ;
#53883=CARTESIAN_POINT ( 'NONE',  ( 40.95595929481465447, 405.2208686710653183, 27.85131585683114963 ) ) ;
#53885=CARTESIAN_POINT ( 'NONE',  ( 41.71937287857456056, 325.3183896825876786, 5.429541239482419179 ) ) ;
#53893=CARTESIAN_POINT ( 'NONE',  ( 46.00000000000000711, 488.0062820891759543, 1.479102482845579658 ) ) ;
#53896=CARTESIAN_POINT ( 'NONE',  ( 0.000000000000000000, 37.86482112153537116, -10.52123582012687919 ) ) ;
#53901=CARTESIAN_POINT ( 'NONE',  ( -44.49616267108482504, 470.0857873864311500, 4.037868210216608134 ) ) ;
#53904=CARTESIAN_POINT ( 'NONE',  ( -30.00000000000000000, 461.8163627757383551, 11.11111419091028729 ) ) ;
#53906=ORIENTED_EDGE ( 'NONE', *, *, #19572, .T. ) ;
#53920=ORIENTED_EDGE ( 'NONE', *, *, #57357, .T. ) ;
#53925=CARTESIAN_POINT ( 'NONE',  ( 44.14911905790289381, 464.3766534542008344, 9.623404994951240354 ) ) ;
#53944=CARTESIAN_POINT ( 'NONE',  ( -40.07586470527510158, 337.7832441655235129, 20.21182470898328631 ) ) ;
#53950=ORIENTED_EDGE ( 'NONE', *, *, #783, .T. ) ;
#53962=FACE_OUTER_BOUND ( 'NONE', #105127, .T. ) ;
#53982=ORIENTED_EDGE ( 'NONE', *, *, #33997, .T. ) ;
#53986=EDGE_LOOP ( 'NONE', ( #90653, #52097, #65305, #18549 ) ) ;
#53987=CARTESIAN_POINT ( 'NONE',  ( -36.34301548518092062, 333.8034728139880372, -2.455839358024256569 ) ) ;
#53992=CARTESIAN_POINT ( 'NONE',  ( 0.000000000000000000, 273.9999999999999432, 0.000000000000000000 ) ) ;
#53996=EDGE_CURVE ( 'NONE', #88846, #97550, #67690, .T. ) ;
#54006=CARTESIAN_POINT ( 'NONE',  ( 46.00000000000000000, 437.9690125970931831, 14.09127711025711349 ) ) ;
#54027=CARTESIAN_POINT ( 'NONE',  ( 43.43869229197127169, 464.9661605157749591, 13.42065392471465834 ) ) ;
#54048=CARTESIAN_POINT ( 'NONE',  ( -32.94352307842197547, 463.6326549538489985, 6.941370215387414611 ) ) ;
#54052=DIRECTION ( 'NONE',  ( -1.000000000000000000, -0.000000000000000000, -0.000000000000000000 ) ) ;
#54065=CARTESIAN_POINT ( 'NONE',  ( 39.57869015843260740, 437.2512761492686195, 5.285341955750249454 ) ) ;
#54067=CARTESIAN_POINT ( 'NONE',  ( 33.81356276710358344, 316.6001882432930188, -6.691973795892937282 ) ) ;
#54078=FACE_OUTER_BOUND ( 'NONE', #24768, .T. ) ;
#54083=CARTESIAN_POINT ( 'NONE',  ( -33.00000000000000000, 463.5362553048592531, 6.739467187734380360 ) ) ;
#54092=CARTESIAN_POINT ( 'NONE',  ( -43.50718830201091691, 484.7945958152782282, 4.126963862728817212 ) ) ;
#54099=VERTEX_POINT ( 'NONE', #32760 ) ;
#54100=CARTESIAN_POINT ( 'NONE',  ( 33.33990657616778464, 464.2315420232596921, 17.97851960990114151 ) ) ;
#54108=ORIENTED_EDGE ( 'NONE', *, *, #74995, .F. ) ;
#54109=AXIS2_PLACEMENT_3D ( 'NONE', #46279, #74778, #42423 ) ;
#54115=ORIENTED_EDGE ( 'NONE', *, *, #57720, .T. ) ;
#54126=( BOUNDED_SURFACE ( )  B_SPLINE_SURFACE ( 3, 2, ( 
 ( #37620, #3625, #70483 ),
 ( #29525, #30567, #79092 ),
 ( #22489, #106001, #105488 ),
 ( #14872, #96873, #87203 ) ),
 .UNSPECIFIED., .F., .F., .T. ) 
 B_SPLINE_SURFACE_WITH_KNOTS ( ( 4, 4 ),
 ( 3, 3 ),
 ( -3.035766082959412415E-18, 0.002033478645168744405 ),
 ( 0.000000000000000000, 1.000000000000000000 ),
 .UNSPECIFIED. ) 
 GEOMETRIC_REPRESENTATION_ITEM ( )  RATIONAL_B_SPLINE_SURFACE ( (
 ( 1.000000000000000000, 0.8239349643288668146, 1.000000000000000000),
 ( 1.000000000000000000, 0.8158483196103311075, 1.000000000000000000),
 ( 1.000000000000000000, 0.8066624588212628622, 1.000000000000000000),
 ( 1.000000000000000000, 0.7976994903569351036, 1.000000000000000000) ) ) 
 REPRESENTATION_ITEM ( '' )  SURFACE ( )  );
#54133=CIRCLE ( 'NONE', #100659, 12.00000000000001066 ) ;
#54135=VERTEX_POINT ( 'NONE', #39777 ) ;
#54147=CARTESIAN_POINT ( 'NONE',  ( 32.99999999999997868, 439.0771093100264011, 24.89389206971034341 ) ) ;
#54157=CARTESIAN_POINT ( 'NONE',  ( 33.35361065611909481, 318.9767138392345487, -6.332425068735285656 ) ) ;
#54158=CARTESIAN_POINT ( 'NONE',  ( -3.493042281569127550, 304.8518027749427119, -10.00000000028269298 ) ) ;
#54161=CARTESIAN_POINT ( 'NONE',  ( 32.99999999999962341, 465.3568906370355762, 17.69306951624823654 ) ) ;
#54167=DIRECTION ( 'NONE',  ( 0.000000000000000000, -0.9405207353770788092, 0.3397362893859868782 ) ) ;
#54184=CARTESIAN_POINT ( 'NONE',  ( 42.85049267684065910, 321.7985655941586174, -3.456638000609795647 ) ) ;
#54195=CARTESIAN_POINT ( 'NONE',  ( -44.00767003729956883, 435.4943399909807340, 9.943675474308832918 ) ) ;
#54207=CARTESIAN_POINT ( 'NONE',  ( 33.95156263172585653, 464.5083255208626838, 6.608064661821390295 ) ) ;
#54221=ORIENTED_EDGE ( 'NONE', *, *, #3504, .F. ) ;
#54232=ORIENTED_EDGE ( 'NONE', *, *, #70142, .T. ) ;
#54235=CARTESIAN_POINT ( 'NONE',  ( -40.15309039158411508, 485.1828724906129082, -4.320808352504673877 ) ) ;
#54236=CARTESIAN_POINT ( 'NONE',  ( 7.737898857161403576, 302.4298210949973509, -10.02991386142804231 ) ) ;
#54239=FACE_OUTER_BOUND ( 'NONE', #92124, .T. ) ;
#54241=CARTESIAN_POINT ( 'NONE',  ( -42.68083702883377839, 436.2686870323770449, 7.148029379848837905 ) ) ;
#54244=ORIENTED_EDGE ( 'NONE', *, *, #53710, .F. ) ;
#54249=FACE_OUTER_BOUND ( 'NONE', #82041, .T. ) ;
#54251=MECHANICAL_DESIGN_GEOMETRIC_PRESENTATION_REPRESENTATION('',(#35371),#81817);
#54252=FACE_OUTER_BOUND ( 'NONE', #95799, .T. ) ;
#54262=CARTESIAN_POINT ( 'NONE',  ( 34.17980567228813271, 435.1524039838096201, 10.79291224410167338 ) ) ;
#54263=( BOUNDED_SURFACE ( )  B_SPLINE_SURFACE ( 3, 2, ( 
 ( #46301, #45765, #12322 ),
 ( #102944, #28553, #70581 ),
 ( #11786, #79190, #78126 ),
 ( #77605, #20493, #22041 ),
 ( #45247, #78641, #53331 ),
 ( #103988, #53848, #54352 ),
 ( #4245, #86779, #61434 ),
 ( #29108, #12848, #38234 ),
 ( #4779, #52787, #44716 ),
 ( #103468, #71098, #29617 ),
 ( #86250, #3723, #11247 ),
 ( #94330, #30132, #60898 ),
 ( #63018, #95916, #62489 ),
 ( #3179, #28029, #54897 ),
 ( #95380, #68994, #21518 ),
 ( #44176, #77065, #101869 ),
 ( #93788, #36653, #19947 ),
 ( #65666, #55942, #88881 ),
 ( #88359, #6888, #56492 ),
 ( #14970, #47867, #5827 ),
 ( #13907, #55426, #30673 ),
 ( #105069, #48403, #81293 ),
 ( #105584, #80773, #38748 ),
 ( #64610, #31724, #98547 ),
 ( #81819, #96970, #32249 ),
 ( #106641, #32792, #14435 ),
 ( #24698, #97479, #46821 ),
 ( #89421, #23634, #39809 ),
 ( #89936, #15513, #72683 ),
 ( #7409, #39283, #40322 ),
 ( #47345, #57022, #73199 ),
 ( #106101, #72161, #65130 ),
 ( #16043, #7943, #48923 ),
 ( #98026, #24178, #40849 ),
 ( #73742, #87828, #79718 ),
 ( #71617, #104519, #63559 ),
 ( #96452, #22589, #80237 ),
 ( #6341, #31209, #64094 ),
 ( #23105, #18200, #67794 ),
 ( #50521, #82374, #83971 ),
 ( #75337, #68332, #57548 ),
 ( #41914, #2513, #50006 ),
 ( #83436, #1438, #90469 ),
 ( #26320, #16581, #99615 ),
 ( #58648, #33319, #59717 ),
 ( #91550, #99072, #9534 ),
 ( #10082, #74800, #25236 ),
 ( #17658, #92592, #67275 ),
 ( #9008, #75879, #42446 ),
 ( #51597, #18748, #42991 ),
 ( #34399, #100155, #59181 ),
 ( #1979, #8481, #92060 ),
 ( #84516, #66191, #49467 ),
 ( #10605, #66731, #34926 ),
 ( #882, #100680, #33859 ),
 ( #51054, #26846, #43523 ),
 ( #76399, #58093, #91022 ),
 ( #35460, #101229, #41386 ),
 ( #74277, #17128, #351 ),
 ( #25792, #82911, #11126 ),
 ( #94748, #20898, #53210 ),
 ( #78530, #70458, #94200 ),
 ( #3055, #53732, #37056 ),
 ( #12730, #45133, #44596 ),
 ( #61851, #68877, #86660 ),
 ( #103355, #77486, #3598 ),
 ( #101750, #102282, #86130 ),
 ( #36535, #69400, #19304 ),
 ( #27384, #36005, #44052 ),
 ( #27920, #20370, #45653 ),
 ( #28430, #60783, #93673 ),
 ( #4661, #12203, #28985 ),
 ( #19824, #60264, #78010 ),
 ( #61311, #4127, #52659 ),
 ( #69924, #85590, #37595 ),
 ( #29503, #93133, #102823 ),
 ( #11664, #52128, #85044 ),
 ( #76942, #51393, #91868 ),
 ( #27170, #50330, #51925 ),
 ( #101555, #17993, #50854 ) ),
 .UNSPECIFIED., .F., .F., .F. ) 
 B_SPLINE_SURFACE_WITH_KNOTS ( ( 4, 2, 2, 2, 2, 2, 2, 2, 2, 2, 2, 2, 2, 2, 2, 2, 2, 2, 2, 2, 2, 2, 2, 2, 2, 2, 2, 2, 2, 2, 2, 2, 2, 2, 2, 2, 2, 2, 2, 4 ),
 ( 3, 3 ),
 ( 0.07172314469012842919, 0.08973265255323484291, 0.1077421604163412705, 0.1257516682794476703, 0.1347564222110008703, 0.1437611761425540979, 0.1617706840056605255, 0.1707754379372137254, 0.1797801918687669254, 0.1820313803516552253, 0.1842825688345435253, 0.1887849458003201253, 0.1932873227660967252, 0.1955385112489850252, 0.1977896997318733252, 0.1989152939733174752, 0.1994780910940395502, 0.2000408882147616252, 0.2022920766976499252, 0.2045432651805382251, 0.2051060623012603001, 0.2053874608616213515, 0.2056688594219823751, 0.2067944536634265251, 0.2079200479048706751, 0.2080607471850511869, 0.2082014464652316987, 0.2084828450255927501, 0.2090456421463148251, 0.2101712363877589751, 0.2104526349481199987, 0.2107340335084810501, 0.2112968306292031251, 0.2124224248706472751, 0.2129852219913693501, 0.2130555716314596060, 0.2131259212715498896, 0.2132666205517304014, 0.2135480191120914251, 0.2157992075949797528 ),
 ( 0.000000000000000000, 1.000000000000000000 ),
 .UNSPECIFIED. ) 
 GEOMETRIC_REPRESENTATION_ITEM ( )  RATIONAL_B_SPLINE_SURFACE ( (
 ( 1.000000000000000000, 0.7071066916777324352, 1.000000000000000000),
 ( 1.000000000000000000, 0.7071066384723879716, 1.000000000000000000),
 ( 1.000000000000000000, 0.7071067819036740421, 1.000000000000000000),
 ( 1.000000000000000000, 0.7071067819036740421, 1.000000000000000000),
 ( 1.000000000000000000, 0.7071067821253883556, 1.000000000000000000),
 ( 1.000000000000000000, 0.7071067821253883556, 1.000000000000000000),
 ( 1.000000000000000000, 0.7071082347912200916, 1.000000000000000000),
 ( 1.000000000000000000, 0.7071090860269371170, 1.000000000000000000),
 ( 1.000000000000000000, 0.7071085999063239091, 1.000000000000000000),
 ( 1.000000000000000000, 0.7071071393025897267, 1.000000000000000000),
 ( 1.000000000000000000, 0.7071064603873742360, 1.000000000000000000),
 ( 1.000000000000000000, 0.7071084468636777975, 1.000000000000000000),
 ( 1.000000000000000000, 0.7071099459167716761, 1.000000000000000000),
 ( 1.000000000000000000, 0.7071070620195699652, 1.000000000000000000),
 ( 1.000000000000000000, 0.7071067638254444621, 1.000000000000000000),
 ( 1.000000000000000000, 0.7071094983174432969, 1.000000000000000000),
 ( 1.000000000000000000, 0.7071073521351076696, 1.000000000000000000),
 ( 1.000000000000000000, 0.7071067110094644281, 1.000000000000000000),
 ( 1.000000000000000000, 0.7071074718365022438, 1.000000000000000000),
 ( 1.000000000000000000, 0.7071137944410639253, 1.000000000000000000),
 ( 1.000000000000000000, 0.7071181761060342241, 1.000000000000000000),
 ( 1.000000000000000000, 0.7071288868279509421, 1.000000000000000000),
 ( 1.000000000000000000, 0.7071314869358752420, 1.000000000000000000),
 ( 1.000000000000000000, 0.7071211158780618122, 1.000000000000000000),
 ( 1.000000000000000000, 0.7071075228484042796, 1.000000000000000000),
 ( 1.000000000000000000, 0.7071064472611667817, 1.000000000000000000),
 ( 1.000000000000000000, 0.7071094939932405232, 1.000000000000000000),
 ( 1.000000000000000000, 0.7071117979890746419, 1.000000000000000000),
 ( 1.000000000000000000, 0.7071112387139774080, 1.000000000000000000),
 ( 1.000000000000000000, 0.7071089882604711940, 1.000000000000000000),
 ( 1.000000000000000000, 0.7071080815320003321, 1.000000000000000000),
 ( 1.000000000000000000, 0.7071071532410159177, 1.000000000000000000),
 ( 1.000000000000000000, 0.7071069183921528944, 1.000000000000000000),
 ( 1.000000000000000000, 0.7071067316882134746, 1.000000000000000000),
 ( 1.000000000000000000, 0.7071072160745824897, 1.000000000000000000),
 ( 1.000000000000000000, 0.7071281552871109266, 1.000000000000000000),
 ( 1.000000000000000000, 0.7071788308493717201, 1.000000000000000000),
 ( 1.000000000000000000, 0.7072040914959526470, 1.000000000000000000),
 ( 1.000000000000000000, 0.7071729554399738271, 1.000000000000000000),
 ( 1.000000000000000000, 0.7071271541534743799, 1.000000000000000000),
 ( 1.000000000000000000, 0.7071184695976129309, 1.000000000000000000),
 ( 1.000000000000000000, 0.7071100320398184813, 1.000000000000000000),
 ( 1.000000000000000000, 0.7071080004622726234, 1.000000000000000000),
 ( 1.000000000000000000, 0.7071063588341449657, 1.000000000000000000),
 ( 1.000000000000000000, 0.7071068098800528112, 1.000000000000000000),
 ( 1.000000000000000000, 0.7071083434742995166, 1.000000000000000000),
 ( 1.000000000000000000, 0.7071118442609979349, 1.000000000000000000),
 ( 1.000000000000000000, 0.7071122315782686352, 1.000000000000000000),
 ( 1.000000000000000000, 0.7071084657487585190, 1.000000000000000000),
 ( 1.000000000000000000, 0.7071069086593241293, 1.000000000000000000),
 ( 1.000000000000000000, 0.7071067970953980319, 1.000000000000000000),
 ( 1.000000000000000000, 0.7071067683750767996, 1.000000000000000000),
 ( 1.000000000000000000, 0.7071066806290805529, 1.000000000000000000),
 ( 1.000000000000000000, 0.7071060773180442016, 1.000000000000000000),
 ( 1.000000000000000000, 0.7071053327435640190, 1.000000000000000000),
 ( 1.000000000000000000, 0.7071028992638964672, 1.000000000000000000),
 ( 1.000000000000000000, 0.7071010927699721282, 1.000000000000000000),
 ( 1.000000000000000000, 0.7070987750015783613, 1.000000000000000000),
 ( 1.000000000000000000, 0.7071026859636611039, 1.000000000000000000),
 ( 1.000000000000000000, 0.7071061702207726007, 1.000000000000000000),
 ( 1.000000000000000000, 0.7071067000110781153, 1.000000000000000000),
 ( 1.000000000000000000, 0.7071068455174084333, 1.000000000000000000),
 ( 1.000000000000000000, 0.7071077971994959022, 1.000000000000000000),
 ( 1.000000000000000000, 0.7071127875002619634, 1.000000000000000000),
 ( 1.000000000000000000, 0.7071176651463569884, 1.000000000000000000),
 ( 1.000000000000000000, 0.7071258132918983863, 1.000000000000000000),
 ( 1.000000000000000000, 0.7071208017052891259, 1.000000000000000000),
 ( 1.000000000000000000, 0.7071102148083360239, 1.000000000000000000),
 ( 1.000000000000000000, 0.7071068024654432183, 1.000000000000000000),
 ( 1.000000000000000000, 0.7071067786309011005, 1.000000000000000000),
 ( 1.000000000000000000, 0.7071068737807520987, 1.000000000000000000),
 ( 1.000000000000000000, 0.7071072399035752687, 1.000000000000000000),
 ( 1.000000000000000000, 0.7071075080362204668, 1.000000000000000000),
 ( 1.000000000000000000, 0.7071085168092843265, 1.000000000000000000),
 ( 1.000000000000000000, 0.7071094604126808569, 1.000000000000000000),
 ( 1.000000000000000000, 0.7071127524153103527, 1.000000000000000000),
 ( 1.000000000000000000, 0.7071155430753355287, 1.000000000000000000),
 ( 1.000000000000000000, 0.7071398610474239899, 1.000000000000000000),
 ( 1.000000000000000000, 0.7071223203621870290, 1.000000000000000000),
 ( 1.000000000000000000, 0.7071067811865479058, 1.000000000000000000) ) ) 
 REPRESENTATION_ITEM ( '' )  SURFACE ( )  );
#54266=CARTESIAN_POINT ( 'NONE',  ( -32.17646412119387378, 464.6980787822280377, 10.84896803612861227 ) ) ;
#54274=EDGE_CURVE ( 'NONE', #35120, #61182, #94580, .T. ) ;
#54277=CARTESIAN_POINT ( 'NONE',  ( 38.94709829052286665, 485.6592143718137891, -4.427571171338303913 ) ) ;
#54278=CARTESIAN_POINT ( 'NONE',  ( 42.10086803841213765, 435.6552064019005570, 19.95582312411065828 ) ) ;
#54283=CARTESIAN_POINT ( 'NONE',  ( 40.53597741959072920, 485.1143729953953994, -4.195250914663321673 ) ) ;
#54285=B_SPLINE_CURVE_WITH_KNOTS ( 'NONE', 3,
 ( #55254, #54719, #27990, #5655 ),
 .UNSPECIFIED., .F., .F.,
 ( 4, 4 ),
 ( 0.000000000000000000, 0.001193002000561244275 ),
 .UNSPECIFIED. ) ;
#54287=CARTESIAN_POINT ( 'NONE',  ( 42.61340452791776556, 486.8925439250688783, 7.464118458850346194 ) ) ;
#54291=CARTESIAN_POINT ( 'NONE',  ( 32.45420636192083919, 439.3281579392075855, 23.70224716321920511 ) ) ;
#54292=CARTESIAN_POINT ( 'NONE',  ( -34.62906189774859200, 434.6650141781096295, 8.921436296112648989 ) ) ;
#54300=CARTESIAN_POINT ( 'NONE',  ( -28.61915886549734367, 318.3715675768729056, 12.26331061709428205 ) ) ;
#54305=ORIENTED_EDGE ( 'NONE', *, *, #98498, .F. ) ;
#54331=CARTESIAN_POINT ( 'NONE',  ( 46.00000000000000000, 459.9277931459794786, 6.461582622334601567 ) ) ;
#54343=EDGE_CURVE ( 'NONE', #4192, #68930, #4014, .T. ) ;
#54344=CARTESIAN_POINT ( 'NONE',  ( 3.364021409948656505, 294.8518027753228807, 9.936999415087239385 ) ) ;
#54352=CARTESIAN_POINT ( 'NONE',  ( 42.78192394157753142, 397.2994584770452775, 19.86614811632973598 ) ) ;
#54357=ORIENTED_EDGE ( 'NONE', *, *, #32190, .T. ) ;
#54364=CARTESIAN_POINT ( 'NONE',  ( -33.40011937205945713, 300.9684309835628824, 3.319491984095645609 ) ) ;
#54383=EDGE_CURVE ( 'NONE', #80103, #72660, #9147, .T. ) ;
#54392=CARTESIAN_POINT ( 'NONE',  ( 42.99999999999997158, 487.9285348210859752, 8.903916466042435474 ) ) ;
#54400=ORIENTED_EDGE ( 'NONE', *, *, #15396, .T. ) ;
#54403=CIRCLE ( 'NONE', #39058, 1.000000000000002887 ) ;
#54408=B_SPLINE_CURVE_WITH_KNOTS ( 'NONE', 3,
 ( #16528, #18148, #17611, #26794 ),
 .UNSPECIFIED., .F., .F.,
 ( 4, 4 ),
 ( 1.430489624538199204E-17, 0.001025896622541432783 ),
 .UNSPECIFIED. ) ;
#54429=FACE_OUTER_BOUND ( 'NONE', #64970, .T. ) ;
#54431=ORIENTED_EDGE ( 'NONE', *, *, #97106, .F. ) ;
#54456=CARTESIAN_POINT ( 'NONE',  ( -38.68218982724705057, 320.0845437455996603, 16.10279619727025135 ) ) ;
#54481=CARTESIAN_POINT ( 'NONE',  ( -32.10935363747667992, 436.4604647151550125, 19.52607623436714235 ) ) ;
#54483=CARTESIAN_POINT ( 'NONE',  ( -32.94539137533611495, 488.0149952105289799, 9.145905951731817751 ) ) ;
#54489=CARTESIAN_POINT ( 'NONE',  ( -33.79918201874539818, 300.9799874190337050, -0.6176716706728464512 ) ) ;
#54496=CARTESIAN_POINT ( 'NONE',  ( 46.00000000000000000, 438.4646224975062978, 9.895601460515761616 ) ) ;
#54509=CARTESIAN_POINT ( 'NONE',  ( -34.79310559888947552, 439.9468627087276786, 24.33501443703186595 ) ) ;
#54511=CARTESIAN_POINT ( 'NONE',  ( -37.61437702004904793, 372.0126153848854074, 4.442514472280413962 ) ) ;
#54513=DIRECTION ( 'NONE',  ( 1.000000000000000000, -0.000000000000000000, -0.000000000000000000 ) ) ;
#54514=DIRECTION ( 'NONE',  ( 0.000000000000000000, 0.000000000000000000, 1.000000000000000000 ) ) ;
#54520=CARTESIAN_POINT ( 'NONE',  ( -5.286264417172181318, 298.2069408986629355, 8.503413131156435156 ) ) ;
#54523=CARTESIAN_POINT ( 'NONE',  ( 34.86892506086162058, 473.1724825694047354, 16.84267233553793730 ) ) ;
#54526=CARTESIAN_POINT ( 'NONE',  ( 9.789044728060206424, 294.6486233851416614, -2.043184600578050070 ) ) ;
#54527=DIRECTION ( 'NONE',  ( -0.9133097175882186614, 0.1295276157526884797, -0.3861190962855272080 ) ) ;
#54561=( BOUNDED_SURFACE ( )  B_SPLINE_SURFACE ( 3, 3, ( 
 ( #55993, #87351, #104038, #80286 ),
 ( #94920, #86826, #63613, #15025 ),
 ( #96502, #12895, #72730, #21057 ),
 ( #78696, #6399, #95427, #55472 ),
 ( #53896, #72215, #88934, #14480 ),
 ( #31773, #39334, #79766, #63069 ) ),
 .UNSPECIFIED., .F., .F., .F. ) 
 B_SPLINE_SURFACE_WITH_KNOTS ( ( 4, 1, 1, 4 ),
 ( 4, 4 ),
 ( 0.000000000000000000, 0.4213833399777465738, 0.5213833399777465516, 0.9843640123765011740 ),
 ( 0.000000000000000000, 1.000000000000000000 ),
 .UNSPECIFIED. ) 
 GEOMETRIC_REPRESENTATION_ITEM ( )  RATIONAL_B_SPLINE_SURFACE ( (
 ( 1.000000000000000000, 0.3333333333333334259, 0.3333333333333334259, 1.000000000000000000),
 ( 1.000000000000000000, 0.3333333333333334259, 0.3333333333333334259, 1.000000000000000000),
 ( 1.000000000000000000, 0.3333333333333334259, 0.3333333333333334259, 1.000000000000000000),
 ( 1.000000000000000000, 0.3333333333333334259, 0.3333333333333334259, 1.000000000000000000),
 ( 1.000000000000000000, 0.3333333333333334259, 0.3333333333333334259, 1.000000000000000000),
 ( 1.000000000000000000, 0.3333333333333334259, 0.3333333333333334259, 1.000000000000000000) ) ) 
 REPRESENTATION_ITEM ( '' )  SURFACE ( )  );
#54563=DIRECTION ( 'NONE',  ( 1.000000000000000000, -0.000000000000000000, -0.000000000000000000 ) ) ;
#54566=CARTESIAN_POINT ( 'NONE',  ( -31.96880777819857045, 486.7849213999251674, 6.761697820930809399 ) ) ;
#54584=CARTESIAN_POINT ( 'NONE',  ( -40.66024587926896317, 485.8034863302605686, -4.843677042986813674 ) ) ;
#54586=CARTESIAN_POINT ( 'NONE',  ( 36.36817526240515974, 355.1924107066273564, 1.711800795617328674 ) ) ;
#54588=CARTESIAN_POINT ( 'NONE',  ( 32.10528697966002909, 486.1671898930081852, 5.449875171707255106 ) ) ;
#54593=EDGE_CURVE ( 'NONE', #37271, #29166, #75761, .T. ) ;
#54594=CARTESIAN_POINT ( 'NONE',  ( 30.49216875706506613, 308.5483047407621484, -8.695710891432577583 ) ) ;
#54603=ORIENTED_EDGE ( 'NONE', *, *, #81449, .T. ) ;
#54625=CIRCLE ( 'NONE', #4692, 5.000000000000000888 ) ;
#54654=DIRECTION ( 'NONE',  ( 0.000000000000000000, -0.9846968979781752784, 0.1742756985702797745 ) ) ;
#54663=DIRECTION ( 'NONE',  ( -0.9576481418713199689, -0.1523715402840224442, 0.2443214073344433801 ) ) ;
#54679=EDGE_CURVE ( 'NONE', #337, #104099, #102171, .T. ) ;
#54681=ADVANCED_FACE ( 'NONE', ( #12237 ), #43653, .T. ) ;
#54692=CARTESIAN_POINT ( 'NONE',  ( 35.53798519183398952, 391.1361556355759603, 6.673662436208735116 ) ) ;
#54698=FACE_OUTER_BOUND ( 'NONE', #7775, .T. ) ;
#54705=CARTESIAN_POINT ( 'NONE',  ( -36.29689614689283417, 464.0084101677746844, 19.58142058293961796 ) ) ;
#54709=CARTESIAN_POINT ( 'NONE',  ( 42.51305782314333470, 484.3273291304252552, -1.912516135257525063 ) ) ;
#54715=CARTESIAN_POINT ( 'NONE',  ( 37.19218851650311564, 306.1703911487554137, 0.6387774021538068503 ) ) ;
#54719=CARTESIAN_POINT ( 'NONE',  ( 41.98109406947479272, 462.0607394890938622, 3.143716936936550965 ) ) ;
#54723=CARTESIAN_POINT ( 'NONE',  ( -33.00000000000000000, 490.5636507776930557, 7.413185101875094496 ) ) ;
#54757=ORIENTED_EDGE ( 'NONE', *, *, #58917, .T. ) ;
#54758=B_SPLINE_CURVE_WITH_KNOTS ( 'NONE', 3,
 ( #41874, #1938, #59675, #34889, #35421, #842, #103183, #100643, #26802, #92555, #18704, #84474, #27348, #80472, #39517, #21237, #29851, #7118, #22816, #6585, #87012, #54067, #38982, #37952, #97193, #31442, #13615, #88587, #54594, #13082, #72393, #5538, #96153, #70811, #64321, #71856, #104761, #38463, #63261, #103704, #46012, #62728, #78891, #14668, #46530, #5018, #72908, #71330, #22286, #105297, #96678, #23339 ),
 .UNSPECIFIED., .F., .F.,
 ( 4, 2, 2, 2, 2, 2, 2, 2, 2, 2, 2, 2, 2, 2, 2, 2, 2, 2, 2, 2, 2, 2, 2, 2, 2, 4 ),
 ( 0.0004542633818371057141, 0.01826920472356173900, 0.03608414606528637103, 0.05389908740701100653, 0.06280655807787331735, 0.07171402874873562816, 0.08952897009046026366, 0.09843644076132258836, 0.1073439114321848992, 0.1162513821030472100, 0.1207051174384784625, 0.1251588527739097012, 0.1273857204416252442, 0.1296125881093407872, 0.1318394557770563302, 0.1329528896109141711, 0.1340663234447720120, 0.1351797572786298252, 0.1362931911124876661, 0.1385200587802032646, 0.1396334926140610777, 0.1407469264479188908, 0.1418603602817767317, 0.1424170771987056106, 0.1426954356571700777, 0.1429737941156345449 ),
 .UNSPECIFIED. ) ;
#54768=EDGE_CURVE ( 'NONE', #29831, #45028, #51295, .T. ) ;
#54772=DIRECTION ( 'NONE',  ( -0.3820442156493231156, 0.000000000000000000, -0.9241440457465999181 ) ) ;
#54776=EDGE_CURVE ( 'NONE', #36626, #86195, #84745, .T. ) ;
#54777=CARTESIAN_POINT ( 'NONE',  ( 3.010530670969122191, 299.5657343207403756, -10.00571837425012056 ) ) ;
#54781=CARTESIAN_POINT ( 'NONE',  ( 41.30899790313412723, 464.6556986078166460, 16.43539577153557474 ) ) ;
#54800=CARTESIAN_POINT ( 'NONE',  ( 6.632170054159806760, 303.7449822509489081, 9.914291111224208919 ) ) ;
#54803=CARTESIAN_POINT ( 'NONE',  ( 34.25394585371702050, 436.6001602354167517, 6.438439818649023039 ) ) ;
#54807=CARTESIAN_POINT ( 'NONE',  ( -37.20102314025923107, 438.1443282426989185, 4.012575796191243604 ) ) ;
#54814=CARTESIAN_POINT ( 'NONE',  ( -40.85671901238235648, 460.0093920008615100, 2.030256043170402869 ) ) ;
#54836=CARTESIAN_POINT ( 'NONE',  ( -39.24156521425334176, 307.7088117867400001, -7.003459073692002157 ) ) ;
#54846=CARTESIAN_POINT ( 'NONE',  ( -24.03059336844976457, 306.3081475125345605, 9.259463793422938238 ) ) ;
#54848=CARTESIAN_POINT ( 'NONE',  ( 19.73463816634111012, 304.7971333121959105, 8.925379062039139555 ) ) ;
#54849=CARTESIAN_POINT ( 'NONE',  ( -41.50820411079202188, 461.5963371455320612, 2.703439750996428081 ) ) ;
#54854=CARTESIAN_POINT ( 'NONE',  ( 46.00000000000000000, 488.0072389889706983, 1.487873763369907731 ) ) ;
#54867=CARTESIAN_POINT ( 'NONE',  ( 40.85671901238074355, 460.0093920008611121, 2.030256043169934799 ) ) ;
#54870=CARTESIAN_POINT ( 'NONE',  ( 42.23079339798727716, 460.7352525929352964, 2.726051457480584972 ) ) ;
#54877=( NAMED_UNIT ( * ) SI_UNIT ( $, .STERADIAN. ) SOLID_ANGLE_UNIT ( ) );
#54888=CARTESIAN_POINT ( 'NONE',  ( 20.17756551592414738, 302.8253764644769035, 1.931382329378719565 ) ) ;
#54897=CARTESIAN_POINT ( 'NONE',  ( 42.19505042255748606, 346.2110904243742198, 13.96664619797273765 ) ) ;
#54898=DIRECTION ( 'NONE',  ( -0.2276885448028014569, 0.1882482561681204369, 0.9553640775197926871 ) ) ;
#54903=CARTESIAN_POINT ( 'NONE',  ( -39.69724611604759446, 460.7042697230087356, 2.103486822546675405 ) ) ;
#54904=( BOUNDED_SURFACE ( )  B_SPLINE_SURFACE ( 3, 2, ( 
 ( #78127, #87295, #105070 ),
 ( #37718, #13908, #46302 ),
 ( #71099, #86780, #61977 ),
 ( #102946, #5315, #46822 ) ),
 .UNSPECIFIED., .F., .F., .F. ) 
 B_SPLINE_SURFACE_WITH_KNOTS ( ( 4, 4 ),
 ( 3, 3 ),
 ( -6.748074321549779597E-16, 0.001833990318204585914 ),
 ( 0.000000000000000000, 1.000000000000000000 ),
 .UNSPECIFIED. ) 
 GEOMETRIC_REPRESENTATION_ITEM ( )  RATIONAL_B_SPLINE_SURFACE ( (
 ( 1.000000000000000000, 0.7977970988453257917, 1.000000000000000000),
 ( 1.000000000000000000, 0.7897979397240961763, 1.000000000000000000),
 ( 1.000000000000000000, 0.7817839364700170934, 1.000000000000000000),
 ( 1.000000000000000000, 0.7737149417968423037, 1.000000000000000000) ) ) 
 REPRESENTATION_ITEM ( '' )  SURFACE ( )  );
#54906=EDGE_CURVE ( 'NONE', #1493, #105760, #29380, .T. ) ;
#54907=CARTESIAN_POINT ( 'NONE',  ( -43.00000000000000000, 450.0000000000002274, -1.797577426246302013 ) ) ;
#54908=CARTESIAN_POINT ( 'NONE',  ( -37.24172479535138791, 460.4836853723022614, 2.466600708395719987 ) ) ;
#54913=CARTESIAN_POINT ( 'NONE',  ( -24.95548294633412922, 304.5552599523065851, 10.31336939286802057 ) ) ;
#54918=B_SPLINE_CURVE_WITH_KNOTS ( 'NONE', 3,
 ( #101800, #70509, #103397, #27966, #62420, #87224, #60831, #21446, #52711, #43568, #85639, #11712, #23033, #38677, #5240, #30065, #48325, #46751 ),
 .UNSPECIFIED., .F., .F.,
 ( 4, 2, 2, 2, 2, 2, 2, 2, 4 ),
 ( 9.813077866773594792E-18, 0.001533449630763184185, 0.003066899261526358830, 0.004600348892289532823, 0.006133798523052707251, 0.007667248153815881678, 0.009200697784579056973, 0.01073414741534223227, 0.01226759704610540583 ),
 .UNSPECIFIED. ) ;
#54935=CARTESIAN_POINT ( 'NONE',  ( 33.85195725564128821, 465.2464970902066739, 17.18122764674265568 ) ) ;
#54938=CARTESIAN_POINT ( 'NONE',  ( 39.13885763974980136, 324.4948203046521371, 17.18769520460729439 ) ) ;
#54951=AXIS2_PLACEMENT_3D ( 'NONE', #17192, #37119, #11721 ) ;
#54955=ADVANCED_FACE ( 'NONE', ( #30454 ), #45484, .F. ) ;
#54967=CARTESIAN_POINT ( 'NONE',  ( -40.43320803012392162, 490.2964122661026067, 11.44029694117851470 ) ) ;
#54979=CARTESIAN_POINT ( 'NONE',  ( 46.00000000000000000, 488.3725375423206287, 3.127739281036224117 ) ) ;
#54997=CARTESIAN_POINT ( 'NONE',  ( -40.93435977689158989, 414.3154843149413296, 27.72243992809649527 ) ) ;
#55001=ADVANCED_FACE ( 'NONE', ( #35779 ), #70985, .F. ) ;
#55018=VECTOR ( 'NONE', #64982, 1000.000000000000000 ) ;
#55020=CARTESIAN_POINT ( 'NONE',  ( 33.47662383457161184, 484.3276029205048872, 3.198141044865411509 ) ) ;
#55029=CARTESIAN_POINT ( 'NONE',  ( -33.01596977466600435, 300.1579362232981225, -0.8105850584072464837 ) ) ;
#55037=CARTESIAN_POINT ( 'NONE',  ( 25.96281893151035547, 308.9845124497657594, 9.902154178306897592 ) ) ;
#55041=EDGE_CURVE ( 'NONE', #93551, #29166, #33442, .T. ) ;
#55042=CIRCLE ( 'NONE', #84399, 3.000000000000025313 ) ;
#55051=CARTESIAN_POINT ( 'NONE',  ( -34.73480652773373833, 320.8284291698271318, -5.623717432936989447 ) ) ;
#55069=CIRCLE ( 'NONE', #67188, 1.000000000000000000 ) ;
#55092=ORIENTED_EDGE ( 'NONE', *, *, #34064, .F. ) ;
#55101=B_SPLINE_CURVE_WITH_KNOTS ( 'NONE', 3,
 ( #23035, #95846, #5759, #87226, #31657, #55356, #88285, #21976, #46753, #71027 ),
 .UNSPECIFIED., .F., .F.,
 ( 4, 2, 2, 2, 4 ),
 ( 9.528354594820111479E-17, 0.002534017993125006665, 0.003167522491406251500, 0.003801026989687495469, 0.005068035986249990778 ),
 .UNSPECIFIED. ) ;
#55117=CARTESIAN_POINT ( 'NONE',  ( 32.17606763898039191, 486.0066785907656026, 5.076925403379587642 ) ) ;
#55133=CARTESIAN_POINT ( 'NONE',  ( -36.01341068374667742, 304.0053153259133296, 0.1072131788699336868 ) ) ;
#55137=CARTESIAN_POINT ( 'NONE',  ( -34.88193003739208820, 463.4309577930944783, 4.853706708583048979 ) ) ;
#55140=VERTEX_POINT ( 'NONE', #95569 ) ;
#55146=CARTESIAN_POINT ( 'NONE',  ( 45.49982102694234953, 388.3127959276886827, 7.886590035822850453 ) ) ;
#55156=CARTESIAN_POINT ( 'NONE',  ( 0.000000000000000000, 0.000000000000000000, 5.000000000000000000 ) ) ;
#55165=CARTESIAN_POINT ( 'NONE',  ( 32.14348086320123343, 424.2599792281723126, 25.05014283909958550 ) ) ;
#55174=AXIS2_PLACEMENT_3D ( 'NONE', #12318, #69514, #71093 ) ;
#55175=DIRECTION ( 'NONE',  ( -0.2107607412277919534, 0.000000000000000000, 0.9775376770013071148 ) ) ;
#55185=CARTESIAN_POINT ( 'NONE',  ( 9.846493085561697001, 302.6513179331840320, 9.894389155799661495 ) ) ;
#55207=( BOUNDED_SURFACE ( )  B_SPLINE_SURFACE ( 3, 2, ( 
 ( #299, #106593, #97975 ),
 ( #24126, #56971, #33266 ),
 ( #106048, #42392, #32743 ),
 ( #99018, #66138, #1381 ),
 ( #90422, #57499, #58040 ),
 ( #82319, #15998, #17073 ),
 ( #25182, #90965, #24649 ),
 ( #34349, #17609, #49950 ),
 ( #65077, #8956, #67222 ),
 ( #65613, #32201, #89887 ) ),
 .UNSPECIFIED., .F., .F., .F. ) 
 B_SPLINE_SURFACE_WITH_KNOTS ( ( 4, 2, 2, 2, 4 ),
 ( 3, 3 ),
 ( -1.704365815147212970E-16, 0.002113969294778948911, 0.004227938589558067825, 0.006341907884337186739, 0.008455877179116305653 ),
 ( 0.000000000000000000, 1.000000000000000000 ),
 .UNSPECIFIED. ) 
 GEOMETRIC_REPRESENTATION_ITEM ( )  RATIONAL_B_SPLINE_SURFACE ( (
 ( 1.000000000000000000, 0.8812198548864833558, 1.000000000000000000),
 ( 1.000000000000000000, 0.8727879050781297554, 1.000000000000000000),
 ( 1.000000000000000000, 0.8622329439289413422, 1.000000000000000000),
 ( 1.000000000000000000, 0.8382107008196204578, 1.000000000000000000),
 ( 1.000000000000000000, 0.8245773560043481165, 1.000000000000000000),
 ( 1.000000000000000000, 0.7968578133382318018, 1.000000000000000000),
 ( 1.000000000000000000, 0.7826775888808733539, 1.000000000000000000),
 ( 1.000000000000000000, 0.7555830611713857392, 1.000000000000000000),
 ( 1.000000000000000000, 0.7430233494878055733, 1.000000000000000000),
 ( 1.000000000000000000, 0.7328671738315102324, 1.000000000000000000) ) ) 
 REPRESENTATION_ITEM ( '' )  SURFACE ( )  );
#55228=ORIENTED_EDGE ( 'NONE', *, *, #20423, .T. ) ;
#55229=CARTESIAN_POINT ( 'NONE',  ( 35.03733779313870400, 344.2465118914557820, -0.5854008046465184467 ) ) ;
#55230=CARTESIAN_POINT ( 'NONE',  ( 32.28930913498017929, 488.2717154064768579, 9.213726894932253941 ) ) ;
#55241=CARTESIAN_POINT ( 'NONE',  ( -37.31252934617396022, 464.0480400141152018, 19.52723141531950191 ) ) ;
#55250=CARTESIAN_POINT ( 'NONE',  ( 37.74156130160795897, 305.1789513982170092, -7.619069046267780365 ) ) ;
#55251=DIRECTION ( 'NONE',  ( 0.9576481418713256311, -0.1523715402840490341, 0.2443214073344040227 ) ) ;
#55254=CARTESIAN_POINT ( 'NONE',  ( 42.19180677453719142, 462.2931784592651638, 3.389262873192005809 ) ) ;
#55289=B_SPLINE_CURVE_WITH_KNOTS ( 'NONE', 3,
 ( #87754, #21443, #88279, #14892 ),
 .UNSPECIFIED., .F., .F.,
 ( 4, 4 ),
 ( 0.000000000000000000, 0.002232172794141575132 ),
 .UNSPECIFIED. ) ;
#55291=ORIENTED_EDGE ( 'NONE', *, *, #52062, .F. ) ;
#55292=ORIENTED_EDGE ( 'NONE', *, *, #30086, .T. ) ;
#55295=CARTESIAN_POINT ( 'NONE',  ( -42.10086803841218739, 435.6552064019005002, 19.95582312411058368 ) ) ;
#55303=ORIENTED_EDGE ( 'NONE', *, *, #7586, .T. ) ;
#55306=CARTESIAN_POINT ( 'NONE',  ( -41.50869271558325124, 485.4378639541363896, -3.633045570221354659 ) ) ;
#55309=VERTEX_POINT ( 'NONE', #67454 ) ;
#55311=CARTESIAN_POINT ( 'NONE',  ( -34.88900972249400212, 464.6206820655984870, 18.69027339340994232 ) ) ;
#55312=CARTESIAN_POINT ( 'NONE',  ( -33.00000000000000000, 500.0000000000002274, 0.000000000000000000 ) ) ;
#55313=DIRECTION ( 'NONE',  ( -2.312964634635742898E-14, 0.9952410070626638294, -0.09744402424415100905 ) ) ;
#55336=CARTESIAN_POINT ( 'NONE',  ( -41.14976906663522271, 484.9007963630877498, -3.779285786479841480 ) ) ;
#55339=CARTESIAN_POINT ( 'NONE',  ( 43.02661387979662067, 465.7449615347606482, 11.43319743843943392 ) ) ;
#55355=ORIENTED_EDGE ( 'NONE', *, *, #90372, .T. ) ;
#55356=CARTESIAN_POINT ( 'NONE',  ( -43.72576364275317218, 464.6794755336276808, 7.643080537327061386 ) ) ;
#55361=ADVANCED_FACE ( 'NONE', ( #67973, #10774 ), #100862, .F. ) ;
#55376=CARTESIAN_POINT ( 'NONE',  ( -27.18509476864008079, 312.1746170569358583, 10.69926602037820196 ) ) ;
#55399=CARTESIAN_POINT ( 'NONE',  ( 3.416848052085409204, 304.8518027757643267, -9.000000000397495370 ) ) ;
#55400=CARTESIAN_POINT ( 'NONE',  ( 34.94338628507543376, 342.5355909536760350, -0.9693026116843473927 ) ) ;
#55401=EDGE_LOOP ( 'NONE', ( #71751, #97256, #11063, #94922 ) ) ;
#55409=ORIENTED_EDGE ( 'NONE', *, *, #39965, .T. ) ;
#55414=CARTESIAN_POINT ( 'NONE',  ( -44.20877944490916178, 435.3144825228398531, 11.13781432399559890 ) ) ;
#55426=CARTESIAN_POINT ( 'NONE',  ( 39.22194103031748824, 325.7770611439928530, 17.47603589310227434 ) ) ;
#55437=CARTESIAN_POINT ( 'NONE',  ( -35.42017376419228469, 370.0793824939161141, 4.722754217616025763 ) ) ;
#55438=CARTESIAN_POINT ( 'NONE',  ( -26.18007569671338786, 305.7834980030482370, 10.60090293758347535 ) ) ;
#55445=AXIS2_PLACEMENT_3D ( 'NONE', #78043, #69956, #29531 ) ;
#55447=ORIENTED_EDGE ( 'NONE', *, *, #83337, .F. ) ;
#55452=CARTESIAN_POINT ( 'NONE',  ( 35.65219468668975367, 436.9652430364860720, 4.678245027581728444 ) ) ;
#55466=CARTESIAN_POINT ( 'NONE',  ( -34.12349128637492157, 490.1895789250393705, 12.63944770676173057 ) ) ;
#55472=CARTESIAN_POINT ( 'NONE',  ( 2.422472278927138205E-15, -0.1944580884125578779, 19.78098730681987405 ) ) ;
#55484=B_SPLINE_CURVE_WITH_KNOTS ( 'NONE', 3,
 ( #62989, #37147, #102911, #20982, #45222, #22556, #21487, #5282, #54867, #12293, #87795, #29077, #38717, #45735 ),
 .UNSPECIFIED., .F., .F.,
 ( 4, 2, 2, 2, 2, 2, 4 ),
 ( 1.710314408003578897E-16, 0.001025149392783061874, 0.001537724089174507267, 0.002050298785565952443, 0.002562873481957398270, 0.003075448178348843230, 0.004100597571131750496 ),
 .UNSPECIFIED. ) ;
#55499=CARTESIAN_POINT ( 'NONE',  ( -9.819056950928635175, 294.6481068335448299, 1.893705519456528652 ) ) ;
#55506=B_SPLINE_CURVE_WITH_KNOTS ( 'NONE', 3,
 ( #11931, #3860, #85303, #4920, #28699, #20630 ),
 .UNSPECIFIED., .F., .F.,
 ( 4, 2, 4 ),
 ( 2.255140518769848915E-17, 0.002095085863784774613, 0.004190171727569526675 ),
 .UNSPECIFIED. ) ;
#55508=ORIENTED_EDGE ( 'NONE', *, *, #70117, .T. ) ;
#55519=CARTESIAN_POINT ( 'NONE',  ( -42.36162206505707672, 485.1874691988857649, -2.398526663485948340 ) ) ;
#55520=CARTESIAN_POINT ( 'NONE',  ( -37.51854390953261742, 313.5286481325095451, 14.45587837336505999 ) ) ;
#55526=CARTESIAN_POINT ( 'NONE',  ( -36.69878522477553418, 484.6513904560026162, -2.872853880317824071 ) ) ;
#55541=CARTESIAN_POINT ( 'NONE',  ( 29.99999999999919709, 464.1079104336375849, 10.87617013709114744 ) ) ;
#55543=CARTESIAN_POINT ( 'NONE',  ( -31.45742208051316169, 439.3234620524921752, 23.14668034959422727 ) ) ;
#55545=CARTESIAN_POINT ( 'NONE',  ( -35.72342988946527242, 379.5409829981540497, 4.793340659205911791 ) ) ;
#55547=AXIS2_PLACEMENT_3D ( 'NONE', #11516, #13112, #63287 ) ;
#55551=ORIENTED_EDGE ( 'NONE', *, *, #60950, .T. ) ;
#55554=CARTESIAN_POINT ( 'NONE',  ( -29.42522989588877635, 307.1650680246546017, -9.025740850171580121 ) ) ;
#55561=CARTESIAN_POINT ( 'NONE',  ( 21.16904338951196962, 305.0382894998002143, 8.976822404920172360 ) ) ;
#55567=EDGE_LOOP ( 'NONE', ( #1791, #53813 ) ) ;
#55573=CARTESIAN_POINT ( 'NONE',  ( -27.45361451126541752, 305.3287645444004852, -9.452926980072254182 ) ) ;
#55586=EDGE_CURVE ( 'NONE', #44580, #37591, #55101, .T. ) ;
#55592=DIRECTION ( 'NONE',  ( 0.000000000000000000, 0.000000000000000000, 1.000000000000000000 ) ) ;
#55596=CARTESIAN_POINT ( 'NONE',  ( -43.38825400968192980, 436.1092026048715411, 18.83721859163727430 ) ) ;
#55600=CARTESIAN_POINT ( 'NONE',  ( 43.00000000000000000, 500.0000000000002274, 0.000000000000000000 ) ) ;
#55642=CARTESIAN_POINT ( 'NONE',  ( 36.28838933700914282, 352.2791627080521835, 1.187119259579878738 ) ) ;
#55658=FACE_OUTER_BOUND ( 'NONE', #50657, .T. ) ;
#55662=CARTESIAN_POINT ( 'NONE',  ( -31.11679462788039530, 441.4271381875185511, 23.27438508043199406 ) ) ;
#55674=ORIENTED_EDGE ( 'NONE', *, *, #16127, .F. ) ;
#55697=ORIENTED_EDGE ( 'NONE', *, *, #70424, .T. ) ;
#55710=EDGE_CURVE ( 'NONE', #77744, #88227, #74404, .T. ) ;
#55716=CARTESIAN_POINT ( 'NONE',  ( 32.85555225121232326, 465.7063523440039603, 11.00064571225391852 ) ) ;
#55738=CARTESIAN_POINT ( 'NONE',  ( -42.09210974227526947, 317.4093497706929270, -4.557617623460385126 ) ) ;
#55744=CARTESIAN_POINT ( 'NONE',  ( 35.76699745686483567, 397.0856500282078514, 5.951853049970027065 ) ) ;
#55748=CARTESIAN_POINT ( 'NONE',  ( -21.32035683309257124, 303.9777306799145435, -9.973210722144571605 ) ) ;
#55758=CARTESIAN_POINT ( 'NONE',  ( -33.21585456068780928, 485.3968598107930461, 4.030361751305823859 ) ) ;
#55765=CARTESIAN_POINT ( 'NONE',  ( 30.92869529702126385, 309.2766731770143451, -8.518754327849393349 ) ) ;
#55781=CARTESIAN_POINT ( 'NONE',  ( 43.46689911038843235, 485.4921130118005408, 4.095024577346555894 ) ) ;
#55789=CARTESIAN_POINT ( 'NONE',  ( 37.72113205395461222, 461.3706430627456712, 2.610878261945020373 ) ) ;
#55795=B_SPLINE_CURVE_WITH_KNOTS ( 'NONE', 3,
 ( #106049, #106594, #57501, #74751, #40273, #7891, #15457, #73147, #8957, #33802, #32202, #300 ),
 .UNSPECIFIED., .F., .F.,
 ( 4, 2, 2, 2, 2, 4 ),
 ( 0.000000000000000000, 0.0007243314081738727811, 0.001086497112260805323, 0.001448662816347737973, 0.002172994224521602839, 0.002897325632695468139 ),
 .UNSPECIFIED. ) ;
#55804=ORIENTED_EDGE ( 'NONE', *, *, #72338, .T. ) ;
#55807=CARTESIAN_POINT ( 'NONE',  ( 43.95556679493488872, 485.1369594940165371, -0.2799375260811446942 ) ) ;
#55809=CARTESIAN_POINT ( 'NONE',  ( -35.26357035561092346, 324.0757595391598329, -4.811724253201282053 ) ) ;
#55811=FACE_OUTER_BOUND ( 'NONE', #22047, .T. ) ;
#55814=EDGE_LOOP ( 'NONE', ( #6408, #28786, #66739, #54603, #32574, #71353 ) ) ;
#55815=CARTESIAN_POINT ( 'NONE',  ( 0.000000000000000000, 0.000000000000000000, 0.000000000000000000 ) ) ;
#55818=CARTESIAN_POINT ( 'NONE',  ( -38.94709829050781735, 485.6592143718707462, -4.427571171334746758 ) ) ;
#55825=( BOUNDED_SURFACE ( )  B_SPLINE_SURFACE ( 3, 2, ( 
 ( #68062, #9807, #10345 ),
 ( #41659, #51866, #17935 ),
 ( #1163, #99340, #2243 ),
 ( #58375, #1720, #27653 ) ),
 .UNSPECIFIED., .F., .F., .F. ) 
 B_SPLINE_SURFACE_WITH_KNOTS ( ( 4, 4 ),
 ( 3, 3 ),
 ( 0.01809742499366328097, 0.04402311302153927297 ),
 ( 0.000000000000000000, 1.000000000000000000 ),
 .UNSPECIFIED. ) 
 GEOMETRIC_REPRESENTATION_ITEM ( )  RATIONAL_B_SPLINE_SURFACE ( (
 ( 1.000000000000000000, 0.8381406085707386877, 1.000000000000000000),
 ( 1.000000000000000000, 0.8381408009587134611, 1.000000000000000000),
 ( 1.000000000000000000, 0.8381407633130539825, 1.000000000000000000),
 ( 1.000000000000000000, 0.8381405729626264511, 1.000000000000000000) ) ) 
 REPRESENTATION_ITEM ( '' )  SURFACE ( )  );
#55832=FILL_AREA_STYLE_COLOUR ( '', #14195 ) ;
#55834=DIRECTION ( 'NONE',  ( 0.000000000000000000, 0.000000000000000000, -1.000000000000000000 ) ) ;
#55841=CARTESIAN_POINT ( 'NONE',  ( 3.334874873180000421, 304.8518027755578146, 8.936999414886647841 ) ) ;
#55851=CARTESIAN_POINT ( 'NONE',  ( 44.11327388758706292, 464.4313852428374503, 9.822198357557169857 ) ) ;
#55853=CARTESIAN_POINT ( 'NONE',  ( -32.20917000857141943, 464.7502426416677395, 11.12081798558170753 ) ) ;
#55854=CARTESIAN_POINT ( 'NONE',  ( -43.70848695378470694, 435.5669781845214743, 16.96397918787651449 ) ) ;
#55864=CARTESIAN_POINT ( 'NONE',  ( 39.30282183805196894, 437.8662848125126175, 22.91975680305879948 ) ) ;
#55869=ORIENTED_EDGE ( 'NONE', *, *, #47456, .T. ) ;
#55871=EDGE_CURVE ( 'NONE', #696, #942, #97505, .T. ) ;
#55880=CARTESIAN_POINT ( 'NONE',  ( -43.04469050570867239, 434.7734435962895532, 9.248231035232468145 ) ) ;
#55888=CARTESIAN_POINT ( 'NONE',  ( -25.08362175616396073, 307.4904678873484158, 9.538446063109352835 ) ) ;
#55899=CARTESIAN_POINT ( 'NONE',  ( 46.00000000000000711, 486.3992880160790264, 3.759606857460338958 ) ) ;
#55910=CARTESIAN_POINT ( 'NONE',  ( -43.78304604341450812, 434.3019790015192143, 13.50139152689284749 ) ) ;
#55914=ORIENTED_EDGE ( 'NONE', *, *, #35335, .T. ) ;
#55927=ORIENTED_EDGE ( 'NONE', *, *, #5995, .T. ) ;
#55929=CARTESIAN_POINT ( 'NONE',  ( 43.40846727559856078, 434.3587631105147011, 15.36753962297099996 ) ) ;
#55930=CARTESIAN_POINT ( 'NONE',  ( -40.82244327980126286, 464.4949134188678954, 17.11270441416877475 ) ) ;
#55942=CARTESIAN_POINT ( 'NONE',  ( 39.48390856328317966, 328.8151482415006512, 18.19106243202422846 ) ) ;
#55951=CARTESIAN_POINT ( 'NONE',  ( 41.84005600619870791, 337.9971086773677484, 12.28340151619240572 ) ) ;
#55960=CARTESIAN_POINT ( 'NONE',  ( -32.75974658096314585, 300.2740040294210644, 3.156099462989093940 ) ) ;
#55963=CARTESIAN_POINT ( 'NONE',  ( 30.00000000000000000, 500.0000000000002274, 0.000000000000000000 ) ) ;
#55975=CARTESIAN_POINT ( 'NONE',  ( 35.50215413662375141, 437.6258544849006284, 4.714593920600838040 ) ) ;
#55981=CARTESIAN_POINT ( 'NONE',  ( 42.60801198157294323, 467.2314309137090049, 12.94843827108660150 ) ) ;
#55993=CARTESIAN_POINT ( 'NONE',  ( 0.000000000000000000, -19.99999999999998934, 0.000000000000000000 ) ) ;
#55997=ORIENTED_EDGE ( 'NONE', *, *, #39210, .F. ) ;
#56031=CARTESIAN_POINT ( 'NONE',  ( -21.29975379448946171, 294.8969325209483259, -1.990407376643346327 ) ) ;
#56038=ORIENTED_EDGE ( 'NONE', *, *, #20361, .T. ) ;
#56041=VERTEX_POINT ( 'NONE', #62694 ) ;
#56047=DIRECTION ( 'NONE',  ( -0.9995674975569808218, -0.02876390015675800785, -0.006120120541885477189 ) ) ;
#56050=CARTESIAN_POINT ( 'NONE',  ( 35.80932576324499905, 491.2997492151453116, 12.22805875982020041 ) ) ;
#56073=CARTESIAN_POINT ( 'NONE',  ( -27.00275465088504134, 305.0213443944945197, -9.522733346438251090 ) ) ;
#56081=CARTESIAN_POINT ( 'NONE',  ( 27.96090922204301421, 315.0246767492035360, 11.41898043927315243 ) ) ;
#56094=CARTESIAN_POINT ( 'NONE',  ( 44.10119824970315960, 485.7576817097466915, 4.111374810962455939 ) ) ;
#56115=DIRECTION ( 'NONE',  ( -0.5516836157922510031, 0.3133352674422950623, -0.7729593768389471098 ) ) ;
#56129=DIRECTION ( 'NONE',  ( 0.2277538186084659411, 0.3726643368264558887, 0.8995829534661936577 ) ) ;
#56130=CARTESIAN_POINT ( 'NONE',  ( -6.744191224192673140, 304.7396466505883268, -9.023845512521328160 ) ) ;
#56131=FACE_OUTER_BOUND ( 'NONE', #63300, .T. ) ;
#56133=CARTESIAN_POINT ( 'NONE',  ( 35.64643974835689022, 491.6938676210180006, 12.49042095397455832 ) ) ;
#56138=ADVANCED_FACE ( 'NONE', ( #56693 ), #59332, .F. ) ;
#56140=( BOUNDED_SURFACE ( )  B_SPLINE_SURFACE ( 3, 2, ( 
 ( #15630, #80895, #7006 ),
 ( #39926, #46936, #79835 ),
 ( #5433, #48523, #71736 ),
 ( #81414, #7525, #106221 ),
 ( #32383, #24297, #5941 ),
 ( #65255, #98145, #57146 ),
 ( #104110, #30254, #63683 ),
 ( #38868, #104645, #30797 ),
 ( #96571, #55543, #74917 ),
 ( #9125, #98666, #76934 ),
 ( #58219, #3045, #52650 ),
 ( #91144, #28422, #11656 ),
 ( #85034, #25358, #102273 ),
 ( #1001, #99195, #57670 ),
 ( #32911, #44586, #69390 ),
 ( #17254, #25913, #8602 ) ),
 .UNSPECIFIED., .F., .F., .T. ) 
 B_SPLINE_SURFACE_WITH_KNOTS ( ( 4, 2, 2, 2, 2, 2, 2, 4 ),
 ( 3, 3 ),
 ( 5.453536927602087303E-17, 0.0004174911443143812235, 0.0008349822886287079117, 0.001252473432943034546, 0.001669964577257361180, 0.002087455721571688030, 0.002504946865886014448, 0.003339929154514667715 ),
 ( 0.000000000000000000, 1.000000000000000000 ),
 .UNSPECIFIED. ) 
 GEOMETRIC_REPRESENTATION_ITEM ( )  RATIONAL_B_SPLINE_SURFACE ( (
 ( 1.000000000000000000, 0.9103180234519283598, 1.000000000000000000),
 ( 1.000000000000000000, 0.9132534515339265635, 1.000000000000000000),
 ( 1.000000000000000000, 0.9163167995291866541, 1.000000000000000000),
 ( 1.000000000000000000, 0.9224552667423359109, 1.000000000000000000),
 ( 1.000000000000000000, 0.9255672299892768740, 1.000000000000000000),
 ( 1.000000000000000000, 0.9311188777562252605, 1.000000000000000000),
 ( 1.000000000000000000, 0.9335889460075816881, 1.000000000000000000),
 ( 1.000000000000000000, 0.9372750707310617546, 1.000000000000000000),
 ( 1.000000000000000000, 0.9384199839903416551, 1.000000000000000000),
 ( 1.000000000000000000, 0.9386115400575140155, 1.000000000000000000),
 ( 1.000000000000000000, 0.9376241860046977683, 1.000000000000000000),
 ( 1.000000000000000000, 0.9330615520477972824, 1.000000000000000000),
 ( 1.000000000000000000, 0.9294866642001711199, 1.000000000000000000),
 ( 1.000000000000000000, 0.9147413655461451576, 1.000000000000000000),
 ( 1.000000000000000000, 0.9000454066029738298, 1.000000000000000000),
 ( 1.000000000000000000, 0.8805984182417286865, 1.000000000000000000) ) ) 
 REPRESENTATION_ITEM ( '' )  SURFACE ( )  );
#56144=EDGE_CURVE ( 'NONE', #65357, #93970, #81820, .T. ) ;
#56145=CARTESIAN_POINT ( 'NONE',  ( 30.00000000000000355, 461.9728594894706362, 12.10976292102180274 ) ) ;
#56147=CARTESIAN_POINT ( 'NONE',  ( 32.80207110003819082, 464.7310103173837774, 6.970203097363561362 ) ) ;
#56153=CARTESIAN_POINT ( 'NONE',  ( -43.52075891743682234, 484.7805561108189636, 4.063293749114582631 ) ) ;
#56161=CARTESIAN_POINT ( 'NONE',  ( 32.94021323899732323, 485.0599191339522349, 5.361609822540970072 ) ) ;
#56171=CARTESIAN_POINT ( 'NONE',  ( 46.00000000000000000, 461.5923978621210608, 9.841791816131641113 ) ) ;
#56191=CARTESIAN_POINT ( 'NONE',  ( -31.02212611900126760, 360.5725590293961318, 22.12937154125974715 ) ) ;
#56196=CARTESIAN_POINT ( 'NONE',  ( -31.41956809189580468, 380.3364241731395055, 23.41894105902489542 ) ) ;
#56198=CIRCLE ( 'NONE', #99240, 15.00000000000001421 ) ;
#56200=CARTESIAN_POINT ( 'NONE',  ( -43.51067860848493751, 485.4417974898085504, 3.909400899866710688 ) ) ;
#56203=CARTESIAN_POINT ( 'NONE',  ( -34.64166250171400918, 490.4813561613901811, 11.60003975507708951 ) ) ;
#56211=PLANE ( 'NONE',  #88024 ) ;
#56230=CARTESIAN_POINT ( 'NONE',  ( 9.047629367966660396, 302.6745984409856760, 9.899357940741596806 ) ) ;
#56242=AXIS2_PLACEMENT_3D ( 'NONE', #90, #66458, #99334 ) ;
#56249=CARTESIAN_POINT ( 'NONE',  ( 40.50010235193833097, 437.8098891827066268, 21.96267907499429128 ) ) ;
#56264=CARTESIAN_POINT ( 'NONE',  ( 36.94903695760955742, 463.9900885034069802, 19.60515700096699021 ) ) ;
#56268=CARTESIAN_POINT ( 'NONE',  ( -44.66387834505498944, 341.6072687625629101, 1.189588019127773677 ) ) ;
#56274=CARTESIAN_POINT ( 'NONE',  ( 20.37278541768182549, 303.8378246129573768, -10.00297115033341910 ) ) ;
#56279=EDGE_CURVE ( 'NONE', #23322, #49860, #48412, .T. ) ;
#56281=CARTESIAN_POINT ( 'NONE',  ( 40.97069641804722551, 488.3783578779278969, 10.59734101651493532 ) ) ;
#56283=CARTESIAN_POINT ( 'NONE',  ( 42.80674739067560353, 434.8200538645568827, 17.89665983759098467 ) ) ;
#56297=CARTESIAN_POINT ( 'NONE',  ( 33.35692847815791851, 315.0479610517062952, -7.083729467381872702 ) ) ;
#56302=DIRECTION ( 'NONE',  ( 0.000000000000000000, 0.000000000000000000, 1.000000000000000000 ) ) ;
#56317=( BOUNDED_SURFACE ( )  B_SPLINE_SURFACE ( 3, 2, ( 
 ( #7300, #773, #89837 ),
 ( #79216, #17018, #15938 ),
 ( #49893, #90360, #16472 ),
 ( #32689, #8373, #13404 ) ),
 .UNSPECIFIED., .F., .F., .F. ) 
 B_SPLINE_SURFACE_WITH_KNOTS ( ( 4, 4 ),
 ( 3, 3 ),
 ( 1.634976876108140686E-16, 0.002404295360965568069 ),
 ( 0.000000000000000000, 1.000000000000000000 ),
 .UNSPECIFIED. ) 
 GEOMETRIC_REPRESENTATION_ITEM ( )  RATIONAL_B_SPLINE_SURFACE ( (
 ( 1.000000000000000000, 0.7927020107002132887, 1.000000000000000000),
 ( 1.000000000000000000, 0.8018372346785949123, 1.000000000000000000),
 ( 1.000000000000000000, 0.8104306387029213132, 1.000000000000000000),
 ( 1.000000000000000000, 0.8162384603568832997, 1.000000000000000000) ) ) 
 REPRESENTATION_ITEM ( '' )  SURFACE ( )  );
#56319=EDGE_CURVE ( 'NONE', #101726, #75387, #31829, .T. ) ;
#56327=CARTESIAN_POINT ( 'NONE',  ( -43.64002961914418677, 465.1123652286068477, 8.841020312859518171 ) ) ;
#56330=( BOUNDED_SURFACE ( )  B_SPLINE_SURFACE ( 3, 2, ( 
 ( #28561, #36662, #77076 ),
 ( #86258, #19428, #101879 ),
 ( #59853, #69005, #68468 ),
 ( #19956, #61445, #28040 ) ),
 .UNSPECIFIED., .F., .F., .F. ) 
 B_SPLINE_SURFACE_WITH_KNOTS ( ( 4, 4 ),
 ( 3, 3 ),
 ( -5.399326818977812081E-17, 0.0009998946722929585862 ),
 ( 0.000000000000000000, 1.000000000000000000 ),
 .UNSPECIFIED. ) 
 GEOMETRIC_REPRESENTATION_ITEM ( )  RATIONAL_B_SPLINE_SURFACE ( (
 ( 1.000000000000000000, 0.9103180234519401282, 1.000000000000000000),
 ( 1.000000000000000000, 0.9095686419922741628, 1.000000000000000000),
 ( 1.000000000000000000, 0.9074000141362769112, 1.000000000000000000),
 ( 1.000000000000000000, 0.9039444415360021745, 1.000000000000000000) ) ) 
 REPRESENTATION_ITEM ( '' )  SURFACE ( )  );
#56333=VERTEX_POINT ( 'NONE', #100348 ) ;
#56347=CARTESIAN_POINT ( 'NONE',  ( 25.67074776827756111, 305.1949030138181911, 10.46162487402293628 ) ) ;
#56348=CARTESIAN_POINT ( 'NONE',  ( -37.12084974767950740, 348.0368284732711572, 0.6131544078700962297 ) ) ;
#56350=CARTESIAN_POINT ( 'NONE',  ( -46.00000000000000000, 487.9611973796579605, 0.4748239133093615782 ) ) ;
#56356=CARTESIAN_POINT ( 'NONE',  ( 0.000000000000000000, 273.9999999999999432, -7.999999999999983125 ) ) ;
#56357=CARTESIAN_POINT ( 'NONE',  ( -40.72262571688549571, 485.0559992917259819, -4.084589505543824828 ) ) ;
#56362=CARTESIAN_POINT ( 'NONE',  ( 40.80994823946819139, 464.4919611264104446, 17.10586550060336819 ) ) ;
#56369=CIRCLE ( 'NONE', #63347, 0.9999999999999993339 ) ;
#56376=CARTESIAN_POINT ( 'NONE',  ( -43.54152132068637115, 464.9591243096638777, 12.86066449444578907 ) ) ;
#56381=CARTESIAN_POINT ( 'NONE',  ( 11.59897338065259653, 303.6009977575001244, 9.883690276519013551 ) ) ;
#56388=CARTESIAN_POINT ( 'NONE',  ( -41.46910480218704009, 484.7338956289818270, -3.418960549715579500 ) ) ;
#56419=CARTESIAN_POINT ( 'NONE',  ( 0.000000000000000000, 0.000000000000000000, -5.000000000000003553 ) ) ;
#56422=CARTESIAN_POINT ( 'NONE',  ( -23.95564068939877345, 305.6666757346319514, -9.824255363916352124 ) ) ;
#56432=CARTESIAN_POINT ( 'NONE',  ( -26.74960312389934458, 311.3359961673855878, 11.49087433988725238 ) ) ;
#56443=CARTESIAN_POINT ( 'NONE',  ( 44.20107474623475241, 485.5083548284977724, 3.133049558774994026 ) ) ;
#56463=CARTESIAN_POINT ( 'NONE',  ( 32.54922218626916930, 319.8023524069591303, -6.363686095274232457 ) ) ;
#56483=CARTESIAN_POINT ( 'NONE',  ( -40.05614242505708233, 464.9362658514420445, 17.76104857941754744 ) ) ;
#56492=CARTESIAN_POINT ( 'NONE',  ( 41.26978454293845999, 329.6851661251676546, 10.40276537497734921 ) ) ;
#56494=CARTESIAN_POINT ( 'NONE',  ( -41.17144925627792418, 461.2585203975968398, 2.461466063511708047 ) ) ;
#56500=CARTESIAN_POINT ( 'NONE',  ( -35.50583740947284639, 381.5806922893717683, 5.955873595989558567 ) ) ;
#56501=CARTESIAN_POINT ( 'NONE',  ( -31.32820169690777945, 299.5760797589559843, 10.99770074658509422 ) ) ;
#56517=CARTESIAN_POINT ( 'NONE',  ( 36.33173443512200862, 437.9974107914312640, 4.196572296725481266 ) ) ;
#56522=CARTESIAN_POINT ( 'NONE',  ( -46.00000000000000000, 500.0000000000002274, 0.000000000000000000 ) ) ;
#56526=CARTESIAN_POINT ( 'NONE',  ( 9.549008551961874147, 295.0805096965325447, -10.04182235106940446 ) ) ;
#56553=DIRECTION ( 'NONE',  ( -0.000000000000000000, -1.000000000000000000, -0.000000000000000000 ) ) ;
#56567=CARTESIAN_POINT ( 'NONE',  ( -42.99999999999998579, 487.9285348210859752, 8.903916466042446132 ) ) ;
#56575=CARTESIAN_POINT ( 'NONE',  ( -20.24579557674108088, 304.8297271373347144, -10.00469232190996749 ) ) ;
#56585=CARTESIAN_POINT ( 'NONE',  ( -1.488823952716137988, 295.3362597640263516, -10.00085782936719880 ) ) ;
#56593=CARTESIAN_POINT ( 'NONE',  ( -15.86549515342121452, 294.5609651447646229, 9.875179695847329242 ) ) ;
#56601=EDGE_LOOP ( 'NONE', ( #74328, #94385, #298, #11778, #57324 ) ) ;
#56613=CARTESIAN_POINT ( 'NONE',  ( -42.71735565817839131, 428.6843791680139475, 18.96713788493819663 ) ) ;
#56617=CARTESIAN_POINT ( 'NONE',  ( -30.72240112801715384, 310.9384333019646078, -8.350412465344515311 ) ) ;
#56621=CARTESIAN_POINT ( 'NONE',  ( -43.71217423904473520, 435.6632154632215475, 9.092528312227507570 ) ) ;
#56624=CARTESIAN_POINT ( 'NONE',  ( -34.42777433040655666, 300.8302020014492655, -8.658268271844590913 ) ) ;
#56631=CARTESIAN_POINT ( 'NONE',  ( -42.55893460000644524, 435.1566242046031334, 18.92048169488384346 ) ) ;
#56632=CARTESIAN_POINT ( 'NONE',  ( 20.45590100891671526, 304.8998341874647622, 8.947178418926538868 ) ) ;
#56639=CARTESIAN_POINT ( 'NONE',  ( -33.00496812084397646, 465.6658704666172639, 15.15901827095664522 ) ) ;
#56643=CARTESIAN_POINT ( 'NONE',  ( -35.73338497923415957, 439.1098013319271445, 24.04626675101893696 ) ) ;
#56645=CARTESIAN_POINT ( 'NONE',  ( -31.03678703374875880, 438.6650838204938054, 21.86890379898545334 ) ) ;
#56647=CARTESIAN_POINT ( 'NONE',  ( 40.38558041326821524, 460.4656361498749675, 1.744807035484959634 ) ) ;
#56668=EDGE_CURVE ( 'NONE', #29831, #2324, #76692, .T. ) ;
#56682=FACE_OUTER_BOUND ( 'NONE', #81813, .T. ) ;
#56686=CARTESIAN_POINT ( 'NONE',  ( 32.00044432194599153, 486.9480297505133990, 7.098288108114727990 ) ) ;
#56693=FACE_OUTER_BOUND ( 'NONE', #70049, .T. ) ;
#56699=CARTESIAN_POINT ( 'NONE',  ( -43.18057774162383566, 485.1460640375049707, 5.477159825600939946 ) ) ;
#56713=CARTESIAN_POINT ( 'NONE',  ( 35.59152797293441495, 464.2026968846542445, 19.31774162833587383 ) ) ;
#56715=CARTESIAN_POINT ( 'NONE',  ( -43.32918576489194606, 484.9664181796746902, 4.870614540792155722 ) ) ;
#56720=CARTESIAN_POINT ( 'NONE',  ( 46.00000000000000000, 461.2902899409244242, 8.859728897585586793 ) ) ;
#56733=ORIENTED_EDGE ( 'NONE', *, *, #70664, .F. ) ;
#56738=CARTESIAN_POINT ( 'NONE',  ( 44.66387834505498944, 341.6072687625629101, 1.189588019127773677 ) ) ;
#56743=CARTESIAN_POINT ( 'NONE',  ( -28.74870929803160635, 319.1494203397336378, 12.45838930289386504 ) ) ;
#56745=CARTESIAN_POINT ( 'NONE',  ( -42.18756898894582719, 484.4522853017719513, -2.425645685620470449 ) ) ;
#56779=CARTESIAN_POINT ( 'NONE',  ( 20.97754405179124504, 294.8763868968453608, 9.942224931492244622 ) ) ;
#56786=ORIENTED_EDGE ( 'NONE', *, *, #12563, .T. ) ;
#56789=CARTESIAN_POINT ( 'NONE',  ( -37.62595466100675168, 491.2446780561949140, 12.18850516984412735 ) ) ;
#56806=AXIS2_PLACEMENT_3D ( 'NONE', #34826, #19714, #101114 ) ;
#56813=CARTESIAN_POINT ( 'NONE',  ( 33.84761347220318584, 488.7471039746334895, 11.01988148152525504 ) ) ;
#56815=CARTESIAN_POINT ( 'NONE',  ( -40.75641113481592726, 360.0948485545300741, 24.37153223514695100 ) ) ;
#56818=CARTESIAN_POINT ( 'NONE',  ( -45.50145573691759182, 405.2496736015978627, 8.430338687477670234 ) ) ;
#56822=CARTESIAN_POINT ( 'NONE',  ( 21.87703882378025710, 304.0646303204994751, -9.954777887710193340 ) ) ;
#56834=CARTESIAN_POINT ( 'NONE',  ( -35.47684105139835253, 436.4843629120474588, 5.043999258399300523 ) ) ;
#56844=AXIS2_PLACEMENT_3D ( 'NONE', #100611, #52588, #2443 ) ;
#56861=ORIENTED_EDGE ( 'NONE', *, *, #24359, .T. ) ;
#56864=CARTESIAN_POINT ( 'NONE',  ( 36.23800438212097674, 462.2863016840603336, 3.479460024273059560 ) ) ;
#56873=CARTESIAN_POINT ( 'NONE',  ( 30.00000000000000000, 464.2362426119078691, 15.22860355415621925 ) ) ;
#56879=EDGE_LOOP ( 'NONE', ( #32881, #57262, #47753, #1924 ) ) ;
#56880=DIRECTION ( 'NONE',  ( -0.4804656623126268844, -0.6318279369468200457, -0.6082320325599548383 ) ) ;
#56881=CARTESIAN_POINT ( 'NONE',  ( 44.19369980509995344, 485.2130927455154961, 1.003348617673237131 ) ) ;
#56883=CARTESIAN_POINT ( 'NONE',  ( 33.15568924549393870, 409.3318216629285757, 25.92143113850746872 ) ) ;
#56884=CARTESIAN_POINT ( 'NONE',  ( -34.91408493170087013, 321.8851433098943744, -5.358867272492853218 ) ) ;
#56886=CARTESIAN_POINT ( 'NONE',  ( -46.00000000000003553, 486.3928777044199592, 3.761659546714874125 ) ) ;
#56893=FACE_OUTER_BOUND ( 'NONE', #11181, .T. ) ;
#56922=CARTESIAN_POINT ( 'NONE',  ( -39.67558661318489044, 485.2175335192594048, -4.383050085588370059 ) ) ;
#56928=CARTESIAN_POINT ( 'NONE',  ( -38.83413156602095739, 459.9242647137451740, 1.954013010003036621 ) ) ;
#56945=EDGE_CURVE ( 'NONE', #84380, #38837, #61312, .T. ) ;
#56952=CARTESIAN_POINT ( 'NONE',  ( 28.99461337544303774, 306.6923402040300175, -9.137068254448493576 ) ) ;
#56962=( BOUNDED_SURFACE ( )  B_SPLINE_SURFACE ( 3, 2, ( 
 ( #77484, #20897, #28429 ),
 ( #20368, #55306, #97360 ),
 ( #79070, #62377, #15387 ),
 ( #22462, #96334, #23514 ),
 ( #56357, #21397, #88233 ),
 ( #14313, #47217, #38631 ),
 ( #80118, #39158, #103864 ),
 ( #54235, #62900, #105466 ),
 ( #40192, #95267, #89293 ),
 ( #39687, #87175, #73069 ),
 ( #5705, #6221, #30014 ),
 ( #63968, #31606, #72039 ),
 ( #5190, #55818, #46178 ),
 ( #104947, #13256, #31089 ) ),
 .UNSPECIFIED., .F., .F., .T. ) 
 B_SPLINE_SURFACE_WITH_KNOTS ( ( 4, 2, 2, 2, 2, 2, 4 ),
 ( 3, 3 ),
 ( -1.455432996344541152E-15, 0.001037790322795861028, 0.001556685484194519258, 0.002075580645593177488, 0.002594475806991835935, 0.003113370968390493949, 0.004151161291187810409 ),
 ( 0.000000000000000000, 1.000000000000000000 ),
 .UNSPECIFIED. ) 
 GEOMETRIC_REPRESENTATION_ITEM ( )  RATIONAL_B_SPLINE_SURFACE ( (
 ( 1.000000000000000000, 0.8266506655094397749, 1.000000000000000000),
 ( 1.000000000000000000, 0.8403402121237507627, 1.000000000000000000),
 ( 1.000000000000000000, 0.8527375874848021065, 1.000000000000000000),
 ( 1.000000000000000000, 0.8685816477878300912, 1.000000000000000000),
 ( 1.000000000000000000, 0.8733924426121236761, 1.000000000000000000),
 ( 1.000000000000000000, 0.8815965360754977054, 1.000000000000000000),
 ( 1.000000000000000000, 0.8850417602709202969, 1.000000000000000000),
 ( 1.000000000000000000, 0.8904811663259585286, 1.000000000000000000),
 ( 1.000000000000000000, 0.8924856662908452476, 1.000000000000000000),
 ( 1.000000000000000000, 0.8947492012711196763, 1.000000000000000000),
 ( 1.000000000000000000, 0.8950270886643441060, 1.000000000000000000),
 ( 1.000000000000000000, 0.8933353874821594598, 1.000000000000000000),
 ( 1.000000000000000000, 0.8887179207565071293, 1.000000000000000000),
 ( 1.000000000000000000, 0.8812198548863955372, 1.000000000000000000) ) ) 
 REPRESENTATION_ITEM ( '' )  SURFACE ( )  );
#56964=EDGE_CURVE ( 'NONE', #62284, #11843, #68133, .T. ) ;
#56969=CARTESIAN_POINT ( 'NONE',  ( -23.33774967493778263, 304.7266520059388881, 10.12724404418439939 ) ) ;
#56970=VERTEX_POINT ( 'NONE', #106050 ) ;
#56971=CARTESIAN_POINT ( 'NONE',  ( 38.08399829462226904, 485.5430321159580558, -4.039315524879443231 ) ) ;
#56974=DIRECTION ( 'NONE',  ( -0.7611201562154610301, 0.000000000000000000, -0.6486109063240860229 ) ) ;
#56980=CARTESIAN_POINT ( 'NONE',  ( 45.99999999999995026, 436.1515134926989390, 9.232507626554589564 ) ) ;
#56993=CARTESIAN_POINT ( 'NONE',  ( 40.85254446136673323, 441.7500193615117610, 25.53625856138344474 ) ) ;
#56996=CARTESIAN_POINT ( 'NONE',  ( 31.03867016165222026, 468.3124986733989772, 18.90871194958903345 ) ) ;
#57022=CARTESIAN_POINT ( 'NONE',  ( 36.73804107120987794, 310.3495191438393022, 13.65122708957765241 ) ) ;
#57028=CARTESIAN_POINT ( 'NONE',  ( 32.68253575351396023, 486.6530702916748510, 8.413834116604476776 ) ) ;
#57033=DIRECTION ( 'NONE',  ( 0.000000000000000000, 0.000000000000000000, 1.000000000000000000 ) ) ;
#57034=CARTESIAN_POINT ( 'NONE',  ( -19.96162532426522773, 302.8116070918645164, 9.928455558879878851 ) ) ;
#57040=CARTESIAN_POINT ( 'NONE',  ( 6.962581867957212012, 296.7069905224671515, 7.199939672562493342 ) ) ;
#57045=ORIENTED_EDGE ( 'NONE', *, *, #95812, .T. ) ;
#57048=CARTESIAN_POINT ( 'NONE',  ( 34.88259098417261583, 437.7046102974892960, 4.606877878020303463 ) ) ;
#57056=AXIS2_PLACEMENT_3D ( 'NONE', #52202, #28502, #19371 ) ;
#57078=AXIS2_PLACEMENT_3D ( 'NONE', #69588, #102478, #28624 ) ;
#57094=CARTESIAN_POINT ( 'NONE',  ( 30.15836800272330365, 323.6799505684332985, 14.82125230496755641 ) ) ;
#57099=ORIENTED_EDGE ( 'NONE', *, *, #52609, .F. ) ;
#57135=CARTESIAN_POINT ( 'NONE',  ( -34.16642289233710983, 463.8422268500497125, 18.98106911353875148 ) ) ;
#57137=AXIS2_PLACEMENT_3D ( 'NONE', #4680, #62391, #36022 ) ;
#57138=ORIENTED_EDGE ( 'NONE', *, *, #99693, .T. ) ;
#57140=ORIENTED_EDGE ( 'NONE', *, *, #106081, .F. ) ;
#57146=CARTESIAN_POINT ( 'NONE',  ( -31.66959486501912124, 439.0151181633245301, 23.43702844066392998 ) ) ;
#57148=CARTESIAN_POINT ( 'NONE',  ( -30.37040671822360238, 310.2650604196215909, -8.515671380529434842 ) ) ;
#57155=CARTESIAN_POINT ( 'NONE',  ( -21.29975379448944750, 294.8969325209484396, -1.990407376643355430 ) ) ;
#57158=CIRCLE ( 'NONE', #21041, 8.000000000000014211 ) ;
#57162=CARTESIAN_POINT ( 'NONE',  ( -42.35645304355714558, 435.3801053262068308, 19.45913382674001113 ) ) ;
#57163=CARTESIAN_POINT ( 'NONE',  ( 31.43654395834863280, 409.1920974130434843, 24.49082746238584107 ) ) ;
#57164=CARTESIAN_POINT ( 'NONE',  ( -38.45248457205872938, 463.5270362811817222, 19.68931241193499915 ) ) ;
#57169=DIRECTION ( 'NONE',  ( 0.000000000000000000, 0.2755684261024844983, -0.9612814585413576030 ) ) ;
#57174=VERTEX_POINT ( 'NONE', #68694 ) ;
#57189=VERTEX_POINT ( 'NONE', #36354 ) ;
#57197=ORIENTED_EDGE ( 'NONE', *, *, #14245, .T. ) ;
#57208=CARTESIAN_POINT ( 'NONE',  ( 0.000000000000000000, 294.8518027762758038, -10.00000000000000355 ) ) ;
#57209=CARTESIAN_POINT ( 'NONE',  ( 26.54817876223620488, 310.6276912632132507, 11.31208242866018132 ) ) ;
#57212=CARTESIAN_POINT ( 'NONE',  ( 32.18423816190075115, 486.1452344075074734, 5.458209535234520793 ) ) ;
#57215=ORIENTED_EDGE ( 'NONE', *, *, #16038, .T. ) ;
#57221=DIRECTION ( 'NONE',  ( -0.000000000000000000, -1.000000000000000000, -0.000000000000000000 ) ) ;
#57227=DIRECTION ( 'NONE',  ( 0.000000000000000000, -0.9253863139535718485, 0.3790252893243686305 ) ) ;
#57251=DIRECTION ( 'NONE',  ( -1.000000000000000000, -0.000000000000000000, -0.000000000000000000 ) ) ;
#57253=CARTESIAN_POINT ( 'NONE',  ( -34.23737646655726508, 301.4688704001253541, -0.5023635973111234554 ) ) ;
#57260=CARTESIAN_POINT ( 'NONE',  ( 43.78231969043036997, 434.3019752265855118, 13.50801524699893186 ) ) ;
#57262=ORIENTED_EDGE ( 'NONE', *, *, #64968, .F. ) ;
#57263=FACE_OUTER_BOUND ( 'NONE', #6896, .T. ) ;
#57264=CARTESIAN_POINT ( 'NONE',  ( 45.48003679188781234, 379.8448106960472614, 7.220331889307936457 ) ) ;
#57269=CARTESIAN_POINT ( 'NONE',  ( -37.71459991402550571, 437.7716825518407973, 4.505118785440077822 ) ) ;
#57290=EDGE_CURVE ( 'NONE', #36676, #97864, #33823, .T. ) ;
#57294=ORIENTED_EDGE ( 'NONE', *, *, #7452, .F. ) ;
#57305=CARTESIAN_POINT ( 'NONE',  ( -21.79395256997316110, 303.1333420030371713, 9.997488266507673416 ) ) ;
#57306=CARTESIAN_POINT ( 'NONE',  ( -31.35596682365705945, 438.0939828603719093, 22.55458131664414267 ) ) ;
#57321=CARTESIAN_POINT ( 'NONE',  ( 38.13886201901005535, 438.4571414526099034, 23.48832422888811067 ) ) ;
#57324=ORIENTED_EDGE ( 'NONE', *, *, #34162, .T. ) ;
#57332=CARTESIAN_POINT ( 'NONE',  ( 37.31409640255603932, 464.0485063763027824, 19.52659819501504046 ) ) ;
#57338=CARTESIAN_POINT ( 'NONE',  ( -34.95237279327285762, 304.8277712208536627, 12.26231981495593537 ) ) ;
#57340=CARTESIAN_POINT ( 'NONE',  ( -40.61216075948964033, 351.1469683695276558, 22.89433108575548914 ) ) ;
#57344=CARTESIAN_POINT ( 'NONE',  ( 25.01177788099232657, 306.1649447482250821, -9.713921147030010417 ) ) ;
#57346=ORIENTED_EDGE ( 'NONE', *, *, #37020, .F. ) ;
#57357=EDGE_CURVE ( 'NONE', #34141, #47279, #31633, .T. ) ;
#57374=FILL_AREA_STYLE_COLOUR ( '', #96159 ) ;
#57392=CARTESIAN_POINT ( 'NONE',  ( -32.71902930631085837, 485.4797908183046502, 6.287473911063091059 ) ) ;
#57393=EDGE_LOOP ( 'NONE', ( #76312, #87766, #15581, #61947 ) ) ;
#57396=CARTESIAN_POINT ( 'NONE',  ( 37.85390227844803945, 460.2287157790690344, 2.227471321855208242 ) ) ;
#57400=CARTESIAN_POINT ( 'NONE',  ( -37.72498816019726320, 463.3860965757806412, 19.97126500436749907 ) ) ;
#57404=CARTESIAN_POINT ( 'NONE',  ( 30.00000000000000355, 461.8887775513395013, 11.55279652843918825 ) ) ;
#57405=CARTESIAN_POINT ( 'NONE',  ( 46.00000000000000000, 461.6622277975422435, 10.18145404766785589 ) ) ;
#57409=EDGE_LOOP ( 'NONE', ( #13250, #25151, #15659, #75211 ) ) ;
#57411=DIRECTION ( 'NONE',  ( -0.1270361284032274773, 0.9918980905719693153, 0.000000000000000000 ) ) ;
#57412=CARTESIAN_POINT ( 'NONE',  ( -32.45623693502356133, 464.7023894946334508, 16.04003527244881866 ) ) ;
#57414=CARTESIAN_POINT ( 'NONE',  ( -45.43249564040426947, 375.4183832217576082, 6.657994069051931696 ) ) ;
#57415=CARTESIAN_POINT ( 'NONE',  ( 32.64147241561500579, 439.6779429780671649, 24.07034118911087006 ) ) ;
#57421=CARTESIAN_POINT ( 'NONE',  ( 6.763850406535977022, 294.7356673863635592, 9.912314076180619438 ) ) ;
#57428=CARTESIAN_POINT ( 'NONE',  ( -33.00000000000000000, 463.5362553048592531, 6.739467187734380360 ) ) ;
#57430=ORIENTED_EDGE ( 'NONE', *, *, #25787, .T. ) ;
#57445=AXIS2_PLACEMENT_3D ( 'NONE', #16197, #81980, #27531 ) ;
#57453=AXIS2_PLACEMENT_3D ( 'NONE', #33751, #18091, #41810 ) ;
#57462=FACE_OUTER_BOUND ( 'NONE', #79616, .T. ) ;
#57479=CARTESIAN_POINT ( 'NONE',  ( 31.94399449188606965, 299.1674248799971565, -1.040763782016456362 ) ) ;
#57485=CARTESIAN_POINT ( 'NONE',  ( -34.94338628507543376, 342.5355909536760350, -0.9693026116538068226 ) ) ;
#57490=CARTESIAN_POINT ( 'NONE',  ( -33.24561022503097263, 485.0000549217730281, 0.3114934373726880867 ) ) ;
#57491=CARTESIAN_POINT ( 'NONE',  ( 37.63786767139364287, 432.3659482643442402, 5.163126625230292532 ) ) ;
#57492=CARTESIAN_POINT ( 'NONE',  ( 44.27172743695263790, 463.5980762766301950, 7.352902973909428930 ) ) ;
#57493=EDGE_LOOP ( 'NONE', ( #39078, #72559, #23753, #31299 ) ) ;
#57499=CARTESIAN_POINT ( 'NONE',  ( 36.04707687143260841, 485.1891289572317874, -2.470783067951639378 ) ) ;
#57501=CARTESIAN_POINT ( 'NONE',  ( 30.98778555464372886, 438.9951436325601435, 22.21946372908199407 ) ) ;
#57504=ORIENTED_EDGE ( 'NONE', *, *, #14563, .T. ) ;
#57507=CARTESIAN_POINT ( 'NONE',  ( 46.00000000000000000, 437.8943772434384414, 13.39121328441395953 ) ) ;
#57520=CARTESIAN_POINT ( 'NONE',  ( 40.73878142687892279, 503.7113041876743864, 10.19672445236252045 ) ) ;
#57521=CARTESIAN_POINT ( 'NONE',  ( -46.00000000000000000, 500.0000000000002274, 0.000000000000000000 ) ) ;
#57523=CARTESIAN_POINT ( 'NONE',  ( -32.32362562572921405, 488.2653032247410465, 9.218764297502717753 ) ) ;
#57535=ORIENTED_EDGE ( 'NONE', *, *, #87735, .F. ) ;
#57538=CARTESIAN_POINT ( 'NONE',  ( 42.69811214730273718, 434.9611672192513652, 18.34625614733210242 ) ) ;
#57545=CARTESIAN_POINT ( 'NONE',  ( 33.11888822396143439, 438.9412710830782203, 23.90522241289666994 ) ) ;
#57547=CARTESIAN_POINT ( 'NONE',  ( 32.82876496518922949, 434.9825001184026974, 12.61068621696671244 ) ) ;
#57548=CARTESIAN_POINT ( 'NONE',  ( 35.70121033104481256, 304.3670428735860582, 4.138962953855986449 ) ) ;
#57557=CARTESIAN_POINT ( 'NONE',  ( -22.10619625089826101, 303.2187564606320507, 10.01583238429591383 ) ) ;
#57564=CARTESIAN_POINT ( 'NONE',  ( 11.57593719571816848, 303.6016380201557467, 9.883826392888126477 ) ) ;
#57582=CARTESIAN_POINT ( 'NONE',  ( -32.94021323899823983, 485.0599191339510980, 5.361609822537303671 ) ) ;
#57589=AXIS2_PLACEMENT_3D ( 'NONE', #28461, #63999, #48823 ) ;
#57604=CARTESIAN_POINT ( 'NONE',  ( 42.16858620283969827, 461.4629983908274085, 3.513115262088578383 ) ) ;
#57609=CARTESIAN_POINT ( 'NONE',  ( -8.392066182232479576, 294.6889698295346989, -5.445651201154610987 ) ) ;
#57616=CARTESIAN_POINT ( 'NONE',  ( 31.39117689105021114, 374.8518552428220687, 22.89618308279878534 ) ) ;
#57642=CARTESIAN_POINT ( 'NONE',  ( -3.610928090092041298, 295.9072949364792748, -10.00534087566827957 ) ) ;
#57652=CARTESIAN_POINT ( 'NONE',  ( -41.72794603366239130, 484.6317694608798092, -3.103777363567681746 ) ) ;
#57654=CARTESIAN_POINT ( 'NONE',  ( 37.49684268403980525, 491.2987049188978972, 12.22740886045582087 ) ) ;
#57670=CARTESIAN_POINT ( 'NONE',  ( -31.32094825172531571, 438.4579161125127484, 22.73291248390550834 ) ) ;
#57672=CARTESIAN_POINT ( 'NONE',  ( -30.24048965269528821, 312.5841310900376584, -7.180294356216179175 ) ) ;
#57680=CARTESIAN_POINT ( 'NONE',  ( -23.30980644977553595, 303.3900546958402060, -9.884505219500150375 ) ) ;
#57686=CARTESIAN_POINT ( 'NONE',  ( -37.82123075315000449, 485.6920212717419645, -4.511793510526142192 ) ) ;
#57687=CARTESIAN_POINT ( 'NONE',  ( -40.87566242051374132, 372.2907203791197617, 25.85377625089821763 ) ) ;
#57704=AXIS2_PLACEMENT_3D ( 'NONE', #69118, #27623, #63544 ) ;
#57720=EDGE_CURVE ( 'NONE', #2280, #29160, #71735, .T. ) ;
#57737=CARTESIAN_POINT ( 'NONE',  ( 41.86527866917096929, 465.6949979513468065, 15.31736901429372111 ) ) ;
#57749=CARTESIAN_POINT ( 'NONE',  ( 33.74362713068862973, 463.9326864247046274, 7.533159870298671734 ) ) ;
#57750=ORIENTED_EDGE ( 'NONE', *, *, #94376, .F. ) ;
#57751=CARTESIAN_POINT ( 'NONE',  ( -18.95009283723106108, 304.6966536337758384, 8.904021447602946893 ) ) ;
#57778=FACE_OUTER_BOUND ( 'NONE', #97860, .T. ) ;
#57779=CARTESIAN_POINT ( 'NONE',  ( -36.19631612776445451, 463.3208255589807436, 20.09850791239178136 ) ) ;
#57783=CARTESIAN_POINT ( 'NONE',  ( -27.40885254791232484, 296.4310517681949477, -1.657890121573132758 ) ) ;
#57784=EDGE_CURVE ( 'NONE', #105451, #71046, #85693, .T. ) ;
#57799=CARTESIAN_POINT ( 'NONE',  ( 33.08751701378358945, 301.6823158026044780, 11.49690784967660662 ) ) ;
#57807=CARTESIAN_POINT ( 'NONE',  ( -31.36487372896283432, 435.2119976784319419, 22.89286986970661886 ) ) ;
#57808=DIRECTION ( 'NONE',  ( 0.2280158659356096851, 0.1533051183531252970, 0.9615125093145531210 ) ) ;
#57815=ORIENTED_EDGE ( 'NONE', *, *, #17145, .T. ) ;
#57819=CARTESIAN_POINT ( 'NONE',  ( 31.92850365111794986, 356.8979959129785584, 21.71365648330940346 ) ) ;
#57836=CARTESIAN_POINT ( 'NONE',  ( -24.82643806938782660, 304.4615624795510485, 10.29204873707470291 ) ) ;
#57837=CARTESIAN_POINT ( 'NONE',  ( -33.74586796234814301, 434.0087061791907104, 12.79535379566283027 ) ) ;
#57838=EDGE_CURVE ( 'NONE', #27223, #58214, #59898, .T. ) ;
#57850=CARTESIAN_POINT ( 'NONE',  ( 34.11633748533821375, 439.1270573268431008, 24.05964454602017710 ) ) ;
#57861=EDGE_LOOP ( 'NONE', ( #63549, #41262, #1551, #49760, #79830, #43811, #24772, #54305 ) ) ;
#57864=VECTOR ( 'NONE', #68200, 1000.000000000000114 ) ;
#57866=CARTESIAN_POINT ( 'NONE',  ( 36.69890166230473483, 463.9786769757893694, 19.62055820434390441 ) ) ;
#57874=CARTESIAN_POINT ( 'NONE',  ( -22.20318009218133071, 295.0333587257888439, 9.975590323731541531 ) ) ;
#57879=CARTESIAN_POINT ( 'NONE',  ( 30.01939835712524030, 309.6846599134693747, -8.656694015688147559 ) ) ;
#57894=CARTESIAN_POINT ( 'NONE',  ( -35.46984665180946905, 438.0686027085576484, 4.109636340060087711 ) ) ;
#57901=ORIENTED_EDGE ( 'NONE', *, *, #41239, .F. ) ;
#57913=( LENGTH_UNIT ( ) NAMED_UNIT ( * ) SI_UNIT ( .MILLI., .METRE. ) );
#57915=CARTESIAN_POINT ( 'NONE',  ( 43.00000000000000000, 436.0987441542287115, 7.567257455462728544 ) ) ;
#57916=EDGE_CURVE ( 'NONE', #27903, #41040, #39044, .T. ) ;
#57918=B_SPLINE_CURVE_WITH_KNOTS ( 'NONE', 3,
 ( #65533, #31080, #57415, #63959 ),
 .UNSPECIFIED., .F., .F.,
 ( 4, 4 ),
 ( 0.000000000000000000, 0.0007558628827956282055 ),
 .UNSPECIFIED. ) ;
#57934=CARTESIAN_POINT ( 'NONE',  ( -35.67416790563066087, 463.3851398029171946, 19.97299141547693324 ) ) ;
#57939=CARTESIAN_POINT ( 'NONE',  ( 40.62042009609988469, 488.7249922674043887, 10.90475042733721978 ) ) ;
#57942=CARTESIAN_POINT ( 'NONE',  ( -46.00000000000000000, 450.0000000000002274, 13.20242257375370976 ) ) ;
#57945=( LENGTH_UNIT ( ) NAMED_UNIT ( * ) SI_UNIT ( .MILLI., .METRE. ) );
#57947=CARTESIAN_POINT ( 'NONE',  ( 23.56341839161319740, 303.7214408960188621, 10.12591315008080706 ) ) ;
#57950=CARTESIAN_POINT ( 'NONE',  ( -45.46260347522193968, 379.8339907270314484, 7.111986633017085779 ) ) ;
#57958=CARTESIAN_POINT ( 'NONE',  ( 42.74056876569563457, 464.8122885126885535, 15.63399960026069024 ) ) ;
#57962=AXIS2_PLACEMENT_3D ( 'NONE', #105267, #31, #90145 ) ;
#57977=CARTESIAN_POINT ( 'NONE',  ( -35.17753024347793911, 490.3634983170154555, 12.17893648721504007 ) ) ;
#58001=CARTESIAN_POINT ( 'NONE',  ( -37.50059943756144776, 490.7879993827797307, 12.38039871356719246 ) ) ;
#58013=VERTEX_POINT ( 'NONE', #99114 ) ;
#58018=AXIS2_PLACEMENT_3D ( 'NONE', #102211, #20824, #94678 ) ;
#58019=CARTESIAN_POINT ( 'NONE',  ( 29.85885434071563438, 307.6868234535251645, -8.901958748380083719 ) ) ;
#58023=CARTESIAN_POINT ( 'NONE',  ( 32.15166163075728178, 486.0589784586659903, 5.199393881400817818 ) ) ;
#58038=CARTESIAN_POINT ( 'NONE',  ( -21.11705751644940676, 305.0273488488396083, 8.974472976378370603 ) ) ;
#58040=CARTESIAN_POINT ( 'NONE',  ( 36.23096140414229183, 484.5285253001270007, -2.435173044881263404 ) ) ;
#58048=CARTESIAN_POINT ( 'NONE',  ( 46.00000000000000000, 435.9844294008496490, 14.35633708101140193 ) ) ;
#58060=CARTESIAN_POINT ( 'NONE',  ( 24.60488647473181345, 306.9835580411500473, 10.41807558718820914 ) ) ;
#58069=DIRECTION ( 'NONE',  ( -0.000000000000000000, 0.2521971900442987469, 0.9676758637755517034 ) ) ;
#58078=CARTESIAN_POINT ( 'NONE',  ( -33.94783393359910662, 484.1261039197349305, 1.321740980884785532 ) ) ;
#58082=CARTESIAN_POINT ( 'NONE',  ( -31.35993980847401374, 436.8059452921889942, 22.71850044363437249 ) ) ;
#58089=B_SPLINE_CURVE_WITH_KNOTS ( 'NONE', 3,
 ( #36145, #36674, #78144, #94886, #21537, #21030, #53866, #69536, #101890, #44739 ),
 .UNSPECIFIED., .F., .F.,
 ( 4, 2, 2, 2, 4 ),
 ( 1.734723475976807094E-18, 0.001638027434153875844, 0.003276054868307749952, 0.004914082302461623628, 0.006552109736615498170 ),
 .UNSPECIFIED. ) ;
#58093=CARTESIAN_POINT ( 'NONE',  ( 30.53436373644603563, 298.8120125249405419, 10.81965208238480614 ) ) ;
#58094=AXIS2_PLACEMENT_3D ( 'NONE', #42749, #20119, #19051 ) ;
#58097=CARTESIAN_POINT ( 'NONE',  ( -41.70256300459701038, 461.0340457114389210, 3.032228049028218297 ) ) ;
#58102=CARTESIAN_POINT ( 'NONE',  ( -22.22335123492370101, 303.2512051409928517, 10.02280941442790585 ) ) ;
#58124=AXIS2_PLACEMENT_3D ( 'NONE', #102210, #53657, #27842 ) ;
#58126=B_SPLINE_CURVE_WITH_KNOTS ( 'NONE', 3,
 ( #81906, #99700, #51137, #8022, #25870, #65746, #2056, #24254 ),
 .UNSPECIFIED., .F., .F.,
 ( 4, 2, 2, 4 ),
 ( 0.000000000000000000, 0.002002078253806423812, 0.003003117380709634850, 0.004004156507612845889 ),
 .UNSPECIFIED. ) ;
#58135=CARTESIAN_POINT ( 'NONE',  ( -31.47286749730675837, 438.9570384604948572, 23.21156150463603396 ) ) ;
#58142=AXIS2_PLACEMENT_3D ( 'NONE', #2643, #52797, #61444 ) ;
#58145=CARTESIAN_POINT ( 'NONE',  ( 38.51502786939645517, 460.0233756673477501, 2.043034587343977027 ) ) ;
#58158=CARTESIAN_POINT ( 'NONE',  ( -9.403135590048261605, 294.6596552050577316, -3.414844070320783853 ) ) ;
#58166=CARTESIAN_POINT ( 'NONE',  ( 29.98619893519776980, 322.2519330491974756, 14.47105243112991424 ) ) ;
#58167=ADVANCED_FACE ( 'NONE', ( #76441 ), #93030, .T. ) ;
#58170=ORIENTED_EDGE ( 'NONE', *, *, #42854, .T. ) ;
#58190=CARTESIAN_POINT ( 'NONE',  ( -0.2504595177851753895, 295.3551702422010976, -10.00003484568030743 ) ) ;
#58202=CARTESIAN_POINT ( 'NONE',  ( 36.22417390464762121, 491.4095951024645501, 12.30556361670505261 ) ) ;
#58209=CARTESIAN_POINT ( 'NONE',  ( -4.240603921359149098, 300.6920857498121791, -10.01075349357188671 ) ) ;
#58214=VERTEX_POINT ( 'NONE', #33901 ) ;
#58219=CARTESIAN_POINT ( 'NONE',  ( -31.09458889425144434, 439.4642108243003236, 22.89797391519575598 ) ) ;
#58220=CARTESIAN_POINT ( 'NONE',  ( -35.41617299308384759, 356.1013257493688116, 1.637565765989996924 ) ) ;
#58225=ORIENTED_EDGE ( 'NONE', *, *, #83337, .T. ) ;
#58227=CARTESIAN_POINT ( 'NONE',  ( -25.32031312100193787, 295.7141235396721868, -1.814807454844818091 ) ) ;
#58233=CARTESIAN_POINT ( 'NONE',  ( -33.13280996007087964, 418.5609396882045985, 25.60171976399747962 ) ) ;
#58246=PLANE ( 'NONE',  #63458 ) ;
#58268=DIRECTION ( 'NONE',  ( 0.000000000000000000, 1.000000000000000000, 0.000000000000000000 ) ) ;
#58287=CARTESIAN_POINT ( 'NONE',  ( 31.00389226249483698, 502.9289871839745842, 8.047326149841639520 ) ) ;
#58291=CARTESIAN_POINT ( 'NONE',  ( 30.00000000000000355, 488.9470845376470152, 4.704489282115695836 ) ) ;
#58298=EDGE_CURVE ( 'NONE', #71668, #22245, #3137, .T. ) ;
#58302=CARTESIAN_POINT ( 'NONE',  ( 32.10528697966009304, 486.1671898930079578, 5.449875171705039989 ) ) ;
#58328=CARTESIAN_POINT ( 'NONE',  ( 44.08794255037973642, 463.0964040308558651, 6.207849963035648955 ) ) ;
#58345=CARTESIAN_POINT ( 'NONE',  ( 43.81012751977134911, 434.3196218770722226, 12.85389645199637876 ) ) ;
#58353=CARTESIAN_POINT ( 'NONE',  ( -43.87189908090044810, 464.7380721632326299, 11.09531536897684845 ) ) ;
#58360=ADVANCED_FACE ( 'NONE', ( #29539 ), #89570, .T. ) ;
#58366=CARTESIAN_POINT ( 'NONE',  ( 29.38364792612947696, 318.1686199073527064, 13.45560025562014239 ) ) ;
#58371=FACE_OUTER_BOUND ( 'NONE', #62041, .T. ) ;
#58375=CARTESIAN_POINT ( 'NONE',  ( -41.46829470068448131, 485.6020146962604258, -3.691375462659010065 ) ) ;
#58387=( BOUNDED_SURFACE ( )  B_SPLINE_SURFACE ( 3, 2, ( 
 ( #66140, #49419, #59663 ),
 ( #17075, #99561, #75829 ),
 ( #92545, #1383, #83386 ),
 ( #49952, #92012, #25741 ),
 ( #9484, #51004, #83922 ),
 ( #34351, #8958, #67225 ),
 ( #25184, #10033, #82321 ),
 ( #100101, #42394, #26268 ) ),
 .UNSPECIFIED., .F., .F., .F. ) 
 B_SPLINE_SURFACE_WITH_KNOTS ( ( 4, 2, 2, 4 ),
 ( 3, 3 ),
 ( -2.788567987632717404E-16, 0.002319727980553370865, 0.003479591970830195943, 0.004639455961107021020 ),
 ( 0.000000000000000000, 1.000000000000000000 ),
 .UNSPECIFIED. ) 
 GEOMETRIC_REPRESENTATION_ITEM ( )  RATIONAL_B_SPLINE_SURFACE ( (
 ( 1.000000000000000000, 0.8162384603568769714, 1.000000000000000000),
 ( 1.000000000000000000, 0.8233098591463237081, 1.000000000000000000),
 ( 1.000000000000000000, 0.8247006568299118934, 1.000000000000000000),
 ( 1.000000000000000000, 0.8207129887245617761, 1.000000000000000000),
 ( 1.000000000000000000, 0.8182997519101262718, 1.000000000000000000),
 ( 1.000000000000000000, 0.8111528056802195241, 1.000000000000000000),
 ( 1.000000000000000000, 0.8064385712632257119, 1.000000000000000000),
 ( 1.000000000000000000, 0.8001746426090996511, 1.000000000000000000) ) ) 
 REPRESENTATION_ITEM ( '' )  SURFACE ( )  );
#58388=CARTESIAN_POINT ( 'NONE',  ( -33.07157046098463837, 370.7458470923621121, 23.83779455093726440 ) ) ;
#58391=ORIENTED_EDGE ( 'NONE', *, *, #12027, .T. ) ;
#58393=CIRCLE ( 'NONE', #11876, 1.000000000000001554 ) ;
#58402=CARTESIAN_POINT ( 'NONE',  ( 11.70976969407574586, 294.5933519376489471, -2.054959583466348327 ) ) ;
#58406=CARTESIAN_POINT ( 'NONE',  ( 37.86095226302548156, 439.1110924549081460, 23.53113382162239375 ) ) ;
#58428=CARTESIAN_POINT ( 'NONE',  ( 0.000000000000000000, 81.00000000000000000, -8.000000000000007105 ) ) ;
#58430=CARTESIAN_POINT ( 'NONE',  ( -20.97754405179121662, 294.8763868968453608, 9.942224931492262385 ) ) ;
#58433=CARTESIAN_POINT ( 'NONE',  ( 26.13430946603648763, 305.6458041140454611, -9.606786330514147210 ) ) ;
#58434=ORIENTED_EDGE ( 'NONE', *, *, #58972, .F. ) ;
#58447=CARTESIAN_POINT ( 'NONE',  ( -36.54117467508550021, 437.9945884957556359, 4.200333155677842711 ) ) ;
#58476=ADVANCED_FACE ( 'NONE', ( #57462 ), #26300, .T. ) ;
#58477=CARTESIAN_POINT ( 'NONE',  ( 27.38488877681253797, 307.9860580968508543, -8.296557478737108582 ) ) ;
#58478=ORIENTED_EDGE ( 'NONE', *, *, #53710, .T. ) ;
#58489=CARTESIAN_POINT ( 'NONE',  ( -35.85186990248676864, 464.1122956640483039, 19.44147592470968533 ) ) ;
#58496=CARTESIAN_POINT ( 'NONE',  ( 6.624059643703564149, 294.7379298340728724, -10.02420444108935449 ) ) ;
#58503=SURFACE_STYLE_USAGE ( .BOTH. , #43381 ) ;
#58507=CARTESIAN_POINT ( 'NONE',  ( -34.04237759262028362, 317.4902085936202525, -6.467307987191631469 ) ) ;
#58508=CARTESIAN_POINT ( 'NONE',  ( -1.262177448353618889E-25, 303.8518027762757470, -10.00000000000000533 ) ) ;
#58513=ORIENTED_EDGE ( 'NONE', *, *, #64113, .F. ) ;
#58521=B_SPLINE_CURVE_WITH_KNOTS ( 'NONE', 3,
 ( #5027, #48110, #46539, #6596 ),
 .UNSPECIFIED., .F., .F.,
 ( 4, 4 ),
 ( 8.842683793321775393E-16, 0.002118337988231762566 ),
 .UNSPECIFIED. ) ;
#58531=CIRCLE ( 'NONE', #53362, 3.000000000000001332 ) ;
#58535=CARTESIAN_POINT ( 'NONE',  ( -36.90171438448089702, 490.9796882048097473, 12.46551445837863170 ) ) ;
#58545=VERTEX_POINT ( 'NONE', #83348 ) ;
#58568=EDGE_LOOP ( 'NONE', ( #14945, #87851, #4718, #59738, #31590, #81084 ) ) ;
#58572=CARTESIAN_POINT ( 'NONE',  ( -42.61862769184566702, 462.7773997383516189, 13.89716539804779849 ) ) ;
#58579=CARTESIAN_POINT ( 'NONE',  ( 30.28764838604852017, 297.9584608233138283, -1.316668081967330872 ) ) ;
#58589=CARTESIAN_POINT ( 'NONE',  ( 45.42661373406953373, 432.5777411345648602, 6.977553785134991138 ) ) ;
#58591=ORIENTED_EDGE ( 'NONE', *, *, #7373, .T. ) ;
#58596=FACE_OUTER_BOUND ( 'NONE', #5456, .T. ) ;
#58597=EDGE_CURVE ( 'NONE', #16697, #72766, #17289, .T. ) ;
#58606=CARTESIAN_POINT ( 'NONE',  ( 35.40719753841921857, 462.9391285011967057, 4.212165350506638539 ) ) ;
#58608=CIRCLE ( 'NONE', #98233, 1.000000000000020872 ) ;
#58609=ADVANCED_FACE ( 'NONE', ( #100594 ), #37311, .F. ) ;
#58615=CARTESIAN_POINT ( 'NONE',  ( 40.75641113481592726, 360.0948485545300741, 24.37153223514695100 ) ) ;
#58617=CARTESIAN_POINT ( 'NONE',  ( 20.37278541768179352, 303.8378246129572631, -10.00297115033344042 ) ) ;
#58618=CARTESIAN_POINT ( 'NONE',  ( -30.00000000000557066, 486.8872575320209535, 5.529676739975230682 ) ) ;
#58631=CARTESIAN_POINT ( 'NONE',  ( -32.11723946003972685, 433.0660616616644916, 24.32198794831119315 ) ) ;
#58632=ORIENTED_EDGE ( 'NONE', *, *, #15856, .T. ) ;
#58642=FACE_OUTER_BOUND ( 'NONE', #66127, .T. ) ;
#58648=CARTESIAN_POINT ( 'NONE',  ( 26.92115534363001927, 306.8708247227045263, 10.86266092317258014 ) ) ;
#58652=CARTESIAN_POINT ( 'NONE',  ( -40.38232636938239040, 459.8969133356654311, 1.930624307836338538 ) ) ;
#58653=CARTESIAN_POINT ( 'NONE',  ( 35.26876087351732991, 303.5869067510492414, 3.947903635018046753 ) ) ;
#58655=ADVANCED_FACE ( 'NONE', ( #11575 ), #89155, .F. ) ;
#58658=CARTESIAN_POINT ( 'NONE',  ( -24.63377937114793070, 295.6205676188575922, 10.10213930309776487 ) ) ;
#58660=DIRECTION ( 'NONE',  ( -0.4127509058087894256, -0.1524945595932338249, 0.8979878056234892325 ) ) ;
#58661=CARTESIAN_POINT ( 'NONE',  ( 1.012484905089438447, 302.8485832885119180, 9.936327107362844302 ) ) ;
#58665=CARTESIAN_POINT ( 'NONE',  ( 9.508870726040163035, 294.7346411812065412, 3.160106868736997754 ) ) ;
#58667=CARTESIAN_POINT ( 'NONE',  ( 43.71039113854127578, 464.8436985699679553, 11.74907638618312689 ) ) ;
#58672=DIRECTION ( 'NONE',  ( 0.000000000000000000, 0.000000000000000000, -1.000000000000000000 ) ) ;
#58684=CARTESIAN_POINT ( 'NONE',  ( -31.33625597974778998, 438.2397719845374695, 22.62029172958331102 ) ) ;
#58685=CARTESIAN_POINT ( 'NONE',  ( -37.83989825151947173, 491.6297408768480750, 12.44743998624971049 ) ) ;
#58697=( BOUNDED_SURFACE ( )  B_SPLINE_SURFACE ( 3, 2, ( 
 ( #48625, #40550, #8180 ),
 ( #80466, #16270, #47571 ),
 ( #40028, #105811, #24924 ),
 ( #58328, #81510, #33543 ),
 ( #98772, #99299, #23876 ),
 ( #73969, #33023, #25472 ),
 ( #50, #80997, #56720 ),
 ( #49702, #64832, #39511 ),
 ( #106325, #7112, #56171 ),
 ( #6578, #32492, #31437 ) ),
 .UNSPECIFIED., .F., .F., .F. ) 
 B_SPLINE_SURFACE_WITH_KNOTS ( ( 4, 2, 2, 2, 4 ),
 ( 3, 3 ),
 ( 0.006110147660091587093, 0.007140910106262555491, 0.008171672552433523889, 0.009202434998604493155, 0.01023319744477546242 ),
 ( 0.1475238061142898349, 1.000000000000000000 ),
 .UNSPECIFIED. ) 
 GEOMETRIC_REPRESENTATION_ITEM ( )  RATIONAL_B_SPLINE_SURFACE ( (
 ( 0.9263311855299185549, 0.7503155036109609988, 1.000000000000000000),
 ( 0.9308198837936185743, 0.7655289745141671265, 1.000000000000000000),
 ( 0.9348045508654743152, 0.7790341408219316754, 1.000000000000000000),
 ( 0.9412515216610307656, 0.8008847524803706097, 1.000000000000000000),
 ( 0.9437092470908616804, 0.8092146806952340565, 1.000000000000000000),
 ( 0.9465994843889277144, 0.8190105142430310625, 1.000000000000000000),
 ( 0.9470205592359524083, 0.8204376562688353580, 1.000000000000000000),
 ( 0.9455968065556910052, 0.8156121548200778726, 1.000000000000000000),
 ( 0.9437572519950128136, 0.8093773829241677209, 1.000000000000000000),
 ( 0.9409237764627873535, 0.7997739310920261024, 1.000000000000000000) ) ) 
 REPRESENTATION_ITEM ( '' )  SURFACE ( )  );
#58704=ORIENTED_EDGE ( 'NONE', *, *, #98498, .T. ) ;
#58705=CARTESIAN_POINT ( 'NONE',  ( 32.22503847990217452, 485.9064490506207790, 4.829857536092636572 ) ) ;
#58719=CARTESIAN_POINT ( 'NONE',  ( 29.25197604607760837, 322.6282941308829777, 13.32234211285258851 ) ) ;
#58730=CARTESIAN_POINT ( 'NONE',  ( -43.87115969799085491, 464.7386531662417042, 11.09928998703223613 ) ) ;
#58731=CARTESIAN_POINT ( 'NONE',  ( -24.60488647473181345, 306.9835580411500473, 10.41807558718820914 ) ) ;
#58739=VECTOR ( 'NONE', #74274, 1000.000000000000000 ) ;
#58742=CARTESIAN_POINT ( 'NONE',  ( 36.04632348377495532, 437.4611277465810986, 4.334040331412323255 ) ) ;
#58743=CARTESIAN_POINT ( 'NONE',  ( -9.970195021759460374, 302.6460196488378642, -10.04373974541436887 ) ) ;
#58750=CARTESIAN_POINT ( 'NONE',  ( -19.03547406814728404, 294.6738091296812740, 9.899165902142932794 ) ) ;
#58751=EDGE_CURVE ( 'NONE', #66199, #55140, #44348, .T. ) ;
#58770=CARTESIAN_POINT ( 'NONE',  ( 32.65817089032879750, 465.7881089174891827, 12.85132715800152425 ) ) ;
#58774=CARTESIAN_POINT ( 'NONE',  ( -34.84618260875200946, 489.9833681528629654, 11.97975507378840732 ) ) ;
#58784=CARTESIAN_POINT ( 'NONE',  ( -36.53342718661301802, 485.2762471673754590, -2.915875507118013577 ) ) ;
#58785=CARTESIAN_POINT ( 'NONE',  ( -42.72184728503030726, 427.3449066199571575, 19.12547310894770547 ) ) ;
#58786=CARTESIAN_POINT ( 'NONE',  ( -32.10528697966014278, 486.1671898930081284, 5.449875171704950283 ) ) ;
#58790=AXIS2_PLACEMENT_3D ( 'NONE', #72635, #14386, #88309 ) ;
#58797=CARTESIAN_POINT ( 'NONE',  ( -40.16961380562399597, 438.0191182675681034, 22.24568332716581764 ) ) ;
#58817=CARTESIAN_POINT ( 'NONE',  ( 31.46099760824767344, 298.7896251960808627, -1.127419728356056972 ) ) ;
#58854=CARTESIAN_POINT ( 'NONE',  ( -18.13825514061547040, 304.6380168175756467, 9.891557803754992051 ) ) ;
#58883=CARTESIAN_POINT ( 'NONE',  ( -29.99999999998746603, 464.1079104336457704, 10.87617013708814895 ) ) ;
#58884=EDGE_CURVE ( 'NONE', #26380, #72809, #72669, .T. ) ;
#58894=CARTESIAN_POINT ( 'NONE',  ( 43.78405977006951844, 434.9821340022160712, 12.01170688373657747 ) ) ;
#58905=CARTESIAN_POINT ( 'NONE',  ( -25.95735158692081512, 308.9733421463816399, 9.899401087310158331 ) ) ;
#58912=CARTESIAN_POINT ( 'NONE',  ( 42.51801476543153768, 435.0274750839332114, 8.236762145192395579 ) ) ;
#58913=CARTESIAN_POINT ( 'NONE',  ( 43.03357534759653191, 463.2291678140142608, 4.675918524165872725 ) ) ;
#58914=CARTESIAN_POINT ( 'NONE',  ( 24.32063559030665090, 305.3189669248208133, 10.26072861867763031 ) ) ;
#58917=EDGE_CURVE ( 'NONE', #97550, #88846, #2991, .T. ) ;
#58930=CARTESIAN_POINT ( 'NONE',  ( 32.25691083757155297, 485.8985639246220103, 4.832559767444084997 ) ) ;
#58932=CARTESIAN_POINT ( 'NONE',  ( -33.14133759817422487, 415.2060550120342555, 25.73546352636587287 ) ) ;
#58933=CARTESIAN_POINT ( 'NONE',  ( -32.04918168811659740, 435.9039269519959134, 19.85355728535080644 ) ) ;
#58935=VERTEX_POINT ( 'NONE', #14758 ) ;
#58936=( GEOMETRIC_REPRESENTATION_CONTEXT ( 3 ) GLOBAL_UNCERTAINTY_ASSIGNED_CONTEXT ( ( #50501 ) ) GLOBAL_UNIT_ASSIGNED_CONTEXT ( ( #65367, #31954, #40554 ) ) REPRESENTATION_CONTEXT ( 'NONE', 'WORKASPACE' ) );
#58937=CARTESIAN_POINT ( 'NONE',  ( -1.128077836147719282, 302.8478239976500390, 9.936168295454388399 ) ) ;
#58945=CARTESIAN_POINT ( 'NONE',  ( 41.36052874979234417, 437.1976709138604065, 21.04111601629670858 ) ) ;
#58946=VERTEX_POINT ( 'NONE', #25566 ) ;
#58951=B_SPLINE_CURVE_WITH_KNOTS ( 'NONE', 3,
 ( #35674, #9211, #33524, #100358 ),
 .UNSPECIFIED., .F., .F.,
 ( 4, 4 ),
 ( 6.938893903907227607E-18, 0.001714393297546037542 ),
 .UNSPECIFIED. ) ;
#58972=EDGE_CURVE ( 'NONE', #80654, #56333, #84132, .T. ) ;
#58984=FACE_OUTER_BOUND ( 'NONE', #35313, .T. ) ;
#59011=CARTESIAN_POINT ( 'NONE',  ( 28.72726883065406156, 309.6741498678223365, -7.894823244335800183 ) ) ;
#59019=DIRECTION ( 'NONE',  ( -1.000000000000000000, -0.000000000000000000, -0.000000000000000000 ) ) ;
#59021=CARTESIAN_POINT ( 'NONE',  ( -33.77559172535808329, 464.7834715296605737, 7.192701217093241617 ) ) ;
#59023=CARTESIAN_POINT ( 'NONE',  ( -37.13212445136107931, 463.5388707510370523, 19.67708231431734234 ) ) ;
#59027=FACE_OUTER_BOUND ( 'NONE', #38307, .T. ) ;
#59042=CARTESIAN_POINT ( 'NONE',  ( -35.84216525457394198, 303.7309719522399405, 0.04073617280396817086 ) ) ;
#59047=VERTEX_POINT ( 'NONE', #90797 ) ;
#59059=B_SPLINE_CURVE_WITH_KNOTS ( 'NONE', 3,
 ( #82781, #57958, #18067, #90883, #98429, #8355, #16998, #42314, #74144, #17535, #8883, #50925 ),
 .UNSPECIFIED., .F., .F.,
 ( 4, 2, 2, 2, 2, 4 ),
 ( 5.204170427930421283E-18, 0.001828837400933321523, 0.002743256101399958215, 0.003657674801866594907, 0.005486512202799889541, 0.007315349603733184609 ),
 .UNSPECIFIED. ) ;
#59076=CARTESIAN_POINT ( 'NONE',  ( 32.89379909751026076, 463.7243792478176942, 7.148845075438556407 ) ) ;
#59103=B_SPLINE_CURVE_WITH_KNOTS ( 'NONE', 3,
 ( #56031, #39884, #46382, #79271, #105143, #5395, #7486, #38830 ),
 .UNSPECIFIED., .F., .F.,
 ( 4, 2, 2, 4 ),
 ( -5.999999999613023197E-08, 0.002878992039937437828, 0.005758044079874871830, 0.01151614815974974504 ),
 .UNSPECIFIED. ) ;
#59104=CARTESIAN_POINT ( 'NONE',  ( -42.58872141072839668, 362.7331401274527138, 16.77583143465006899 ) ) ;
#59112=CARTESIAN_POINT ( 'NONE',  ( 29.27755364888704648, 297.1129628640473470, -9.507834925361459355 ) ) ;
#59113=CARTESIAN_POINT ( 'NONE',  ( 24.37088254901632567, 295.3567874699774620, -9.892597027135842325 ) ) ;
#59115=CARTESIAN_POINT ( 'NONE',  ( -43.00000000000000000, 488.9831568219305495, 4.757012338623821890 ) ) ;
#59122=CARTESIAN_POINT ( 'NONE',  ( 43.65263200446639047, 415.3088531594569304, 15.97955559133532688 ) ) ;
#59123=EDGE_LOOP ( 'NONE', ( #45475, #28949, #73426, #66146 ) ) ;
#59124=B_SPLINE_CURVE_WITH_KNOTS ( 'NONE', 3,
 ( #2825, #101538, #44366, #93457 ),
 .UNSPECIFIED., .F., .F.,
 ( 4, 4 ),
 ( 1.250926888277100303E-17, 0.001935030059085742068 ),
 .UNSPECIFIED. ) ;
#59126=CARTESIAN_POINT ( 'NONE',  ( -19.70764564238368877, 304.7954121406193053, 9.925013215726828264 ) ) ;
#59134=CARTESIAN_POINT ( 'NONE',  ( 46.00000000000000000, 436.1561742938424118, 10.01163487455054657 ) ) ;
#59148=CARTESIAN_POINT ( 'NONE',  ( 23.61963550967466574, 306.0340374937824777, 10.19690224617928287 ) ) ;
#59151=CARTESIAN_POINT ( 'NONE',  ( -30.00000000000000355, 490.5636507776912367, 7.413185101876573313 ) ) ;
#59168=CARTESIAN_POINT ( 'NONE',  ( -32.72541600402464468, 465.0324911293606647, 11.87889517178131982 ) ) ;
#59172=CARTESIAN_POINT ( 'NONE',  ( 37.98996485649870891, 439.4613508614656325, 23.87710038502308763 ) ) ;
#59175=ORIENTED_EDGE ( 'NONE', *, *, #90372, .F. ) ;
#59178=CARTESIAN_POINT ( 'NONE',  ( 33.12944332324993013, 439.4248878830264857, 23.85028906779293223 ) ) ;
#59181=CARTESIAN_POINT ( 'NONE',  ( 32.84946521457204227, 300.3690703675980558, 3.178420029388444146 ) ) ;
#59199=DIRECTION ( 'NONE',  ( 0.000000000000000000, 0.000000000000000000, 1.000000000000000000 ) ) ;
#59244=CARTESIAN_POINT ( 'NONE',  ( -1.140137277112188485, 294.8483051625062217, -9.950919916537934284 ) ) ;
#59252=CARTESIAN_POINT ( 'NONE',  ( 30.38819389726869602, 339.6136208926041604, 18.22926607251833531 ) ) ;
#59264=CARTESIAN_POINT ( 'NONE',  ( -22.91885868373643831, 305.6172567281201964, 10.10309701371861912 ) ) ;
#59285=EDGE_CURVE ( 'NONE', #696, #98784, #28996, .T. ) ;
#59287=B_SPLINE_CURVE_WITH_KNOTS ( 'NONE', 3,
 ( #9255, #99322, #25496, #34119, #100933, #83678, #27092, #17914, #35170, #33047, #41641, #83159 ),
 .UNSPECIFIED., .F., .F.,
 ( 4, 2, 2, 2, 2, 4 ),
 ( 9.220181747203676555E-18, 0.002064083228126805183, 0.003096124842190242903, 0.004128166456253680623, 0.006192249684380478868, 0.008256332912507276245 ),
 .UNSPECIFIED. ) ;
#59302=CARTESIAN_POINT ( 'NONE',  ( -23.81822736121795003, 305.6269812178131247, -9.833007305667777587 ) ) ;
#59314=CARTESIAN_POINT ( 'NONE',  ( -42.08109764087019755, 343.1592929535903522, 13.36121580716647372 ) ) ;
#59315=FACE_OUTER_BOUND ( 'NONE', #62547, .T. ) ;
#59323=CARTESIAN_POINT ( 'NONE',  ( -40.30332470629049624, 437.2182582767285908, 22.21307012533235792 ) ) ;
#59325=CARTESIAN_POINT ( 'NONE',  ( -39.56197461363974810, -0.1944580884125578779, -19.78098730681986339 ) ) ;
#59332=( BOUNDED_SURFACE ( )  B_SPLINE_SURFACE ( 3, 2, ( 
 ( #48069, #31925, #89085 ),
 ( #98739, #32465, #80969 ),
 ( #40525, #31409, #90140 ),
 ( #7088, #57749, #40001 ) ),
 .UNSPECIFIED., .F., .F., .F. ) 
 B_SPLINE_SURFACE_WITH_KNOTS ( ( 4, 4 ),
 ( 3, 3 ),
 ( -4.996003610813204432E-16, 0.003677210556160862790 ),
 ( 0.000000000000000000, 1.000000000000000000 ),
 .UNSPECIFIED. ) 
 GEOMETRIC_REPRESENTATION_ITEM ( )  RATIONAL_B_SPLINE_SURFACE ( (
 ( 1.000000000000000000, 0.7874655377939757672, 1.000000000000000000),
 ( 1.000000000000000000, 0.7709584336437098617, 1.000000000000000000),
 ( 1.000000000000000000, 0.7542748649868799005, 1.000000000000000000),
 ( 1.000000000000000000, 0.7370557512815874013, 1.000000000000000000) ) ) 
 REPRESENTATION_ITEM ( '' )  SURFACE ( )  );
#59333=CIRCLE ( 'NONE', #761, 10.00000000000000533 ) ;
#59346=CARTESIAN_POINT ( 'NONE',  ( 25.93947128054312756, 296.0094280503604978, 10.18659011856751384 ) ) ;
#59353=CARTESIAN_POINT ( 'NONE',  ( -17.24303157407923237, 294.5700599009814482, 9.877113118490870036 ) ) ;
#59358=CARTESIAN_POINT ( 'NONE',  ( -41.58466061806753800, 465.5764877067418865, 15.80465680671442819 ) ) ;
#59371=CIRCLE ( 'NONE', #9370, 15.00000000000001421 ) ;
#59372=CARTESIAN_POINT ( 'NONE',  ( -16.85961028550735463, 304.5626392334940533, -9.061460871365316194 ) ) ;
#59373=CARTESIAN_POINT ( 'NONE',  ( 35.57955382936916067, 363.3973965622570859, 2.919629247011395368 ) ) ;
#59374=CARTESIAN_POINT ( 'NONE',  ( 40.21064024339792553, 459.8708642436264995, 1.907892319915238888 ) ) ;
#59379=ORIENTED_EDGE ( 'NONE', *, *, #42280, .T. ) ;
#59385=CARTESIAN_POINT ( 'NONE',  ( -11.89098014788630664, 303.5914335720564168, -10.05534211649429643 ) ) ;
#59388=CARTESIAN_POINT ( 'NONE',  ( 31.99156825197944798, 486.4558694464275277, 6.110232253381057355 ) ) ;
#59391=CARTESIAN_POINT ( 'NONE',  ( -32.99999999999993605, 464.4386723251832905, 6.308603495333271916 ) ) ;
#59392=CARTESIAN_POINT ( 'NONE',  ( 43.20037042670922744, 463.4262835534589158, 5.016616955632313690 ) ) ;
#59416=CARTESIAN_POINT ( 'NONE',  ( -22.42417502586373246, 305.3961751430792333, 10.05444931189341773 ) ) ;
#59419=CARTESIAN_POINT ( 'NONE',  ( 37.52579488121515539, 438.0832148649091096, 4.091984033318603053 ) ) ;
#59424=CARTESIAN_POINT ( 'NONE',  ( -32.11826742301046522, 487.8588087913806817, 8.620620385259270435 ) ) ;
#59425=ORIENTED_EDGE ( 'NONE', *, *, #73750, .T. ) ;
#59429=VERTEX_POINT ( 'NONE', #82837 ) ;
#59442=CARTESIAN_POINT ( 'NONE',  ( -33.74742351813127073, 478.7265835501554534, 3.791636934804474279 ) ) ;
#59443=VERTEX_POINT ( 'NONE', #77942 ) ;
#59461=CARTESIAN_POINT ( 'NONE',  ( -44.17094014566056615, 463.2864587933497091, 6.608468562565803950 ) ) ;
#59463=DIRECTION ( 'NONE',  ( 1.000000000000000000, 0.000000000000000000, 0.000000000000000000 ) ) ;
#59464=EDGE_LOOP ( 'NONE', ( #78102, #75330, #59484, #103003 ) ) ;
#59465=CARTESIAN_POINT ( 'NONE',  ( -11.72692804380855591, 302.5954534377697200, -10.05449581651908453 ) ) ;
#59468=CARTESIAN_POINT ( 'NONE',  ( 29.99999999999996092, 486.4444101590605101, 4.645498354857360290 ) ) ;
#59471=CARTESIAN_POINT ( 'NONE',  ( -29.56778029646497075, 314.0584236046759656, 12.66027079984575821 ) ) ;
#59475=EDGE_CURVE ( 'NONE', #99399, #29309, #37364, .T. ) ;
#59476=DIRECTION ( 'NONE',  ( 0.000000000000000000, 0.000000000000000000, -1.000000000000000000 ) ) ;
#59483=CARTESIAN_POINT ( 'NONE',  ( 41.84139522851419457, 436.8002711404864726, 20.35041468290338429 ) ) ;
#59484=ORIENTED_EDGE ( 'NONE', *, *, #103994, .T. ) ;
#59485=CARTESIAN_POINT ( 'NONE',  ( 43.00000000000000000, 500.0000000000002274, 0.000000000000000000 ) ) ;
#59492=CARTESIAN_POINT ( 'NONE',  ( -30.00000000000000355, 462.0139486977119532, 13.78583326881746096 ) ) ;
#59494=CARTESIAN_POINT ( 'NONE',  ( 31.80647371913423171, 437.2005603137831145, 20.73398510949202489 ) ) ;
#59501=CARTESIAN_POINT ( 'NONE',  ( 0.000000000000000000, 0.000000000000000000, 0.000000000000000000 ) ) ;
#59515=DIRECTION ( 'NONE',  ( -1.224646799147353454E-16, 0.000000000000000000, -1.000000000000000000 ) ) ;
#59534=PRODUCT_DEFINITION_SHAPE ( 'NONE', 'NONE',  #19320 ) ;
#59550=CARTESIAN_POINT ( 'NONE',  ( 34.54626167956425320, 338.5217528747888309, -0.8335436382952816636 ) ) ;
#59551=EDGE_LOOP ( 'NONE', ( #35066, #91267, #11720, #24707 ) ) ;
#59556=CARTESIAN_POINT ( 'NONE',  ( -44.26939524490970967, 485.3791217652519663, 2.298766312372937826 ) ) ;
#59559=CARTESIAN_POINT ( 'NONE',  ( 32.71046359557010419, 465.7618366408551651, 11.82978892796172765 ) ) ;
#59560=CARTESIAN_POINT ( 'NONE',  ( -36.69926874265555483, 463.5184712008561974, 19.71956904107290143 ) ) ;
#59561=ORIENTED_EDGE ( 'NONE', *, *, #5866, .F. ) ;
#59565=DIRECTION ( 'NONE',  ( 0.000000000000000000, 0.000000000000000000, 1.000000000000000000 ) ) ;
#59575=DIRECTION ( 'NONE',  ( 0.000000000000000000, 0.000000000000000000, 1.000000000000000000 ) ) ;
#59579=CARTESIAN_POINT ( 'NONE',  ( -39.22939421798824355, 311.7623099566353062, 2.037218283543303698 ) ) ;
#59580=CARTESIAN_POINT ( 'NONE',  ( -46.00000000000000000, 450.0000000000002274, 13.20242257375370976 ) ) ;
#59596=ORIENTED_EDGE ( 'NONE', *, *, #104943, .F. ) ;
#59614=ORIENTED_EDGE ( 'NONE', *, *, #15609, .T. ) ;
#59622=EDGE_LOOP ( 'NONE', ( #54232, #27436, #45756, #98947 ) ) ;
#59633=EDGE_LOOP ( 'NONE', ( #54400, #94139, #57430, #10064, #80951 ) ) ;
#59637=FACE_OUTER_BOUND ( 'NONE', #33244, .T. ) ;
#59638=CARTESIAN_POINT ( 'NONE',  ( -42.77874154194343248, 403.4964952544876837, 19.98380564842762652 ) ) ;
#59644=CARTESIAN_POINT ( 'NONE',  ( 25.15391212174589342, 295.6014252248689331, -9.839392187590416228 ) ) ;
#59645=CARTESIAN_POINT ( 'NONE',  ( 43.29658055318886767, 324.1952503670673877, -2.852919881210743913 ) ) ;
#59655=CARTESIAN_POINT ( 'NONE',  ( 51.01037695545453232, 450.0000000000002274, 8.202422573753707979 ) ) ;
#59657=CARTESIAN_POINT ( 'NONE',  ( 43.71037717921920773, 462.3391554988764369, 4.824299547763891027 ) ) ;
#59659=CARTESIAN_POINT ( 'NONE',  ( 31.31558333044079845, 439.0792886710837593, 22.75757024719011667 ) ) ;
#59661=( BOUNDED_SURFACE ( )  B_SPLINE_SURFACE ( 3, 2, ( 
 ( #16830, #8724, #75588 ),
 ( #34110, #41632, #82622 ),
 ( #50249, #593, #74516 ),
 ( #23891, #17906, #33038 ),
 ( #82075, #42693, #48639 ),
 ( #98269, #58894, #73447 ),
 ( #1687, #33558, #25486 ),
 ( #91785, #83150, #32506 ),
 ( #58345, #98785, #66433 ),
 ( #57260, #50759, #99314 ),
 ( #91264, #83667, #66982 ),
 ( #42156, #75038, #8193 ) ),
 .UNSPECIFIED., .F., .F., .F. ) 
 B_SPLINE_SURFACE_WITH_KNOTS ( ( 4, 2, 2, 2, 2, 4 ),
 ( 3, 3 ),
 ( -7.849623728795052102E-17, 0.001471464792628909357, 0.002942929585257897211, 0.003678661981572391246, 0.004414394377886885282, 0.005885859170515872485 ),
 ( 0.000000000000000000, 1.000000000000000000 ),
 .UNSPECIFIED. ) 
 GEOMETRIC_REPRESENTATION_ITEM ( )  RATIONAL_B_SPLINE_SURFACE ( (
 ( 1.000000000000000000, 0.8274249441181704690, 1.000000000000000000),
 ( 1.000000000000000000, 0.8369779515072608422, 1.000000000000000000),
 ( 1.000000000000000000, 0.8428664650367967415, 1.000000000000000000),
 ( 1.000000000000000000, 0.8506961607541885240, 1.000000000000000000),
 ( 1.000000000000000000, 0.8526029425214399771, 1.000000000000000000),
 ( 1.000000000000000000, 0.8531612821180112327, 1.000000000000000000),
 ( 1.000000000000000000, 0.8529462785843203720, 1.000000000000000000),
 ( 1.000000000000000000, 0.8517601151918051672, 1.000000000000000000),
 ( 1.000000000000000000, 0.8507906177104697099, 1.000000000000000000),
 ( 1.000000000000000000, 0.8467143344647574121, 1.000000000000000000),
 ( 1.000000000000000000, 0.8424736042939275915, 1.000000000000000000),
 ( 1.000000000000000000, 0.8360809698953391988, 1.000000000000000000) ) ) 
 REPRESENTATION_ITEM ( '' )  SURFACE ( )  );
#59663=CARTESIAN_POINT ( 'NONE',  ( 32.28930913498002298, 488.2717154064769147, 9.213726894932324996 ) ) ;
#59667=DIRECTION ( 'NONE',  ( -0.3108677890940485522, 0.06041750367991206849, 0.9485309393756568008 ) ) ;
#59675=CARTESIAN_POINT ( 'NONE',  ( 37.65939668336066148, 425.4643409788083659, 5.784973202707226037 ) ) ;
#59680=ORIENTED_EDGE ( 'NONE', *, *, #81241, .T. ) ;
#59682=AXIS2_PLACEMENT_3D ( 'NONE', #55466, #45290, #13418 ) ;
#59684=CARTESIAN_POINT ( 'NONE',  ( -43.99367409961224240, 462.7719748076324322, 5.584664003525471543 ) ) ;
#59696=ADVANCED_FACE ( 'NONE', ( #73004 ), #97118, .F. ) ;
#59697=CARTESIAN_POINT ( 'NONE',  ( -27.73415475396909358, 311.1673401819404603, 11.68908720022844783 ) ) ;
#59698=ORIENTED_EDGE ( 'NONE', *, *, #64576, .F. ) ;
#59702=CARTESIAN_POINT ( 'NONE',  ( -32.12958771267405211, 464.7275665249412668, 11.12424126545829495 ) ) ;
#59705=CARTESIAN_POINT ( 'NONE',  ( -18.18913180585775180, 303.6389006221185696, 9.891726125135546610 ) ) ;
#59708=CARTESIAN_POINT ( 'NONE',  ( -31.16747616410718180, 425.0719001433796507, 24.76640343511496312 ) ) ;
#59717=CARTESIAN_POINT ( 'NONE',  ( 35.23215581420184606, 303.5527974176312114, 3.940093505360380721 ) ) ;
#59719=CARTESIAN_POINT ( 'NONE',  ( 37.62251730745840916, 437.3427388312647395, 4.535622330043188377 ) ) ;
#59723=DIRECTION ( 'NONE',  ( 0.000000000000000000, 1.000000000000000000, -1.224646799147353207E-16 ) ) ;
#59731=CARTESIAN_POINT ( 'NONE',  ( 7.169685563733668943, 294.7252197711828785, 1.910215062213532544 ) ) ;
#59738=ORIENTED_EDGE ( 'NONE', *, *, #83198, .F. ) ;
#59740=CARTESIAN_POINT ( 'NONE',  ( 41.49004662521136311, 469.3948935002796929, 1.006167576246231654 ) ) ;
#59753=DIRECTION ( 'NONE',  ( -1.000000000000000000, 0.000000000000000000, 0.000000000000000000 ) ) ;
#59762=EDGE_LOOP ( 'NONE', ( #51465, #75168, #94733, #90825 ) ) ;
#59770=EDGE_CURVE ( 'NONE', #42175, #104525, #77637, .T. ) ;
#59772=CARTESIAN_POINT ( 'NONE',  ( -36.04676067413578977, 437.4614642643933848, 4.333815353352441058 ) ) ;
#59780=CARTESIAN_POINT ( 'NONE',  ( 0.000000000000000000, 294.8518027762758038, -10.00000000000000178 ) ) ;
#59789=CARTESIAN_POINT ( 'NONE',  ( 25.77159080061642982, 308.6327058502350837, 9.816061668938694140 ) ) ;
#59796=CARTESIAN_POINT ( 'NONE',  ( 31.56688555236322102, 439.0033367035658216, 23.33558518086852374 ) ) ;
#59799=CARTESIAN_POINT ( 'NONE',  ( -34.72474116627837759, 338.3618661353910966, -1.881472242819908436 ) ) ;
#59802=CARTESIAN_POINT ( 'NONE',  ( -43.55333112596417067, 465.2342844084853937, 9.238213423004422609 ) ) ;
#59808=DIRECTION ( 'NONE',  ( 1.000000000000000000, -0.000000000000000000, -0.000000000000000000 ) ) ;
#59820=EDGE_CURVE ( 'NONE', #58545, #22313, #34043, .T. ) ;
#59824=ORIENTED_EDGE ( 'NONE', *, *, #51619, .T. ) ;
#59827=CARTESIAN_POINT ( 'NONE',  ( -44.28898793531455880, 435.1858057187417899, 13.53393906085753784 ) ) ;
#59834=ORIENTED_EDGE ( 'NONE', *, *, #18767, .F. ) ;
#59839=AXIS2_PLACEMENT_3D ( 'NONE', #30456, #6141, #73521 ) ;
#59841=CARTESIAN_POINT ( 'NONE',  ( -23.07177167684715258, 305.3941994803996067, -8.883507296546389043 ) ) ;
#59844=( BOUNDED_SURFACE ( )  B_SPLINE_SURFACE ( 3, 2, ( 
 ( #38012, #95677, #70346 ),
 ( #85473, #103765, #69297 ),
 ( #5599, #28320, #53620 ),
 ( #29903, #94641, #62789 ) ),
 .UNSPECIFIED., .F., .F., .T. ) 
 B_SPLINE_SURFACE_WITH_KNOTS ( ( 4, 4 ),
 ( 3, 3 ),
 ( 0.01539444365212263265, 0.01716277291646237796 ),
 ( 0.000000000000000000, 0.8371568960141710924 ),
 .UNSPECIFIED. ) 
 GEOMETRIC_REPRESENTATION_ITEM ( )  RATIONAL_B_SPLINE_SURFACE ( (
 ( 1.000000000000000000, 0.7548024220745215285, 0.9201425306416157746),
 ( 1.000000000000000000, 0.7704228259270500256, 0.9252298807393316560),
 ( 1.000000000000000000, 0.7855210260306706438, 0.9301471562782772651),
 ( 1.000000000000000000, 0.8001206121096573476, 0.9349020401062981822) ) ) 
 REPRESENTATION_ITEM ( '' )  SURFACE ( )  );
#59848=CARTESIAN_POINT ( 'NONE',  ( -43.78231969043007155, 434.3019752265992679, 13.50801524700046663 ) ) ;
#59851=EDGE_LOOP ( 'NONE', ( #78203, #60793, #1963, #55292, #17936, #58591, #31193, #85487, #18262, #80407 ) ) ;
#59853=CARTESIAN_POINT ( 'NONE',  ( -32.74881744694416597, 438.8767316144407573, 23.82550921047223014 ) ) ;
#59856=CARTESIAN_POINT ( 'NONE',  ( -35.10875260009915877, 305.4746754961840338, 12.42697074198600049 ) ) ;
#59875=EDGE_CURVE ( 'NONE', #22095, #1493, #24937, .T. ) ;
#59880=EDGE_CURVE ( 'NONE', #4655, #71461, #94258, .T. ) ;
#59884=CARTESIAN_POINT ( 'NONE',  ( 9.041223236726795065, 295.5670253727153067, -10.03755077321263123 ) ) ;
#59885=CARTESIAN_POINT ( 'NONE',  ( 45.49982102694234953, 388.3127959276886827, 7.886590035822850453 ) ) ;
#59890=CARTESIAN_POINT ( 'NONE',  ( -43.71039113854124736, 464.8436985699681827, 11.74907638618257444 ) ) ;
#59892=CARTESIAN_POINT ( 'NONE',  ( 1.224646799147353256E-15, 80.00000000000000000, 10.00000000000000000 ) ) ;
#59898=B_SPLINE_CURVE_WITH_KNOTS ( 'NONE', 3,
 ( #28597, #12364, #21559, #29663 ),
 .UNSPECIFIED., .F., .F.,
 ( 4, 4 ),
 ( 1.040834085586084257E-17, 0.002002928617504300471 ),
 .UNSPECIFIED. ) ;
#59899=CARTESIAN_POINT ( 'NONE',  ( -44.14911905790387436, 464.3766534541992996, 9.623404994945699897 ) ) ;
#59905=CARTESIAN_POINT ( 'NONE',  ( 46.00000000000000000, 450.0000000000002274, 13.20242257375370976 ) ) ;
#59914=CARTESIAN_POINT ( 'NONE',  ( 31.02212611900126760, 360.5725590293961318, 22.12937154125974715 ) ) ;
#59915=CARTESIAN_POINT ( 'NONE',  ( 40.71513924616333213, 459.9692486989943063, 1.994549889840352419 ) ) ;
#59927=CARTESIAN_POINT ( 'NONE',  ( 42.79755424932702113, 462.9502418795238441, 4.193817862676425534 ) ) ;
#59950=ORIENTED_EDGE ( 'NONE', *, *, #38653, .F. ) ;
#59957=CARTESIAN_POINT ( 'NONE',  ( -31.00389226642222340, 485.8187364282109115, 14.27494812388583512 ) ) ;
#59958=CARTESIAN_POINT ( 'NONE',  ( 43.51882896341788864, 485.1238987962695433, -1.698943142573151599 ) ) ;
#59980=CARTESIAN_POINT ( 'NONE',  ( -22.55472503455973410, 305.4464812988970834, 9.065450513355358453 ) ) ;
#59991=ORIENTED_EDGE ( 'NONE', *, *, #10236, .T. ) ;
#59993=CARTESIAN_POINT ( 'NONE',  ( 42.80417301746438596, 434.8807528697740281, 8.723038671912201281 ) ) ;
#59995=CARTESIAN_POINT ( 'NONE',  ( 25.78981311250976916, 306.9324440203532731, 10.64094596872064358 ) ) ;
#60005=EDGE_LOOP ( 'NONE', ( #97322, #38025, #78761, #60287 ) ) ;
#60009=ORIENTED_EDGE ( 'NONE', *, *, #66231, .F. ) ;
#60010=CARTESIAN_POINT ( 'NONE',  ( -32.20052651335440430, 485.9558351764622444, 4.953748807553719935 ) ) ;
#60028=CARTESIAN_POINT ( 'NONE',  ( 42.78577943797455418, 436.7963452923233376, 20.33379556194504900 ) ) ;
#60030=ORIENTED_EDGE ( 'NONE', *, *, #50364, .F. ) ;
#60031=CARTESIAN_POINT ( 'NONE',  ( 39.64792090968624905, 485.8593029974497881, -5.004078333543738211 ) ) ;
#60036=ORIENTED_EDGE ( 'NONE', *, *, #1396, .T. ) ;
#60038=CARTESIAN_POINT ( 'NONE',  ( 35.99392181574479821, 473.1311165566888235, 18.08664358306795705 ) ) ;
#60042=CARTESIAN_POINT ( 'NONE',  ( 31.32079490055140170, 437.4203400336787126, 20.45846139775142802 ) ) ;
#60081=CARTESIAN_POINT ( 'NONE',  ( -43.00000000000000000, 450.0000000000002274, 13.20242257375370976 ) ) ;
#60083=CARTESIAN_POINT ( 'NONE',  ( 33.96241883181121324, 322.0929539439751466, -5.546615967778726564 ) ) ;
#60090=CARTESIAN_POINT ( 'NONE',  ( 39.62826361664807706, 437.5693818447161334, 4.806172978292440945 ) ) ;
#60107=CARTESIAN_POINT ( 'NONE',  ( -44.24885999147608828, 485.2873706794252371, 1.656249348737429683 ) ) ;
#60112=CARTESIAN_POINT ( 'NONE',  ( 32.70293721676337384, 464.5899875799881897, 16.75272535697877885 ) ) ;
#60127=CARTESIAN_POINT ( 'NONE',  ( -38.29550411296874302, 308.8267097740885561, 1.300001675379448551 ) ) ;
#60128=FACE_OUTER_BOUND ( 'NONE', #22719, .T. ) ;
#60143=CARTESIAN_POINT ( 'NONE',  ( -37.62251730745840916, 437.3427388312646258, 4.535622330043208805 ) ) ;
#60159=B_SPLINE_CURVE_WITH_KNOTS ( 'NONE', 3,
 ( #83853, #84929, #43410, #84400 ),
 .UNSPECIFIED., .F., .F.,
 ( 4, 4 ),
 ( 0.0008553712708089381608, 0.02105700498847944482 ),
 .UNSPECIFIED. ) ;
#60163=CARTESIAN_POINT ( 'NONE',  ( 43.62595639791993563, 434.3202349548960797, 14.43462880160996953 ) ) ;
#60167=MECHANICAL_DESIGN_GEOMETRIC_PRESENTATION_REPRESENTATION('',(#63616),#80756);
#60180=ADVANCED_FACE ( 'NONE', ( #88031 ), #18489, .F. ) ;
#60191=CARTESIAN_POINT ( 'NONE',  ( -36.73878763022428728, 390.5162264143924062, 5.892410784837893267 ) ) ;
#60192=CARTESIAN_POINT ( 'NONE',  ( 39.74142865886215503, 490.7355817146180357, 11.79841936045182926 ) ) ;
#60196=CARTESIAN_POINT ( 'NONE',  ( 20.49977525862258076, 302.8459220885799823, -10.00124997875689203 ) ) ;
#60197=CARTESIAN_POINT ( 'NONE',  ( 22.91651842568165165, 295.0901107613288445, -9.949346074078587066 ) ) ;
#60206=CARTESIAN_POINT ( 'NONE',  ( 41.63141214886829999, 315.3601224161185428, -5.077054131032955553 ) ) ;
#60209=ORIENTED_EDGE ( 'NONE', *, *, #43432, .T. ) ;
#60212=CARTESIAN_POINT ( 'NONE',  ( 31.48563847630141765, 438.9650070649207123, 23.22938501193561223 ) ) ;
#60219=CARTESIAN_POINT ( 'NONE',  ( 43.00000000000000000, 464.8825480873695710, 15.07585856869435936 ) ) ;
#60231=CARTESIAN_POINT ( 'NONE',  ( -43.37536761788616957, 434.6169042472839692, 10.05068736166123067 ) ) ;
#60244=ADVANCED_FACE ( 'NONE', ( #71299 ), #96499, .T. ) ;
#60245=CARTESIAN_POINT ( 'NONE',  ( -24.59793477076208035, 305.5470220219680755, 10.31311235332461962 ) ) ;
#60246=ORIENTED_EDGE ( 'NONE', *, *, #94511, .F. ) ;
#60248=EDGE_LOOP ( 'NONE', ( #6837, #23034, #49919, #67319 ) ) ;
#60250=CARTESIAN_POINT ( 'NONE',  ( -32.65804572401754058, 465.7880960007716453, 12.84163515238938658 ) ) ;
#60255=CARTESIAN_POINT ( 'NONE',  ( -31.21592496536052153, 336.6237673982246292, 17.82514839731485168 ) ) ;
#60264=CARTESIAN_POINT ( 'NONE',  ( 24.52975191904706165, 295.5903344108262445, 10.09557803800713316 ) ) ;
#60272=CARTESIAN_POINT ( 'NONE',  ( -44.61777206441702504, 434.3429578869024112, 14.57557122161328600 ) ) ;
#60280=CARTESIAN_POINT ( 'NONE',  ( 32.99999999999930367, 489.5971041675264246, 10.80646835458744803 ) ) ;
#60283=CARTESIAN_POINT ( 'NONE',  ( 46.00000000000000000, 461.7884530657001392, 10.79543072748596977 ) ) ;
#60287=ORIENTED_EDGE ( 'NONE', *, *, #19652, .F. ) ;
#60297=CARTESIAN_POINT ( 'NONE',  ( 18.69420657816679210, 304.6310092840336097, -10.04693110555010982 ) ) ;
#60309=EDGE_CURVE ( 'NONE', #75687, #35302, #9410, .T. ) ;
#60311=ORIENTED_EDGE ( 'NONE', *, *, #29511, .T. ) ;
#60313=CARTESIAN_POINT ( 'NONE',  ( -36.56384560112791604, 437.5716728810670588, 4.260240708029983558 ) ) ;
#60324=CARTESIAN_POINT ( 'NONE',  ( 8.838746709400247425, 294.6759852208345478, -4.712208899071270274 ) ) ;
#60328=EDGE_LOOP ( 'NONE', ( #50119, #105258, #36433, #58478, #76683, #13322 ) ) ;
#60330=CARTESIAN_POINT ( 'NONE',  ( 24.23626286421126252, 305.2563944236501356, 10.24644595435697880 ) ) ;
#60338=CIRCLE ( 'NONE', #68955, 2.999999999999999112 ) ;
#60350=CARTESIAN_POINT ( 'NONE',  ( -8.019147853987105279, 302.4786514485144835, -10.03165473704664201 ) ) ;
#60361=CARTESIAN_POINT ( 'NONE',  ( 43.61075255792288630, 434.4875743724471135, 10.88293886035321734 ) ) ;
#60378=CARTESIAN_POINT ( 'NONE',  ( -25.59639872491835177, 305.3408274204018653, -9.675241084463289454 ) ) ;
#60382=CARTESIAN_POINT ( 'NONE',  ( -43.71675722380574314, 435.0430370928003185, 11.37024750954368635 ) ) ;
#60391=CARTESIAN_POINT ( 'NONE',  ( -31.17618607851400725, 315.1976444128995354, -6.525171466224566785 ) ) ;
#60392=CARTESIAN_POINT ( 'NONE',  ( -31.53578816574763266, 327.5873836966717931, 15.99885046268745548 ) ) ;
#60408=CARTESIAN_POINT ( 'NONE',  ( -42.61140200160144786, 465.9030374194822457, 13.21253569360411895 ) ) ;
#60422=CARTESIAN_POINT ( 'NONE',  ( 6.864655157673967167, 294.7328080983106133, -7.282300054020917734 ) ) ;
#60423=CARTESIAN_POINT ( 'NONE',  ( 45.40507512465600115, 439.2794387026467575, 6.273370203490043373 ) ) ;
#60428=CARTESIAN_POINT ( 'NONE',  ( 0.000000000000000000, 294.8518027762758038, 9.936999415352289589 ) ) ;
#60430=ORIENTED_EDGE ( 'NONE', *, *, #3666, .T. ) ;
#60431=DIRECTION ( 'NONE',  ( -0.8714291948011178013, 0.000000000000000000, -0.4905213129398923178 ) ) ;
#60451=CARTESIAN_POINT ( 'NONE',  ( 40.38232636938073483, 459.8969133356638963, 1.930624307834942321 ) ) ;
#60452=CARTESIAN_POINT ( 'NONE',  ( -35.32911723019088157, 437.0667969981770966, 5.602639083907458684 ) ) ;
#60455=CARTESIAN_POINT ( 'NONE',  ( -43.61500121660905904, 434.9783708497643602, 14.40566113421481553 ) ) ;
#60468=CARTESIAN_POINT ( 'NONE',  ( 43.51760155599759372, 464.6236256767953137, 9.550830537168854661 ) ) ;
#60476=ORIENTED_EDGE ( 'NONE', *, *, #74995, .T. ) ;
#60477=CARTESIAN_POINT ( 'NONE',  ( 0.000000000000000000, 300.0000000000000000, 9.936999415352289589 ) ) ;
#60495=EDGE_CURVE ( 'NONE', #69309, #31339, #42625, .T. ) ;
#60498=CARTESIAN_POINT ( 'NONE',  ( -33.00540147334732666, 487.4196752801200887, 9.523982417603956918 ) ) ;
#60499=EDGE_CURVE ( 'NONE', #88227, #48464, #90917, .T. ) ;
#60504=DIRECTION ( 'NONE',  ( 0.9077394194966191820, -0.1875825441123765147, 0.3752624887145921684 ) ) ;
#60514=ORIENTED_EDGE ( 'NONE', *, *, #43835, .F. ) ;
#60518=VERTEX_POINT ( 'NONE', #28107 ) ;
#60530=CARTESIAN_POINT ( 'NONE',  ( -45.99999999999995737, 461.9152041119569390, 5.112156919902204777 ) ) ;
#60548=CARTESIAN_POINT ( 'NONE',  ( 1.224646799147353454E-15, 0.000000000000000000, 10.00000000000000178 ) ) ;
#60551=ORIENTED_EDGE ( 'NONE', *, *, #55586, .F. ) ;
#60553=CARTESIAN_POINT ( 'NONE',  ( 40.16087957073692394, 485.8454018306723015, -4.964645702805086103 ) ) ;
#60562=CARTESIAN_POINT ( 'NONE',  ( 37.50813744631010849, 482.1291867456659475, 15.12800786539085784 ) ) ;
#60566=TOROIDAL_SURFACE ( 'NONE', #76083, 12.00000000000000711, 3.000000000000000000 ) ;
#60567=CARTESIAN_POINT ( 'NONE',  ( 33.05104704987640929, 434.2951118972601421, 15.74527730978287110 ) ) ;
#60583=CARTESIAN_POINT ( 'NONE',  ( 33.88469969133011261, 464.6054137899092211, 6.797944932417496311 ) ) ;
#60608=CARTESIAN_POINT ( 'NONE',  ( 23.29688253297234724, 304.4092765216364000, -9.880365301581617743 ) ) ;
#60616=CARTESIAN_POINT ( 'NONE',  ( 40.54863160047459303, 437.2386745228082532, 5.317148167334600828 ) ) ;
#60629=CARTESIAN_POINT ( 'NONE',  ( -35.74483125092430669, 413.6409941285803598, 6.029078300230034770 ) ) ;
#60634=CARTESIAN_POINT ( 'NONE',  ( -35.22347075582651144, 464.3861918352932889, 19.05313339797837102 ) ) ;
#60639=CARTESIAN_POINT ( 'NONE',  ( -36.68211027471578234, 426.6599842481110159, 5.461410629243083292 ) ) ;
#60651=CARTESIAN_POINT ( 'NONE',  ( -37.65068595401864116, 305.0254819914457016, -7.656417700763605616 ) ) ;
#60660=EDGE_CURVE ( 'NONE', #94269, #66369, #6509, .T. ) ;
#60662=ORIENTED_EDGE ( 'NONE', *, *, #5866, .T. ) ;
#60672=CARTESIAN_POINT ( 'NONE',  ( -43.02621584241282449, 434.6128289108255558, 16.97888786059002086 ) ) ;
#60680=CARTESIAN_POINT ( 'NONE',  ( 32.20054824794733861, 485.9557913861509633, 4.953638954094006230 ) ) ;
#60682=CARTESIAN_POINT ( 'NONE',  ( 32.99999999999998579, 463.5362553048591963, 6.739467187734351938 ) ) ;
#60699=CARTESIAN_POINT ( 'NONE',  ( -31.23718509250011621, 439.6127102907155404, 23.21745058978948251 ) ) ;
#60710=CARTESIAN_POINT ( 'NONE',  ( -24.29519218197498631, 295.4518972802553094, 2.065840140822523541 ) ) ;
#60713=CARTESIAN_POINT ( 'NONE',  ( 39.98830517851552457, 490.5859057859975110, 11.67971501230864995 ) ) ;
#60717=CARTESIAN_POINT ( 'NONE',  ( 23.32842889633158379, 295.1981192840830772, -1.925701350189481076 ) ) ;
#60718=CARTESIAN_POINT ( 'NONE',  ( 35.74363442581862671, 380.1068966271811860, 4.951945592532029927 ) ) ;
#60726=CARTESIAN_POINT ( 'NONE',  ( 30.00000000000000000, 450.0000000000002274, 8.202422573753707979 ) ) ;
#60727=CARTESIAN_POINT ( 'NONE',  ( 42.33262710065869783, 332.4327577417291195, 7.108190472527923021 ) ) ;
#60728=CARTESIAN_POINT ( 'NONE',  ( 33.73990888920651088, 486.9635397366919278, 1.197403147134062706 ) ) ;
#60730=CARTESIAN_POINT ( 'NONE',  ( -3.493042281569127550, 304.8518027749427119, -10.00000000028269120 ) ) ;
#60740=( GEOMETRIC_REPRESENTATION_CONTEXT ( 3 ) GLOBAL_UNCERTAINTY_ASSIGNED_CONTEXT ( ( #23003 ) ) GLOBAL_UNIT_ASSIGNED_CONTEXT ( ( #7295, #39170, #40736 ) ) REPRESENTATION_CONTEXT ( 'NONE', 'WORKASPACE' ) );
#60748=EDGE_CURVE ( 'NONE', #75902, #51548, #58126, .T. ) ;
#60767=CARTESIAN_POINT ( 'NONE',  ( -32.13490731594677641, 427.1953081090705950, 24.83868860164863079 ) ) ;
#60771=CARTESIAN_POINT ( 'NONE',  ( -32.68851106860801536, 465.0799323318227607, 13.83425062237807879 ) ) ;
#60774=CARTESIAN_POINT ( 'NONE',  ( 35.53294979701562539, 439.9362927074972731, 24.32573494709669149 ) ) ;
#60783=CARTESIAN_POINT ( 'NONE',  ( 24.62657823539835178, 295.6185519456691395, 10.10170238537927823 ) ) ;
#60791=TOROIDAL_SURFACE ( 'NONE', #52134, 5.999999999999994671, 1.000000000000000444 ) ;
#60792=CARTESIAN_POINT ( 'NONE',  ( 34.42332229506718022, 302.2847767890208956, 3.633360753947871391 ) ) ;
#60793=ORIENTED_EDGE ( 'NONE', *, *, #33886, .T. ) ;
#60797=CARTESIAN_POINT ( 'NONE',  ( -32.81992448453860334, 465.7192846569213884, 11.17271167765305862 ) ) ;
#60816=CARTESIAN_POINT ( 'NONE',  ( 34.84618260875170392, 489.9833681528626812, 11.97975507378813731 ) ) ;
#60820=CARTESIAN_POINT ( 'NONE',  ( 41.71840012517787244, 489.3048647944241907, 10.52957302900621350 ) ) ;
#60821=CARTESIAN_POINT ( 'NONE',  ( 43.47539511674882817, 487.0683156417112514, 3.561597533069202903 ) ) ;
#60825=CARTESIAN_POINT ( 'NONE',  ( 40.08499133126954206, 485.6798096563408649, -4.492259481486891914 ) ) ;
#60831=CARTESIAN_POINT ( 'NONE',  ( -40.55047790000728014, 438.3493795828572388, 22.65582424288032826 ) ) ;
#60832=ORIENTED_EDGE ( 'NONE', *, *, #15396, .F. ) ;
#60840=CYLINDRICAL_SURFACE ( 'NONE', #87716, 5.000000000000001776 ) ;
#60851=CARTESIAN_POINT ( 'NONE',  ( 24.60286054134615341, 307.0080087803624451, 10.42432472471663907 ) ) ;
#60854=VERTEX_POINT ( 'NONE', #74873 ) ;
#60859=CARTESIAN_POINT ( 'NONE',  ( 0.000000000000000000, 0.000000000000000000, 0.000000000000000000 ) ) ;
#60869=ORIENTED_EDGE ( 'NONE', *, *, #85737, .T. ) ;
#60871=CARTESIAN_POINT ( 'NONE',  ( -8.984970058492191214, 294.6717433611603383, -4.394086705153881667 ) ) ;
#60885=ORIENTED_EDGE ( 'NONE', *, *, #26652, .T. ) ;
#60888=CIRCLE ( 'NONE', #14344, 12.00000000000001066 ) ;
#60898=CARTESIAN_POINT ( 'NONE',  ( 42.57386119057987628, 361.2124773204089934, 16.59441752729008357 ) ) ;
#60899=CARTESIAN_POINT ( 'NONE',  ( -20.37278541768182905, 303.8378246129573199, -10.00297115033341910 ) ) ;
#60904=( BOUNDED_SURFACE ( )  B_SPLINE_SURFACE ( 3, 2, ( 
 ( #104420, #71000, #103893 ),
 ( #39708, #80668, #55841 ),
 ( #54800, #32148, #6789 ),
 ( #56381, #23007, #5215 ),
 ( #88782, #72060, #40219 ),
 ( #23539, #80144, #15410 ),
 ( #63997, #64512, #46206 ),
 ( #73089, #46723, #30037 ),
 ( #38145, #31110, #97922 ),
 ( #104969, #65025, #6244 ) ),
 .UNSPECIFIED., .F., .F., .F. ) 
 B_SPLINE_SURFACE_WITH_KNOTS ( ( 4, 2, 2, 2, 4 ),
 ( 3, 3 ),
 ( 0.009720546615277408931, 0.01966181957347580903, 0.02463245605257501081, 0.02711777429212460996, 0.02960309253167420912 ),
 ( 0.000000000000000000, 1.000000000000000000 ),
 .UNSPECIFIED. ) 
 GEOMETRIC_REPRESENTATION_ITEM ( )  RATIONAL_B_SPLINE_SURFACE ( (
 ( 1.000000000000000000, 0.7071067811865475727, 1.000000000000000000),
 ( 1.000000000000000000, 0.7071067811865475727, 1.000000000000000000),
 ( 1.000000000000000000, 0.7071032135351020820, 1.000000000000000000),
 ( 1.000000000000000000, 0.7071081509336487603, 1.000000000000000000),
 ( 1.000000000000000000, 0.7071048030563258369, 1.000000000000000000),
 ( 1.000000000000000000, 0.7071073475032796374, 1.000000000000000000),
 ( 1.000000000000000000, 0.7070920504567346221, 1.000000000000000000),
 ( 1.000000000000000000, 0.7070828650738152366, 1.000000000000000000),
 ( 1.000000000000000000, 0.7071010094004099855, 1.000000000000000000),
 ( 1.000000000000000000, 0.7071067811865505703, 1.000000000000000000) ) ) 
 REPRESENTATION_ITEM ( '' )  SURFACE ( )  );
#60908=EDGE_CURVE ( 'NONE', #26579, #58946, #15714, .T. ) ;
#60915=CARTESIAN_POINT ( 'NONE',  ( -36.39696100913531751, 309.1476423045306774, 13.34792222534698780 ) ) ;
#60930=CARTESIAN_POINT ( 'NONE',  ( 15.63139425945679228, 304.5550792278134509, 8.873930317195700468 ) ) ;
#60933=( BOUNDED_SURFACE ( )  B_SPLINE_SURFACE ( 3, 2, ( 
 ( #2413, #68227, #8908 ),
 ( #83332, #66623, #84939 ),
 ( #100049, #101118, #60163 ),
 ( #76836, #27281, #93027 ) ),
 .UNSPECIFIED., .F., .F., .F. ) 
 B_SPLINE_SURFACE_WITH_KNOTS ( ( 4, 4 ),
 ( 3, 3 ),
 ( 2.810685711951421695E-15, 0.0002131933143105659131 ),
 ( 0.000000000000000000, 1.000000000000000000 ),
 .UNSPECIFIED. ) 
 GEOMETRIC_REPRESENTATION_ITEM ( )  RATIONAL_B_SPLINE_SURFACE ( (
 ( 1.000000000000000000, 0.8328393170029404491, 1.000000000000000000),
 ( 1.000000000000000000, 0.8339687546429958021, 1.000000000000000000),
 ( 1.000000000000000000, 0.8350496135189969804, 1.000000000000000000),
 ( 1.000000000000000000, 0.8360809698955812275, 1.000000000000000000) ) ) 
 REPRESENTATION_ITEM ( '' )  SURFACE ( )  );
#60940=CARTESIAN_POINT ( 'NONE',  ( 1.488823952408661500, 295.3362597639684850, -10.00085782936185730 ) ) ;
#60941=CARTESIAN_POINT ( 'NONE',  ( 35.96492786661492858, 302.4488314805894902, -8.278427239160079054 ) ) ;
#60944=CARTESIAN_POINT ( 'NONE',  ( -6.624059643703564149, 294.7379298340728724, -10.02420444108935271 ) ) ;
#60947=ORIENTED_EDGE ( 'NONE', *, *, #17733, .F. ) ;
#60950=EDGE_CURVE ( 'NONE', #49860, #64798, #54285, .T. ) ;
#60952=AXIS2_PLACEMENT_3D ( 'NONE', #38638, #12737, #55313 ) ;
#60977=ORIENTED_EDGE ( 'NONE', *, *, #89658, .T. ) ;
#61005=CIRCLE ( 'NONE', #67916, 0.9999999999999854561 ) ;
#61012=CARTESIAN_POINT ( 'NONE',  ( -27.97565635352651015, 315.9216507687758053, 12.64980990155120999 ) ) ;
#61020=CARTESIAN_POINT ( 'NONE',  ( -32.65915130202685646, 487.2382554987376579, 8.056573295088265141 ) ) ;
#61030=CARTESIAN_POINT ( 'NONE',  ( -32.82257518192243140, 434.5279504693334616, 16.69869453570042239 ) ) ;
#61052=CARTESIAN_POINT ( 'NONE',  ( -46.00000000004283152, 462.0224066507940961, 5.460670579100258770 ) ) ;
#61054=ORIENTED_EDGE ( 'NONE', *, *, #90079, .T. ) ;
#61065=CARTESIAN_POINT ( 'NONE',  ( -4.406980464011021503, 299.0165906089773671, 8.990614526116086580 ) ) ;
#61069=AXIS2_PLACEMENT_3D ( 'NONE', #93671, #19823, #69921 ) ;
#61075=CARTESIAN_POINT ( 'NONE',  ( 0.000000000000000000, -19.99999999999998934, 0.000000000000000000 ) ) ;
#61087=CARTESIAN_POINT ( 'NONE',  ( 33.51592517449224573, 434.0196043323697381, 13.78155809957686628 ) ) ;
#61093=CARTESIAN_POINT ( 'NONE',  ( 0.000000000000000000, 304.8518027762758038, -9.000000000000005329 ) ) ;
#61098=ORIENTED_EDGE ( 'NONE', *, *, #97820, .F. ) ;
#61133=ADVANCED_FACE ( 'NONE', ( #105930 ), #105416, .F. ) ;
#61134=CARTESIAN_POINT ( 'NONE',  ( 38.22195112133615424, 437.6732586221723409, 4.643349236001768965 ) ) ;
#61138=CARTESIAN_POINT ( 'NONE',  ( 34.64166250171371786, 490.4813561613897832, 11.60003975507683194 ) ) ;
#61142=CARTESIAN_POINT ( 'NONE',  ( 37.69506754384874370, 484.8919167041208880, -3.620297613832784478 ) ) ;
#61153=CARTESIAN_POINT ( 'NONE',  ( -35.05476482818383488, 463.5208552852804473, 19.69826870375476346 ) ) ;
#61158=CARTESIAN_POINT ( 'NONE',  ( -35.58239268463962190, 364.8620502323183246, 3.031411369397770450 ) ) ;
#61182=VERTEX_POINT ( 'NONE', #98892 ) ;
#61197=CARTESIAN_POINT ( 'NONE',  ( -33.00000000000000000, 488.8442721620238558, 4.433647275927475206 ) ) ;
#61198=CARTESIAN_POINT ( 'NONE',  ( -37.20098947015251412, 438.1443347308166381, 4.012567541568420992 ) ) ;
#61216=ADVANCED_FACE ( 'NONE', ( #15339 ), #15220, .T. ) ;
#61221=AXIS2_PLACEMENT_3D ( 'NONE', #15357, #97331, #7784 ) ;
#61224=FILL_AREA_STYLE_COLOUR ( '', #73196 ) ;
#61231=( BOUNDED_SURFACE ( )  B_SPLINE_SURFACE ( 3, 2, ( 
 ( #44905, #20129, #102051 ),
 ( #69702, #60038, #19062 ),
 ( #60562, #43293, #84816 ),
 ( #51903, #95051, #69181 ) ),
 .UNSPECIFIED., .F., .F., .F. ) 
 B_SPLINE_SURFACE_WITH_KNOTS ( ( 4, 4 ),
 ( 3, 3 ),
 ( 0.01840331564793163538, 0.04646555858147861234 ),
 ( 0.000000000000000000, 1.000000000000000000 ),
 .UNSPECIFIED. ) 
 GEOMETRIC_REPRESENTATION_ITEM ( )  RATIONAL_B_SPLINE_SURFACE ( (
 ( 1.000000000000000000, 0.8381405999065927315, 1.000000000000000000),
 ( 1.000000000000000000, 0.8381408041605379333, 1.000000000000000000),
 ( 1.000000000000000000, 0.8381407647121852378, 1.000000000000000000),
 ( 1.000000000000000000, 0.8381405645739014032, 1.000000000000000000) ) ) 
 REPRESENTATION_ITEM ( '' )  SURFACE ( )  );
#61240=CARTESIAN_POINT ( 'NONE',  ( 23.32831762434326706, 303.3951354536446274, -9.883407546016623968 ) ) ;
#61241=CARTESIAN_POINT ( 'NONE',  ( 45.29905483467455696, 497.0732240353902398, -8.041250874568902418 ) ) ;
#61252=CARTESIAN_POINT ( 'NONE',  ( 42.96915577533521713, 322.5831792346974680, -3.261277637034701637 ) ) ;
#61253=CARTESIAN_POINT ( 'NONE',  ( 38.88026172477386666, 468.9844931099165706, 0.4637734290235665524 ) ) ;
#61256=CARTESIAN_POINT ( 'NONE',  ( 31.01615627852296342, 439.2622192783163086, 22.57221946846627958 ) ) ;
#61270=EDGE_CURVE ( 'NONE', #35302, #90326, #70290, .T. ) ;
#61274=CARTESIAN_POINT ( 'NONE',  ( 33.89250494191496443, 463.6575930728431558, 6.993601543837897339 ) ) ;
#61281=CARTESIAN_POINT ( 'NONE',  ( 43.27291153936506873, 435.9049899631326070, 8.045225097063040565 ) ) ;
#61292=B_SPLINE_CURVE_WITH_KNOTS ( 'NONE', 3,
 ( #95484, #5926, #22691, #55526, #88466, #14540, #47449, #17765, #90579, #98652, #40429, #7510 ),
 .UNSPECIFIED., .F., .F.,
 ( 4, 2, 2, 2, 2, 4 ),
 ( 4.384643301807188419E-15, 0.001900005895290834707, 0.003800011790577284467, 0.005700017685863734661, 0.006650020633506964311, 0.007600023581150194829 ),
 .UNSPECIFIED. ) ;
#61297=CARTESIAN_POINT ( 'NONE',  ( -43.66706706802315807, 409.2729596023213503, 16.12745813032958608 ) ) ;
#61308=CARTESIAN_POINT ( 'NONE',  ( 31.55246551994505921, 436.6870800834244051, 19.28475619652349593 ) ) ;
#61311=CARTESIAN_POINT ( 'NONE',  ( 22.25695985037653202, 303.2606861724426608, 10.02485155946911810 ) ) ;
#61312=CIRCLE ( 'NONE', #75047, 1.000000000000000222 ) ;
#61331=CARTESIAN_POINT ( 'NONE',  ( 2.422472278927138994E-15, -0.1944580884125578779, 19.78098730681987405 ) ) ;
#61340=CARTESIAN_POINT ( 'NONE',  ( 30.00000000000000000, 461.8887775513396150, 11.55279652844105698 ) ) ;
#61358=ORIENTED_EDGE ( 'NONE', *, *, #21094, .T. ) ;
#61359=CARTESIAN_POINT ( 'NONE',  ( 39.65839090363501640, 485.8593493675161312, -5.004208577436686234 ) ) ;
#61365=ORIENTED_EDGE ( 'NONE', *, *, #72563, .T. ) ;
#61367=EDGE_CURVE ( 'NONE', #23591, #66369, #90227, .T. ) ;
#61381=CIRCLE ( 'NONE', #52731, 1.000000000000000888 ) ;
#61385=CARTESIAN_POINT ( 'NONE',  ( 22.84363777014927877, 305.5774054537097868, 9.094444372195162885 ) ) ;
#61394=CARTESIAN_POINT ( 'NONE',  ( -43.55333112596419909, 465.2342844084849389, 9.238213423004411951 ) ) ;
#61408=VERTEX_POINT ( 'NONE', #20175 ) ;
#61412=( NAMED_UNIT ( * ) PLANE_ANGLE_UNIT ( ) SI_UNIT ( $, .RADIAN. ) );
#61419=ORIENTED_EDGE ( 'NONE', *, *, #9276, .F. ) ;
#61434=CARTESIAN_POINT ( 'NONE',  ( 42.78153023264098209, 391.2922209041898327, 19.62706161876795363 ) ) ;
#61436=AXIS2_PLACEMENT_3D ( 'NONE', #87600, #54663, #104287 ) ;
#61440=CARTESIAN_POINT ( 'NONE',  ( -43.80952869898561630, 434.9438303799926189, 12.65470026211868237 ) ) ;
#61444=DIRECTION ( 'NONE',  ( 0.000000000000000000, 0.000000000000000000, 1.000000000000000000 ) ) ;
#61445=CARTESIAN_POINT ( 'NONE',  ( -33.00795325653169243, 439.3958174160654835, 23.82489859418955191 ) ) ;
#61446=ORIENTED_EDGE ( 'NONE', *, *, #76985, .T. ) ;
#61448=CARTESIAN_POINT ( 'NONE',  ( -28.40381499265910392, 310.0606719538530456, 11.65298042467015449 ) ) ;
#61477=CARTESIAN_POINT ( 'NONE',  ( 4.240736524178923439, 300.6921934601160729, -10.01075408398112643 ) ) ;
#61478=CARTESIAN_POINT ( 'NONE',  ( 45.43339346675878687, 430.7348383325900727, 7.234598910837349628 ) ) ;
#61479=CARTESIAN_POINT ( 'NONE',  ( 38.04621267582680133, 308.1715813180469468, 1.136581563559742269 ) ) ;
#61483=CARTESIAN_POINT ( 'NONE',  ( -6.763850406535977022, 294.7356673863635592, 9.912314076180619438 ) ) ;
#61484=CIRCLE ( 'NONE', #42512, 12.00000000000001066 ) ;
#61505=CARTESIAN_POINT ( 'NONE',  ( 16.46332378338231095, 294.5649011048989792, 1.876034907501067828 ) ) ;
#61521=DIRECTION ( 'NONE',  ( 0.000000000000000000, 0.000000000000000000, -1.000000000000000000 ) ) ;
#61524=CARTESIAN_POINT ( 'NONE',  ( 44.11327388758677870, 464.4313852428367682, 9.822198357555455672 ) ) ;
#61545=AXIS2_PLACEMENT_3D ( 'NONE', #104181, #78318, #62171 ) ;
#61550=CARTESIAN_POINT ( 'NONE',  ( 22.42417502586373246, 305.3961751430792333, 10.05444931189341773 ) ) ;
#61578=ORIENTED_EDGE ( 'NONE', *, *, #40871, .F. ) ;
#61583=CARTESIAN_POINT ( 'NONE',  ( 39.83065760000189215, 436.5763539059782374, 5.509783410166992468 ) ) ;
#61591=CARTESIAN_POINT ( 'NONE',  ( -43.90320859248178209, 462.7132367860276076, 5.469326048303289056 ) ) ;
#61616=CARTESIAN_POINT ( 'NONE',  ( 13.28162482383687859, 294.5489039831744549, -10.06438307193624304 ) ) ;
#61619=DIRECTION ( 'NONE',  ( 0.2259255479511208531, 0.3692254281733069465, 0.9014600545632757145 ) ) ;
#61669=CARTESIAN_POINT ( 'NONE',  ( -33.78656477175679385, 463.8460037826917528, 7.347243016405096583 ) ) ;
#61673=TOROIDAL_SURFACE ( 'NONE', #90905, 7.025805963803935406, 3.000000000000000000 ) ;
#61682=CARTESIAN_POINT ( 'NONE',  ( 32.11956073034194503, 486.1307440743741495, 5.366431738779005478 ) ) ;
#61690=AXIS2_PLACEMENT_3D ( 'NONE', #87380, #105661, #79268 ) ;
#61691=CARTESIAN_POINT ( 'NONE',  ( 34.12349128637462314, 490.8027302422241291, 11.84948222508890403 ) ) ;
#61698=CARTESIAN_POINT ( 'NONE',  ( -44.15895461026264712, 485.1651389999502157, 0.5848183293849077424 ) ) ;
#61701=FACE_OUTER_BOUND ( 'NONE', #29486, .T. ) ;
#61740=EDGE_CURVE ( 'NONE', #37996, #22095, #96737, .T. ) ;
#61748=CARTESIAN_POINT ( 'NONE',  ( 33.83651168703158163, 463.7543666047810120, 7.167145050618551672 ) ) ;
#61755=EDGE_CURVE ( 'NONE', #96036, #61182, #78208, .T. ) ;
#61774=CARTESIAN_POINT ( 'NONE',  ( 35.45196906070734855, 373.3971792367692615, 5.126420406680051833 ) ) ;
#61777=CARTESIAN_POINT ( 'NONE',  ( 34.34679764914265121, 491.0133751866268312, 12.01297952733224150 ) ) ;
#61781=CARTESIAN_POINT ( 'NONE',  ( 39.36919468843574066, 490.3664410044918895, 11.50853341535465368 ) ) ;
#61784=CARTESIAN_POINT ( 'NONE',  ( 44.19066549755432760, 435.2576907183105845, 14.58870676253211762 ) ) ;
#61799=CARTESIAN_POINT ( 'NONE',  ( 45.37874805213238716, 369.5478906911545778, 5.965867277830504634 ) ) ;
#61800=CARTESIAN_POINT ( 'NONE',  ( 34.73928765630499527, 485.6865374000855127, -2.860106678717950324 ) ) ;
#61802=CARTESIAN_POINT ( 'NONE',  ( -20.24579557674103469, 304.8297271373346575, -10.00469232190998525 ) ) ;
#61804=CARTESIAN_POINT ( 'NONE',  ( 31.61511976764354870, 439.3933909026691822, 23.34297217120054313 ) ) ;
#61819=ORIENTED_EDGE ( 'NONE', *, *, #49109, .F. ) ;
#61822=CARTESIAN_POINT ( 'NONE',  ( 34.63382419943125257, 462.0010168197948701, 4.189557279629578801 ) ) ;
#61851=CARTESIAN_POINT ( 'NONE',  ( 23.85675658565387991, 303.8681536343033258, 10.15842353693015809 ) ) ;
#61863=EDGE_LOOP ( 'NONE', ( #91744, #83642, #86075, #42381 ) ) ;
#61899=CARTESIAN_POINT ( 'NONE',  ( 40.83852310120747120, 485.7816305618702586, -4.779469532616784200 ) ) ;
#61905=ORIENTED_EDGE ( 'NONE', *, *, #60748, .T. ) ;
#61909=CARTESIAN_POINT ( 'NONE',  ( 42.89416850988997254, 486.3091028892278587, 6.394136786127195826 ) ) ;
#61911=EDGE_CURVE ( 'NONE', #80767, #12476, #101682, .T. ) ;
#61922=ORIENTED_EDGE ( 'NONE', *, *, #70359, .F. ) ;
#61923=EDGE_CURVE ( 'NONE', #85977, #69148, #82381, .T. ) ;
#61926=CARTESIAN_POINT ( 'NONE',  ( 26.90838114744199672, 308.9771128992503577, 11.14144682951946308 ) ) ;
#61947=ORIENTED_EDGE ( 'NONE', *, *, #32719, .F. ) ;
#61955=B_SPLINE_SURFACE_WITH_KNOTS ( 'NONE', 1, 3, ( 
 ( #25019, #57874, #24504, #16913, #82154, #89205, #90799, #31525, #81605, #57338, #73523, #96771, #105385, #8267, #65457, #8801, #6678, #90260, #56815, #39606, #105897, #48718, #80558, #64925, #32047, #64406, #41180, #15305 ),
 ( #97809, #98350, #23975, #71953, #89740, #97279, #147, #104858, #40116, #22901, #23431, #15835, #55738, #7732, #88672, #14762, #56268, #48191, #81094, #72991, #19072, #52440, #68102, #41709, #42765, #101002, #92907, #35785 ) ),
 .UNSPECIFIED., .F., .F., .F.,
 ( 2, 2 ),
 ( 4, 2, 2, 2, 2, 2, 2, 2, 2, 2, 2, 2, 2, 4 ),
 ( 0.000000000000000000, 1.000000000000000000 ),
 ( 0.08901491201581737678, 0.1032490540155679704, 0.1174831960153185778, 0.1317173380150691853, 0.1459514800148197788, 0.1744197640143299588, 0.2028880480138401388, 0.2598246160128514504, 0.3167611840118632616, 0.4306343200098861623, 0.5445074560079088410, 0.6583805920059359051, 0.7722537280039543095, 1.000000000000000000 ),
 .UNSPECIFIED. ) ;
#61960=VERTEX_POINT ( 'NONE', #18570 ) ;
#61963=CARTESIAN_POINT ( 'NONE',  ( -43.91156819296970326, 435.5051061888428308, 9.836736652448470508 ) ) ;
#61977=CARTESIAN_POINT ( 'NONE',  ( -43.54152071279120406, 464.9591243512669507, 12.86066780445021962 ) ) ;
#61980=CARTESIAN_POINT ( 'NONE',  ( -39.69617136735454466, 460.2157148251831700, 2.207451131567688574 ) ) ;
#61984=EDGE_CURVE ( 'NONE', #4725, #2640, #79972, .T. ) ;
#61989=CARTESIAN_POINT ( 'NONE',  ( -36.82997274950742650, 306.6632309731772352, 4.707311215296837048 ) ) ;
#62014=CARTESIAN_POINT ( 'NONE',  ( 9.148737761749414332, 294.6669993733608521, -4.042064116745931024 ) ) ;
#62016=CARTESIAN_POINT ( 'NONE',  ( 43.63596364813231787, 421.7880994604767011, 15.67549955746410184 ) ) ;
#62022=EDGE_LOOP ( 'NONE', ( #55914, #87815, #69043, #34765 ) ) ;
#62033=CARTESIAN_POINT ( 'NONE',  ( -41.44325370401499953, 477.1517044324976951, -1.084963556091905534 ) ) ;
#62041=EDGE_LOOP ( 'NONE', ( #34516, #77016, #93695, #84919 ) ) ;
#62046=CARTESIAN_POINT ( 'NONE',  ( 44.11327388758692081, 464.4313852428372797, 9.822198357557351045 ) ) ;
#62061=DIRECTION ( 'NONE',  ( -1.000000000000000000, -0.000000000000000000, -0.000000000000000000 ) ) ;
#62103=CARTESIAN_POINT ( 'NONE',  ( -33.05281441019222655, 434.2935209264010723, 15.73787673445679225 ) ) ;
#62120=CARTESIAN_POINT ( 'NONE',  ( 43.49620567743568245, 471.8615734360752754, 7.936790638082919180 ) ) ;
#62125=CARTESIAN_POINT ( 'NONE',  ( -42.69811214730272297, 434.9611672192513652, 18.34625614733208820 ) ) ;
#62133=CARTESIAN_POINT ( 'NONE',  ( -23.07924577400106969, 303.3257072796955072, -9.898399575382260451 ) ) ;
#62149=CARTESIAN_POINT ( 'NONE',  ( 15.60168599250222243, 302.5584640164269103, -10.06235166778797208 ) ) ;
#62152=CARTESIAN_POINT ( 'NONE',  ( -37.26717676828223347, 490.8904373082769439, 12.42641029562198618 ) ) ;
#62171=DIRECTION ( 'NONE',  ( 0.000000000000000000, 0.000000000000000000, 1.000000000000000000 ) ) ;
#62180=ADVANCED_FACE ( 'NONE', ( #53448 ), #19369, .F. ) ;
#62200=CARTESIAN_POINT ( 'NONE',  ( -32.89395609998138070, 463.7240567052280653, 7.148062722717972051 ) ) ;
#62208=CARTESIAN_POINT ( 'NONE',  ( -39.64792090968533245, 485.8593029974498450, -5.004078333543798607 ) ) ;
#62210=CARTESIAN_POINT ( 'NONE',  ( 36.68484412175028808, 425.7526927197205282, 5.533094624903789338 ) ) ;
#62212=CARTESIAN_POINT ( 'NONE',  ( 32.86259851300478374, 485.9239370913665539, 5.440925357812795404 ) ) ;
#62217=CARTESIAN_POINT ( 'NONE',  ( 38.10433946279106010, 437.2340514686391089, 4.662695304591946588 ) ) ;
#62221=CARTESIAN_POINT ( 'NONE',  ( -34.14642055599488657, 464.2253822571460091, 6.054698699017524888 ) ) ;
#62231=FACE_OUTER_BOUND ( 'NONE', #96523, .T. ) ;
#62235=DIRECTION ( 'NONE',  ( 1.000000000000000000, 0.000000000000000000, 0.000000000000000000 ) ) ;
#62252=CARTESIAN_POINT ( 'NONE',  ( -16.45446808530939009, 304.5657599011952925, 8.876165325073888113 ) ) ;
#62273=DIRECTION ( 'NONE',  ( -0.000000000000000000, 0.3548932414479616382, 0.9349068334195439478 ) ) ;
#62284=VERTEX_POINT ( 'NONE', #30243 ) ;
#62298=CARTESIAN_POINT ( 'NONE',  ( 33.07871186279389519, 322.7520366298887211, -5.621988175703525492 ) ) ;
#62299=CARTESIAN_POINT ( 'NONE',  ( -11.82165952410163356, 294.5900423753296309, -10.05563889079273387 ) ) ;
#62303=CARTESIAN_POINT ( 'NONE',  ( -27.08705420553263821, 306.3021870952275094, -9.457589952739034800 ) ) ;
#62307=ORIENTED_EDGE ( 'NONE', *, *, #57784, .F. ) ;
#62314=FACE_OUTER_BOUND ( 'NONE', #13510, .T. ) ;
#62315=CARTESIAN_POINT ( 'NONE',  ( 43.00000000000000000, 438.4646224975062978, 9.895601460515774050 ) ) ;
#62318=CARTESIAN_POINT ( 'NONE',  ( 44.12118527028935944, 333.2930620178879622, -0.6804749548666318981 ) ) ;
#62319=CARTESIAN_POINT ( 'NONE',  ( 44.26701432269690883, 464.1304138491097433, 8.787925729982960732 ) ) ;
#62322=AXIS2_PLACEMENT_3D ( 'NONE', #66372, #42094, #31907 ) ;
#62331=CARTESIAN_POINT ( 'NONE',  ( 42.10086803841213765, 435.6552064019005570, 19.95582312411065828 ) ) ;
#62342=VERTEX_POINT ( 'NONE', #38347 ) ;
#62367=CARTESIAN_POINT ( 'NONE',  ( -37.71361324390009884, 391.6894161628994198, 6.182277153786067458 ) ) ;
#62377=CARTESIAN_POINT ( 'NONE',  ( -41.32135724059589421, 485.4908763545977877, -3.838542627834635734 ) ) ;
#62385=EDGE_CURVE ( 'NONE', #96664, #21098, #66913, .T. ) ;
#62386=ORIENTED_EDGE ( 'NONE', *, *, #23812, .F. ) ;
#62388=CARTESIAN_POINT ( 'NONE',  ( 42.88690404153408764, 465.8389234275369972, 12.02232841035013422 ) ) ;
#62391=DIRECTION ( 'NONE',  ( -0.2270551762890244685, 0.1092888915761295876, 0.9677302749725364972 ) ) ;
#62393=CARTESIAN_POINT ( 'NONE',  ( 44.17139329880469489, 463.1540488235348789, 6.319274787421930384 ) ) ;
#62399=DIRECTION ( 'NONE',  ( -0.000000000000000000, -1.000000000000000000, -0.000000000000000000 ) ) ;
#62406=CARTESIAN_POINT ( 'NONE',  ( 43.99295543328099711, 464.6035880628708128, 10.45302038925775179 ) ) ;
#62411=CARTESIAN_POINT ( 'NONE',  ( 46.00000000000000000, 486.5369520448867888, 4.408549137149760710 ) ) ;
#62416=CARTESIAN_POINT ( 'NONE',  ( 39.23335254075882261, 485.6839217479536046, -4.505383133704073728 ) ) ;
#62420=CARTESIAN_POINT ( 'NONE',  ( -41.61208469664205722, 437.6914194411011181, 21.78364932966315237 ) ) ;
#62426=EDGE_CURVE ( 'NONE', #8963, #84380, #2718, .T. ) ;
#62429=CARTESIAN_POINT ( 'NONE',  ( -43.29658055318886767, 324.1952503670673877, -2.852919881210743913 ) ) ;
#62431=CARTESIAN_POINT ( 'NONE',  ( 32.42250183443744760, 438.8720138150355297, 23.74901013937720506 ) ) ;
#62437=ORIENTED_EDGE ( 'NONE', *, *, #70072, .T. ) ;
#62438=CARTESIAN_POINT ( 'NONE',  ( -30.59165872538332209, 327.9687303963079330, 15.85230159117361914 ) ) ;
#62440=FACE_OUTER_BOUND ( 'NONE', #20639, .T. ) ;
#62472=DIRECTION ( 'NONE',  ( 0.3893994694821809044, 0.000000000000000000, 0.9210689730780189377 ) ) ;
#62478=CARTESIAN_POINT ( 'NONE',  ( -46.00000000000000000, 436.1583201866848754, 9.603910868008647128 ) ) ;
#62481=ORIENTED_EDGE ( 'NONE', *, *, #48723, .T. ) ;
#62489=CARTESIAN_POINT ( 'NONE',  ( 42.47229554058168333, 355.2072415732512241, 15.63453588980991427 ) ) ;
#62490=DIRECTION ( 'NONE',  ( 0.9727555100395927079, 0.000000000000000000, 0.2318333834623737266 ) ) ;
#62494=( BOUNDED_SURFACE ( )  B_SPLINE_SURFACE ( 3, 2, ( 
 ( #75421, #32867, #90548 ),
 ( #98624, #34481, #97555 ),
 ( #91097, #49003, #15587 ),
 ( #56567, #24252, #50080 ) ),
 .UNSPECIFIED., .F., .F., .F. ) 
 B_SPLINE_SURFACE_WITH_KNOTS ( ( 4, 4 ),
 ( 3, 3 ),
 ( -9.540979117872439019E-18, 0.001771883439666498226 ),
 ( 0.000000000000000000, 1.000000000000000000 ),
 .UNSPECIFIED. ) 
 GEOMETRIC_REPRESENTATION_ITEM ( )  RATIONAL_B_SPLINE_SURFACE ( (
 ( 1.000000000000000000, 0.7699558187665761499, 1.000000000000000000),
 ( 1.000000000000000000, 0.7661160612247130963, 1.000000000000000000),
 ( 1.000000000000000000, 0.7602452393654992591, 1.000000000000000000),
 ( 1.000000000000000000, 0.7533433155455192543, 1.000000000000000000) ) ) 
 REPRESENTATION_ITEM ( '' )  SURFACE ( )  );
#62502=ORIENTED_EDGE ( 'NONE', *, *, #11228, .F. ) ;
#62504=CARTESIAN_POINT ( 'NONE',  ( -21.14842190820295187, 304.9658827179694072, -8.975750559732306399 ) ) ;
#62505=CARTESIAN_POINT ( 'NONE',  ( -29.32492077227583493, 297.8361219291210773, 10.59529383611387132 ) ) ;
#62519=ADVANCED_FACE ( 'NONE', ( #28018 ), #104037, .T. ) ;
#62530=CARTESIAN_POINT ( 'NONE',  ( 42.36735105587926142, 487.4262793962163300, 8.281278960740705131 ) ) ;
#62532=CARTESIAN_POINT ( 'NONE',  ( 39.44851073818434628, 312.5366107982540598, 2.232686811542719862 ) ) ;
#62547=EDGE_LOOP ( 'NONE', ( #76063, #105216, #106298, #82777 ) ) ;
#62559=VERTEX_POINT ( 'NONE', #22029 ) ;
#62563=CARTESIAN_POINT ( 'NONE',  ( 31.12255221142792294, 439.8596962522411786, 23.32261708534639411 ) ) ;
#62573=CARTESIAN_POINT ( 'NONE',  ( -10.00233396054510493, 294.6427044336463723, 0.2481344758280235319 ) ) ;
#62584=DIRECTION ( 'NONE',  ( 0.000000000000000000, 0.000000000000000000, 1.000000000000000000 ) ) ;
#62594=DIRECTION ( 'NONE',  ( 0.2517716543986374678, 0.000000000000000000, 0.9677866676294797355 ) ) ;
#62616=CARTESIAN_POINT ( 'NONE',  ( -32.13673779510316564, 435.4387075916259846, 16.27397328763151663 ) ) ;
#62624=CARTESIAN_POINT ( 'NONE',  ( -32.65872443253056190, 299.8117513331611690, -0.8913389630357930749 ) ) ;
#62637=EDGE_CURVE ( 'NONE', #67806, #70575, #31045, .T. ) ;
#62645=CARTESIAN_POINT ( 'NONE',  ( -35.57915322819296478, 439.9237900209715804, 24.31413808603394955 ) ) ;
#62647=CARTESIAN_POINT ( 'NONE',  ( -32.49199191497101680, 312.4199643528780825, -7.743724379035653804 ) ) ;
#62655=CARTESIAN_POINT ( 'NONE',  ( 1.128130203593064484, 301.8985493317087503, 9.936162350049338343 ) ) ;
#62668=ORIENTED_EDGE ( 'NONE', *, *, #56279, .T. ) ;
#62692=CARTESIAN_POINT ( 'NONE',  ( 46.00000000000000000, 450.0000000000002274, 13.20242257375370976 ) ) ;
#62693=ADVANCED_FACE ( 'NONE', ( #12312 ), #8274, .F. ) ;
#62694=CARTESIAN_POINT ( 'NONE',  ( -33.21102376836597614, 438.9613914113129454, 23.92328486949907074 ) ) ;
#62705=ORIENTED_EDGE ( 'NONE', *, *, #57290, .T. ) ;
#62708=ORIENTED_EDGE ( 'NONE', *, *, #94444, .F. ) ;
#62712=CARTESIAN_POINT ( 'NONE',  ( -32.15310320217076878, 439.7024266304582625, 23.94087012106557211 ) ) ;
#62715=ORIENTED_EDGE ( 'NONE', *, *, #47769, .F. ) ;
#62719=CARTESIAN_POINT ( 'NONE',  ( 36.70734217215343165, 381.5765345362427752, 5.207851135035667767 ) ) ;
#62721=CARTESIAN_POINT ( 'NONE',  ( 32.15166163075745942, 486.0589784586658197, 5.199393881399715589 ) ) ;
#62727=CARTESIAN_POINT ( 'NONE',  ( -39.43902656928035100, 312.5010541801748900, 2.223703621048137347 ) ) ;
#62728=CARTESIAN_POINT ( 'NONE',  ( 23.44736835841093026, 303.4251214680779185, -9.876957852573138297 ) ) ;
#62753=VERTEX_POINT ( 'NONE', #57538 ) ;
#62765=FACE_OUTER_BOUND ( 'NONE', #93057, .T. ) ;
#62775=ORIENTED_EDGE ( 'NONE', *, *, #99802, .T. ) ;
#62789=CARTESIAN_POINT ( 'NONE',  ( -44.10862079528641999, 485.7176850333842708, 3.977867558419631244 ) ) ;
#62819=CARTESIAN_POINT ( 'NONE',  ( 32.60563673599508405, 321.1394446977577672, -5.024823039848338446 ) ) ;
#62820=CARTESIAN_POINT ( 'NONE',  ( 0.000000000000000000, 304.8518027762758038, -9.000000000000005329 ) ) ;
#62825=CARTESIAN_POINT ( 'NONE',  ( -21.13173862753238907, 303.9465108651830292, -9.979862028335890756 ) ) ;
#62826=CARTESIAN_POINT ( 'NONE',  ( 40.62197427625243762, 488.7236279320703716, 10.90363067260340380 ) ) ;
#62829=ORIENTED_EDGE ( 'NONE', *, *, #60309, .F. ) ;
#62833=CARTESIAN_POINT ( 'NONE',  ( -32.95646543402900619, 485.7809766657131831, 5.067016726494650847 ) ) ;
#62846=CARTESIAN_POINT ( 'NONE',  ( 39.72561652656278852, 309.2274488375438750, -6.620765666067498501 ) ) ;
#62848=CARTESIAN_POINT ( 'NONE',  ( -30.00000000000000000, 462.0217650461273706, 12.66663979487288572 ) ) ;
#62874=CARTESIAN_POINT ( 'NONE',  ( -30.00000000000000000, 489.2902422664049027, 5.500203528953035104 ) ) ;
#62891=CARTESIAN_POINT ( 'NONE',  ( -37.65606885761010147, 426.5576088575361950, 5.696479835041206030 ) ) ;
#62893=CARTESIAN_POINT ( 'NONE',  ( -45.99999999999999289, 485.7126260709432586, -0.7245019728194501685 ) ) ;
#62900=CARTESIAN_POINT ( 'NONE',  ( -40.22629662632770930, 485.6695299957992233, -4.459425866590305709 ) ) ;
#62905=EDGE_CURVE ( 'NONE', #74471, #2708, #48129, .T. ) ;
#62929=CARTESIAN_POINT ( 'NONE',  ( 34.01866702109263230, 436.1375402535096555, 7.445741394046557105 ) ) ;
#62938=CARTESIAN_POINT ( 'NONE',  ( -41.46910480218704009, 484.7338956289818270, -3.418960549715579500 ) ) ;
#62965=CARTESIAN_POINT ( 'NONE',  ( -30.82828255813691953, 330.8479429521501629, 16.52448723566699584 ) ) ;
#62968=CARTESIAN_POINT ( 'NONE',  ( -41.18667489362677969, 461.2717826764276197, 2.470602812283182015 ) ) ;
#62987=ADVANCED_FACE ( 'NONE', ( #99328 ), #29748, .T. ) ;
#62989=CARTESIAN_POINT ( 'NONE',  ( 38.51502786939645517, 460.0233756673477501, 2.043034587343977027 ) ) ;
#62996=ORIENTED_EDGE ( 'NONE', *, *, #3064, .T. ) ;
#63001=( NAMED_UNIT ( * ) PLANE_ANGLE_UNIT ( ) SI_UNIT ( $, .RADIAN. ) );
#63008=CARTESIAN_POINT ( 'NONE',  ( -46.00000000000000000, 436.1502960164518754, 10.01001013570486364 ) ) ;
#63009=CARTESIAN_POINT ( 'NONE',  ( 6.624059643703564149, 294.7379298340728724, -10.02420444108935271 ) ) ;
#63018=CARTESIAN_POINT ( 'NONE',  ( 32.85498697112881672, 354.4200440325224690, 21.54103032174089805 ) ) ;
#63027=CARTESIAN_POINT ( 'NONE',  ( -35.61279199273527496, 462.7776672770684172, 4.031031541873562496 ) ) ;
#63030=CARTESIAN_POINT ( 'NONE',  ( -35.44793164930461415, 372.9548512003073597, 5.074121509499998517 ) ) ;
#63031=CARTESIAN_POINT ( 'NONE',  ( -32.72936687177245574, 300.2420673382501946, 3.148605481384946891 ) ) ;
#63037=VERTEX_POINT ( 'NONE', #24956 ) ;
#63055=CARTESIAN_POINT ( 'NONE',  ( 8.019147853953672467, 302.4786514485326165, -10.03165473704643595 ) ) ;
#63069=CARTESIAN_POINT ( 'NONE',  ( 1.227754105814700372E-15, 67.05096163904791240, 10.02537308446411402 ) ) ;
#63090=ORIENTED_EDGE ( 'NONE', *, *, #66231, .T. ) ;
#63091=CARTESIAN_POINT ( 'NONE',  ( 41.96713667498180911, 484.5369099524149874, -2.773154793583016531 ) ) ;
#63107=CARTESIAN_POINT ( 'NONE',  ( 42.57704743493908950, 486.1612337113410263, 7.852296464539637810 ) ) ;
#63120=CARTESIAN_POINT ( 'NONE',  ( 32.22120753352783140, 464.6691781026584636, 10.60621122532586291 ) ) ;
#63121=( BOUNDED_SURFACE ( )  B_SPLINE_SURFACE ( 3, 2, ( 
 ( #16820, #1126, #82611 ),
 ( #8715, #26025, #99850 ),
 ( #41622, #50238, #9237 ),
 ( #15746, #49159, #24929 ) ),
 .UNSPECIFIED., .F., .F., .F. ) 
 B_SPLINE_SURFACE_WITH_KNOTS ( ( 4, 4 ),
 ( 3, 3 ),
 ( -5.282232984349377602E-16, 0.0002932702099348026580 ),
 ( 0.000000000000000000, 1.000000000000000000 ),
 .UNSPECIFIED. ) 
 GEOMETRIC_REPRESENTATION_ITEM ( )  RATIONAL_B_SPLINE_SURFACE ( (
 ( 1.000000000000000000, 0.7964893136846440402, 1.000000000000000000),
 ( 1.000000000000000000, 0.7948324867097400492, 1.000000000000000000),
 ( 1.000000000000000000, 0.7930891386530558584, 1.000000000000000000),
 ( 1.000000000000000000, 0.7912633096140525568, 1.000000000000000000) ) ) 
 REPRESENTATION_ITEM ( '' )  SURFACE ( )  );
#63136=ORIENTED_EDGE ( 'NONE', *, *, #30933, .T. ) ;
#63144=CARTESIAN_POINT ( 'NONE',  ( -32.48517913958589531, 435.0118361155008415, 18.08961438120518039 ) ) ;
#63145=CARTESIAN_POINT ( 'NONE',  ( -36.66354163798878574, 432.5726246612500177, 4.913532023235378077 ) ) ;
#63146=CARTESIAN_POINT ( 'NONE',  ( -31.31921715863741085, 437.4259532257088949, 20.46640379489214823 ) ) ;
#63152=ORIENTED_EDGE ( 'NONE', *, *, #97789, .F. ) ;
#63154=CARTESIAN_POINT ( 'NONE',  ( -34.81025666956482922, 301.2271517761568020, -8.565222899818694557 ) ) ;
#63168=CARTESIAN_POINT ( 'NONE',  ( 1.316107777606558615, 302.2275528426508799, 9.913267165427164684 ) ) ;
#63175=CARTESIAN_POINT ( 'NONE',  ( -23.44105230970441767, 303.4233223010897973, -9.877347747162149361 ) ) ;
#63183=ORIENTED_EDGE ( 'NONE', *, *, #73750, .F. ) ;
#63191=CARTESIAN_POINT ( 'NONE',  ( 9.740083726526400199, 294.6493269980093714, -10.04303756037254658 ) ) ;
#63197=DIRECTION ( 'NONE',  ( -1.000000000000000000, 0.000000000000000000, 0.000000000000000000 ) ) ;
#63198=CARTESIAN_POINT ( 'NONE',  ( 30.00000000000000000, 500.0000000000002274, 0.000000000000000000 ) ) ;
#63207=ORIENTED_EDGE ( 'NONE', *, *, #65158, .T. ) ;
#63220=ORIENTED_EDGE ( 'NONE', *, *, #78794, .F. ) ;
#63245=AXIS2_PLACEMENT_3D ( 'NONE', #91246, #50227, #32482 ) ;
#63249=CARTESIAN_POINT ( 'NONE',  ( -38.47428897412184767, 485.7788508071988645, -4.770630528146724281 ) ) ;
#63251=CARTESIAN_POINT ( 'NONE',  ( 36.64823341582350480, 437.5392299810053487, 4.281405873620231617 ) ) ;
#63260=CARTESIAN_POINT ( 'NONE',  ( -43.35910211857093088, 356.0870169904675322, 11.85899587691387147 ) ) ;
#63261=CARTESIAN_POINT ( 'NONE',  ( 25.55145341416758242, 304.1863475718637346, -9.710152639138275532 ) ) ;
#63262=VERTEX_POINT ( 'NONE', #13509 ) ;
#63272=CARTESIAN_POINT ( 'NONE',  ( 23.43684916743750080, 295.2641918988800285, 10.02474406024658293 ) ) ;
#63287=DIRECTION ( 'NONE',  ( 0.000000000000000000, 0.000000000000000000, 1.000000000000000000 ) ) ;
#63290=CARTESIAN_POINT ( 'NONE',  ( 32.09911992168216699, 438.9232547152094526, 23.66653216045977359 ) ) ;
#63295=DIRECTION ( 'NONE',  ( -0.5356766697699718582, -0.1574227122302049586, 0.8296195484306275736 ) ) ;
#63300=EDGE_LOOP ( 'NONE', ( #83691, #29980, #29835, #10975 ) ) ;
#63314=CARTESIAN_POINT ( 'NONE',  ( 17.19026434692938565, 294.5876779312053486, 9.880857241781999534 ) ) ;
#63318=B_SPLINE_CURVE_WITH_KNOTS ( 'NONE', 3,
 ( #104531, #81303, #6353, #39295 ),
 .UNSPECIFIED., .F., .F.,
 ( 4, 4 ),
 ( 1.908195823574487804E-17, 0.0002807886668484363022 ),
 .UNSPECIFIED. ) ;
#63339=CARTESIAN_POINT ( 'NONE',  ( -38.11055680731723783, 437.2326489915187153, 4.664335030333703891 ) ) ;
#63343=VERTEX_POINT ( 'NONE', #8079 ) ;
#63344=CARTESIAN_POINT ( 'NONE',  ( -43.27291153936683088, 435.9049899631313565, 8.045225097066092346 ) ) ;
#63347=AXIS2_PLACEMENT_3D ( 'NONE', #12158, #59667, #93630 ) ;
#63348=CARTESIAN_POINT ( 'NONE',  ( 37.88504238421511872, 463.4171042825134350, 19.90923349043885437 ) ) ;
#63356=B_SPLINE_CURVE_WITH_KNOTS ( 'NONE', 3,
 ( #9916, #1814, #11502, #67645, #93519, #26681, #101058, #44429 ),
 .UNSPECIFIED., .F., .F.,
 ( 4, 2, 2, 4 ),
 ( 3.469446951953614189E-18, 0.001701863333577075541, 0.003403726667154147612, 0.006807453334308237111 ),
 .UNSPECIFIED. ) ;
#63357=B_SPLINE_CURVE_WITH_KNOTS ( 'NONE', 3,
 ( #64063, #96937, #55910, #88850, #14940, #34897, #76909, #18164, #44018, #60231, #1402, #17630 ),
 .UNSPECIFIED., .F., .F.,
 ( 4, 2, 2, 2, 2, 4 ),
 ( 0.000000000000000000, 0.001314793157745834488, 0.001972189736618751299, 0.002629586315491668543, 0.003944379473237499996, 0.005259172630983331015 ),
 .UNSPECIFIED. ) ;
#63360=CARTESIAN_POINT ( 'NONE',  ( 32.84830840339214575, 322.5517557799010433, -4.669727346969580140 ) ) ;
#63364=CARTESIAN_POINT ( 'NONE',  ( 41.74605044188654546, 488.3336308464836861, 9.449957167453774787 ) ) ;
#63375=ADVANCED_FACE ( 'NONE', ( #73874 ), #33841, .F. ) ;
#63386=CARTESIAN_POINT ( 'NONE',  ( 30.48226588409197291, 308.5642027897181947, -8.691376423780738492 ) ) ;
#63426=EDGE_LOOP ( 'NONE', ( #40299, #83957, #94688, #70115 ) ) ;
#63439=CARTESIAN_POINT ( 'NONE',  ( -32.09911992168218831, 438.9232547152092252, 23.66653216045979491 ) ) ;
#63440=CARTESIAN_POINT ( 'NONE',  ( 32.93513049338658760, 465.6726574193327792, 10.66039033145146142 ) ) ;
#63446=CARTESIAN_POINT ( 'NONE',  ( 37.67124221001638773, 463.6239404278543930, 19.49545380201351463 ) ) ;
#63458=AXIS2_PLACEMENT_3D ( 'NONE', #17280, #90089, #8632 ) ;
#63470=CYLINDRICAL_SURFACE ( 'NONE', #10710, 10.00000000000000355 ) ;
#63475=CARTESIAN_POINT ( 'NONE',  ( -38.85446894546474539, 460.8903912184078422, 2.218456751110488678 ) ) ;
#63482=CARTESIAN_POINT ( 'NONE',  ( 36.44482444458351011, 439.0054583426050954, 23.96131986156384031 ) ) ;
#63486=CARTESIAN_POINT ( 'NONE',  ( 40.78808449138612957, 461.0038402359687097, 2.292482253616458632 ) ) ;
#63487=ORIENTED_EDGE ( 'NONE', *, *, #14452, .T. ) ;
#63494=CARTESIAN_POINT ( 'NONE',  ( -45.31383884518383098, 362.9196860876334085, 5.161789940898600548 ) ) ;
#63495=VERTEX_POINT ( 'NONE', #10723 ) ;
#63503=CARTESIAN_POINT ( 'NONE',  ( -29.24981464811047260, 322.6110501364183847, 13.31810279652815510 ) ) ;
#63513=CARTESIAN_POINT ( 'NONE',  ( 44.24678642376221660, 485.3508677736838308, 2.236524924813607207 ) ) ;
#63517=AXIS2_PLACEMENT_3D ( 'NONE', #64941, #14250, #5642 ) ;
#63520=CIRCLE ( 'NONE', #37751, 1.000000000000002442 ) ;
#63528=CARTESIAN_POINT ( 'NONE',  ( 1.496989374907367739E-10, 304.8518027762758607, -10.00000000000000533 ) ) ;
#63529=CARTESIAN_POINT ( 'NONE',  ( 28.21644434148578640, 308.7733337496239301, -9.112255642778062992 ) ) ;
#63544=DIRECTION ( 'NONE',  ( -2.775557561562873681E-14, 0.9795142562460142921, -0.2013748291391392609 ) ) ;
#63549=ORIENTED_EDGE ( 'NONE', *, *, #22066, .F. ) ;
#63559=CARTESIAN_POINT ( 'NONE',  ( 37.81751640206508114, 309.3200808856390722, 5.370049675488317575 ) ) ;
#63569=CARTESIAN_POINT ( 'NONE',  ( -38.73386039799286351, 460.3889633641963428, 2.371405894922548274 ) ) ;
#63572=CARTESIAN_POINT ( 'NONE',  ( -42.60956082011767165, 435.9305394648018250, 18.66091589584682708 ) ) ;
#63574=CARTESIAN_POINT ( 'NONE',  ( -33.01221401996102145, 301.6247609887375916, 11.48415791863079427 ) ) ;
#63584=ADVANCED_FACE ( 'NONE', ( #38239 ), #44852, .F. ) ;
#63589=CARTESIAN_POINT ( 'NONE',  ( 36.54117467508514494, 437.9945884957556927, 4.200333155679382813 ) ) ;
#63600=CARTESIAN_POINT ( 'NONE',  ( 9.789044728060074974, 294.6486233851414909, -2.043184600578055843 ) ) ;
#63601=CARTESIAN_POINT ( 'NONE',  ( 40.73878142687892279, 503.7113041876743864, 10.19672445236252045 ) ) ;
#63605=CIRCLE ( 'NONE', #75656, 2.999999999999999112 ) ;
#63609=ORIENTED_EDGE ( 'NONE', *, *, #20142, .F. ) ;
#63613=CARTESIAN_POINT ( 'NONE',  ( 18.00000000000001421, -20.00000000000001776, 9.000000000000007105 ) ) ;
#63616=STYLED_ITEM ( 'NONE', ( #33924 ), #45229 ) ;
#63654=CARTESIAN_POINT ( 'NONE',  ( 32.84951609414348894, 478.7804999730052486, 7.701738758139213381 ) ) ;
#63661=CARTESIAN_POINT ( 'NONE',  ( -6.646264631202571493, 302.7439589117898322, 9.914178208445832752 ) ) ;
#63663=CARTESIAN_POINT ( 'NONE',  ( -40.95420997525301487, 387.0967036739339164, 27.26945002580065136 ) ) ;
#63668=CARTESIAN_POINT ( 'NONE',  ( -33.75766768372585602, 485.0582975308881259, 1.699565690038850274 ) ) ;
#63681=FACE_OUTER_BOUND ( 'NONE', #56601, .T. ) ;
#63683=CARTESIAN_POINT ( 'NONE',  ( -31.61871763008401715, 439.0122406652411655, 23.38971322451639168 ) ) ;
#63686=CARTESIAN_POINT ( 'NONE',  ( -36.74064224167297965, 397.1769660793155481, 6.182558990302069013 ) ) ;
#63691=ORIENTED_EDGE ( 'NONE', *, *, #27848, .F. ) ;
#63693=CARTESIAN_POINT ( 'NONE',  ( -35.39714039450764460, 301.8757354096758263, -8.412418780513528205 ) ) ;
#63701=DIRECTION ( 'NONE',  ( 0.9915366780650395340, -0.1269898409407454742, -0.02699252395739042479 ) ) ;
#63702=CARTESIAN_POINT ( 'NONE',  ( 29.00671329096065421, 320.5761524563107514, 12.81707940767795506 ) ) ;
#63711=CARTESIAN_POINT ( 'NONE',  ( -46.00000000000000000, 461.5066419892383465, 9.508543545636769068 ) ) ;
#63712=CARTESIAN_POINT ( 'NONE',  ( -37.10378445358433908, 439.7078499482008738, 24.11597218741631465 ) ) ;
#63729=CIRCLE ( 'NONE', #17220, 0.9999999999999993339 ) ;
#63732=FACE_OUTER_BOUND ( 'NONE', #90426, .T. ) ;
#63740=CARTESIAN_POINT ( 'NONE',  ( 43.71217423904096222, 435.6632154632235938, 9.092528312217307729 ) ) ;
#63748=CARTESIAN_POINT ( 'NONE',  ( 29.45362385905110969, 325.9253963054578662, 15.14270878922920716 ) ) ;
#63763=EDGE_CURVE ( 'NONE', #31339, #74683, #73251, .T. ) ;
#63787=CARTESIAN_POINT ( 'NONE',  ( -32.80436725737452974, 485.2967250516979902, 5.900038805304054890 ) ) ;
#63799=VERTEX_POINT ( 'NONE', #35467 ) ;
#63800=CARTESIAN_POINT ( 'NONE',  ( 34.29149597935467852, 464.1889238633704622, 18.11295844621604445 ) ) ;
#63805=CARTESIAN_POINT ( 'NONE',  ( 21.51569398614858031, 294.9107018935607130, -9.987480606144490736 ) ) ;
#63806=CARTESIAN_POINT ( 'NONE',  ( -33.00795325653299983, 439.3958174160655403, 23.82489859418982192 ) ) ;
#63807=CARTESIAN_POINT ( 'NONE',  ( -33.95156263172582101, 464.5083255208627975, 6.608064661821575037 ) ) ;
#63812=VECTOR ( 'NONE', #26792, 1000.000000000000000 ) ;
#63830=ORIENTED_EDGE ( 'NONE', *, *, #11277, .F. ) ;
#63845=EDGE_CURVE ( 'NONE', #97864, #50155, #102698, .T. ) ;
#63864=CIRCLE ( 'NONE', #79315, 1.000000000000021316 ) ;
#63882=CARTESIAN_POINT ( 'NONE',  ( -32.22503847990287795, 485.9064490506194716, 4.829857536089223302 ) ) ;
#63887=CARTESIAN_POINT ( 'NONE',  ( 35.76597479665002055, 391.1875820052122776, 5.701159071636620723 ) ) ;
#63891=CARTESIAN_POINT ( 'NONE',  ( -28.21762564305430487, 307.3147646130399835, -9.222953370498792935 ) ) ;
#63893=CARTESIAN_POINT ( 'NONE',  ( -32.43164319908640891, 464.5283015133046547, 9.485638277864330448 ) ) ;
#63899=ADVANCED_FACE ( 'NONE', ( #96342 ), #75101, .T. ) ;
#63902=CARTESIAN_POINT ( 'NONE',  ( -32.22503847990285664, 485.9064490506194716, 4.829857536089268599 ) ) ;
#63910=CARTESIAN_POINT ( 'NONE',  ( 1.224646799147353848E-15, 274.9999999999999432, 10.00000000000000533 ) ) ;
#63911=CARTESIAN_POINT ( 'NONE',  ( 35.63739937222026555, 303.4054289079292630, -0.03810013948418256025 ) ) ;
#63912=CARTESIAN_POINT ( 'NONE',  ( -30.00000000000000355, 461.9594878872932213, 14.33673855776301131 ) ) ;
#63919=CARTESIAN_POINT ( 'NONE',  ( 43.03265099500018920, 484.2747968070553952, -0.8099405866666991027 ) ) ;
#63928=DIRECTION ( 'NONE',  ( 0.9807128367236916944, 0.000000000000000000, 0.1954541682476217956 ) ) ;
#63952=ORIENTED_EDGE ( 'NONE', *, *, #55041, .F. ) ;
#63956=CARTESIAN_POINT ( 'NONE',  ( -39.99722689368601891, 437.4316783397098334, 22.45542938418691037 ) ) ;
#63957=CARTESIAN_POINT ( 'NONE',  ( 33.07261358295323816, 370.8611101514977122, 23.85133237395751493 ) ) ;
#63958=CARTESIAN_POINT ( 'NONE',  ( -36.35895093008763013, 334.2607040896156718, -2.357503963907021216 ) ) ;
#63959=CARTESIAN_POINT ( 'NONE',  ( 32.88333705524082973, 439.7317646416722141, 24.13381181826093069 ) ) ;
#63960=CARTESIAN_POINT ( 'NONE',  ( -45.99999999999426592, 485.9565049917123929, 0.8651369461898777979 ) ) ;
#63967=CARTESIAN_POINT ( 'NONE',  ( 16.96954359408614366, 304.5683848806726814, 9.876757081930351845 ) ) ;
#63968=CARTESIAN_POINT ( 'NONE',  ( -39.28947510688171008, 485.2043936288998225, -4.359233426732905592 ) ) ;
#63973=CARTESIAN_POINT ( 'NONE',  ( 42.99999999999995737, 464.8825480873695710, 15.07585856869434515 ) ) ;
#63980=B_SPLINE_CURVE_WITH_KNOTS ( 'NONE', 3,
 ( #105004, #88815, #74210, #97416 ),
 .UNSPECIFIED., .F., .F.,
 ( 4, 4 ),
 ( 0.000000000000000000, 0.0002123325198302290187 ),
 .UNSPECIFIED. ) ;
#63981=AXIS2_PLACEMENT_3D ( 'NONE', #3820, #36757, #53434 ) ;
#63997=CARTESIAN_POINT ( 'NONE',  ( 16.55741780412212449, 303.5680256153840446, 9.876668742581960814 ) ) ;
#63999=DIRECTION ( 'NONE',  ( -1.000000000000000000, 0.000000000000000000, 0.000000000000000000 ) ) ;
#64004=CIRCLE ( 'NONE', #65671, 12.00000000000001066 ) ;
#64009=CARTESIAN_POINT ( 'NONE',  ( -41.74778363246318236, 460.3875427940050145, 2.379529480112096529 ) ) ;
#64010=CARTESIAN_POINT ( 'NONE',  ( -32.14284448310063880, 464.7823907227477775, 11.45521013154555234 ) ) ;
#64017=CIRCLE ( 'NONE', #98406, 5.000000000000000888 ) ;
#64023=CARTESIAN_POINT ( 'NONE',  ( 41.50820411079202898, 461.5963371455317770, 2.703439750996501800 ) ) ;
#64024=EDGE_LOOP ( 'NONE', ( #19909, #34267, #74910, #275 ) ) ;
#64040=CARTESIAN_POINT ( 'NONE',  ( -30.08887150021950774, 331.1717924776848463, 15.36326397572592661 ) ) ;
#64043=CARTESIAN_POINT ( 'NONE',  ( -34.16642289233710983, 464.7650419733863600, 19.36631221619108700 ) ) ;
#64049=CARTESIAN_POINT ( 'NONE',  ( 46.00000000000000000, 488.1813821183642972, 2.479370420756042748 ) ) ;
#64060=B_SPLINE_CURVE_WITH_KNOTS ( 'NONE', 3,
 ( #87079, #78429, #88134, #4555, #37492, #87607, #71939, #86563, #22887, #46082, #63339, #96233 ),
 .UNSPECIFIED., .F., .F.,
 ( 4, 2, 2, 2, 2, 4 ),
 ( 0.000000000000000000, 0.001521572489514788412, 0.003043144979029576824, 0.003803931223786971572, 0.004564717468544366753, 0.006086289958059119820 ),
 .UNSPECIFIED. ) ;
#64063=CARTESIAN_POINT ( 'NONE',  ( -43.63899620156477965, 434.3182181978404515, 14.37213632273176422 ) ) ;
#64072=CARTESIAN_POINT ( 'NONE',  ( 46.00000000000000711, 461.5914298688537656, 9.837083399362915870 ) ) ;
#64077=B_SPLINE_CURVE_WITH_KNOTS ( 'NONE', 3,
 ( #4735, #70535, #101310, #105543 ),
 .UNSPECIFIED., .F., .F.,
 ( 4, 4 ),
 ( 1.034338964446688375E-15, 0.002502641776601218122 ),
 .UNSPECIFIED. ) ;
#64080=VERTEX_POINT ( 'NONE', #98579 ) ;
#64082=CARTESIAN_POINT ( 'NONE',  ( 33.16501691561000342, 438.9509064377053846, 23.91453236866924215 ) ) ;
#64083=CARTESIAN_POINT ( 'NONE',  ( 43.21801493134148586, 434.4543138599221948, 16.17410598210216222 ) ) ;
#64084=CARTESIAN_POINT ( 'NONE',  ( 3.269135563215229023, 294.8518027752268722, -10.00000000024436275 ) ) ;
#64094=CARTESIAN_POINT ( 'NONE',  ( 36.83410552012148997, 306.6732998202488147, 4.709818881448565975 ) ) ;
#64098=CARTESIAN_POINT ( 'NONE',  ( -39.26668904306311703, 460.2385666352529938, 2.228751329586619701 ) ) ;
#64101=CARTESIAN_POINT ( 'NONE',  ( 32.67323224503917345, 485.6332095909920099, 6.597358449831840055 ) ) ;
#64102=CARTESIAN_POINT ( 'NONE',  ( -36.10337418012809962, 461.0502312562470593, 3.050677930906189772 ) ) ;
#64106=CARTESIAN_POINT ( 'NONE',  ( -34.53449118956828556, 302.4528159859040670, 3.673939189084939105 ) ) ;
#64112=STYLED_ITEM ( 'NONE', ( #64958 ), #19858 ) ;
#64113=EDGE_CURVE ( 'NONE', #13857, #23677, #21721, .T. ) ;
#64122=CARTESIAN_POINT ( 'NONE',  ( 42.57704743493908950, 486.1612337113410263, 7.852296464539637810 ) ) ;
#64128=TOROIDAL_SURFACE ( 'NONE', #86546, 12.00000000000001066, 3.000000000000000000 ) ;
#64130=AXIS2_PLACEMENT_3D ( 'NONE', #42822, #1811, #24021 ) ;
#64133=FACE_OUTER_BOUND ( 'NONE', #58568, .T. ) ;
#64137=CARTESIAN_POINT ( 'NONE',  ( 40.88293604215247967, 432.5779639752643675, 26.56799667982232549 ) ) ;
#64142=CARTESIAN_POINT ( 'NONE',  ( 43.49286403356602193, 484.8086342565614473, 4.190194857772357118 ) ) ;
#64147=ORIENTED_EDGE ( 'NONE', *, *, #46579, .F. ) ;
#64148=EDGE_LOOP ( 'NONE', ( #65124, #70425, #91940, #1655, #84563 ) ) ;
#64150=CARTESIAN_POINT ( 'NONE',  ( -44.12589798587348611, 464.4133173135365382, 9.756011010160211328 ) ) ;
#64159=EDGE_LOOP ( 'NONE', ( #75123, #43968, #93781, #61819 ) ) ;
#64160=CIRCLE ( 'NONE', #76222, 5.000000000000001776 ) ;
#64174=CARTESIAN_POINT ( 'NONE',  ( -23.95564068939877345, 305.6666757346319514, -9.824255363917307804 ) ) ;
#64181=CARTESIAN_POINT ( 'NONE',  ( -33.97359119245066239, 434.1099241184709285, 11.80501937577158778 ) ) ;
#64191=CARTESIAN_POINT ( 'NONE',  ( -7.447697371462428606, 302.7211807851450658, 9.909313283245410275 ) ) ;
#64192=CARTESIAN_POINT ( 'NONE',  ( -42.18756898894582008, 484.4522853017719513, -2.425645685620466452 ) ) ;
#64199=MECHANICAL_DESIGN_GEOMETRIC_PRESENTATION_REPRESENTATION('',(#74473),#12498);
#64200=EDGE_LOOP ( 'NONE', ( #23930, #6873 ) ) ;
#64201=ORIENTED_EDGE ( 'NONE', *, *, #86543, .T. ) ;
#64207=ORIENTED_EDGE ( 'NONE', *, *, #88787, .T. ) ;
#64211=CARTESIAN_POINT ( 'NONE',  ( 32.25199865210457517, 464.6771562214399296, 10.60479922512074147 ) ) ;
#64215=CARTESIAN_POINT ( 'NONE',  ( -35.35381222550667957, 364.7255732624930147, 3.995359698804311854 ) ) ;
#64217=CARTESIAN_POINT ( 'NONE',  ( -32.25691083757232747, 485.8985639246204187, 4.832559767440749887 ) ) ;
#64223=CARTESIAN_POINT ( 'NONE',  ( -33.06064406479386975, 299.5759903008183755, -8.949493189068455479 ) ) ;
#64242=CARTESIAN_POINT ( 'NONE',  ( 41.49038059205248885, 469.1084758719956085, 1.096707336962226442 ) ) ;
#64244=FACE_OUTER_BOUND ( 'NONE', #88564, .T. ) ;
#64266=FACE_BOUND ( 'NONE', #90910, .T. ) ;
#64286=EDGE_CURVE ( 'NONE', #9120, #33881, #42473, .T. ) ;
#64292=DIRECTION ( 'NONE',  ( 0.000000000000000000, 0.000000000000000000, -1.000000000000000000 ) ) ;
#64303=ADVANCED_FACE ( 'NONE', ( #85615 ), #41366, .F. ) ;
#64307=ORIENTED_EDGE ( 'NONE', *, *, #71198, .F. ) ;
#64314=CARTESIAN_POINT ( 'NONE',  ( 34.67263685779008853, 485.1278622359851624, -2.016271555161434303 ) ) ;
#64320=CARTESIAN_POINT ( 'NONE',  ( -43.61687410915253338, 428.0539954125393933, 15.22877806374068932 ) ) ;
#64321=CARTESIAN_POINT ( 'NONE',  ( 28.05001115153095270, 305.7972385202601231, -9.345431085968183282 ) ) ;
#64324=VERTEX_POINT ( 'NONE', #61340 ) ;
#64335=CARTESIAN_POINT ( 'NONE',  ( 27.47093694407817210, 296.2799286419132727, -9.692114557243211692 ) ) ;
#64337=FACE_OUTER_BOUND ( 'NONE', #39268, .T. ) ;
#64347=FACE_OUTER_BOUND ( 'NONE', #20964, .T. ) ;
#64364=ORIENTED_EDGE ( 'NONE', *, *, #49060, .F. ) ;
#64367=ORIENTED_EDGE ( 'NONE', *, *, #33933, .T. ) ;
#64373=CARTESIAN_POINT ( 'NONE',  ( 16.30148223401143071, 294.5672717626525809, 9.876519804568172134 ) ) ;
#64376=DIRECTION ( 'NONE',  ( 0.000000000000000000, 0.000000000000000000, -1.000000000000000000 ) ) ;
#64386=CARTESIAN_POINT ( 'NONE',  ( 39.98585230618361663, 437.4394976705481781, 22.46424175529162426 ) ) ;
#64394=CARTESIAN_POINT ( 'NONE',  ( -45.99999999996033750, 464.1057728260254294, 11.12967041736123797 ) ) ;
#64406=CARTESIAN_POINT ( 'NONE',  ( -40.77380256327629837, 468.8478597483947965, 21.13608272249925690 ) ) ;
#64408=CARTESIAN_POINT ( 'NONE',  ( -45.31383884518383098, 362.9196860876334085, 5.161789940898600548 ) ) ;
#64412=CARTESIAN_POINT ( 'NONE',  ( 29.65316434010261304, 311.3236015583557901, -7.491929621755849311 ) ) ;
#64414=ORIENTED_EDGE ( 'NONE', *, *, #60495, .F. ) ;
#64419=B_SPLINE_CURVE_WITH_KNOTS ( 'NONE', 3,
 ( #71176, #104070, #97559, #104601 ),
 .UNSPECIFIED., .F., .F.,
 ( 4, 4 ),
 ( 5.204170427930421283E-18, 0.001842998688486628808 ),
 .UNSPECIFIED. ) ;
#64422=CARTESIAN_POINT ( 'NONE',  ( -42.09158233638501656, 465.7816406625409513, 14.79318349170026003 ) ) ;
#64423=DIRECTION ( 'NONE',  ( 0.000000000000000000, 0.000000000000000000, 1.000000000000000000 ) ) ;
#64435=CARTESIAN_POINT ( 'NONE',  ( 40.91975823258974998, 312.7996260062327565, -5.723410787371364883 ) ) ;
#64436=CARTESIAN_POINT ( 'NONE',  ( -30.00000000000000000, 462.0143252985370736, 13.78012569455894720 ) ) ;
#64443=CARTESIAN_POINT ( 'NONE',  ( 43.68669919769894960, 485.1453384654001866, 2.541696494115609273 ) ) ;
#64445=CARTESIAN_POINT ( 'NONE',  ( 43.74985542820358830, 435.5770091380369422, 16.96136490515564788 ) ) ;
#64458=CARTESIAN_POINT ( 'NONE',  ( 35.40410126533816282, 462.9417065736251402, 4.215193980341727986 ) ) ;
#64460=CARTESIAN_POINT ( 'NONE',  ( -43.69307663853834356, 464.9794299858425006, 8.444152807401959393 ) ) ;
#64480=CARTESIAN_POINT ( 'NONE',  ( 22.87192968767251955, 303.4467615960384705, 10.06536293368748680 ) ) ;
#64481=CARTESIAN_POINT ( 'NONE',  ( -42.72097986434771855, 338.4462485437400687, 8.451945447247039667 ) ) ;
#64506=CARTESIAN_POINT ( 'NONE',  ( -37.51493083963608655, 491.7337707781560425, 12.51683509955429408 ) ) ;
#64512=CARTESIAN_POINT ( 'NONE',  ( 16.53374548247488462, 304.5679859715410771, 9.876672295198167362 ) ) ;
#64523=CARTESIAN_POINT ( 'NONE',  ( -30.00000000000000355, 461.8887775513397287, 11.55279652844096994 ) ) ;
#64536=CIRCLE ( 'NONE', #9453, 1.000000000000002220 ) ;
#64544=( BOUNDED_SURFACE ( )  B_SPLINE_SURFACE ( 3, 2, ( 
 ( #48694, #56789, #81068 ),
 ( #16891, #97259, #49771 ),
 ( #48167, #7180, #89714 ),
 ( #40094, #32020, #74041 ),
 ( #24483, #81580, #98837 ),
 ( #73502, #106400, #123 ),
 ( #90236, #33093, #71929 ),
 ( #104830, #30974, #96746 ),
 ( #35215, #91834, #50298 ),
 ( #84805, #27676, #35764 ),
 ( #43804, #9831, #2809 ),
 ( #19049, #84270, #10888 ) ),
 .UNSPECIFIED., .F., .F., .F. ) 
 B_SPLINE_SURFACE_WITH_KNOTS ( ( 4, 2, 2, 2, 2, 4 ),
 ( 3, 3 ),
 ( -8.946836327350382589E-16, 0.001912832793471382726, 0.002869249190207521540, 0.003825665586943660136, 0.005738498380415937329, 0.007651331173888214522 ),
 ( 0.000000000000000000, 1.000000000000000000 ),
 .UNSPECIFIED. ) 
 GEOMETRIC_REPRESENTATION_ITEM ( )  RATIONAL_B_SPLINE_SURFACE ( (
 ( 1.000000000000000000, 0.8904848454311998784, 1.000000000000000000),
 ( 1.000000000000000000, 0.8829526975545493039, 1.000000000000000000),
 ( 1.000000000000000000, 0.8737225350168510429, 1.000000000000000000),
 ( 1.000000000000000000, 0.8580093906384770319, 1.000000000000000000),
 ( 1.000000000000000000, 0.8524583445354902977, 1.000000000000000000),
 ( 1.000000000000000000, 0.8408236507810400440, 1.000000000000000000),
 ( 1.000000000000000000, 0.8347220996876830723, 1.000000000000000000),
 ( 1.000000000000000000, 0.8161438705883578004, 1.000000000000000000),
 ( 1.000000000000000000, 0.8032788134801324142, 1.000000000000000000),
 ( 1.000000000000000000, 0.7776932730515783154, 1.000000000000000000),
 ( 1.000000000000000000, 0.7649057602317937965, 1.000000000000000000),
 ( 1.000000000000000000, 0.7533433155455840913, 1.000000000000000000) ) ) 
 REPRESENTATION_ITEM ( '' )  SURFACE ( )  );
#64548=CARTESIAN_POINT ( 'NONE',  ( -22.18906107735381283, 305.1406206946286943, -9.938500898755204815 ) ) ;
#64556=CARTESIAN_POINT ( 'NONE',  ( -26.27602720945015236, 310.0396763463044181, 11.16635102967653026 ) ) ;
#64558=CARTESIAN_POINT ( 'NONE',  ( 21.10321973014934827, 305.0244315187235884, 8.973846506840480686 ) ) ;
#64576=EDGE_CURVE ( 'NONE', #41809, #5324, #85293, .T. ) ;
#64581=DIRECTION ( 'NONE',  ( -0.000000000000000000, -1.000000000000000000, -0.000000000000000000 ) ) ;
#64584=CARTESIAN_POINT ( 'NONE',  ( 35.57955382936916067, 363.3973965622570859, 2.919629247011395368 ) ) ;
#64592=PRESENTATION_STYLE_ASSIGNMENT (( #65109 ) ) ;
#64594=FACE_BOUND ( 'NONE', #100055, .T. ) ;
#64595=VERTEX_POINT ( 'NONE', #8380 ) ;
#64610=CARTESIAN_POINT ( 'NONE',  ( 30.72158347774164611, 320.3865038906847644, 14.25020464585016278 ) ) ;
#64617=CARTESIAN_POINT ( 'NONE',  ( 42.71830997089508486, 375.3504811699607444, 18.35052788392003364 ) ) ;
#64622=CARTESIAN_POINT ( 'NONE',  ( -35.49087625329003259, 378.7048482322750260, 5.690525758283039082 ) ) ;
#64623=CARTESIAN_POINT ( 'NONE',  ( -27.03877384839983833, 307.0702461234657221, 10.91122626378502503 ) ) ;
#64633=CARTESIAN_POINT ( 'NONE',  ( 35.94513182849205180, 437.3829582663516362, 4.385777999725890552 ) ) ;
#64640=CARTESIAN_POINT ( 'NONE',  ( -44.10120706205752583, 485.7576699374420741, 4.111328371166674600 ) ) ;
#64641=ORIENTED_EDGE ( 'NONE', *, *, #7251, .F. ) ;
#64657=ORIENTED_EDGE ( 'NONE', *, *, #57838, .T. ) ;
#64666=CARTESIAN_POINT ( 'NONE',  ( 0.000000000000000000, 273.9999999999999432, 0.000000000000000000 ) ) ;
#64673=CIRCLE ( 'NONE', #54109, 10.02537308446410869 ) ;
#64704=CARTESIAN_POINT ( 'NONE',  ( -8.363902830498242125, 294.6905147064353514, 1.902776017109438556 ) ) ;
#64710=CARTESIAN_POINT ( 'NONE',  ( 35.58515402554368023, 490.6697164559536191, 12.32566724388707513 ) ) ;
#64711=CARTESIAN_POINT ( 'NONE',  ( -36.01602535166301067, 463.8907346520921351, 20.04892332327189308 ) ) ;
#64714=EDGE_LOOP ( 'NONE', ( #14491, #53386, #7226, #90119 ) ) ;
#64729=CARTESIAN_POINT ( 'NONE',  ( -34.77877198785877511, 338.7120930708800302, -1.786898488397636875 ) ) ;
#64735=CARTESIAN_POINT ( 'NONE',  ( -26.71843530640310505, 304.8394554359867925, -9.563866172168349777 ) ) ;
#64741=DIRECTION ( 'NONE',  ( 0.000000000000000000, 0.000000000000000000, 1.000000000000000000 ) ) ;
#64743=CARTESIAN_POINT ( 'NONE',  ( 24.36647833307484490, 306.6270560823984397, 9.333673104374161866 ) ) ;
#64756=CARTESIAN_POINT ( 'NONE',  ( -33.59588613957706116, 439.5203103051574089, 23.94499399079802160 ) ) ;
#64776=DIRECTION ( 'NONE',  ( -0.9230641662213927567, 0.000000000000000000, 0.3846459996386352720 ) ) ;
#64781=ORIENTED_EDGE ( 'NONE', *, *, #83797, .T. ) ;
#64793=CARTESIAN_POINT ( 'NONE',  ( 37.83989825151499531, 491.6297408768496098, 12.44743998625077630 ) ) ;
#64798=VERTEX_POINT ( 'NONE', #53626 ) ;
#64802=B_SPLINE_CURVE_WITH_KNOTS ( 'NONE', 3,
 ( #4805, #45794, #13405, #60408 ),
 .UNSPECIFIED., .F., .F.,
 ( 4, 4 ),
 ( 0.000000000000000000, 0.001833966606958285740 ),
 .UNSPECIFIED. ) ;
#64815=CARTESIAN_POINT ( 'NONE',  ( -43.68875470849008025, 484.4240665651603877, 2.019269197006389849 ) ) ;
#64819=ORIENTED_EDGE ( 'NONE', *, *, #10824, .T. ) ;
#64823=CARTESIAN_POINT ( 'NONE',  ( 0.000000000000000000, 80.00000000000000000, -8.000000000000010658 ) ) ;
#64825=CARTESIAN_POINT ( 'NONE',  ( 35.81083583144190641, 464.1171150618853289, 19.43519701782722464 ) ) ;
#64832=CARTESIAN_POINT ( 'NONE',  ( 45.99999999999995737, 463.3824904069770128, 8.976947363133223945 ) ) ;
#64838=CARTESIAN_POINT ( 'NONE',  ( -42.97908324528840751, 343.6987997973317874, 9.561931291602665084 ) ) ;
#64844=CARTESIAN_POINT ( 'NONE',  ( 34.16642289233133312, 463.8422268500519294, 18.98106911353331938 ) ) ;
#64848=CARTESIAN_POINT ( 'NONE',  ( -22.91885868373643831, 305.6172567281201964, 10.10309701371861912 ) ) ;
#64852=CARTESIAN_POINT ( 'NONE',  ( -38.10433946279282935, 437.2340514686374604, 4.662695304592548773 ) ) ;
#64853=CARTESIAN_POINT ( 'NONE',  ( -31.39953160533619325, 423.6490974968072010, 23.88548958732392435 ) ) ;
#64865=CARTESIAN_POINT ( 'NONE',  ( 0.000000000000000000, 70.00000000000000000, 0.000000000000000000 ) ) ;
#64884=CARTESIAN_POINT ( 'NONE',  ( 8.763303353751069835, 294.6787833753287487, 1.900260937711448328 ) ) ;
#64904=CARTESIAN_POINT ( 'NONE',  ( 34.07726008484836200, 439.5806258003244693, 24.00265428230595433 ) ) ;
#64925=CARTESIAN_POINT ( 'NONE',  ( -40.88293604215247967, 432.5779639752643675, 26.56799667982232549 ) ) ;
#64926=CARTESIAN_POINT ( 'NONE',  ( -43.29658055318886767, 324.1952503670673877, -2.852919881210743913 ) ) ;
#64931=CARTESIAN_POINT ( 'NONE',  ( 27.07237153509079874, 306.2907637360925719, -9.460208576581653261 ) ) ;
#64938=CARTESIAN_POINT ( 'NONE',  ( -42.23079339798738374, 460.7352525929354101, 2.726051457480726636 ) ) ;
#64941=CARTESIAN_POINT ( 'NONE',  ( 0.000000000000000000, 69.00000000000000000, -5.999999999999994671 ) ) ;
#64948=DIRECTION ( 'NONE',  ( 0.000000000000000000, 0.9795142562459571156, -0.2013748291394176493 ) ) ;
#64958=PRESENTATION_STYLE_ASSIGNMENT (( #8837 ) ) ;
#64965=DIRECTION ( 'NONE',  ( -0.1946996363145598874, 0.08778327892740174498, 0.9769268895673475228 ) ) ;
#64968=EDGE_CURVE ( 'NONE', #50361, #93305, #83622, .T. ) ;
#64970=EDGE_LOOP ( 'NONE', ( #105059, #10037, #801, #106519 ) ) ;
#64975=CARTESIAN_POINT ( 'NONE',  ( -16.40059842617682051, 294.5680859342442659, -10.06030655347179703 ) ) ;
#64982=DIRECTION ( 'NONE',  ( 1.000000000000000000, 0.000000000000000000, 0.000000000000000000 ) ) ;
#64994=CARTESIAN_POINT ( 'NONE',  ( 30.40486732246983337, 318.3402785233949430, 13.73959638705492026 ) ) ;
#64995=CARTESIAN_POINT ( 'NONE',  ( -42.27245208472728422, 331.6484278788518623, 6.927277335194249375 ) ) ;
#65003=EDGE_CURVE ( 'NONE', #100861, #89689, #80945, .T. ) ;
#65004=CIRCLE ( 'NONE', #73608, 15.00000000000001243 ) ;
#65007=CIRCLE ( 'NONE', #9856, 0.9999999999999800160 ) ;
#65014=ADVANCED_FACE ( 'NONE', ( #75645 ), #71561, .T. ) ;
#65016=SURFACE_STYLE_FILL_AREA ( #32138 ) ;
#65019=CARTESIAN_POINT ( 'NONE',  ( -37.02702338563431539, 490.9575081778414187, 12.45591594067345120 ) ) ;
#65025=CARTESIAN_POINT ( 'NONE',  ( 19.70764564238366390, 304.7954121406192485, 9.925013215726748328 ) ) ;
#65033=CARTESIAN_POINT ( 'NONE',  ( -40.18077987341683865, 485.1789679560215518, -4.313737565909713467 ) ) ;
#65039=CARTESIAN_POINT ( 'NONE',  ( -39.85564080104247608, 459.8412824357644126, 1.882109076563900363 ) ) ;
#65041=CARTESIAN_POINT ( 'NONE',  ( -46.00000000000000000, 438.3878896346935221, 16.22878885428545104 ) ) ;
#65058=CIRCLE ( 'NONE', #85725, 5.000000000000000888 ) ;
#65061=CARTESIAN_POINT ( 'NONE',  ( 27.30955641668146328, 305.2295048154397250, -9.475470306339881077 ) ) ;
#65066=CARTESIAN_POINT ( 'NONE',  ( -35.56416567323501710, 480.2820146177156175, -4.363888856302766683 ) ) ;
#65075=CARTESIAN_POINT ( 'NONE',  ( -21.63763341358889392, 304.1253123683783315, 9.995563593792510915 ) ) ;
#65077=CARTESIAN_POINT ( 'NONE',  ( 33.21930856118554942, 484.9903775147098486, 0.3261662439072586794 ) ) ;
#65085=CARTESIAN_POINT ( 'NONE',  ( 46.00000000000000000, 438.4646224975067526, 9.895601460514084735 ) ) ;
#65102=CARTESIAN_POINT ( 'NONE',  ( 31.00389226249483698, 502.9289871839745842, 8.047326149841639520 ) ) ;
#65109=SURFACE_STYLE_USAGE ( .BOTH. , #46804 ) ;
#65112=ORIENTED_EDGE ( 'NONE', *, *, #3866, .T. ) ;
#65120=CIRCLE ( 'NONE', #49630, 0.9999999999999934497 ) ;
#65121=CARTESIAN_POINT ( 'NONE',  ( -38.70871301288035227, 463.8566175871105770, 18.97601667485638544 ) ) ;
#65124=ORIENTED_EDGE ( 'NONE', *, *, #46579, .T. ) ;
#65130=CARTESIAN_POINT ( 'NONE',  ( 38.37563681287258532, 311.1791213484684704, 5.838097343055311583 ) ) ;
#65132=DIRECTION ( 'NONE',  ( 0.9722532735311555374, 0.000000000000000000, 0.2339306993704594051 ) ) ;
#65134=CARTESIAN_POINT ( 'NONE',  ( -40.66084078640387389, 460.3808361429900060, 2.363412739912913452 ) ) ;
#65136=CARTESIAN_POINT ( 'NONE',  ( 32.80395775117305845, 487.0274233559335357, 8.980975396778106301 ) ) ;
#65139=CARTESIAN_POINT ( 'NONE',  ( -43.00000000000000000, 436.5989882784185738, 19.94133085611155920 ) ) ;
#65141=CARTESIAN_POINT ( 'NONE',  ( 9.819056950928633398, 294.6481068335447731, 1.893705519456528208 ) ) ;
#65146=CARTESIAN_POINT ( 'NONE',  ( 19.01537497148453681, 303.6985849714293408, 9.904431725647269147 ) ) ;
#65151=ORIENTED_EDGE ( 'NONE', *, *, #53539, .F. ) ;
#65153=CARTESIAN_POINT ( 'NONE',  ( 36.35757485292823077, 437.5916776841876299, 4.247500867393328328 ) ) ;
#65155=CARTESIAN_POINT ( 'NONE',  ( 0.000000000000000000, 274.9999999999999432, 0.000000000000000000 ) ) ;
#65158=EDGE_CURVE ( 'NONE', #41040, #16697, #84784, .T. ) ;
#65162=AXIS2_PLACEMENT_3D ( 'NONE', #46033, #70834, #103725 ) ;
#65165=EDGE_CURVE ( 'NONE', #54135, #15655, #89939, .T. ) ;
#65185=ORIENTED_EDGE ( 'NONE', *, *, #783, .F. ) ;
#65199=ORIENTED_EDGE ( 'NONE', *, *, #74780, .F. ) ;
#65201=CARTESIAN_POINT ( 'NONE',  ( 30.59246000750163219, 327.9779158149556793, 15.85446903023333221 ) ) ;
#65226=CARTESIAN_POINT ( 'NONE',  ( -0.9108375754614689290, 296.5938209096384526, -10.00058097679043634 ) ) ;
#65233=CARTESIAN_POINT ( 'NONE',  ( -15.77381400630083164, 302.5604448265047495, 9.875089995772468043 ) ) ;
#65239=DIRECTION ( 'NONE',  ( 0.000000000000000000, -0.3964176948853116444, -0.9180702648391440013 ) ) ;
#65255=CARTESIAN_POINT ( 'NONE',  ( -31.50909062064772570, 439.7150268719240671, 23.57203536488566797 ) ) ;
#65256=CARTESIAN_POINT ( 'NONE',  ( -35.04726026986955389, 344.4762064160754562, -0.5379253706595517048 ) ) ;
#65264=CARTESIAN_POINT ( 'NONE',  ( -23.76958652213907541, 303.5250860149631080, -9.855208255818627805 ) ) ;
#65271=CARTESIAN_POINT ( 'NONE',  ( 31.27150491832618329, 363.0626246711562999, 21.43651293828456161 ) ) ;
#65272=CARTESIAN_POINT ( 'NONE',  ( -41.72129495923037723, 464.4839086838818503, 17.13525251804149008 ) ) ;
#65281=CARTESIAN_POINT ( 'NONE',  ( -41.39445455245019190, 437.1938976948999880, 21.06043167853144737 ) ) ;
#65282=EDGE_LOOP ( 'NONE', ( #55303, #59614, #8926, #55697, #49058 ) ) ;
#65291=EDGE_CURVE ( 'NONE', #73045, #29160, #50929, .T. ) ;
#65298=EDGE_CURVE ( 'NONE', #3581, #63037, #71637, .T. ) ;
#65300=CARTESIAN_POINT ( 'NONE',  ( 20.19866560624230090, 294.7559120050365777, -2.020382211974508735 ) ) ;
#65305=ORIENTED_EDGE ( 'NONE', *, *, #88020, .T. ) ;
#65324=CARTESIAN_POINT ( 'NONE',  ( 19.70764564238371719, 304.7954121406193622, 9.925013215726785631 ) ) ;
#65357=VERTEX_POINT ( 'NONE', #59892 ) ;
#65364=CARTESIAN_POINT ( 'NONE',  ( -37.56208910882862995, 463.3609840191068088, 20.02047205468374358 ) ) ;
#65367=( LENGTH_UNIT ( ) NAMED_UNIT ( * ) SI_UNIT ( .MILLI., .METRE. ) );
#65368=CARTESIAN_POINT ( 'NONE',  ( -21.29975379448946171, 294.8969325209483259, -1.990407376643346327 ) ) ;
#65370=B_SPLINE_CURVE_WITH_KNOTS ( 'NONE', 3,
 ( #87891, #12386, #13444, #94936, #61505, #70106, #36723, #20563 ),
 .UNSPECIFIED., .F., .F.,
 ( 4, 2, 2, 4 ),
 ( -5.999999998302399854E-08, 0.002844838416977306123, 0.005689736833954595410, 0.01137953366790916965 ),
 .UNSPECIFIED. ) ;
#65378=DIRECTION ( 'NONE',  ( -0.9167413600884036784, 0.000000000000000000, -0.3994812620177121132 ) ) ;
#65379=TOROIDAL_SURFACE ( 'NONE', #11937, 12.00000000000000711, 3.000000000000000000 ) ;
#65383=CARTESIAN_POINT ( 'NONE',  ( -23.61963550967466574, 306.0340374937824777, 10.19690224617928287 ) ) ;
#65388=CARTESIAN_POINT ( 'NONE',  ( -39.62826361664709651, 437.5693818447127796, 4.806172978297276188 ) ) ;
#65435=CARTESIAN_POINT ( 'NONE',  ( 39.08940286296796529, 438.6059018380323096, 22.97295384703932086 ) ) ;
#65452=CARTESIAN_POINT ( 'NONE',  ( 36.00698207622300373, 463.3390700132977713, 20.06331035628539183 ) ) ;
#65457=CARTESIAN_POINT ( 'NONE',  ( -39.13885763974980136, 324.4948203046521371, 17.18769520460729439 ) ) ;
#65459=CARTESIAN_POINT ( 'NONE',  ( -23.43684916743750080, 295.2641918988800285, 10.02474406024658293 ) ) ;
#65462=CARTESIAN_POINT ( 'NONE',  ( 26.46671012315133353, 307.0860250144660881, -9.505648234697030574 ) ) ;
#65472=VERTEX_POINT ( 'NONE', #18811 ) ;
#65476=CARTESIAN_POINT ( 'NONE',  ( -36.07271708247948538, 437.4941479923684255, 4.311972135658442618 ) ) ;
#65511=CARTESIAN_POINT ( 'NONE',  ( -16.92109608899381001, 302.5811311245806223, -10.05744425352880533 ) ) ;
#65514=CARTESIAN_POINT ( 'NONE',  ( -36.12805158198089117, 463.5537319797288092, 19.64593688561376794 ) ) ;
#65519=CARTESIAN_POINT ( 'NONE',  ( 32.16723388112094284, 464.8262935154354523, 14.67703231816536658 ) ) ;
#65527=EDGE_LOOP ( 'NONE', ( #51496, #90670 ) ) ;
#65532=CARTESIAN_POINT ( 'NONE',  ( -43.65150702672222138, 382.1424289287486999, 15.13344470041056411 ) ) ;
#65533=CARTESIAN_POINT ( 'NONE',  ( 32.15310320217080431, 439.7024266304582056, 23.94087012106557211 ) ) ;
#65551=FACE_OUTER_BOUND ( 'NONE', #87674, .T. ) ;
#65567=CARTESIAN_POINT ( 'NONE',  ( -32.94021323899823983, 485.0599191339510980, 5.361609822537303671 ) ) ;
#65577=CARTESIAN_POINT ( 'NONE',  ( -43.87333262554025026, 435.3945242957007054, 16.14343998352092413 ) ) ;
#65588=EDGE_CURVE ( 'NONE', #30899, #28630, #52476, .T. ) ;
#65594=CARTESIAN_POINT ( 'NONE',  ( 29.84172392461965728, 297.6780703762060512, -1.379986926139241676 ) ) ;
#65605=CARTESIAN_POINT ( 'NONE',  ( 45.50350659930133190, 397.4670913484075072, 8.242918921510581143 ) ) ;
#65607=CARTESIAN_POINT ( 'NONE',  ( 44.17588657940204655, 463.1658906400379578, 6.343983253506471520 ) ) ;
#65610=CARTESIAN_POINT ( 'NONE',  ( -22.90481894975329880, 305.6283220865303178, 10.10585484844669502 ) ) ;
#65613=CARTESIAN_POINT ( 'NONE',  ( 32.99999999999987210, 485.0303364503728289, 0.9535057477322441688 ) ) ;
#65629=CARTESIAN_POINT ( 'NONE',  ( 30.00000000000000000, 500.0000000000002274, 0.000000000000000000 ) ) ;
#65635=CARTESIAN_POINT ( 'NONE',  ( 24.93816302196866275, 307.4233949143036284, 10.52291764336465008 ) ) ;
#65639=CARTESIAN_POINT ( 'NONE',  ( 31.21933008645656926, 405.2090764464551853, 25.56980379099173817 ) ) ;
#65650=DIRECTION ( 'NONE',  ( 0.000000000000000000, 0.000000000000000000, -1.000000000000000000 ) ) ;
#65653=VERTEX_POINT ( 'NONE', #46238 ) ;
#65666=CARTESIAN_POINT ( 'NONE',  ( 31.72480828332957614, 329.8229909459315650, 16.52334145234448926 ) ) ;
#65671=AXIS2_PLACEMENT_3D ( 'NONE', #6870, #49985, #40306 ) ;
#65675=CARTESIAN_POINT ( 'NONE',  ( -23.22454000777809924, 295.1922764084953315, 2.010205026916556115 ) ) ;
#65685=CARTESIAN_POINT ( 'NONE',  ( 0.000000000000000000, -0.1944580884125599318, -19.78098730681987760 ) ) ;
#65692=DIRECTION ( 'NONE',  ( 0.000000000000000000, -1.000000000000000000, -0.000000000000000000 ) ) ;
#65712=CARTESIAN_POINT ( 'NONE',  ( 32.99999999999992895, 485.0303364503728289, 0.9535057477322521624 ) ) ;
#65739=CARTESIAN_POINT ( 'NONE',  ( 30.08932219074489112, 331.1778411216668019, 15.36465306623354188 ) ) ;
#65743=ADVANCED_FACE ( 'NONE', ( #88294 ), #81567, .F. ) ;
#65746=CARTESIAN_POINT ( 'NONE',  ( -32.70943946516481304, 465.7622690753373149, 11.83845320051247363 ) ) ;
#65753=CARTESIAN_POINT ( 'NONE',  ( -43.52578837347117258, 465.2717874277799979, 9.360669990305815702 ) ) ;
#65758=CARTESIAN_POINT ( 'NONE',  ( -1.853816988907133201, 295.4475851226396230, -10.00136337793561658 ) ) ;
#65761=CARTESIAN_POINT ( 'NONE',  ( 42.31104777394612171, 465.8656652864358421, 14.28483731023800551 ) ) ;
#65766=CARTESIAN_POINT ( 'NONE',  ( -17.32323128014020241, 302.5970885151348284, 9.883177281172553563 ) ) ;
#65770=CARTESIAN_POINT ( 'NONE',  ( 35.17753024347895519, 490.3634983170069859, 12.17893648721826594 ) ) ;
#65777=CARTESIAN_POINT ( 'NONE',  ( -9.970195021759442611, 302.6460196488377505, -10.04373974541436887 ) ) ;
#65790=CARTESIAN_POINT ( 'NONE',  ( -36.38929466959749703, 356.0392961366259215, 1.859378810536674198 ) ) ;
#65802=CARTESIAN_POINT ( 'NONE',  ( -39.48063050920401906, 328.7742392842140475, 18.18155475394569365 ) ) ;
#65811=PLANE ( 'NONE',  #40227 ) ;
#65834=CARTESIAN_POINT ( 'NONE',  ( 36.74148664940359765, 437.9559008978175143, 4.252305828303467372 ) ) ;
#65842=ORIENTED_EDGE ( 'NONE', *, *, #69210, .F. ) ;
#65845=B_SPLINE_CURVE_WITH_KNOTS ( 'NONE', 3,
 ( #68051, #58912, #59993, #19019 ),
 .UNSPECIFIED., .F., .F.,
 ( 4, 4 ),
 ( 3.469446951953614189E-18, 0.001748759895715563256 ),
 .UNSPECIFIED. ) ;
#65849=CARTESIAN_POINT ( 'NONE',  ( 43.52075891743746894, 484.7805561108181109, 4.063293749111048569 ) ) ;
#65852=CARTESIAN_POINT ( 'NONE',  ( -32.85550102723723853, 465.7063702548733204, 11.00086562319487626 ) ) ;
#65876=CARTESIAN_POINT ( 'NONE',  ( -43.70013511063233835, 484.4793062204365128, 2.436320700791212879 ) ) ;
#65889=CARTESIAN_POINT ( 'NONE',  ( -35.69355135759316511, 463.3819780847709922, 19.97922827668330470 ) ) ;
#65892=SURFACE_SIDE_STYLE ('',( #32496 ) ) ;
#65909=CARTESIAN_POINT ( 'NONE',  ( -43.26971690803510029, 435.9072580013543643, 8.039630127097252554 ) ) ;
#65931=CARTESIAN_POINT ( 'NONE',  ( 30.17572460893185493, 323.8315592358100048, 14.85820515551728782 ) ) ;
#65936=EDGE_LOOP ( 'NONE', ( #20843, #38408, #85109, #69874 ) ) ;
#65940=DIRECTION ( 'NONE',  ( 0.000000000000000000, 0.000000000000000000, -1.000000000000000000 ) ) ;
#65948=CARTESIAN_POINT ( 'NONE',  ( -31.72650767699502339, 329.8019043314008059, 16.51996880882650132 ) ) ;
#65960=CARTESIAN_POINT ( 'NONE',  ( 35.54116392775497957, 439.5951022651032076, 24.01691468013297737 ) ) ;
#65972=CARTESIAN_POINT ( 'NONE',  ( 37.54237687664871004, 463.5961191363963962, 19.55587387186555048 ) ) ;
#65983=CARTESIAN_POINT ( 'NONE',  ( -42.09210974227526947, 317.4093497706929270, -4.557617623460385126 ) ) ;
#65987=CARTESIAN_POINT ( 'NONE',  ( 20.24579557674105246, 304.8297271373347144, -10.00469232190991598 ) ) ;
#66000=CARTESIAN_POINT ( 'NONE',  ( -34.53029562237181693, 437.2884171348779887, 5.234332900502464803 ) ) ;
#66008=CARTESIAN_POINT ( 'NONE',  ( -43.00000000000000000, 461.6622277975412771, 10.18145404766302065 ) ) ;
#66009=PLANE ( 'NONE',  #4662 ) ;
#66012=CIRCLE ( 'NONE', #67796, 5.000000000000001776 ) ;
#66014=LINE ( 'NONE', #24005, #81109 ) ;
#66027=CARTESIAN_POINT ( 'NONE',  ( 34.81143942477683595, 344.1812935971262277, 0.3927586600043628251 ) ) ;
#66036=CARTESIAN_POINT ( 'NONE',  ( -13.41614109918367248, 302.5494791983582559, -10.06425368032961210 ) ) ;
#66039=FACE_OUTER_BOUND ( 'NONE', #75323, .T. ) ;
#66040=ORIENTED_EDGE ( 'NONE', *, *, #74108, .F. ) ;
#66045=CARTESIAN_POINT ( 'NONE',  ( 6.953930663124324063, 304.7325910270068334, -10.02533923955978956 ) ) ;
#66049=ORIENTED_EDGE ( 'NONE', *, *, #34779, .F. ) ;
#66050=ORIENTED_EDGE ( 'NONE', *, *, #7452, .T. ) ;
#66054=CARTESIAN_POINT ( 'NONE',  ( 31.02114370244065356, 322.6370389015594924, 14.80589093843013160 ) ) ;
#66056=CARTESIAN_POINT ( 'NONE',  ( -42.63617128354209740, 336.9381626248995190, 8.123117897685229849 ) ) ;
#66063=CARTESIAN_POINT ( 'NONE',  ( 7.093721425956736049, 304.7303285792975771, 9.911179277710184365 ) ) ;
#66075=SURFACE_STYLE_USAGE ( .BOTH. , #49347 ) ;
#66077=CARTESIAN_POINT ( 'NONE',  ( -35.00874989808971094, 491.4345812359313186, 12.31435046935995281 ) ) ;
#66081=CARTESIAN_POINT ( 'NONE',  ( 43.47770857297122404, 484.8227827122696567, 4.253339224811428565 ) ) ;
#66085=CARTESIAN_POINT ( 'NONE',  ( -3.587928128302542596, 304.8518027750386636, 9.936999415048941131 ) ) ;
#66103=CARTESIAN_POINT ( 'NONE',  ( -38.02740175685438828, 490.5688714813329057, 12.25042287455428180 ) ) ;
#66121=CARTESIAN_POINT ( 'NONE',  ( 33.54963988678932196, 300.7094765539930563, -0.6813154228844996441 ) ) ;
#66124=CARTESIAN_POINT ( 'NONE',  ( -43.51517875623797948, 462.0595338174562130, 4.327785711300204952 ) ) ;
#66126=CARTESIAN_POINT ( 'NONE',  ( -35.56416567029047116, 496.2909070316903239, -10.19064917708978335 ) ) ;
#66127=EDGE_LOOP ( 'NONE', ( #92700, #41478, #61419, #103441 ) ) ;
#66130=DIRECTION ( 'NONE',  ( 0.000000000000000000, -0.9540597841379422350, 0.2996163017772281445 ) ) ;
#66133=CARTESIAN_POINT ( 'NONE',  ( 37.71362718402959047, 391.7064369608328320, 6.183124041103365442 ) ) ;
#66136=CARTESIAN_POINT ( 'NONE',  ( -22.32457463498002426, 305.3822942928727002, 10.05158438472647475 ) ) ;
#66138=CARTESIAN_POINT ( 'NONE',  ( 36.51457990505107887, 485.2739886279269399, -2.924107101145942522 ) ) ;
#66140=CARTESIAN_POINT ( 'NONE',  ( 33.00540147335372865, 487.4196752801331058, 9.523982417621985164 ) ) ;
#66146=ORIENTED_EDGE ( 'NONE', *, *, #37700, .F. ) ;
#66157=CARTESIAN_POINT ( 'NONE',  ( 38.68218982724705057, 320.0845437455996603, 16.10279619727025135 ) ) ;
#66160=CARTESIAN_POINT ( 'NONE',  ( -29.99999999999437250, 487.0575442883997539, 5.835066518937727764 ) ) ;
#66173=CARTESIAN_POINT ( 'NONE',  ( -42.10086803841218739, 435.6552064019005002, 19.95582312411058368 ) ) ;
#66182=CARTESIAN_POINT ( 'NONE',  ( -41.87034742571102441, 465.6969385752248627, 15.30562829125321933 ) ) ;
#66183=CARTESIAN_POINT ( 'NONE',  ( -30.93356169769148423, 332.2899936558947047, 16.85461323756102558 ) ) ;
#66185=VERTEX_POINT ( 'NONE', #59719 ) ;
#66188=CARTESIAN_POINT ( 'NONE',  ( 32.99999999999999289, 439.7597899781498541, 24.16317522621305258 ) ) ;
#66191=CARTESIAN_POINT ( 'NONE',  ( 31.35831589341289316, 299.6070351798090883, 11.00495117483204055 ) ) ;
#66195=CARTESIAN_POINT ( 'NONE',  ( 42.76745897559497678, 409.8493022072242979, 19.95836708624130296 ) ) ;
#66199=VERTEX_POINT ( 'NONE', #51599 ) ;
#66200=CARTESIAN_POINT ( 'NONE',  ( -22.37854104367661279, 303.2958516734515229, 10.03245274550628885 ) ) ;
#66202=CARTESIAN_POINT ( 'NONE',  ( -46.00000000000000000, 437.9690125970932968, 14.09127711025707796 ) ) ;
#66205=CARTESIAN_POINT ( 'NONE',  ( 2.587364514240426239, 300.7566975493048176, 9.662361691355732418 ) ) ;
#66212=B_SPLINE_CURVE_WITH_KNOTS ( 'NONE', 3,
 ( #86781, #70584, #96972, #96455 ),
 .UNSPECIFIED., .F., .F.,
 ( 4, 4 ),
 ( 0.000000000000000000, 0.001587725418201289037 ),
 .UNSPECIFIED. ) ;
#66222=CARTESIAN_POINT ( 'NONE',  ( -33.00000000000000000, 439.7597899781497972, 24.16317522621304192 ) ) ;
#66230=CARTESIAN_POINT ( 'NONE',  ( 32.93320410570996870, 485.0465637715138314, 1.208268278917676852 ) ) ;
#66231=EDGE_CURVE ( 'NONE', #19129, #96664, #105214, .T. ) ;
#66238=( BOUNDED_SURFACE ( )  B_SPLINE_SURFACE ( 3, 2, ( 
 ( #62721, #62212, #53558 ),
 ( #86489, #12547, #95610 ),
 ( #61682, #96672, #95095 ),
 ( #54588, #21753, #22808 ) ),
 .UNSPECIFIED., .F., .F., .F. ) 
 B_SPLINE_SURFACE_WITH_KNOTS ( ( 4, 4 ),
 ( 3, 3 ),
 ( 1.682681771697502882E-16, 0.0002890157658755999155 ),
 ( 0.000000000000000000, 1.000000000000000000 ),
 .UNSPECIFIED. ) 
 GEOMETRIC_REPRESENTATION_ITEM ( )  RATIONAL_B_SPLINE_SURFACE ( (
 ( 1.000000000000000000, 0.7950530193018341407, 1.000000000000000000),
 ( 1.000000000000000000, 0.7968506399851618127, 1.000000000000000000),
 ( 1.000000000000000000, 0.7985582592109712330, 1.000000000000000000),
 ( 1.000000000000000000, 0.8001746426092147813, 1.000000000000000000) ) ) 
 REPRESENTATION_ITEM ( '' )  SURFACE ( )  );
#66246=ORIENTED_EDGE ( 'NONE', *, *, #51090, .F. ) ;
#66247=CARTESIAN_POINT ( 'NONE',  ( 41.75349605901003258, 461.8279235811430681, 2.915883750441165212 ) ) ;
#66262=CARTESIAN_POINT ( 'NONE',  ( 29.72408284768632214, 326.8902487607700778, 14.35721078449378574 ) ) ;
#66273=CARTESIAN_POINT ( 'NONE',  ( -31.19792890532719198, 414.2215770364159084, 25.44228638033458623 ) ) ;
#66284=CARTESIAN_POINT ( 'NONE',  ( -0.6398555294984749064, 296.1023409385620653, -10.00028515034555809 ) ) ;
#66292=CARTESIAN_POINT ( 'NONE',  ( -20.97754405179124149, 294.8763868968453608, 9.942224931492244622 ) ) ;
#66296=CARTESIAN_POINT ( 'NONE',  ( 36.15790072655332921, 490.9284497187077818, 12.44298047260061679 ) ) ;
#66301=ORIENTED_EDGE ( 'NONE', *, *, #87735, .T. ) ;
#66303=CARTESIAN_POINT ( 'NONE',  ( -5.644657432743346526, 301.6279981551656419, -10.01771144603109853 ) ) ;
#66315=CARTESIAN_POINT ( 'NONE',  ( -29.57614253651134106, 308.9699467501231993, -8.830034548758142421 ) ) ;
#66322=CARTESIAN_POINT ( 'NONE',  ( -25.74471865176096230, 304.2941041679271166, -9.686096690486662553 ) ) ;
#66329=CARTESIAN_POINT ( 'NONE',  ( -40.89628519196639189, 427.9551160164463113, 26.89233021404036705 ) ) ;
#66330=CARTESIAN_POINT ( 'NONE',  ( -32.11963216114055797, 486.1305616887682390, 5.366014163932117498 ) ) ;
#66331=CARTESIAN_POINT ( 'NONE',  ( -38.98358762946092781, 463.6566946817218877, 19.41660091132907695 ) ) ;
#66337=CARTESIAN_POINT ( 'NONE',  ( 43.52075891743747604, 484.7805561108180541, 4.063293749110901132 ) ) ;
#66338=CARTESIAN_POINT ( 'NONE',  ( -39.97975729992978700, 437.4435441785136049, 22.46871538407117441 ) ) ;
#66340=LINE ( 'NONE', #8099, #16941 ) ;
#66341=CARTESIAN_POINT ( 'NONE',  ( 42.37751841893198446, 435.9440627571722757, 7.948837343527293875 ) ) ;
#66348=CARTESIAN_POINT ( 'NONE',  ( 46.00000000000000000, 488.9831568219304927, 4.757012338623754388 ) ) ;
#66360=DIRECTION ( 'NONE',  ( 0.000000000000000000, 0.000000000000000000, 1.000000000000000000 ) ) ;
#66362=CARTESIAN_POINT ( 'NONE',  ( 37.71459991402549861, 437.7716825518404562, 4.505118785439984563 ) ) ;
#66366=ORIENTED_EDGE ( 'NONE', *, *, #255, .F. ) ;
#66369=VERTEX_POINT ( 'NONE', #26714 ) ;
#66372=CARTESIAN_POINT ( 'NONE',  ( -33.00000000000000000, 500.0000000000002274, 0.000000000000000000 ) ) ;
#66377=CARTESIAN_POINT ( 'NONE',  ( 23.95564068939877345, 305.6666757346319514, -9.824255363917307804 ) ) ;
#66380=CARTESIAN_POINT ( 'NONE',  ( 30.00000000000000355, 489.3008774416947517, 5.491695563546554304 ) ) ;
#66397=CARTESIAN_POINT ( 'NONE',  ( 43.50377727019363050, 435.9167426301696082, 18.24083946424737590 ) ) ;
#66411=CARTESIAN_POINT ( 'NONE',  ( 31.96671797320279396, 484.9925651024516355, 5.143045411173839732 ) ) ;
#66416=CARTESIAN_POINT ( 'NONE',  ( 32.45623693501995888, 464.7023894946350993, 16.04003527243817473 ) ) ;
#66419=CARTESIAN_POINT ( 'NONE',  ( -32.18412820475297309, 464.7176420235863361, 10.95006602420806985 ) ) ;
#66433=CARTESIAN_POINT ( 'NONE',  ( 44.35776761200808238, 435.2162786697448382, 12.88191835534477647 ) ) ;
#66437=CARTESIAN_POINT ( 'NONE',  ( -33.00000000000000000, 450.0000000000002274, 13.20242257375370976 ) ) ;
#66438=CARTESIAN_POINT ( 'NONE',  ( 40.73878142687892279, 503.7113041876743864, 10.19672445236252045 ) ) ;
#66441=CARTESIAN_POINT ( 'NONE',  ( -43.02661387979676988, 465.7449615347604208, 11.43319743843887082 ) ) ;
#66442=CIRCLE ( 'NONE', #4459, 15.00000000000000711 ) ;
#66458=DIRECTION ( 'NONE',  ( 1.000000000000000000, 0.000000000000000000, 0.000000000000000000 ) ) ;
#66459=CARTESIAN_POINT ( 'NONE',  ( 22.36190337224704550, 304.3302339434704322, 10.03999859912378589 ) ) ;
#66475=CARTESIAN_POINT ( 'NONE',  ( -31.83737891999024328, 331.2472356323341387, 16.85379648827611376 ) ) ;
#66476=CARTESIAN_POINT ( 'NONE',  ( -32.82247836200028956, 434.5280635633159250, 16.69909682737922552 ) ) ;
#66479=CARTESIAN_POINT ( 'NONE',  ( -1.317676211347249549, 302.2248989068114611, 9.913061446930983678 ) ) ;
#66491=CARTESIAN_POINT ( 'NONE',  ( -36.87655955837857391, 438.2068510013161244, 3.933030107424709598 ) ) ;
#66499=CARTESIAN_POINT ( 'NONE',  ( -30.00000000000469669, 464.1479708722390001, 11.53751907632628360 ) ) ;
#66515=CARTESIAN_POINT ( 'NONE',  ( -24.37088254901632567, 295.3567874699774620, -9.892597027136796228 ) ) ;
#66518=CARTESIAN_POINT ( 'NONE',  ( 23.73340390206779560, 305.5981197995496927, -9.839287018817417518 ) ) ;
#66529=DIRECTION ( 'NONE',  ( 0.000000000000000000, 1.000000000000000000, 0.000000000000000000 ) ) ;
#66530=CARTESIAN_POINT ( 'NONE',  ( -32.28552837373661077, 464.7648866755938570, 15.30384310834759987 ) ) ;
#66533=CARTESIAN_POINT ( 'NONE',  ( -36.14862957314523584, 438.2394791802965983, 3.891583768390257880 ) ) ;
#66542=FACE_OUTER_BOUND ( 'NONE', #42187, .T. ) ;
#66558=CARTESIAN_POINT ( 'NONE',  ( 32.93903373786918110, 323.1113853486734797, -4.529746964764728823 ) ) ;
#66561=EDGE_CURVE ( 'NONE', #93450, #97465, #76962, .T. ) ;
#66563=VERTEX_POINT ( 'NONE', #53601 ) ;
#66569=DIRECTION ( 'NONE',  ( -0.9502668926229251856, 0.000000000000000000, 0.3114367235647877430 ) ) ;
#66570=CARTESIAN_POINT ( 'NONE',  ( -35.20412044861406997, 463.4819191117596233, 19.77841787011475105 ) ) ;
#66583=CARTESIAN_POINT ( 'NONE',  ( -42.51195073777072508, 462.6463319774571232, 3.762330311937251981 ) ) ;
#66589=CARTESIAN_POINT ( 'NONE',  ( -33.34415954575715801, 315.0055737288411137, -7.094410410514097265 ) ) ;
#66590=CARTESIAN_POINT ( 'NONE',  ( -13.58756192037751198, 304.5480426539326118, -9.064568272891900591 ) ) ;
#66612=CARTESIAN_POINT ( 'NONE',  ( -37.08530234603140485, 491.4084519804401907, 12.30481897466476049 ) ) ;
#66615=CARTESIAN_POINT ( 'NONE',  ( 43.03185303983483578, 485.3613526602390493, 6.073233449168488285 ) ) ;
#66623=CARTESIAN_POINT ( 'NONE',  ( 43.60098212335665124, 434.9832094534187377, 14.46717338012452458 ) ) ;
#66638=CARTESIAN_POINT ( 'NONE',  ( -41.58908019493902231, 487.6887286007228681, 9.912025820238323348 ) ) ;
#66645=ORIENTED_EDGE ( 'NONE', *, *, #38414, .T. ) ;
#66659=CARTESIAN_POINT ( 'NONE',  ( 30.43355426543545406, 298.0544874283102104, -1.294920856760706673 ) ) ;
#66660=LINE ( 'NONE', #32727, #67429 ) ;
#66662=CARTESIAN_POINT ( 'NONE',  ( 32.13503062639011176, 486.0946171966414795, 5.282847667695620864 ) ) ;
#66671=CARTESIAN_POINT ( 'NONE',  ( 43.67907128098302394, 391.2096367011267262, 15.78583024887160136 ) ) ;
#66676=CARTESIAN_POINT ( 'NONE',  ( -19.83463548332446535, 303.8035096162419109, 9.926734387303330465 ) ) ;
#66683=B_SPLINE_CURVE_WITH_KNOTS ( 'NONE', 3,
 ( #50005, #81816, #50520, #7942 ),
 .UNSPECIFIED., .F., .F.,
 ( 4, 4 ),
 ( 0.000000000000000000, 0.002170046543135659405 ),
 .UNSPECIFIED. ) ;
#66685=CARTESIAN_POINT ( 'NONE',  ( 46.00000000000000000, 437.9173578870139636, 12.34179081168240799 ) ) ;
#66698=CARTESIAN_POINT ( 'NONE',  ( 21.25502769577498796, 305.0480251235313176, 9.978840188629131802 ) ) ;
#66701=CARTESIAN_POINT ( 'NONE',  ( -34.68355603894254813, 461.9758321905093226, 4.166121198602492193 ) ) ;
#66706=EDGE_LOOP ( 'NONE', ( #30409, #69760, #15842, #70813 ) ) ;
#66711=AXIS2_PLACEMENT_3D ( 'NONE', #55815, #14843, #80640 ) ;
#66719=CARTESIAN_POINT ( 'NONE',  ( -32.03720899075933204, 464.7921976803852999, 11.81820142136001728 ) ) ;
#66722=CARTESIAN_POINT ( 'NONE',  ( -39.76451419608196858, 463.8702996273221402, 18.91610323218967693 ) ) ;
#66723=CARTESIAN_POINT ( 'NONE',  ( -32.11440895090206027, 433.9874903900313257, 24.22985920295750617 ) ) ;
#66726=CARTESIAN_POINT ( 'NONE',  ( 42.60956082013381518, 435.9305394647374214, 18.66091589586977406 ) ) ;
#66731=CARTESIAN_POINT ( 'NONE',  ( 31.19933698203508143, 299.4437075040892751, 10.96669800311853571 ) ) ;
#66739=ORIENTED_EDGE ( 'NONE', *, *, #81367, .T. ) ;
#66740=CARTESIAN_POINT ( 'NONE',  ( -22.26224575421402463, 303.2621863394111870, 10.02517495966816874 ) ) ;
#66746=AXIS2_PLACEMENT_3D ( 'NONE', #101012, #34727, #90811 ) ;
#66752=CARTESIAN_POINT ( 'NONE',  ( 43.85205561063540358, 464.7392644987205585, 11.03676161964373570 ) ) ;
#66757=ORIENTED_EDGE ( 'NONE', *, *, #25505, .T. ) ;
#66763=B_SPLINE_CURVE_WITH_KNOTS ( 'NONE', 3,
 ( #63107, #103041, #12940, #28649 ),
 .UNSPECIFIED., .F., .F.,
 ( 4, 4 ),
 ( 3.898306166456212538E-17, 0.001587725418198030142 ),
 .UNSPECIFIED. ) ;
#66765=CARTESIAN_POINT ( 'NONE',  ( -30.00000000000000000, 500.0000000000002274, -12.00000000000000711 ) ) ;
#66771=CARTESIAN_POINT ( 'NONE',  ( -35.17658899013244422, 491.5165241545290087, 12.37078523472847813 ) ) ;
#66774=CARTESIAN_POINT ( 'NONE',  ( 41.47545032752432803, 461.4488756740975646, 2.700315731345424464 ) ) ;
#66789=EDGE_LOOP ( 'NONE', ( #37655, #14297 ) ) ;
#66792=DIRECTION ( 'NONE',  ( -1.000000000000000000, 0.000000000000000000, 0.000000000000000000 ) ) ;
#66799=CARTESIAN_POINT ( 'NONE',  ( 5.391112028019903413, 294.7725620969052329, -8.441341902468499470 ) ) ;
#66804=CARTESIAN_POINT ( 'NONE',  ( 31.27225709781784957, 363.0917169579986989, 21.44302781083598930 ) ) ;
#66814=CARTESIAN_POINT ( 'NONE',  ( -21.25502769577498796, 305.0480251235313176, 9.978840188629131802 ) ) ;
#66822=VERTEX_POINT ( 'NONE', #15790 ) ;
#66826=CARTESIAN_POINT ( 'NONE',  ( -8.823089264727318692, 295.7038567688371131, -10.03557449692967118 ) ) ;
#66828=ORIENTED_EDGE ( 'NONE', *, *, #67309, .F. ) ;
#66833=CARTESIAN_POINT ( 'NONE',  ( 44.61777206441712451, 434.3429578869022976, 14.57557122161292362 ) ) ;
#66836=CARTESIAN_POINT ( 'NONE',  ( 35.67925427713999653, 491.2490127027394351, 12.19183392504568531 ) ) ;
#66844=CARTESIAN_POINT ( 'NONE',  ( -33.72905809600837301, 464.0430918388251484, 18.49991514059377806 ) ) ;
#66856=CARTESIAN_POINT ( 'NONE',  ( -32.35276657115729648, 315.1152556236738178, -7.307750464049918904 ) ) ;
#66866=CARTESIAN_POINT ( 'NONE',  ( -25.80611886614622819, 295.7843487485618539, -9.799740642693116399 ) ) ;
#66871=CARTESIAN_POINT ( 'NONE',  ( -33.06021938597559995, 369.5034847643744342, 23.69045737582667854 ) ) ;
#66881=CARTESIAN_POINT ( 'NONE',  ( 43.51067860848610991, 485.4417974898067314, 3.909400899861634304 ) ) ;
#66885=ORIENTED_EDGE ( 'NONE', *, *, #62637, .F. ) ;
#66886=DIRECTION ( 'NONE',  ( -1.000000000000000000, -0.000000000000000000, -0.000000000000000000 ) ) ;
#66888=CARTESIAN_POINT ( 'NONE',  ( 0.000000000000000000, 303.8518027762758038, 9.936999415352289589 ) ) ;
#66891=( BOUNDED_SURFACE ( )  B_SPLINE_SURFACE ( 3, 2, ( 
 ( #78274, #77756, #69147 ),
 ( #102014, #28175, #4390 ),
 ( #77220, #79334, #3868 ),
 ( #12993, #37329, #5455 ) ),
 .UNSPECIFIED., .F., .F., .F. ) 
 B_SPLINE_SURFACE_WITH_KNOTS ( ( 4, 4 ),
 ( 3, 3 ),
 ( -1.214306433183764966E-17, 0.003677210556161270016 ),
 ( 0.000000000000000000, 1.000000000000000000 ),
 .UNSPECIFIED. ) 
 GEOMETRIC_REPRESENTATION_ITEM ( )  RATIONAL_B_SPLINE_SURFACE ( (
 ( 1.000000000000000000, 0.7874655377940259493, 1.000000000000000000),
 ( 1.000000000000000000, 0.7709584336437038665, 1.000000000000000000),
 ( 1.000000000000000000, 0.7542748649868507016, 1.000000000000000000),
 ( 1.000000000000000000, 0.7370557512816398038, 1.000000000000000000) ) ) 
 REPRESENTATION_ITEM ( '' )  SURFACE ( )  );
#66892=B_SPLINE_CURVE_WITH_KNOTS ( 'NONE', 3,
 ( #54331, #105562, #105046, #7387, #47843, #31187, #64072, #96947 ),
 .UNSPECIFIED., .F., .F.,
 ( 4, 2, 2, 4 ),
 ( 0.000000000000000000, 0.002052176099994375801, 0.003078264149991564568, 0.004104352199988753336 ),
 .UNSPECIFIED. ) ;
#66903=CYLINDRICAL_SURFACE ( 'NONE', #85427, 15.00000000000001421 ) ;
#66913=B_SPLINE_CURVE_WITH_KNOTS ( 'NONE', 3,
 ( #88471, #80348, #6461, #33430, #23756, #106208, #15621, #25903, #58209, #461, #91134, #66303, #73312, #32371, #99184, #90583, #32902, #65777 ),
 .UNSPECIFIED., .F., .F.,
 ( 4, 2, 2, 2, 2, 2, 2, 2, 4 ),
 ( -1.788854398705523621E-05, 0.003356281543241195105, 0.005043366586855251542, 0.006730451630469307112, 0.007573994152276390841, 0.008417536674083472836, 0.01010462171769764377, 0.01179170676131181296, 0.01347879180492598215 ),
 .UNSPECIFIED. ) ;
#66926=CARTESIAN_POINT ( 'NONE',  ( -11.80096911583921404, 304.5943216053429410, -9.054726665033207667 ) ) ;
#66927=CARTESIAN_POINT ( 'NONE',  ( 30.24427031855517711, 312.0196691915732004, -8.325478004009855937 ) ) ;
#66928=CARTESIAN_POINT ( 'NONE',  ( 41.02721008360133226, 460.5398098099298636, 2.518281297459247448 ) ) ;
#66945=CARTESIAN_POINT ( 'NONE',  ( 43.72105821076075927, 464.5236242685676871, 7.250473608341952314 ) ) ;
#66950=ADVANCED_FACE ( 'NONE', ( #76677 ), #55825, .T. ) ;
#66962=ORIENTED_EDGE ( 'NONE', *, *, #9820, .F. ) ;
#66982=CARTESIAN_POINT ( 'NONE',  ( 44.28914958154554427, 435.2230000814673758, 14.00302124382064761 ) ) ;
#66989=CARTESIAN_POINT ( 'NONE',  ( 42.50679667589145794, 460.9583926513302004, 2.954705527089782624 ) ) ;
#67004=CARTESIAN_POINT ( 'NONE',  ( 30.47402504887697106, 326.6747004222083888, 15.54443406114438453 ) ) ;
#67017=VERTEX_POINT ( 'NONE', #28706 ) ;
#67023=CARTESIAN_POINT ( 'NONE',  ( -24.97496876848101977, 304.5750556681570629, 10.31800315847969429 ) ) ;
#67046=CARTESIAN_POINT ( 'NONE',  ( -30.00000000002245315, 464.1822223165869445, 13.92818874393521966 ) ) ;
#67049=ORIENTED_EDGE ( 'NONE', *, *, #51361, .F. ) ;
#67050=AXIS2_PLACEMENT_3D ( 'NONE', #53218, #46187, #45142 ) ;
#67051=ADVANCED_FACE ( 'NONE', ( #85314 ), #66891, .F. ) ;
#67055=CARTESIAN_POINT ( 'NONE',  ( 19.96162532426522773, 302.8116070918645164, 9.928455558879880627 ) ) ;
#67070=CARTESIAN_POINT ( 'NONE',  ( -43.47770857297121694, 484.8227827122652229, 4.253339224812703101 ) ) ;
#67074=CARTESIAN_POINT ( 'NONE',  ( -35.30457612798088718, 437.1674308734259284, 5.430039551431026901 ) ) ;
#67084=DIRECTION ( 'NONE',  ( -1.000000000000000000, -0.000000000000000000, -0.000000000000000000 ) ) ;
#67100=CARTESIAN_POINT ( 'NONE',  ( 35.51708561081854754, 413.1995985843952894, 6.943723052262567919 ) ) ;
#67103=CIRCLE ( 'NONE', #41222, 7.999999999999994671 ) ;
#67104=EDGE_LOOP ( 'NONE', ( #12010, #21408, #33447, #20264 ) ) ;
#67107=CARTESIAN_POINT ( 'NONE',  ( 9.970195021754669540, 302.6460196488382053, -10.04373974541433689 ) ) ;
#67108=CARTESIAN_POINT ( 'NONE',  ( -11.51023648311793934, 294.5990937745008864, -2.053736347526041506 ) ) ;
#67110=CARTESIAN_POINT ( 'NONE',  ( 32.78378308087458493, 465.0370457078494155, 14.48673668603556663 ) ) ;
#67126=DIRECTION ( 'NONE',  ( 0.9135154255863047190, -0.3026456445944416540, -0.2718366807917715344 ) ) ;
#67128=CARTESIAN_POINT ( 'NONE',  ( -36.02170868991535002, 304.0253897065642263, 0.1122103735631282684 ) ) ;
#67129=CARTESIAN_POINT ( 'NONE',  ( -6.818939631097694409, 304.7371852070875775, -9.024366697556562400 ) ) ;
#67134=ORIENTED_EDGE ( 'NONE', *, *, #70072, .F. ) ;
#67137=B_SPLINE_CURVE_WITH_KNOTS ( 'NONE', 3,
 ( #26882, #100193, #27421, #27956, #11166, #44094, #85624, #44636, #60820, #92096, #93172, #18237 ),
 .UNSPECIFIED., .F., .F.,
 ( 4, 2, 2, 2, 2, 4 ),
 ( 0.000000000000000000, 0.001850948747980105200, 0.002776423121970204855, 0.003701897495960304943, 0.005552846243940486905, 0.007403794991920670601 ),
 .UNSPECIFIED. ) ;
#67143=EDGE_LOOP ( 'NONE', ( #63487, #103639, #103422, #82496 ) ) ;
#67159=DIRECTION ( 'NONE',  ( 0.000000000000000000, 0.000000000000000000, 1.000000000000000000 ) ) ;
#67161=FACE_OUTER_BOUND ( 'NONE', #11867, .T. ) ;
#67162=B_SPLINE_CURVE_WITH_KNOTS ( 'NONE', 3,
 ( #199, #25072, #2354, #74643, #100522, #33163, #92423, #27216, #19132, #67107 ),
 .UNSPECIFIED., .F., .F.,
 ( 4, 2, 2, 2, 4 ),
 ( -5.999999998189896673E-08, 0.001316581415853271785, 0.002633222831706525432, 0.005266505663413042701, 0.01053307132682607290 ),
 .UNSPECIFIED. ) ;
#67163=DIRECTION ( 'NONE',  ( -0.000000000000000000, -1.000000000000000000, -0.000000000000000000 ) ) ;
#67168=DIRECTION ( 'NONE',  ( 1.000000000000000000, 0.000000000000000000, 0.000000000000000000 ) ) ;
#67185=CARTESIAN_POINT ( 'NONE',  ( -43.21801493131978589, 434.4543138596390008, 16.17410598222931029 ) ) ;
#67188=AXIS2_PLACEMENT_3D ( 'NONE', #105908, #159, #84180 ) ;
#67189=CARTESIAN_POINT ( 'NONE',  ( 37.56208910883223240, 463.3609840191073772, 20.02047205468278790 ) ) ;
#67192=CARTESIAN_POINT ( 'NONE',  ( -42.76313255036283323, 461.1833584523140530, 3.199811539384791459 ) ) ;
#67196=CARTESIAN_POINT ( 'NONE',  ( -38.64834039627831430, 312.1053154204562929, 6.072046802107182728 ) ) ;
#67205=CARTESIAN_POINT ( 'NONE',  ( 26.15475286542767819, 304.5035472506963856, -9.639477703573707146 ) ) ;
#67207=EDGE_CURVE ( 'NONE', #24536, #80654, #25387, .T. ) ;
#67213=DIRECTION ( 'NONE',  ( 0.000000000000000000, 0.000000000000000000, -1.000000000000000000 ) ) ;
#67217=CARTESIAN_POINT ( 'NONE',  ( -42.09158233638504498, 465.7816406625409513, 14.79318349170026892 ) ) ;
#67220=CARTESIAN_POINT ( 'NONE',  ( -22.85358936945000252, 305.5818686480074575, 9.095431853656572585 ) ) ;
#67222=CARTESIAN_POINT ( 'NONE',  ( 34.14275462543660922, 484.1047237107248407, 0.7219141280516476744 ) ) ;
#67225=CARTESIAN_POINT ( 'NONE',  ( 32.00986601473097437, 486.4616239121639296, 6.105527853532677796 ) ) ;
#67229=CARTESIAN_POINT ( 'NONE',  ( 44.23810852895211809, 435.1998687191861563, 14.01156801387538309 ) ) ;
#67241=CARTESIAN_POINT ( 'NONE',  ( 51.01037695545453232, 500.0000000000002274, 0.000000000000000000 ) ) ;
#67243=CARTESIAN_POINT ( 'NONE',  ( 40.93435977689158989, 414.3154843149413296, 27.72243992809649527 ) ) ;
#67275=CARTESIAN_POINT ( 'NONE',  ( 33.80977330536913428, 301.4714739734875479, 3.439059217111231082 ) ) ;
#67281=CARTESIAN_POINT ( 'NONE',  ( 35.65344923961711032, 304.2588450519185699, 4.111980580341269231 ) ) ;
#67284=CARTESIAN_POINT ( 'NONE',  ( -22.56879301375676050, 303.3526548909255780, 10.04479196209192615 ) ) ;
#67292=CARTESIAN_POINT ( 'NONE',  ( 46.00000000000000000, 461.8824355614426054, 11.41562375511947458 ) ) ;
#67309=EDGE_CURVE ( 'NONE', #10763, #14964, #40826, .T. ) ;
#67311=CARTESIAN_POINT ( 'NONE',  ( -32.09911992168218831, 438.9232547152092252, 23.66653216045979491 ) ) ;
#67319=ORIENTED_EDGE ( 'NONE', *, *, #96766, .F. ) ;
#67337=CARTESIAN_POINT ( 'NONE',  ( -5.385569124936798957, 294.7724401061256572, -8.430686591128788265 ) ) ;
#67344=CARTESIAN_POINT ( 'NONE',  ( 30.72323423254651686, 348.3287414960516912, 19.95724199425579570 ) ) ;
#67355=FACE_OUTER_BOUND ( 'NONE', #86766, .T. ) ;
#67364=CARTESIAN_POINT ( 'NONE',  ( -9.659964574194615849, 294.6522956596209610, -2.587254427031161264 ) ) ;
#67383=( BOUNDED_SURFACE ( )  B_SPLINE_SURFACE ( 3, 2, ( 
 ( #10502, #92482, #28321 ),
 ( #19184, #18632, #101113 ),
 ( #83861, #3489, #61198 ),
 ( #76297, #93022, #9973 ) ),
 .UNSPECIFIED., .F., .F., .F. ) 
 B_SPLINE_SURFACE_WITH_KNOTS ( ( 4, 4 ),
 ( 3, 3 ),
 ( 6.938893903907228378E-18, 0.001025706331908567614 ),
 ( 0.000000000000000000, 1.000000000000000000 ),
 .UNSPECIFIED. ) 
 GEOMETRIC_REPRESENTATION_ITEM ( )  RATIONAL_B_SPLINE_SURFACE ( (
 ( 1.000000000000000000, 0.9153908114178146427, 1.000000000000000000),
 ( 1.000000000000000000, 0.9167125567853761092, 1.000000000000000000),
 ( 1.000000000000000000, 0.9180307555289068944, 1.000000000000000000),
 ( 1.000000000000000000, 0.9193453746270491278, 1.000000000000000000) ) ) 
 REPRESENTATION_ITEM ( '' )  SURFACE ( )  );
#67393=CARTESIAN_POINT ( 'NONE',  ( -21.14633401031152360, 303.9368958959844917, -9.981912898654558219 ) ) ;
#67395=( BOUNDED_SURFACE ( )  B_SPLINE_SURFACE ( 3, 2, ( 
 ( #79862, #15132, #96067 ),
 ( #87979, #64756, #38900 ),
 ( #104676, #80925, #88507 ),
 ( #97110, #30827, #54509 ),
 ( #71243, #48015, #80389 ),
 ( #22198, #104141, #62645 ),
 ( #56643, #89562, #6498 ),
 ( #78802, #39435, #46963 ),
 ( #95529, #71764, #63712 ),
 ( #7036, #96600, #4934 ),
 ( #37866, #21675, #75489 ),
 ( #98172, #41531, #100296 ),
 ( #26458, #81975, #34011 ),
 ( #66338, #58797, #8630 ),
 ( #59323, #17278, #49077 ),
 ( #8097, #65281, #495 ),
 ( #90624, #16190, #16730 ),
 ( #50656, #41007, #24843 ) ),
 .UNSPECIFIED., .F., .F., .F. ) 
 B_SPLINE_SURFACE_WITH_KNOTS ( ( 4, 2, 2, 2, 2, 2, 2, 2, 4 ),
 ( 3, 3 ),
 ( 0.0001601145914732075891, 0.001714143494069139120, 0.002491157945367104831, 0.003268172396665070759, 0.004822201299261002182, 0.006376230201856934038, 0.007930259104452865027, 0.009484288007048796015, 0.01259234581224065973 ),
 ( 0.000000000000000000, 1.000000000000000000 ),
 .UNSPECIFIED. ) 
 GEOMETRIC_REPRESENTATION_ITEM ( )  RATIONAL_B_SPLINE_SURFACE ( (
 ( 1.000000000000000000, 0.9028401456532980651, 1.000000000000000000),
 ( 1.000000000000000000, 0.9067333287510357387, 1.000000000000000000),
 ( 1.000000000000000000, 0.9090942099086769534, 1.000000000000000000),
 ( 1.000000000000000000, 0.9101952033055793478, 1.000000000000000000),
 ( 1.000000000000000000, 0.9101526397032935201, 1.000000000000000000),
 ( 1.000000000000000000, 0.9092257979258016043, 1.000000000000000000),
 ( 1.000000000000000000, 0.9083503838810818021, 1.000000000000000000),
 ( 1.000000000000000000, 0.9045634707242991013, 1.000000000000000000),
 ( 1.000000000000000000, 0.9004851055695014539, 1.000000000000000000),
 ( 1.000000000000000000, 0.8895482392855161846, 1.000000000000000000),
 ( 1.000000000000000000, 0.8828580819741439489, 1.000000000000000000),
 ( 1.000000000000000000, 0.8675505019241241955, 1.000000000000000000),
 ( 1.000000000000000000, 0.8588864831504116060, 1.000000000000000000),
 ( 1.000000000000000000, 0.8401763864807653137, 1.000000000000000000),
 ( 1.000000000000000000, 0.8302671801042916799, 1.000000000000000000),
 ( 1.000000000000000000, 0.7996378488151107966, 1.000000000000000000),
 ( 1.000000000000000000, 0.7777557150150771204, 1.000000000000000000),
 ( 1.000000000000000000, 0.7583909709667374655, 1.000000000000000000) ) ) 
 REPRESENTATION_ITEM ( '' )  SURFACE ( )  );
#67396=CARTESIAN_POINT ( 'NONE',  ( -33.67444716837063368, 489.3309112354450008, 10.55021651976771757 ) ) ;
#67399=ADVANCED_FACE ( 'NONE', ( #54249 ), #61673, .T. ) ;
#67407=FACE_OUTER_BOUND ( 'NONE', #89414, .T. ) ;
#67409=CARTESIAN_POINT ( 'NONE',  ( -42.70310427752711746, 433.3420030442914594, 18.58178892519891079 ) ) ;
#67419=CARTESIAN_POINT ( 'NONE',  ( 32.94021323899734455, 485.0599191339525191, 5.361609822540892800 ) ) ;
#67421=CARTESIAN_POINT ( 'NONE',  ( 0.000000000000000000, -19.99999999999998934, 0.000000000000000000 ) ) ;
#67429=VECTOR ( 'NONE', #90946, 1000.000000000000000 ) ;
#67431=CIRCLE ( 'NONE', #46785, 5.000000000000000888 ) ;
#67439=CARTESIAN_POINT ( 'NONE',  ( 22.20318009218133071, 295.0333587257888439, 9.975590323731541531 ) ) ;
#67445=CARTESIAN_POINT ( 'NONE',  ( -40.62988512551102360, 465.1694420659723619, 17.16838584799783973 ) ) ;
#67447=DIRECTION ( 'NONE',  ( 0.000000000000000000, 0.000000000000000000, 1.000000000000000000 ) ) ;
#67454=CARTESIAN_POINT ( 'NONE',  ( 46.00000000000000000, 459.9277931459794786, 6.461582622334601567 ) ) ;
#67458=DIRECTION ( 'NONE',  ( -0.8902151594054030781, 0.000000000000000000, 0.4555403055326856521 ) ) ;
#67461=CARTESIAN_POINT ( 'NONE',  ( 40.54048956546203897, 460.8805895396365031, 2.213361020664811996 ) ) ;
#67462=CARTESIAN_POINT ( 'NONE',  ( -33.92709525147871830, 435.0559456452657514, 11.89085117398056113 ) ) ;
#67480=MECHANICAL_DESIGN_GEOMETRIC_PRESENTATION_REPRESENTATION('',(#72616),#58936);
#67492=ORIENTED_EDGE ( 'NONE', *, *, #54343, .T. ) ;
#67517=CARTESIAN_POINT ( 'NONE',  ( 40.85254446136673323, 441.7500193615117610, 25.53625856138344474 ) ) ;
#67523=CARTESIAN_POINT ( 'NONE',  ( -23.21474708200883796, 305.7582702134220085, 9.134669239329348045 ) ) ;
#67536=CARTESIAN_POINT ( 'NONE',  ( 43.27198366478697267, 461.7520071969412925, 3.865882560854753347 ) ) ;
#67537=CARTESIAN_POINT ( 'NONE',  ( 26.98763868050856729, 309.1593988222194866, 11.18671119439325956 ) ) ;
#67547=CARTESIAN_POINT ( 'NONE',  ( -46.00000000000000000, 460.8575856737582512, 7.929402417978877793 ) ) ;
#67553=CARTESIAN_POINT ( 'NONE',  ( 30.00000000000000355, 488.7759232733317845, 4.253593570494768272 ) ) ;
#67556=CARTESIAN_POINT ( 'NONE',  ( -33.16832880629362279, 391.4582360920214796, 25.60486106200601952 ) ) ;
#67557=CARTESIAN_POINT ( 'NONE',  ( -32.48507062769438392, 435.0120188477415581, 18.09005837372713899 ) ) ;
#67566=EDGE_CURVE ( 'NONE', #23677, #13857, #37598, .T. ) ;
#67568=CARTESIAN_POINT ( 'NONE',  ( -31.96161004470367928, 465.6201165449651285, 10.43791023679821883 ) ) ;
#67570=ADVANCED_FACE ( 'NONE', ( #65551 ), #77915, .F. ) ;
#67573=CARTESIAN_POINT ( 'NONE',  ( -35.07439070119946933, 437.8544070495365759, 4.397851634058751458 ) ) ;
#67582=AXIS2_PLACEMENT_3D ( 'NONE', #66437, #17379, #26039 ) ;
#67583=CARTESIAN_POINT ( 'NONE',  ( 32.39555719572166481, 435.1515357145120220, 14.91598548009360670 ) ) ;
#67587=CARTESIAN_POINT ( 'NONE',  ( 16.83213728180786362, 302.5742751247036040, 9.878299632764496963 ) ) ;
#67597=EDGE_CURVE ( 'NONE', #76425, #106028, #60159, .T. ) ;
#67601=CARTESIAN_POINT ( 'NONE',  ( -30.00000000000000000, 461.8163627757383551, 11.11111419091028729 ) ) ;
#67607=CARTESIAN_POINT ( 'NONE',  ( -36.28420329444977455, 437.5777248398061374, 4.256696328374294680 ) ) ;
#67614=EDGE_CURVE ( 'NONE', #105135, #16697, #8207, .T. ) ;
#67620=VERTEX_POINT ( 'NONE', #60672 ) ;
#67624=CARTESIAN_POINT ( 'NONE',  ( 30.07110509900797268, 309.7455132721622135, -8.642324552508243940 ) ) ;
#67644=DIRECTION ( 'NONE',  ( 0.000000000000000000, 0.000000000000000000, -1.000000000000000000 ) ) ;
#67645=CARTESIAN_POINT ( 'NONE',  ( -33.52832263806441659, 435.4519723258069348, 9.506607217394984488 ) ) ;
#67647=CARTESIAN_POINT ( 'NONE',  ( -37.54559764570110048, 464.1143081516183884, 19.43664670202764100 ) ) ;
#67662=CARTESIAN_POINT ( 'NONE',  ( -37.41669077972581192, 304.6406083910922007, -7.749892281362566138 ) ) ;
#67663=CARTESIAN_POINT ( 'NONE',  ( -11.86976244332121233, 303.5920063884646538, -10.05522024194447539 ) ) ;
#67690=CIRCLE ( 'NONE', #103865, 4.999999999999993783 ) ;
#67698=CARTESIAN_POINT ( 'NONE',  ( 32.85155332502863956, 463.8111683108725174, 7.359358840565810134 ) ) ;
#67720=CARTESIAN_POINT ( 'NONE',  ( -41.66331289688267958, 334.8661377240072738, 11.59565765669084847 ) ) ;
#67723=ORIENTED_EDGE ( 'NONE', *, *, #106332, .T. ) ;
#67725=DIRECTION ( 'NONE',  ( 0.9745656835855589506, 0.000000000000000000, 0.2241020490254661268 ) ) ;
#67728=CARTESIAN_POINT ( 'NONE',  ( 41.58649125062324003, 315.0454808444952732, -5.157136739128146630 ) ) ;
#67744=CARTESIAN_POINT ( 'NONE',  ( 30.99921441447351356, 438.8475427232315838, 22.05400630073976131 ) ) ;
#67761=( LENGTH_UNIT ( ) NAMED_UNIT ( * ) SI_UNIT ( .MILLI., .METRE. ) );
#67763=CARTESIAN_POINT ( 'NONE',  ( -43.71335306921091046, 464.5235014653455323, 7.258763594085895221 ) ) ;
#67766=CARTESIAN_POINT ( 'NONE',  ( -35.61495859169594524, 461.3395811758602463, 3.370444927184965689 ) ) ;
#67776=CARTESIAN_POINT ( 'NONE',  ( -26.34324959015004453, 307.8500962193381270, 10.86395315858437804 ) ) ;
#67781=CARTESIAN_POINT ( 'NONE',  ( -32.78378308081553882, 465.0370457077456194, 14.48673668605084153 ) ) ;
#67785=CARTESIAN_POINT ( 'NONE',  ( -31.12255084532423055, 439.8601387403313652, 23.32256247975105978 ) ) ;
#67789=B_SPLINE_CURVE_WITH_KNOTS ( 'NONE', 3,
 ( #66222, #99108, #25270, #91057 ),
 .UNSPECIFIED., .F., .F.,
 ( 4, 4 ),
 ( 0.000000000000000000, 0.0001235227585948107888 ),
 .UNSPECIFIED. ) ;
#67794=CARTESIAN_POINT ( 'NONE',  ( 36.42984981315670723, 305.7557014711401848, 4.481287940851245821 ) ) ;
#67796=AXIS2_PLACEMENT_3D ( 'NONE', #55963, #14449, #32265 ) ;
#67806=VERTEX_POINT ( 'NONE', #99910 ) ;
#67807=CARTESIAN_POINT ( 'NONE',  ( 30.00000000000000000, 461.8163627757383551, 11.11111419091032460 ) ) ;
#67830=CYLINDRICAL_SURFACE ( 'NONE', #77293, 15.00000000000001243 ) ;
#67855=CARTESIAN_POINT ( 'NONE',  ( -2.808418600359145145, 294.8278116980254708, -9.614630257155971194 ) ) ;
#67863=CARTESIAN_POINT ( 'NONE',  ( 28.48717193686734106, 313.7474573396027040, 12.33990598094187341 ) ) ;
#67874=CARTESIAN_POINT ( 'NONE',  ( -33.63427961064055438, 325.9154870834976236, -4.827994974213513757 ) ) ;
#67887=B_SPLINE_CURVE_WITH_KNOTS ( 'NONE', 3,
 ( #853, #39905, #105685, #47968, #72263, #14537, #8983, #31824, #31312, #80877 ),
 .UNSPECIFIED., .F., .F.,
 ( 4, 2, 2, 2, 4 ),
 ( 1.651718721987238896E-28, 0.01019698562015586112, 0.01529547843023379254, 0.01784472483527275305, 0.02039397124031171182 ),
 .UNSPECIFIED. ) ;
#67897=AXIS2_PLACEMENT_3D ( 'NONE', #42153, #23887, #75036 ) ;
#67912=CARTESIAN_POINT ( 'NONE',  ( -24.81120153453596799, 306.0655852089439577, -9.736014901624853835 ) ) ;
#67916=AXIS2_PLACEMENT_3D ( 'NONE', #24117, #41853, #66130 ) ;
#67925=CARTESIAN_POINT ( 'NONE',  ( -34.40608992613577044, 484.1267599597962317, 0.1303963904809097296 ) ) ;
#67926=CARTESIAN_POINT ( 'NONE',  ( -40.85805974307315580, 440.2633714685022710, 25.57337624204853199 ) ) ;
#67932=B_SPLINE_CURVE_WITH_KNOTS ( 'NONE', 3,
 ( #2634, #35580, #42036, #91668, #10196, #9652, #75996, #26436 ),
 .UNSPECIFIED., .F., .F.,
 ( 4, 2, 2, 4 ),
 ( 0.000000000000000000, 0.003573659743918579813, 0.005360489615877896824, 0.007147319487837215136 ),
 .UNSPECIFIED. ) ;
#67936=EDGE_CURVE ( 'NONE', #18077, #4192, #28197, .T. ) ;
#67941=CIRCLE ( 'NONE', #21460, 1.000000000000000888 ) ;
#67956=CARTESIAN_POINT ( 'NONE',  ( 9.398978598878366952, 294.6597737643559185, -3.429745804602678305 ) ) ;
#67957=CARTESIAN_POINT ( 'NONE',  ( 29.07128654445882887, 296.9339959557834163, -9.548856946221640385 ) ) ;
#67961=CARTESIAN_POINT ( 'NONE',  ( -21.51569398614863715, 294.9107018935607130, -9.987480606144506723 ) ) ;
#67973=FACE_BOUND ( 'NONE', #106710, .T. ) ;
#67989=ORIENTED_EDGE ( 'NONE', *, *, #79449, .F. ) ;
#67994=CARTESIAN_POINT ( 'NONE',  ( 43.03357534759661718, 463.2291678140137492, 4.675918524166122303 ) ) ;
#67996=CARTESIAN_POINT ( 'NONE',  ( 32.20528583231335062, 488.0688772979464716, 8.922366577023394640 ) ) ;
#68021=CARTESIAN_POINT ( 'NONE',  ( -26.54817876223620488, 310.6276912632132507, 11.31208242866018132 ) ) ;
#68027=CARTESIAN_POINT ( 'NONE',  ( -32.10528697966002198, 486.1671898930082421, 5.449875171704826826 ) ) ;
#68033=CARTESIAN_POINT ( 'NONE',  ( -42.80559098684942398, 434.8801202232389187, 8.726134940843630616 ) ) ;
#68039=CARTESIAN_POINT ( 'NONE',  ( -26.52730633476061683, 310.2711082345475120, 10.22138833121726442 ) ) ;
#68051=CARTESIAN_POINT ( 'NONE',  ( 42.20041562234358423, 435.2369744135583574, 7.788607701745475786 ) ) ;
#68053=CARTESIAN_POINT ( 'NONE',  ( -34.12349128637492157, 490.8027302422244134, 11.84948222508912252 ) ) ;
#68062=CARTESIAN_POINT ( 'NONE',  ( -41.51027609766077120, 460.7143792095437220, 2.893824450528216019 ) ) ;
#68093=ORIENTED_EDGE ( 'NONE', *, *, #54343, .F. ) ;
#68096=CARTESIAN_POINT ( 'NONE',  ( 32.48450373119614198, 435.0129692059579156, 18.09237844440232124 ) ) ;
#68102=CARTESIAN_POINT ( 'NONE',  ( -45.48126212248870814, 413.7349014071057240, 8.309231847991947362 ) ) ;
#68103=DIRECTION ( 'NONE',  ( -0.000000000000000000, -0.09744402424476124314, -0.9952410070626042105 ) ) ;
#68116=CARTESIAN_POINT ( 'NONE',  ( -30.24427031855517711, 312.0196691915732004, -8.325478004009855937 ) ) ;
#68132=AXIS2_PLACEMENT_3D ( 'NONE', #24550, #48243, #81144 ) ;
#68133=CIRCLE ( 'NONE', #28599, 2.999999999999999112 ) ;
#68148=( BOUNDED_SURFACE ( )  B_SPLINE_SURFACE ( 3, 2, ( 
 ( #63973, #29507, #14856 ),
 ( #104399, #15393, #21930 ),
 ( #89300, #47750, #70982 ),
 ( #104953, #54781, #81180 ),
 ( #23525, #79599, #80649 ),
 ( #6772, #56362, #87710 ),
 ( #87182, #80123, #39692 ),
 ( #22467, #46184, #13792 ),
 ( #79076, #72567, #48279 ),
 ( #7291, #46703, #38126 ),
 ( #5711, #38636, #71500 ),
 ( #30548, #63446, #96341 ) ),
 .UNSPECIFIED., .F., .F., .F. ) 
 B_SPLINE_SURFACE_WITH_KNOTS ( ( 4, 2, 2, 2, 2, 4 ),
 ( 3, 3 ),
 ( 8.673617379884035472E-18, 0.001890581228128788115, 0.002835871842193177835, 0.003781162456257567556, 0.005671743684386346997, 0.007562324912515126438 ),
 ( 0.000000000000000000, 1.000000000000000000 ),
 .UNSPECIFIED. ) 
 GEOMETRIC_REPRESENTATION_ITEM ( )  RATIONAL_B_SPLINE_SURFACE ( (
 ( 1.000000000000000000, 0.7560596356357117687, 1.000000000000000000),
 ( 1.000000000000000000, 0.7675942737806970007, 1.000000000000000000),
 ( 1.000000000000000000, 0.7799842945909555292, 1.000000000000000000),
 ( 1.000000000000000000, 0.7988124055279367530, 1.000000000000000000),
 ( 1.000000000000000000, 0.8051313863604262488, 1.000000000000000000),
 ( 1.000000000000000000, 0.8177136313173961613, 1.000000000000000000),
 ( 1.000000000000000000, 0.8240064671659272921, 1.000000000000000000),
 ( 1.000000000000000000, 0.8422864973116017673, 1.000000000000000000),
 ( 1.000000000000000000, 0.8537348782016001003, 1.000000000000000000),
 ( 1.000000000000000000, 0.8743527270674196217, 1.000000000000000000),
 ( 1.000000000000000000, 0.8835747495209320679, 1.000000000000000000),
 ( 1.000000000000000000, 0.8909749942926241673, 1.000000000000000000) ) ) 
 REPRESENTATION_ITEM ( '' )  SURFACE ( )  );
#68165=CARTESIAN_POINT ( 'NONE',  ( -43.71297783477844234, 485.1278128289774827, -1.116606130290715981 ) ) ;
#68171=CARTESIAN_POINT ( 'NONE',  ( 32.94994279514033053, 464.9549361168423047, 15.12478419437801946 ) ) ;
#68177=ORIENTED_EDGE ( 'NONE', *, *, #71650, .T. ) ;
#68185=CARTESIAN_POINT ( 'NONE',  ( -33.42633708788835634, 315.2810023977556284, -7.024978449121026536 ) ) ;
#68200=DIRECTION ( 'NONE',  ( -0.02699252395738975518, -0.001721171576548164101, 0.9996341536876447442 ) ) ;
#68206=CARTESIAN_POINT ( 'NONE',  ( 32.42271565838718317, 438.8719799267125268, 23.74906467565527635 ) ) ;
#68217=AXIS2_PLACEMENT_3D ( 'NONE', #72377, #54052, #105283 ) ;
#68224=EDGE_CURVE ( 'NONE', #94742, #37271, #13682, .T. ) ;
#68227=CARTESIAN_POINT ( 'NONE',  ( 43.58619280597250167, 434.9882623928570524, 14.52865984557897860 ) ) ;
#68240=CARTESIAN_POINT ( 'NONE',  ( -41.86260695335467830, 487.3392455165196111, 9.527470086611755207 ) ) ;
#68251=CARTESIAN_POINT ( 'NONE',  ( 32.62730128615243785, 485.2399689022752796, 2.794144060394053497 ) ) ;
#68252=CARTESIAN_POINT ( 'NONE',  ( -32.42769167400230401, 299.9084148736556017, 3.070043388578370891 ) ) ;
#68257=CARTESIAN_POINT ( 'NONE',  ( -36.74062794522055952, 396.3876241540195906, 6.156540521676369337 ) ) ;
#68260=CARTESIAN_POINT ( 'NONE',  ( 22.26102485043540824, 295.0200461295465857, -1.964238772177369530 ) ) ;
#68262=CARTESIAN_POINT ( 'NONE',  ( 27.47093694407817210, 296.2799286419132727, -9.692114557244172701 ) ) ;
#68271=CARTESIAN_POINT ( 'NONE',  ( 34.37399270670962181, 318.9891659766902876, -6.087815582663091085 ) ) ;
#68272=CARTESIAN_POINT ( 'NONE',  ( 43.64002961914448520, 465.1123652286975698, 8.841020312837930106 ) ) ;
#68275=CARTESIAN_POINT ( 'NONE',  ( -17.08544069068336668, 304.5690947107618740, -10.06009145438460983 ) ) ;
#68276=CARTESIAN_POINT ( 'NONE',  ( 31.35125168101714976, 439.1949078441656980, 22.91632451326402631 ) ) ;
#68305=ORIENTED_EDGE ( 'NONE', *, *, #70058, .T. ) ;
#68313=CARTESIAN_POINT ( 'NONE',  ( -30.60088410313775853, 328.0742987498344405, 15.87722222682625173 ) ) ;
#68319=CARTESIAN_POINT ( 'NONE',  ( -32.07495350396642664, 464.7631673202369598, 11.47102835347554617 ) ) ;
#68320=ORIENTED_EDGE ( 'NONE', *, *, #70142, .F. ) ;
#68324=CARTESIAN_POINT ( 'NONE',  ( -30.61827153859606909, 339.8037943721997181, 17.27484252342313198 ) ) ;
#68326=VERTEX_POINT ( 'NONE', #34435 ) ;
#68332=CARTESIAN_POINT ( 'NONE',  ( 34.06798233701722012, 303.3571279571132209, 11.90485029882048806 ) ) ;
#68370=CARTESIAN_POINT ( 'NONE',  ( 35.44957237873525457, 490.5771127895677637, 12.28211989808393589 ) ) ;
#68385=AXIS2_PLACEMENT_3D ( 'NONE', #8673, #97674, #7076 ) ;
#68392=CARTESIAN_POINT ( 'NONE',  ( -35.81652876273700770, 437.2229768147630580, 4.496326601633259479 ) ) ;
#68401=CARTESIAN_POINT ( 'NONE',  ( 0.5742487732211798424, 294.8518027760915743, -10.00000000000000533 ) ) ;
#68405=ORIENTED_EDGE ( 'NONE', *, *, #17948, .F. ) ;
#68408=CARTESIAN_POINT ( 'NONE',  ( 25.40751943109334121, 308.2109744773123339, 10.71449383779814113 ) ) ;
#68418=CARTESIAN_POINT ( 'NONE',  ( -29.01988888469873018, 321.8047804620298393, 14.12772110426748284 ) ) ;
#68452=CIRCLE ( 'NONE', #94327, 8.000000000000005329 ) ;
#68456=CARTESIAN_POINT ( 'NONE',  ( -27.52310014629760815, 306.6583113186411538, -9.375678193793236304 ) ) ;
#68468=CARTESIAN_POINT ( 'NONE',  ( -32.64042345616925900, 439.6777095554002699, 24.07006591916626448 ) ) ;
#68470=CARTESIAN_POINT ( 'NONE',  ( -27.01428231532773339, 307.6193483853298289, -8.382184669494519014 ) ) ;
#68471=CARTESIAN_POINT ( 'NONE',  ( -27.27224646721448664, 307.4876125405418748, 11.01357167080802313 ) ) ;
#68473=CARTESIAN_POINT ( 'NONE',  ( -37.50059943756144776, 490.7879993827797307, 12.38039871356719246 ) ) ;
#68476=EDGE_CURVE ( 'NONE', #44795, #89572, #104835, .T. ) ;
#68489=DIRECTION ( 'NONE',  ( -1.224646799147353454E-16, 0.000000000000000000, -1.000000000000000000 ) ) ;
#68500=CARTESIAN_POINT ( 'NONE',  ( 5.433201317513493223, 294.7714280552164041, -8.410911388643073749 ) ) ;
#68529=CARTESIAN_POINT ( 'NONE',  ( 35.56416567323501710, 480.2820146177156175, -4.363888856302766683 ) ) ;
#68530=CARTESIAN_POINT ( 'NONE',  ( 40.86877072095135333, 461.0519673121681876, 2.323807444222599106 ) ) ;
#68535=ORIENTED_EDGE ( 'NONE', *, *, #45450, .T. ) ;
#68536=ORIENTED_EDGE ( 'NONE', *, *, #87301, .F. ) ;
#68556=ORIENTED_EDGE ( 'NONE', *, *, #96164, .T. ) ;
#68572=CARTESIAN_POINT ( 'NONE',  ( -25.95507789760542039, 309.1386286255022924, 10.94030088463808070 ) ) ;
#68573=CARTESIAN_POINT ( 'NONE',  ( 43.71297783477844234, 485.1278128289774827, -1.116606130290200172 ) ) ;
#68586=VERTEX_POINT ( 'NONE', #70358 ) ;
#68593=CARTESIAN_POINT ( 'NONE',  ( -21.52055329178771359, 305.1194042196812575, 8.994324108963519748 ) ) ;
#68611=CARTESIAN_POINT ( 'NONE',  ( -43.59756234217317683, 434.3244621007142996, 14.55946156040369921 ) ) ;
#68621=FACE_OUTER_BOUND ( 'NONE', #30009, .T. ) ;
#68625=CARTESIAN_POINT ( 'NONE',  ( -16.99886460162771584, 302.5644684816759309, -10.06107950202810031 ) ) ;
#68638=CARTESIAN_POINT ( 'NONE',  ( 42.73089261237365832, 435.7309723475635792, 18.11242468272457984 ) ) ;
#68644=AXIS2_PLACEMENT_3D ( 'NONE', #54888, #6331, #22578 ) ;
#68653=CARTESIAN_POINT ( 'NONE',  ( -33.85195725564122426, 465.2464970902066739, 17.18122764674262370 ) ) ;
#68657=CARTESIAN_POINT ( 'NONE',  ( 32.15507750052547919, 435.6575521615077378, 19.42892730969162685 ) ) ;
#68685=ORIENTED_EDGE ( 'NONE', *, *, #91617, .F. ) ;
#68694=CARTESIAN_POINT ( 'NONE',  ( 43.51084452654469459, 465.2903130129626561, 9.421687747985401984 ) ) ;
#68699=CARTESIAN_POINT ( 'NONE',  ( 33.71177684279670927, 320.6764605112623485, -5.903303350106816616 ) ) ;
#68705=CARTESIAN_POINT ( 'NONE',  ( 40.79885302903696243, 436.7553892629202323, 6.138960499418544714 ) ) ;
#68710=CARTESIAN_POINT ( 'NONE',  ( 43.38825400968193691, 436.1092026048715411, 18.83721859163726009 ) ) ;
#68719=CARTESIAN_POINT ( 'NONE',  ( -43.03265099499976998, 484.2747968070553952, -0.8099405866661972819 ) ) ;
#68721=CARTESIAN_POINT ( 'NONE',  ( 32.77384846114002670, 465.0024891621475831, 11.55799621383277476 ) ) ;
#68727=FACE_OUTER_BOUND ( 'NONE', #62022, .T. ) ;
#68738=CARTESIAN_POINT ( 'NONE',  ( -30.91631631796286328, 309.2558939697229334, -8.523808448843370300 ) ) ;
#68739=CARTESIAN_POINT ( 'NONE',  ( -13.58421898291219598, 304.5480222432819346, -10.06457054468338619 ) ) ;
#68743=CARTESIAN_POINT ( 'NONE',  ( -42.83167223030816473, 435.5834305853701949, 17.69761675601652584 ) ) ;
#68759=EDGE_CURVE ( 'NONE', #98535, #26380, #11810, .T. ) ;
#68780=EDGE_LOOP ( 'NONE', ( #71230, #39304, #95149, #3981 ) ) ;
#68787=CARTESIAN_POINT ( 'NONE',  ( 0.000000000000000000, 69.00000000000000000, 0.000000000000000000 ) ) ;
#68793=CARTESIAN_POINT ( 'NONE',  ( -43.00000000000002842, 461.4080316921935605, 3.462976341553847259 ) ) ;
#68796=CARTESIAN_POINT ( 'NONE',  ( 32.82691535583474973, 485.1045372766795367, 1.724905475515037701 ) ) ;
#68797=( BOUNDED_SURFACE ( )  B_SPLINE_SURFACE ( 3, 2, ( 
 ( #18836, #36089, #17745 ),
 ( #51144, #101316, #27465 ),
 ( #51681, #26929, #2062 ),
 ( #76489, #18289, #59802 ) ),
 .UNSPECIFIED., .F., .F., .F. ) 
 B_SPLINE_SURFACE_WITH_KNOTS ( ( 4, 4 ),
 ( 3, 3 ),
 ( -1.347446459964984911E-15, 0.0002182297367799811963 ),
 ( 0.000000000000000000, 1.000000000000000000 ),
 .UNSPECIFIED. ) 
 GEOMETRIC_REPRESENTATION_ITEM ( )  RATIONAL_B_SPLINE_SURFACE ( (
 ( 1.000000000000000000, 0.8274831119534725721, 1.000000000000000000),
 ( 1.000000000000000000, 0.8286506196641503230, 1.000000000000000000),
 ( 1.000000000000000000, 0.8297675374346515920, 1.000000000000000000),
 ( 1.000000000000000000, 0.8308329163124033023, 1.000000000000000000) ) ) 
 REPRESENTATION_ITEM ( '' )  SURFACE ( )  );
#68798=CARTESIAN_POINT ( 'NONE',  ( -25.05812948974611132, 295.6566298158938366, 2.109544210833623090 ) ) ;
#68807=CARTESIAN_POINT ( 'NONE',  ( 26.38526321989008139, 295.9613804530332004, -9.761259522514095011 ) ) ;
#68808=CARTESIAN_POINT ( 'NONE',  ( 35.74483125092430669, 413.6409941285803598, 6.029078300230034770 ) ) ;
#68812=ORIENTED_EDGE ( 'NONE', *, *, #29407, .T. ) ;
#68816=CARTESIAN_POINT ( 'NONE',  ( 44.28689199344569971, 335.5423528813348639, -0.1654540242942443840 ) ) ;
#68823=CARTESIAN_POINT ( 'NONE',  ( 31.43208348565381627, 438.4707862388070794, 22.17802677910626841 ) ) ;
#68857=CARTESIAN_POINT ( 'NONE',  ( -22.70225368124910759, 304.4484656627207073, 10.06577508047792691 ) ) ;
#68876=CARTESIAN_POINT ( 'NONE',  ( -32.93292175078001804, 485.0466323666404378, 1.209345195306022802 ) ) ;
#68877=CARTESIAN_POINT ( 'NONE',  ( 27.42231666649601962, 296.7076166580016547, 10.34122299797418698 ) ) ;
#68887=ORIENTED_EDGE ( 'NONE', *, *, #18813, .T. ) ;
#68891=CARTESIAN_POINT ( 'NONE',  ( -43.47770857297121694, 484.8227827122652229, 4.253339224812703101 ) ) ;
#68892=DIRECTION ( 'NONE',  ( 1.000000000000000000, -0.000000000000000000, -0.000000000000000000 ) ) ;
#68909=CIRCLE ( 'NONE', #46482, 15.00000000000001421 ) ;
#68916=CARTESIAN_POINT ( 'NONE',  ( 41.43589798968741889, 484.8608061051571667, -3.494608281236457614 ) ) ;
#68921=CARTESIAN_POINT ( 'NONE',  ( 40.02990647470488028, 485.1981161833907095, -4.348266463183992236 ) ) ;
#68930=VERTEX_POINT ( 'NONE', #52428 ) ;
#68932=CIRCLE ( 'NONE', #86187, 15.00000000000000711 ) ;
#68934=CARTESIAN_POINT ( 'NONE',  ( -43.52560603733947886, 486.7876375777498197, 7.034422870327485811 ) ) ;
#68945=CARTESIAN_POINT ( 'NONE',  ( 23.32412973071527773, 304.7201357075585406, 10.12579726553843962 ) ) ;
#68955=AXIS2_PLACEMENT_3D ( 'NONE', #29784, #6514, #80938 ) ;
#68966=ORIENTED_EDGE ( 'NONE', *, *, #25370, .F. ) ;
#68967=CARTESIAN_POINT ( 'NONE',  ( -7.697757149361867945, 296.0912719809052760, -10.02629731371196264 ) ) ;
#68989=ORIENTED_EDGE ( 'NONE', *, *, #54768, .F. ) ;
#68994=CARTESIAN_POINT ( 'NONE',  ( 40.24508711046470921, 341.7448991600085151, 21.01852089427141124 ) ) ;
#68998=CARTESIAN_POINT ( 'NONE',  ( -44.33427973454566029, 435.2106362794498295, 13.55537084937450665 ) ) ;
#69004=CIRCLE ( 'NONE', #103476, 2.999999999999999112 ) ;
#69005=CARTESIAN_POINT ( 'NONE',  ( -32.73339311437064936, 439.3386803523824824, 23.76693748282156804 ) ) ;
#69008=CARTESIAN_POINT ( 'NONE',  ( -37.78559634195402595, 315.0293482688398399, 14.83292048122523354 ) ) ;
#69016=ORIENTED_EDGE ( 'NONE', *, *, #77017, .F. ) ;
#69020=ORIENTED_EDGE ( 'NONE', *, *, #88394, .T. ) ;
#69025=CARTESIAN_POINT ( 'NONE',  ( 32.17646412119353272, 464.6980787822281513, 10.84896803613063021 ) ) ;
#69033=CARTESIAN_POINT ( 'NONE',  ( 33.52734911656129668, 435.4192553323662764, 9.514907176917411391 ) ) ;
#69036=CARTESIAN_POINT ( 'NONE',  ( 8.269522720448799546, 294.6925646269233994, -5.661848168216897292 ) ) ;
#69037=CARTESIAN_POINT ( 'NONE',  ( 44.43774958859658142, 337.2802145563449017, 0.2445019049555710311 ) ) ;
#69038=CARTESIAN_POINT ( 'NONE',  ( 36.02979557281435063, 304.0160159841871064, 0.1093096093688138148 ) ) ;
#69043=ORIENTED_EDGE ( 'NONE', *, *, #59820, .F. ) ;
#69055=CARTESIAN_POINT ( 'NONE',  ( 0.000000000000000000, 300.0000000000000000, 0.000000000000000000 ) ) ;
#69061=CARTESIAN_POINT ( 'NONE',  ( -9.819056950928635175, 294.6481068335448299, 1.893705519456528652 ) ) ;
#69067=CARTESIAN_POINT ( 'NONE',  ( -39.71213755904588538, 490.7526980994967403, 11.81179577511689516 ) ) ;
#69072=CARTESIAN_POINT ( 'NONE',  ( 33.80022934467060480, 484.1533297400391120, 1.810399503708082003 ) ) ;
#69081=CARTESIAN_POINT ( 'NONE',  ( 33.00000000000000000, 488.8442721620235716, 4.433647275927634190 ) ) ;
#69089=ORIENTED_EDGE ( 'NONE', *, *, #90940, .T. ) ;
#69092=ORIENTED_EDGE ( 'NONE', *, *, #96316, .T. ) ;
#69101=DIRECTION ( 'NONE',  ( -1.000000000000000000, -0.000000000000000000, -0.000000000000000000 ) ) ;
#69103=CARTESIAN_POINT ( 'NONE',  ( -29.45362385905110969, 325.9253963054578662, 15.14270878922920716 ) ) ;
#69117=DIRECTION ( 'NONE',  ( 0.000000000000000000, 0.000000000000000000, 1.000000000000000000 ) ) ;
#69118=CARTESIAN_POINT ( 'NONE',  ( 43.00000000000000000, 461.6622277975420729, 10.18145404766792161 ) ) ;
#69124=CARTESIAN_POINT ( 'NONE',  ( -20.09607536593551558, 304.8434239371439389, 8.935218438115660078 ) ) ;
#69125=CARTESIAN_POINT ( 'NONE',  ( 31.73457237641028073, 436.7287042522650609, 21.10271224642818666 ) ) ;
#69130=CARTESIAN_POINT ( 'NONE',  ( 34.53191791165118474, 437.2926915873509301, 5.227229271292882729 ) ) ;
#69137=CARTESIAN_POINT ( 'NONE',  ( 43.34934355818124629, 465.4850867214036612, 10.08239944467128346 ) ) ;
#69147=CARTESIAN_POINT ( 'NONE',  ( -32.22120753352774614, 464.6691781026585204, 10.60621122532632832 ) ) ;
#69148=VERTEX_POINT ( 'NONE', #48574 ) ;
#69162=CARTESIAN_POINT ( 'NONE',  ( -6.548324412163373687, 297.0730707799401102, 7.562729261318960283 ) ) ;
#69166=CARTESIAN_POINT ( 'NONE',  ( 43.66727438528342020, 435.6676895479272389, 17.39383282232698136 ) ) ;
#69169=CARTESIAN_POINT ( 'NONE',  ( 16.15440707770680007, 294.5642616619309138, -10.06111921690162880 ) ) ;
#69172=EDGE_LOOP ( 'NONE', ( #66246, #62775, #11243, #24488 ) ) ;
#69175=CARTESIAN_POINT ( 'NONE',  ( -36.24853743861725519, 490.9518012583203586, 12.45319371584819379 ) ) ;
#69176=CIRCLE ( 'NONE', #100182, 1.000000000000002442 ) ;
#69181=CARTESIAN_POINT ( 'NONE',  ( 34.84533103728120551, 490.9263297235970072, 11.68229585404477611 ) ) ;
#69193=CARTESIAN_POINT ( 'NONE',  ( -45.29905483860081716, 480.9466865490944656, -2.171671249451534003 ) ) ;
#69198=EDGE_CURVE ( 'NONE', #34395, #8292, #41161, .T. ) ;
#69210=EDGE_CURVE ( 'NONE', #9645, #15128, #80330, .T. ) ;
#69214=ORIENTED_EDGE ( 'NONE', *, *, #9585, .T. ) ;
#69218=VERTEX_POINT ( 'NONE', #23826 ) ;
#69222=ORIENTED_EDGE ( 'NONE', *, *, #28720, .F. ) ;
#69236=CARTESIAN_POINT ( 'NONE',  ( 37.85084083633365282, 438.0234350436313093, 4.171260309356221718 ) ) ;
#69238=FACE_OUTER_BOUND ( 'NONE', #91263, .T. ) ;
#69242=CARTESIAN_POINT ( 'NONE',  ( 34.04714008975750517, 484.1152113529149688, 1.016147467615621247 ) ) ;
#69244=CARTESIAN_POINT ( 'NONE',  ( -20.52350613252515643, 304.8999024697870937, 9.947223320822450532 ) ) ;
#69246=CARTESIAN_POINT ( 'NONE',  ( -44.12472801210822837, 485.7238370326490440, 3.975897585127424527 ) ) ;
#69249=CARTESIAN_POINT ( 'NONE',  ( 32.81992448453848965, 465.7192846569214453, 11.17271167765358442 ) ) ;
#69253=B_SPLINE_CURVE_WITH_KNOTS ( 'NONE', 3,
 ( #688, #29182, #10408, #76204 ),
 .UNSPECIFIED., .F., .F.,
 ( 4, 4 ),
 ( 0.000000000000000000, 0.002502641776602361305 ),
 .UNSPECIFIED. ) ;
#69255=VECTOR ( 'NONE', #35201, 1000.000000000000000 ) ;
#69257=CARTESIAN_POINT ( 'NONE',  ( -35.68159617069628098, 373.6642197484802068, 4.177052563641423077 ) ) ;
#69273=EDGE_LOOP ( 'NONE', ( #4999, #1642, #28498, #85600, #6292 ) ) ;
#69297=CARTESIAN_POINT ( 'NONE',  ( -43.84752573847097068, 486.0721194390189339, 5.282948175116183975 ) ) ;
#69302=CARTESIAN_POINT ( 'NONE',  ( 32.94352307844687289, 463.6326549538520112, 6.941370215393830811 ) ) ;
#69309=VERTEX_POINT ( 'NONE', #31212 ) ;
#69314=CARTESIAN_POINT ( 'NONE',  ( 43.00000000000000000, 438.3878896346935790, 16.22878885428537998 ) ) ;
#69328=EDGE_CURVE ( 'NONE', #72766, #27223, #66212, .T. ) ;
#69329=CARTESIAN_POINT ( 'NONE',  ( -34.01929857393211165, 322.4300229039442911, -5.462111840924722905 ) ) ;
#69335=CARTESIAN_POINT ( 'NONE',  ( 23.79019632451556276, 303.5314421105786096, -9.853825711238384244 ) ) ;
#69336=CARTESIAN_POINT ( 'NONE',  ( 45.29905483860081716, 480.9466865490944656, -2.171671249451534003 ) ) ;
#69338=DIRECTION ( 'NONE',  ( 0.1270361284032138216, -0.9918980905719710917, 0.000000000000000000 ) ) ;
#69348=CARTESIAN_POINT ( 'NONE',  ( 33.54469842372052568, 315.6888517999274200, -6.922094226970141762 ) ) ;
#69349=CARTESIAN_POINT ( 'NONE',  ( 34.78087288526246823, 461.0373983564574019, 3.662433947940674450 ) ) ;
#69351=CARTESIAN_POINT ( 'NONE',  ( -13.82057366821712030, 304.5462546222179299, 9.872053150317878334 ) ) ;
#69352=CARTESIAN_POINT ( 'NONE',  ( 31.41965566404186205, 438.8991828050834556, 23.11713475969801124 ) ) ;
#69382=DIRECTION ( 'NONE',  ( 0.000000000000000000, -0.1323839925376434634, -0.9911985061125713203 ) ) ;
#69385=VERTEX_POINT ( 'NONE', #22043 ) ;
#69389=CARTESIAN_POINT ( 'NONE',  ( 33.00000000000000000, 500.0000000000002274, 0.000000000000000000 ) ) ;
#69390=CARTESIAN_POINT ( 'NONE',  ( -31.33040145750029382, 438.2830743389437771, 22.63980905922802123 ) ) ;
#69400=CARTESIAN_POINT ( 'NONE',  ( 25.23000825560996319, 295.8049451023007350, 10.14223174299324448 ) ) ;
#69418=CARTESIAN_POINT ( 'NONE',  ( 8.813324044470940422, 294.6780646607570020, 9.900070198401328625 ) ) ;
#69429=CARTESIAN_POINT ( 'NONE',  ( 34.47678062874018678, 437.1474145881098821, 5.468662283308735717 ) ) ;
#69431=AXIS2_PLACEMENT_3D ( 'NONE', #57942, #34785, #213 ) ;
#69441=CARTESIAN_POINT ( 'NONE',  ( -42.61340452791766609, 486.8925439250689351, 7.464118458850250271 ) ) ;
#69447=CARTESIAN_POINT ( 'NONE',  ( 40.50232667759422611, 485.1162572728860596, -4.198421296053016505 ) ) ;
#69455=CARTESIAN_POINT ( 'NONE',  ( 46.00000000000000000, 450.0000000000002274, 13.20242257375370976 ) ) ;
#69461=AXIS2_PLACEMENT_3D ( 'NONE', #11164, #59753, #45168 ) ;
#69468=CARTESIAN_POINT ( 'NONE',  ( 25.25836143086297625, 306.2355318565109883, 10.47456800221746676 ) ) ;
#69492=EDGE_LOOP ( 'NONE', ( #102155, #46595, #47670, #39996 ) ) ;
#69501=ORIENTED_EDGE ( 'NONE', *, *, #18813, .F. ) ;
#69504=ORIENTED_EDGE ( 'NONE', *, *, #29619, .F. ) ;
#69505=EDGE_LOOP ( 'NONE', ( #1943, #75010, #37142, #48507 ) ) ;
#69514=DIRECTION ( 'NONE',  ( -0.2282686145773573927, 0.2753452451907626997, 0.9338513990725574310 ) ) ;
#69521=CARTESIAN_POINT ( 'NONE',  ( -43.79821706558210082, 434.9662578767425885, 12.22743114680390342 ) ) ;
#69531=CARTESIAN_POINT ( 'NONE',  ( -36.56941799720385688, 309.7424336998361696, 13.49796762285306073 ) ) ;
#69536=CARTESIAN_POINT ( 'NONE',  ( 38.88461863710599431, 437.7975295993173290, 4.475058894670842058 ) ) ;
#69558=CARTESIAN_POINT ( 'NONE',  ( -1.435124379509183671E-09, 294.8518027762758038, -10.00000000000000178 ) ) ;
#69564=CARTESIAN_POINT ( 'NONE',  ( 0.000000000000000000, 294.8518027762758038, -10.00000000000000178 ) ) ;
#69588=CARTESIAN_POINT ( 'NONE',  ( 33.00000000000000000, 500.0000000000002274, 0.000000000000000000 ) ) ;
#69595=ORIENTED_EDGE ( 'NONE', *, *, #36116, .T. ) ;
#69599=CARTESIAN_POINT ( 'NONE',  ( 9.970195021754669540, 302.6460196488382053, -10.04373974541433689 ) ) ;
#69611=VERTEX_POINT ( 'NONE', #78063 ) ;
#69619=ORIENTED_EDGE ( 'NONE', *, *, #30046, .T. ) ;
#69628=CARTESIAN_POINT ( 'NONE',  ( -40.77380256327629837, 468.8478597483947965, 21.13608272249925690 ) ) ;
#69635=CARTESIAN_POINT ( 'NONE',  ( -32.76481181362981943, 487.6128877198520399, 8.618969267356323627 ) ) ;
#69639=ORIENTED_EDGE ( 'NONE', *, *, #6649, .F. ) ;
#69647=CIRCLE ( 'NONE', #100662, 12.00000000000000711 ) ;
#69660=CARTESIAN_POINT ( 'NONE',  ( 39.42238789698090784, 436.7568662985880792, 5.264481638451717238 ) ) ;
#69663=CARTESIAN_POINT ( 'NONE',  ( -43.02621584241282449, 434.6128289108255558, 16.97888786059002086 ) ) ;
#69669=CARTESIAN_POINT ( 'NONE',  ( -32.89392925374600907, 485.8745504891352311, 5.316642333917223517 ) ) ;
#69681=CARTESIAN_POINT ( 'NONE',  ( 6.123233995736766282E-16, 0.000000000000000000, -5.000000000000000000 ) ) ;
#69697=CARTESIAN_POINT ( 'NONE',  ( -35.15980092189356299, 490.3457513104292502, 12.17002836721590953 ) ) ;
#69702=CARTESIAN_POINT ( 'NONE',  ( 37.52433673132330938, 473.0012850594927727, 17.54962685244640141 ) ) ;
#69716=( BOUNDED_SURFACE ( )  B_SPLINE_SURFACE ( 3, 2, ( 
 ( #8853, #8323, #91390 ),
 ( #67108, #41227, #81662 ),
 ( #99449, #24551, #66036 ),
 ( #25624, #7256, #90851 ),
 ( #50369, #75173, #48770 ),
 ( #16969, #40166, #73040 ),
 ( #32095, #64975, #49845 ),
 ( #7785, #106481, #65511 ),
 ( #74644, #9369, #83280 ),
 ( #42285, #28276, #44973 ),
 ( #2882, #36900, #92424 ),
 ( #52499, #43362, #28819 ) ),
 .UNSPECIFIED., .F., .F., .T. ) 
 B_SPLINE_SURFACE_WITH_KNOTS ( ( 4, 2, 2, 2, 2, 4 ),
 ( 3, 3 ),
 ( 0.01002139624728706942, 0.01516190422318156386, 0.01580446772016837892, 0.01644703121715519051, 0.01773215821112881369, 0.02030241219907606004 ),
 ( 0.000000000000000000, 1.000000000000000000 ),
 .UNSPECIFIED. ) 
 GEOMETRIC_REPRESENTATION_ITEM ( )  RATIONAL_B_SPLINE_SURFACE ( (
 ( 1.000000000000000000, 0.7071066567438631933, 1.000000000000000000),
 ( 1.000000000000000000, 0.7071033631374191719, 1.000000000000000000),
 ( 1.000000000000000000, 0.7071056790687298976, 1.000000000000000000),
 ( 1.000000000000000000, 0.7071068249174177200, 1.000000000000000000),
 ( 1.000000000000000000, 0.7071068699167430971, 1.000000000000000000),
 ( 1.000000000000000000, 0.7071037064177418952, 1.000000000000000000),
 ( 1.000000000000000000, 0.7071011095179403627, 1.000000000000000000),
 ( 1.000000000000000000, 0.7070931123324023515, 1.000000000000000000),
 ( 1.000000000000000000, 0.7070878456073813600, 1.000000000000000000),
 ( 1.000000000000000000, 0.7070844322698651707, 1.000000000000000000),
 ( 1.000000000000000000, 0.7071028863112219787, 1.000000000000000000),
 ( 1.000000000000000000, 0.7071067811865477948, 1.000000000000000000) ) ) 
 REPRESENTATION_ITEM ( '' )  SURFACE ( )  );
#69728=ADVANCED_FACE ( 'NONE', ( #38682 ), #88308, .F. ) ;
#69744=CARTESIAN_POINT ( 'NONE',  ( -38.63430842791193243, 485.8001267274091219, -4.834053598480790193 ) ) ;
#69746=CARTESIAN_POINT ( 'NONE',  ( 21.85376215082057882, 304.0607632025936482, -9.955599711602641122 ) ) ;
#69752=CARTESIAN_POINT ( 'NONE',  ( 41.20010578034612081, 436.9751675121710832, 5.754626909168208293 ) ) ;
#69760=ORIENTED_EDGE ( 'NONE', *, *, #31519, .F. ) ;
#69761=B_SPLINE_CURVE_WITH_KNOTS ( 'NONE', 3,
 ( #79414, #30357, #56715, #9228 ),
 .UNSPECIFIED., .F., .F.,
 ( 4, 4 ),
 ( 0.000000000000000000, 0.001949579373386174088 ),
 .UNSPECIFIED. ) ;
#69765=FACE_OUTER_BOUND ( 'NONE', #1971, .T. ) ;
#69767=CARTESIAN_POINT ( 'NONE',  ( -43.68566140668959008, 485.0560336449534589, 1.938913452014765282 ) ) ;
#69777=FACE_OUTER_BOUND ( 'NONE', #5250, .T. ) ;
#69791=CARTESIAN_POINT ( 'NONE',  ( 32.86203668624279572, 471.3274586220275069, 9.717589530844561452 ) ) ;
#69794=DIRECTION ( 'NONE',  ( -0.9639005798656382629, -0.1664520902833319382, -0.2078205326116645268 ) ) ;
#69800=VECTOR ( 'NONE', #74571, 1000.000000000000000 ) ;
#69813=CARTESIAN_POINT ( 'NONE',  ( -43.74985542820371620, 435.5770091380364306, 16.96136490515579354 ) ) ;
#69836=AXIS2_PLACEMENT_3D ( 'NONE', #51440, #59019, #67644 ) ;
#69843=CARTESIAN_POINT ( 'NONE',  ( 35.52727618412238542, 408.9004372220593950, 7.035618409970155973 ) ) ;
#69851=CARTESIAN_POINT ( 'NONE',  ( 37.62595466100172814, 491.2446780561967330, 12.18850516984547561 ) ) ;
#69855=CARTESIAN_POINT ( 'NONE',  ( 26.06898045364747318, 295.8628383591220086, -9.782693099516677648 ) ) ;
#69868=CARTESIAN_POINT ( 'NONE',  ( 35.78055020979645207, 327.7515353362224459, -3.901225659782328492 ) ) ;
#69871=CARTESIAN_POINT ( 'NONE',  ( -12.08334041755991706, 304.5866437775407007, -10.05636128505472549 ) ) ;
#69872=CARTESIAN_POINT ( 'NONE',  ( 30.98507422220691154, 439.0250405275747880, 22.25274580565829297 ) ) ;
#69874=ORIENTED_EDGE ( 'NONE', *, *, #62426, .F. ) ;
#69875=VECTOR ( 'NONE', #87867, 1000.000000000000000 ) ;
#69893=CARTESIAN_POINT ( 'NONE',  ( -43.70836520789971757, 463.8610993545743213, 7.295416580046127031 ) ) ;
#69894=CARTESIAN_POINT ( 'NONE',  ( -33.21599328327232570, 465.5375697722676023, 9.463303254740058179 ) ) ;
#69912=CARTESIAN_POINT ( 'NONE',  ( -45.42662042998529159, 432.5755707651378543, 6.977826016421777133 ) ) ;
#69916=ORIENTED_EDGE ( 'NONE', *, *, #65158, .F. ) ;
#69921=DIRECTION ( 'NONE',  ( 0.000000000000000000, 0.000000000000000000, 1.000000000000000000 ) ) ;
#69924=CARTESIAN_POINT ( 'NONE',  ( 22.21815059361560074, 303.2497477512824275, 10.02249569361740988 ) ) ;
#69927=CARTESIAN_POINT ( 'NONE',  ( 4.690999466534710116, 301.0267511969297516, -10.01286717245164937 ) ) ;
#69932=CARTESIAN_POINT ( 'NONE',  ( -40.30492368078586196, 437.3365155501883805, 5.155601643837083969 ) ) ;
#69953=CARTESIAN_POINT ( 'NONE',  ( 33.97359119245064818, 434.1099241184708148, 11.80501937577158600 ) ) ;
#69956=DIRECTION ( 'NONE',  ( -0.000000000000000000, -1.000000000000000000, -0.000000000000000000 ) ) ;
#69972=VERTEX_POINT ( 'NONE', #75808 ) ;
#69986=ORIENTED_EDGE ( 'NONE', *, *, #32601, .F. ) ;
#69991=CARTESIAN_POINT ( 'NONE',  ( 27.85356646027182492, 315.4045181579393784, 12.51841259425152053 ) ) ;
#69992=ADVANCED_FACE ( 'NONE', ( #28360 ), #34857, .T. ) ;
#70016=ORIENTED_EDGE ( 'NONE', *, *, #46973, .F. ) ;
#70029=CARTESIAN_POINT ( 'NONE',  ( -46.00000000000000711, 460.1225022309920973, 6.748346813975271807 ) ) ;
#70039=CARTESIAN_POINT ( 'NONE',  ( 41.92130353534008691, 485.3101580674378397, -3.082360575775040523 ) ) ;
#70042=CARTESIAN_POINT ( 'NONE',  ( -38.73386039799279246, 460.3889633641963997, 2.371405894922581581 ) ) ;
#70049=EDGE_LOOP ( 'NONE', ( #23584, #104081, #57140, #100817 ) ) ;
#70050=CARTESIAN_POINT ( 'NONE',  ( -31.37855721874207404, 315.8766196183444777, -6.353910099583705673 ) ) ;
#70051=CARTESIAN_POINT ( 'NONE',  ( -29.06740789737446207, 312.1932710927672474, 12.18869810040496660 ) ) ;
#70055=CIRCLE ( 'NONE', #1097, 12.00000000000000711 ) ;
#70058=EDGE_CURVE ( 'NONE', #73133, #12603, #39636, .T. ) ;
#70072=EDGE_CURVE ( 'NONE', #26193, #20727, #87830, .T. ) ;
#70081=CARTESIAN_POINT ( 'NONE',  ( 4.691302026839834660, 301.0269659576850358, -10.01286862727946314 ) ) ;
#70082=CARTESIAN_POINT ( 'NONE',  ( 40.73878143178837519, 486.4834083601638213, 16.46716573231486436 ) ) ;
#70095=CARTESIAN_POINT ( 'NONE',  ( -43.84720509323437199, 462.5482003534952469, 5.191543507852187211 ) ) ;
#70096=CARTESIAN_POINT ( 'NONE',  ( -44.48219397478413839, 478.0055753222136445, 1.937693161207713510 ) ) ;
#70106=CARTESIAN_POINT ( 'NONE',  ( 13.61490394126797554, 294.5438152624074064, 1.871499044962292801 ) ) ;
#70108=CARTESIAN_POINT ( 'NONE',  ( 43.00000000000000000, 487.1237704758250402, 9.497510897111922645 ) ) ;
#70115=ORIENTED_EDGE ( 'NONE', *, *, #75133, .F. ) ;
#70117=EDGE_CURVE ( 'NONE', #13401, #72871, #32813, .T. ) ;
#70142=EDGE_CURVE ( 'NONE', #58214, #30899, #17226, .T. ) ;
#70169=CARTESIAN_POINT ( 'NONE',  ( -32.52877124674115805, 435.6736143190897792, 17.82210992056645438 ) ) ;
#70173=EDGE_CURVE ( 'NONE', #104952, #64595, #90666, .T. ) ;
#70191=CARTESIAN_POINT ( 'NONE',  ( -44.25901894362515065, 463.6537623376428314, 7.444378749523244743 ) ) ;
#70195=CARTESIAN_POINT ( 'NONE',  ( -33.79347250503700906, 316.5797005500412524, -6.697218333849672689 ) ) ;
#70205=CARTESIAN_POINT ( 'NONE',  ( -9.384414461224938719, 294.8111600184428767, 3.468918321496474721 ) ) ;
#70214=CARTESIAN_POINT ( 'NONE',  ( 46.00000000000000000, 438.2046082539382610, 15.52554165154988475 ) ) ;
#70220=CARTESIAN_POINT ( 'NONE',  ( -36.50247448621189506, 490.9911319642687317, 12.47041065747709965 ) ) ;
#70264=CARTESIAN_POINT ( 'NONE',  ( -32.85155332502863246, 463.8111683108725174, 7.359358840565855431 ) ) ;
#70272=VERTEX_POINT ( 'NONE', #96784 ) ;
#70274=CARTESIAN_POINT ( 'NONE',  ( -39.30650688511865809, 485.8522658471748628, -4.984147873724826816 ) ) ;
#70276=DIRECTION ( 'NONE',  ( 0.000000000000000000, 0.000000000000000000, -1.000000000000000000 ) ) ;
#70285=CARTESIAN_POINT ( 'NONE',  ( 1.044083592157493498E-15, 70.00000000000000000, 7.025805963803935406 ) ) ;
#70290=CIRCLE ( 'NONE', #37610, 1.000000000000009104 ) ;
#70302=CARTESIAN_POINT ( 'NONE',  ( -42.34430797738168195, 436.4403912042762954, 6.776599765004717391 ) ) ;
#70334=ADVANCED_FACE ( 'NONE', ( #54698 ), #51689, .T. ) ;
#70346=CARTESIAN_POINT ( 'NONE',  ( -43.71503333927389434, 486.3083204931239152, 5.911991965207118227 ) ) ;
#70358=CARTESIAN_POINT ( 'NONE',  ( 43.55333112596303380, 465.2342844084865874, 9.238213423009675296 ) ) ;
#70359=EDGE_CURVE ( 'NONE', #36055, #62753, #22309, .T. ) ;
#70366=B_SPLINE_CURVE_WITH_KNOTS ( 'NONE', 3,
 ( #67419, #90086, #106250, #73894 ),
 .UNSPECIFIED., .F., .F.,
 ( 4, 4 ),
 ( 0.000000000000000000, 0.003511374632867239783 ),
 .UNSPECIFIED. ) ;
#70376=CARTESIAN_POINT ( 'NONE',  ( 36.71487963708168678, 414.8037251387460742, 6.149495645048446590 ) ) ;
#70379=CARTESIAN_POINT ( 'NONE',  ( 36.66272501222901781, 491.8430924522251075, 12.58828741394580497 ) ) ;
#70381=CARTESIAN_POINT ( 'NONE',  ( -20.84783826651100114, 303.9031953955430367, -9.989077431537761953 ) ) ;
#70392=AXIS2_PLACEMENT_3D ( 'NONE', #75234, #100051, #36436 ) ;
#70401=CARTESIAN_POINT ( 'NONE',  ( 44.56450693767920512, 340.0210625335878376, 0.8280807651409033410 ) ) ;
#70405=CARTESIAN_POINT ( 'NONE',  ( -18.69420657816679210, 304.6310092840336097, -10.04693110555010982 ) ) ;
#70413=B_SPLINE_CURVE_WITH_KNOTS ( 'NONE', 3,
 ( #26400, #2060, #92138, #41466 ),
 .UNSPECIFIED., .F., .F.,
 ( 4, 4 ),
 ( 0.0005604261988817112747, 0.02562827970630954244 ),
 .UNSPECIFIED. ) ;
#70416=EDGE_CURVE ( 'NONE', #27128, #79201, #55069, .T. ) ;
#70424=EDGE_CURVE ( 'NONE', #64595, #6722, #98192, .T. ) ;
#70425=ORIENTED_EDGE ( 'NONE', *, *, #6649, .T. ) ;
#70458=CARTESIAN_POINT ( 'NONE',  ( 28.24208341650309961, 297.1533231554286090, 10.44100024085842904 ) ) ;
#70471=CARTESIAN_POINT ( 'NONE',  ( 42.90606796463281825, 465.0680163536576401, 12.12009592768376898 ) ) ;
#70476=CARTESIAN_POINT ( 'NONE',  ( -40.73953790046563483, -18.92596047533412573, 20.36976895023282452 ) ) ;
#70483=CARTESIAN_POINT ( 'NONE',  ( -43.71297783477847787, 485.1278128289774827, -1.116606130290708876 ) ) ;
#70485=DIRECTION ( 'NONE',  ( 0.000000000000000000, 0.000000000000000000, -1.000000000000000000 ) ) ;
#70505=CARTESIAN_POINT ( 'NONE',  ( 41.32135724059154569, 485.4908763545889201, -3.838542627836866394 ) ) ;
#70509=CARTESIAN_POINT ( 'NONE',  ( -42.77491504005183032, 436.8063544398164595, 20.35369978044113992 ) ) ;
#70515=CARTESIAN_POINT ( 'NONE',  ( -32.16694665535142406, 298.7751107022914425, -9.134474995493537364 ) ) ;
#70525=ORIENTED_EDGE ( 'NONE', *, *, #29407, .F. ) ;
#70532=B_SPLINE_CURVE_WITH_KNOTS ( 'NONE', 3,
 ( #68053, #101493, #99888, #3324 ),
 .UNSPECIFIED., .F., .F.,
 ( 4, 4 ),
 ( 9.813077866773594792E-18, 0.001950293525757634773 ),
 .UNSPECIFIED. ) ;
#70535=CARTESIAN_POINT ( 'NONE',  ( 43.40712426123182865, 434.3590067275469551, 15.37327885490085499 ) ) ;
#70560=EDGE_CURVE ( 'NONE', #48477, #49781, #5653, .T. ) ;
#70575=VERTEX_POINT ( 'NONE', #46888 ) ;
#70581=CARTESIAN_POINT ( 'NONE',  ( 42.70315986187589630, 433.3238984461618770, 18.58428708097476445 ) ) ;
#70584=CARTESIAN_POINT ( 'NONE',  ( -42.29287336469099046, 486.6964296286192280, 8.722237745847708723 ) ) ;
#70587=DIRECTION ( 'NONE',  ( 0.1946996363168976285, 0.08778327892717602277, 0.9769268895669018793 ) ) ;
#70589=CARTESIAN_POINT ( 'NONE',  ( -20.59205717438620553, 304.8780392497436651, -8.994432684286490343 ) ) ;
#70590=CARTESIAN_POINT ( 'NONE',  ( -36.33898061045209715, 308.9542109619496841, 13.29915945452285442 ) ) ;
#70601=EDGE_LOOP ( 'NONE', ( #18292, #16346, #21632, #94965, #54431, #41238 ) ) ;
#70616=CARTESIAN_POINT ( 'NONE',  ( 9.720388148916125459, 294.7585724938356293, -10.04291177961258974 ) ) ;
#70618=CARTESIAN_POINT ( 'NONE',  ( 42.97989905721253479, 343.7189603545139676, 9.566017304031658952 ) ) ;
#70639=CARTESIAN_POINT ( 'NONE',  ( 30.00000000000000000, 488.7759337287082531, 4.253621113605315252 ) ) ;
#70643=AXIS2_PLACEMENT_3D ( 'NONE', #95198, #21858, #54167 ) ;
#70647=ORIENTED_EDGE ( 'NONE', *, *, #12563, .F. ) ;
#70653=CARTESIAN_POINT ( 'NONE',  ( -31.88312667699394609, 463.8062602911185195, 15.68962056581293041 ) ) ;
#70660=CARTESIAN_POINT ( 'NONE',  ( 46.00000000000000000, 500.0000000000002274, 0.000000000000000000 ) ) ;
#70664=EDGE_CURVE ( 'NONE', #78629, #34141, #28827, .T. ) ;
#70676=CARTESIAN_POINT ( 'NONE',  ( 34.95237279327285762, 304.8277712208536627, 12.26231981495593537 ) ) ;
#70680=CARTESIAN_POINT ( 'NONE',  ( -27.18908553330205180, 296.5274986157688772, 10.30015177545897842 ) ) ;
#70681=( BOUNDED_SURFACE ( )  B_SPLINE_SURFACE ( 3, 2, ( 
 ( #96044, #14035, #64217 ),
 ( #104113, #4909, #37840 ),
 ( #23230, #21647, #104649 ),
 ( #103075, #80900, #80363 ) ),
 .UNSPECIFIED., .F., .F., .F. ) 
 B_SPLINE_SURFACE_WITH_KNOTS ( ( 4, 4 ),
 ( 3, 3 ),
 ( 0.01376892490370208375, 0.01435419950459561333 ),
 ( 0.000000000000000000, 0.8308924645139164067 ),
 .UNSPECIFIED. ) 
 GEOMETRIC_REPRESENTATION_ITEM ( )  RATIONAL_B_SPLINE_SURFACE ( (
 ( 1.000000000000000000, 0.7566372315800875548, 0.9176910440068761776),
 ( 1.000000000000000000, 0.7618160164815166446, 0.9194425871098625969),
 ( 1.000000000000000000, 0.7669224193548869195, 0.9211696495200920598),
 ( 1.000000000000000000, 0.7719586918116361218, 0.9228729927664867105) ) ) 
 REPRESENTATION_ITEM ( '' )  SURFACE ( )  );
#70682=ADVANCED_FACE ( 'NONE', ( #54429 ), #94628, .T. ) ;
#70685=CARTESIAN_POINT ( 'NONE',  ( -33.81613602126189022, 485.0484310908490784, 1.468412048120518509 ) ) ;
#70702=CARTESIAN_POINT ( 'NONE',  ( -31.55677019160819796, 436.6743556880023789, 19.26287365877006152 ) ) ;
#70703=CARTESIAN_POINT ( 'NONE',  ( -32.04888029241991632, 435.5715400069649945, 16.73152881174828366 ) ) ;
#70709=CARTESIAN_POINT ( 'NONE',  ( -33.89998135744182406, 300.3151453263810140, -8.778418284323066700 ) ) ;
#70726=EDGE_LOOP ( 'NONE', ( #78944, #96818, #102466, #38287 ) ) ;
#70727=CARTESIAN_POINT ( 'NONE',  ( -35.93449038250053462, 329.4584288211232774, -3.491322705308419483 ) ) ;
#70738=DIRECTION ( 'NONE',  ( 0.000000000000000000, -0.8784936690177097551, 0.4777539884666615055 ) ) ;
#70747=CARTESIAN_POINT ( 'NONE',  ( 43.43869229197127169, 464.9661605157749591, 13.42065392471465834 ) ) ;
#70749=B_SPLINE_CURVE_WITH_KNOTS ( 'NONE', 3,
 ( #100231, #58730, #26398, #91629 ),
 .UNSPECIFIED., .F., .F.,
 ( 4, 4 ),
 ( 1.886626427905286316E-16, 0.002002602941640114435 ),
 .UNSPECIFIED. ) ;
#70766=CARTESIAN_POINT ( 'NONE',  ( 43.18779636046989623, 464.9503604947623217, 14.53715779820238829 ) ) ;
#70794=CARTESIAN_POINT ( 'NONE',  ( 32.86259851300461321, 485.9239370913662697, 5.440925357812796292 ) ) ;
#70799=CARTESIAN_POINT ( 'NONE',  ( -41.28039629891594586, 485.7122505962499872, -4.568292046899058434 ) ) ;
#70804=ADVANCED_FACE ( 'NONE', ( #62440 ), #55207, .F. ) ;
#70811=CARTESIAN_POINT ( 'NONE',  ( 28.32844991613795926, 306.0388488792111161, -9.289596639994890381 ) ) ;
#70813=ORIENTED_EDGE ( 'NONE', *, *, #60908, .F. ) ;
#70817=TOROIDAL_SURFACE ( 'NONE', #161, 12.00000000000001066, 3.000000000000000000 ) ;
#70834=DIRECTION ( 'NONE',  ( -0.4804656623127168125, 0.6318279369468263740, 0.6082320325598773447 ) ) ;
#70852=EDGE_CURVE ( 'NONE', #73133, #27254, #17131, .T. ) ;
#70870=CIRCLE ( 'NONE', #27803, 2.999999999999998668 ) ;
#70877=ORIENTED_EDGE ( 'NONE', *, *, #90048, .F. ) ;
#70901=CARTESIAN_POINT ( 'NONE',  ( 35.48039044674744247, 426.6879373334400043, 6.207493775911908429 ) ) ;
#70907=CARTESIAN_POINT ( 'NONE',  ( 41.86630687591735267, 487.3337178530820211, 9.520545777472943172 ) ) ;
#70921=CARTESIAN_POINT ( 'NONE',  ( 36.07326600438810260, 304.1116406225798983, 0.1331827052438417924 ) ) ;
#70930=CIRCLE ( 'NONE', #5483, 5.000000000000000000 ) ;
#70936=CARTESIAN_POINT ( 'NONE',  ( -37.88504238421052861, 463.4171042825119002, 19.90923349044181379 ) ) ;
#70949=CARTESIAN_POINT ( 'NONE',  ( -43.72375837489616401, 464.7599263999740060, 7.850687543227762077 ) ) ;
#70950=CARTESIAN_POINT ( 'NONE',  ( -33.77559172535808329, 464.7834715296605737, 7.192701217093241617 ) ) ;
#70960=EDGE_CURVE ( 'NONE', #75683, #45384, #44001, .T. ) ;
#70961=CIRCLE ( 'NONE', #38268, 2.999999999999974687 ) ;
#70968=CARTESIAN_POINT ( 'NONE',  ( 34.12349128637390550, 490.8027302422246407, 11.84948222508928062 ) ) ;
#70971=ORIENTED_EDGE ( 'NONE', *, *, #56964, .F. ) ;
#70981=ORIENTED_EDGE ( 'NONE', *, *, #89847, .T. ) ;
#70982=CARTESIAN_POINT ( 'NONE',  ( 41.59783515517239039, 465.5823253716133081, 15.80626774175417104 ) ) ;
#70985=( BOUNDED_SURFACE ( )  B_SPLINE_SURFACE ( 3, 2, ( 
 ( #1205, #44362, #34709 ),
 ( #50832, #83736, #75108 ),
 ( #92363, #59494, #60042 ),
 ( #84287, #42761, #19067 ),
 ( #68657, #101536, #36316 ),
 ( #92900, #75651, #102056 ),
 ( #68096, #28217, #1753 ),
 ( #27689, #93455, #100462 ),
 ( #19603, #18512, #10381 ),
 ( #60567, #77260, #3373 ),
 ( #43298, #27153, #67583 ),
 ( #61087, #17447, #76181 ),
 ( #26622, #83217, #9312 ),
 ( #42222, #34173, #26104 ) ),
 .UNSPECIFIED., .F., .F., .F. ) 
 B_SPLINE_SURFACE_WITH_KNOTS ( ( 4, 2, 2, 2, 2, 2, 4 ),
 ( 3, 3 ),
 ( 6.166074595359560817E-15, 0.003029187982864252251, 0.004543781974293295556, 0.006058375965722338427, 0.007572969957151381298, 0.009087563948580424170, 0.01211675193143850991 ),
 ( 0.000000000000000000, 1.000000000000000000 ),
 .UNSPECIFIED. ) 
 GEOMETRIC_REPRESENTATION_ITEM ( )  RATIONAL_B_SPLINE_SURFACE ( (
 ( 1.000000000000000000, 0.8805984182415752537, 1.000000000000000000),
 ( 1.000000000000000000, 0.8693720018072552680, 1.000000000000000000),
 ( 1.000000000000000000, 0.8577088968917530032, 1.000000000000000000),
 ( 1.000000000000000000, 0.8393117846167141849, 1.000000000000000000),
 ( 1.000000000000000000, 0.8329887351665841155, 1.000000000000000000),
 ( 1.000000000000000000, 0.8202097823163787549, 1.000000000000000000),
 ( 1.000000000000000000, 0.8137563009269630498, 1.000000000000000000),
 ( 1.000000000000000000, 0.8006738836228965983, 1.000000000000000000),
 ( 1.000000000000000000, 0.7940450693277653071, 1.000000000000000000),
 ( 1.000000000000000000, 0.7805580043346841412, 1.000000000000000000),
 ( 1.000000000000000000, 0.7736606729360994139, 1.000000000000000000),
 ( 1.000000000000000000, 0.7528757204727521968, 1.000000000000000000),
 ( 1.000000000000000000, 0.7389027884188499318, 1.000000000000000000),
 ( 1.000000000000000000, 0.7246213771201909237, 1.000000000000000000) ) ) 
 REPRESENTATION_ITEM ( '' )  SURFACE ( )  );
#70989=B_SPLINE_CURVE_WITH_KNOTS ( 'NONE', 3,
 ( #96573, #86899, #63146, #96043, #46939, #5435, #29742, #70703, #103593, #71219, #94996, #38871, #103074, #71739 ),
 .UNSPECIFIED., .F., .F.,
 ( 4, 2, 2, 2, 2, 2, 4 ),
 ( 0.000000000000000000, 0.002832064884716075162, 0.004248097327074075447, 0.005664129769432076598, 0.007080162211790077750, 0.008496194654148081504, 0.01132825953886409769 ),
 .UNSPECIFIED. ) ;
#70990=CARTESIAN_POINT ( 'NONE',  ( -32.76922047444635666, 484.1128301720479499, 1.839745883406933569 ) ) ;
#71000=CARTESIAN_POINT ( 'NONE',  ( 2.153051538919528525E-10, 304.8518027762758607, 9.936999415352289589 ) ) ;
#71013=CARTESIAN_POINT ( 'NONE',  ( -38.83522905902818678, 469.0596193260172981, 0.4591931294767716554 ) ) ;
#71021=CARTESIAN_POINT ( 'NONE',  ( 39.78276460673486525, 485.2153259665875566, -4.379159006359480522 ) ) ;
#71027=CARTESIAN_POINT ( 'NONE',  ( -43.55333112596419909, 465.2342844084849389, 9.238213423004411951 ) ) ;
#71034=CARTESIAN_POINT ( 'NONE',  ( -43.74855578046756222, 328.6220886837048170, -1.765109843966993441 ) ) ;
#71036=CARTESIAN_POINT ( 'NONE',  ( 32.09911992168216699, 438.9232547152092252, 23.66653216045978780 ) ) ;
#71037=CARTESIAN_POINT ( 'NONE',  ( -33.97359119245066239, 434.1099241184709285, 11.80501937577158778 ) ) ;
#71045=CARTESIAN_POINT ( 'NONE',  ( -29.42120653936339281, 324.0310542480657432, 13.66637059004188792 ) ) ;
#71046=VERTEX_POINT ( 'NONE', #21352 ) ;
#71047=CARTESIAN_POINT ( 'NONE',  ( 20.39043067447545710, 304.8923525889808843, 9.945639527452529549 ) ) ;
#71061=CARTESIAN_POINT ( 'NONE',  ( -30.00000000000000000, 450.0000000000002274, 13.20242257375370976 ) ) ;
#71072=EDGE_LOOP ( 'NONE', ( #75664, #55092, #88453, #97895 ) ) ;
#71088=EDGE_CURVE ( 'NONE', #63343, #4655, #6799, .T. ) ;
#71093=DIRECTION ( 'NONE',  ( 0.000000000000000000, -0.9591753627731794962, 0.2828119931136929832 ) ) ;
#71098=CARTESIAN_POINT ( 'NONE',  ( 40.87654627980526811, 372.4006569927854571, 25.86602250413524473 ) ) ;
#71099=CARTESIAN_POINT ( 'NONE',  ( -42.74850648162922084, 465.8913842138921950, 12.61550125122446531 ) ) ;
#71102=CARTESIAN_POINT ( 'NONE',  ( -38.85446894546543462, 460.8903912184119349, 2.218456751109336267 ) ) ;
#71106=CARTESIAN_POINT ( 'NONE',  ( -36.52792128174517927, 461.3883473947829543, 3.418819814388621925 ) ) ;
#71111=CARTESIAN_POINT ( 'NONE',  ( -32.49055694945669615, 299.9956992945637353, 3.090866007574196939 ) ) ;
#71124=CARTESIAN_POINT ( 'NONE',  ( 42.61140200160144786, 465.9030374194822457, 13.21253569360410829 ) ) ;
#71128=ADVANCED_FACE ( 'NONE', ( #30493 ), #80098, .F. ) ;
#71129=DIRECTION ( 'NONE',  ( 0.000000000000000000, 0.000000000000000000, -1.000000000000000000 ) ) ;
#71135=CARTESIAN_POINT ( 'NONE',  ( 43.31290673312265227, 487.3457497296887482, 8.045183856868069583 ) ) ;
#71137=CARTESIAN_POINT ( 'NONE',  ( 43.59756234217316972, 434.3244621007173123, 14.55946156040339368 ) ) ;
#71141=AXIS2_PLACEMENT_3D ( 'NONE', #94646, #76300, #78425 ) ;
#71143=EDGE_LOOP ( 'NONE', ( #81421, #99118, #39465, #32092 ) ) ;
#71158=DIRECTION ( 'NONE',  ( -0.000000000000000000, -1.000000000000000000, -0.000000000000000000 ) ) ;
#71168=CARTESIAN_POINT ( 'NONE',  ( 41.72774289521763791, 484.6318496107524538, -3.104024719554764555 ) ) ;
#71176=CARTESIAN_POINT ( 'NONE',  ( -44.08840282922865583, 485.7747746244177165, 4.178803824087112595 ) ) ;
#71186=DIRECTION ( 'NONE',  ( 0.000000000000000000, 1.000000000000000000, 1.224646799147353207E-16 ) ) ;
#71198=EDGE_CURVE ( 'NONE', #19129, #44923, #67103, .T. ) ;
#71205=ORIENTED_EDGE ( 'NONE', *, *, #71088, .F. ) ;
#71219=CARTESIAN_POINT ( 'NONE',  ( -32.30721550124390973, 435.2323396810500071, 15.38116828642125533 ) ) ;
#71223=CIRCLE ( 'NONE', #5775, 0.9999999999999902300 ) ;
#71227=CARTESIAN_POINT ( 'NONE',  ( -33.13312975063780641, 300.2747487025878286, -0.7832785892000783123 ) ) ;
#71230=ORIENTED_EDGE ( 'NONE', *, *, #15844, .T. ) ;
#71242=CARTESIAN_POINT ( 'NONE',  ( -44.17170837311727638, 464.2817441679981698, 9.201374799661154569 ) ) ;
#71243=CARTESIAN_POINT ( 'NONE',  ( -35.03806997136413059, 439.1562646609019680, 24.08350753705479974 ) ) ;
#71245=CARTESIAN_POINT ( 'NONE',  ( -35.78063128285121053, 328.0132667276978395, -3.841611872727749954 ) ) ;
#71251=VERTEX_POINT ( 'NONE', #84333 ) ;
#71264=CARTESIAN_POINT ( 'NONE',  ( 16.12932323837952708, 294.5641184806675028, -2.061087533654167192 ) ) ;
#71288=B_SPLINE_CURVE_WITH_KNOTS ( 'NONE', 3,
 ( #44585, #35451, #10071, #3587, #60774, #18187, #34918, #2504, #59172, #76933, #85033, #44041, #84506, #1428, #9524, #27908, #42982, #11116, #34389, #3044 ),
 .UNSPECIFIED., .F., .F.,
 ( 4, 2, 2, 2, 2, 2, 2, 2, 2, 4 ),
 ( 6.938893903907228378E-18, 0.001523487669260046272, 0.003046975338520085605, 0.004570463007780124938, 0.005332206842410133762, 0.006093950677040142587, 0.007617438346300116868, 0.009140926015560092016, 0.01066441368482006630, 0.01218790135408004058 ),
 .UNSPECIFIED. ) ;
#71290=EDGE_LOOP ( 'NONE', ( #100225, #78265, #39638, #104511 ) ) ;
#71291=AXIS2_PLACEMENT_3D ( 'NONE', #99138, #25300, #16644 ) ;
#71295=DIRECTION ( 'NONE',  ( -0.2043693274459711939, 0.2793933298620141503, 0.9381751143725232112 ) ) ;
#71299=FACE_OUTER_BOUND ( 'NONE', #67143, .T. ) ;
#71313=CARTESIAN_POINT ( 'NONE',  ( 32.20052651336786198, 485.9558351764605391, 4.953748807559890110 ) ) ;
#71330=CARTESIAN_POINT ( 'NONE',  ( 20.96573260866662736, 302.9095451584354919, -9.987686131446045223 ) ) ;
#71332=ORIENTED_EDGE ( 'NONE', *, *, #60660, .F. ) ;
#71337=CARTESIAN_POINT ( 'NONE',  ( 34.68490551323709070, 463.9993046474231733, 18.60480341024938511 ) ) ;
#71338=EDGE_LOOP ( 'NONE', ( #9199, #46844, #66049, #37784 ) ) ;
#71340=CARTESIAN_POINT ( 'NONE',  ( 45.29905483467455696, 497.0732240353902398, -8.041250874568902418 ) ) ;
#71341=CARTESIAN_POINT ( 'NONE',  ( -33.12944332324993013, 439.4248878830265994, 23.85028906779292868 ) ) ;
#71353=ORIENTED_EDGE ( 'NONE', *, *, #101481, .T. ) ;
#71376=CARTESIAN_POINT ( 'NONE',  ( 10.01505413391482868, 294.6430545872282778, 9.892628616759090221 ) ) ;
#71381=CARTESIAN_POINT ( 'NONE',  ( -46.00000000000000000, 488.3725375423296668, 3.127739281037489771 ) ) ;
#71415=CARTESIAN_POINT ( 'NONE',  ( 31.71589149226793936, 316.4455846392050375, -7.213176056726631202 ) ) ;
#71418=CARTESIAN_POINT ( 'NONE',  ( 41.15077806939486749, 488.9683316695932831, 10.18452886344066322 ) ) ;
#71426=ADVANCED_FACE ( 'NONE', ( #104217 ), #66238, .F. ) ;
#71437=CARTESIAN_POINT ( 'NONE',  ( 33.21822485389247959, 314.5903571069972031, -7.199009675068519520 ) ) ;
#71438=CARTESIAN_POINT ( 'NONE',  ( 31.87080426956109136, 439.0384429942135966, 24.63328115755081882 ) ) ;
#71454=CARTESIAN_POINT ( 'NONE',  ( -36.02493936428357557, 463.3371199957071553, 20.06709031638035157 ) ) ;
#71460=( BOUNDED_SURFACE ( )  B_SPLINE_SURFACE ( 3, 2, ( 
 ( #94370, #69558, #44759 ),
 ( #92757, #28067, #76563 ),
 ( #52290, #78165, #43675 ),
 ( #18916, #60940, #84674 ),
 ( #10757, #93830, #12887 ),
 ( #45809, #101391, #53371 ),
 ( #85756, #4285, #19984 ),
 ( #78684, #36695, #68500 ),
 ( #27542, #2673, #52829 ),
 ( #86815, #101910, #102448 ),
 ( #11829, #35626, #60422 ),
 ( #86290, #85201, #77648 ),
 ( #12362, #3225, #102984 ),
 ( #3763, #37212, #69036 ),
 ( #93300, #27003, #29144 ),
 ( #28593, #45286, #35086 ),
 ( #61477, #19455, #20532 ),
 ( #70081, #44218, #62014 ),
 ( #11286, #94909, #21048 ),
 ( #77110, #53882, #67956 ),
 ( #100839, #59884, #36167 ),
 ( #51760, #80273, #88919 ),
 ( #21557, #31247, #15013 ),
 ( #46339, #47906, #22082 ),
 ( #63055, #56526, #5861 ),
 ( #29660, #72719, #71653 ),
 ( #46859, #70616, #23144 ),
 ( #79754, #105621, #63600 ) ),
 .UNSPECIFIED., .F., .F., .F. ) 
 B_SPLINE_SURFACE_WITH_KNOTS ( ( 4, 2, 2, 2, 2, 2, 2, 2, 2, 2, 2, 2, 2, 4 ),
 ( 3, 3 ),
 ( -1.788854400193778127E-05, 0.0008258451467879519836, 0.001669578837577841840, 0.002513312528367731696, 0.003357046219157621553, 0.004200779909947511409, 0.005044513600737401265, 0.006731980982317180978, 0.007575714673107070835, 0.008419448363896960691, 0.01010691574547674040, 0.01095064943626663026, 0.01179438312705652012, 0.01348185050863629983 ),
 ( 0.000000000000000000, 1.000000000000000000 ),
 .UNSPECIFIED. ) 
 GEOMETRIC_REPRESENTATION_ITEM ( )  RATIONAL_B_SPLINE_SURFACE ( (
 ( 1.000000000000000000, 1.000000000000000000, 1.000000000000000000),
 ( 1.000000000000000000, 1.000005597033407190, 1.000000000000000000),
 ( 1.000000000000000000, 0.9981174035066882055, 1.000000000000000000),
 ( 1.000000000000000000, 0.9910941550147043255, 1.000000000000000000),
 ( 1.000000000000000000, 0.9859587391847201010, 1.000000000000000000),
 ( 1.000000000000000000, 0.9732073139058156075, 1.000000000000000000),
 ( 1.000000000000000000, 0.9655956055858216924, 1.000000000000000000),
 ( 1.000000000000000000, 0.9487954604333295183, 1.000000000000000000),
 ( 1.000000000000000000, 0.9396125312399712382, 1.000000000000000000),
 ( 1.000000000000000000, 0.9205547400792526425, 1.000000000000000000),
 ( 1.000000000000000000, 0.9106598259530991335, 1.000000000000000000),
 ( 1.000000000000000000, 0.8910166268726569250, 1.000000000000000000),
 ( 1.000000000000000000, 0.8812839758801553902, 1.000000000000000000),
 ( 1.000000000000000000, 0.8530381836209635082, 1.000000000000000000),
 ( 1.000000000000000000, 0.8355499924318912086, 1.000000000000000000),
 ( 1.000000000000000000, 0.8121180734289953351, 1.000000000000000000),
 ( 1.000000000000000000, 0.8047528071578063935, 1.000000000000000000),
 ( 1.000000000000000000, 0.7908772856467519707, 1.000000000000000000),
 ( 1.000000000000000000, 0.7843397418777237062, 1.000000000000000000),
 ( 1.000000000000000000, 0.7662143347357434076, 1.000000000000000000),
 ( 1.000000000000000000, 0.7560053113367869448, 1.000000000000000000),
 ( 1.000000000000000000, 0.7426428230161424837, 1.000000000000000000),
 ( 1.000000000000000000, 0.7385160411531185298, 1.000000000000000000),
 ( 1.000000000000000000, 0.7308023910627007291, 1.000000000000000000),
 ( 1.000000000000000000, 0.7272503285415187202, 1.000000000000000000),
 ( 1.000000000000000000, 0.7174350756271979934, 1.000000000000000000),
 ( 1.000000000000000000, 0.7119478818691705735, 1.000000000000000000),
 ( 1.000000000000000000, 0.7071066567438651917, 1.000000000000000000) ) ) 
 REPRESENTATION_ITEM ( '' )  SURFACE ( )  );
#71461=VERTEX_POINT ( 'NONE', #87005 ) ;
#71462=ORIENTED_EDGE ( 'NONE', *, *, #40686, .F. ) ;
#71489=CARTESIAN_POINT ( 'NONE',  ( -33.21583695389851698, 487.8294359878406681, 10.09122741356614128 ) ) ;
#71500=CARTESIAN_POINT ( 'NONE',  ( 38.06305853432018438, 464.2388122684127438, 19.21895763407759006 ) ) ;
#71537=EDGE_LOOP ( 'NONE', ( #103561, #31196, #69986 ) ) ;
#71543=CARTESIAN_POINT ( 'NONE',  ( 40.89305344739098302, 461.0673237560015423, 2.333915627062251197 ) ) ;
#71552=CARTESIAN_POINT ( 'NONE',  ( -45.17824257314219949, 354.4244853104167987, 3.762393652172960845 ) ) ;
#71561=TOROIDAL_SURFACE ( 'NONE', #12975, 12.00000000000000711, 3.000000000000000000 ) ;
#71563=CARTESIAN_POINT ( 'NONE',  ( -24.69131919313263523, 306.9777677896850605, 9.416086620544890096 ) ) ;
#71571=CARTESIAN_POINT ( 'NONE',  ( 46.00000000000000000, 488.0504108836742603, 1.820875518052046171 ) ) ;
#71574=CARTESIAN_POINT ( 'NONE',  ( -33.00000000000000000, 500.0000000000002274, 0.000000000000000000 ) ) ;
#71588=CARTESIAN_POINT ( 'NONE',  ( 22.18906107735381283, 305.1406206946286943, -9.938500898754245583 ) ) ;
#71594=AXIS2_PLACEMENT_3D ( 'NONE', #66008, #24528, #64948 ) ;
#71596=AXIS2_PLACEMENT_3D ( 'NONE', #104151, #4945, #20654 ) ;
#71602=ORIENTED_EDGE ( 'NONE', *, *, #68224, .T. ) ;
#71617=CARTESIAN_POINT ( 'NONE',  ( 28.62265479722442763, 310.7111749469181632, 11.81549357303394743 ) ) ;
#71620=ADVANCED_FACE ( 'NONE', ( #57778 ), #58697, .T. ) ;
#71623=EDGE_LOOP ( 'NONE', ( #96049, #60551, #44404, #71462 ) ) ;
#71625=CARTESIAN_POINT ( 'NONE',  ( -36.23923339644125008, 462.2853740901311994, 3.478454459919455122 ) ) ;
#71628=CARTESIAN_POINT ( 'NONE',  ( -35.53650496371267309, 390.2108302089691279, 6.619629604413060697 ) ) ;
#71629=CARTESIAN_POINT ( 'NONE',  ( -31.99696324403842596, 299.5158792032175370, 2.978889298943153907 ) ) ;
#71637=CIRCLE ( 'NONE', #99201, 0.9999999999999998890 ) ;
#71650=EDGE_CURVE ( 'NONE', #15655, #97120, #87802, .T. ) ;
#71651=CARTESIAN_POINT ( 'NONE',  ( 42.57785895164496992, 484.8808303102439936, 8.276426683567752463 ) ) ;
#71653=CARTESIAN_POINT ( 'NONE',  ( 9.738398295825046347, 294.6500605438458820, -2.277702036928785034 ) ) ;
#71664=DIRECTION ( 'NONE',  ( 0.2230022920436083578, -0.09894799074349157342, 0.9697831060969888117 ) ) ;
#71668=VERTEX_POINT ( 'NONE', #43216 ) ;
#71676=DIRECTION ( 'NONE',  ( 0.000000000000000000, 0.000000000000000000, -1.000000000000000000 ) ) ;
#71705=ORIENTED_EDGE ( 'NONE', *, *, #31053, .F. ) ;
#71711=CARTESIAN_POINT ( 'NONE',  ( -2.627668993003716480, 302.8385116830480683, 9.934221043902621062 ) ) ;
#71712=CARTESIAN_POINT ( 'NONE',  ( -39.84233570596349949, 333.3323931548420660, 19.23895789620553032 ) ) ;
#71715=DIRECTION ( 'NONE',  ( 0.5401002696852920115, 0.5464483025172063302, 0.6400671459791846818 ) ) ;
#71718=CARTESIAN_POINT ( 'NONE',  ( -33.86867596911223188, 484.1347864990148082, 1.565332731471725136 ) ) ;
#71722=EDGE_LOOP ( 'NONE', ( #90491, #76209, #14831, #63207 ) ) ;
#71735=CIRCLE ( 'NONE', #23579, 3.000000000000000000 ) ;
#71736=CARTESIAN_POINT ( 'NONE',  ( -31.96652969245341325, 438.9664737494705378, 23.62269400183483725 ) ) ;
#71739=CARTESIAN_POINT ( 'NONE',  ( -33.00000000000000000, 435.0774731480752848, 11.67986145722080948 ) ) ;
#71747=CARTESIAN_POINT ( 'NONE',  ( -34.00613029049673486, 301.2164055778219449, -0.5617985262917791767 ) ) ;
#71751=ORIENTED_EDGE ( 'NONE', *, *, #99230, .T. ) ;
#71759=CARTESIAN_POINT ( 'NONE',  ( -42.09158233638504498, 465.7816406625409513, 14.79318349170026892 ) ) ;
#71760=ORIENTED_EDGE ( 'NONE', *, *, #40564, .F. ) ;
#71763=CIRCLE ( 'NONE', #21848, 0.9999999999999998890 ) ;
#71764=CARTESIAN_POINT ( 'NONE',  ( -36.95591949233575946, 439.3722685534989409, 23.79946508175408937 ) ) ;
#71795=CARTESIAN_POINT ( 'NONE',  ( 44.39546657021049469, 435.2018463496405047, 12.64356380809994995 ) ) ;
#71807=AXIS2_PLACEMENT_3D ( 'NONE', #26702, #19149, #59575 ) ;
#71811=CIRCLE ( 'NONE', #82131, 0.9999999999999968914 ) ;
#71812=CARTESIAN_POINT ( 'NONE',  ( 24.60488647473181345, 306.9835580411500473, 10.41807558718820914 ) ) ;
#71813=DIRECTION ( 'NONE',  ( 0.000000000000000000, 0.000000000000000000, -1.000000000000000000 ) ) ;
#71825=CARTESIAN_POINT ( 'NONE',  ( -13.27220259399123314, 304.5542592310576993, 9.873754584668670731 ) ) ;
#71854=CARTESIAN_POINT ( 'NONE',  ( -40.86217775602844426, 319.2309035517266693, 3.920900997671151078 ) ) ;
#71855=EDGE_CURVE ( 'NONE', #11400, #234, #63729, .T. ) ;
#71856=CARTESIAN_POINT ( 'NONE',  ( 27.46788371183871291, 305.3393767471599176, -9.450502104329384423 ) ) ;
#71857=B_SPLINE_CURVE_WITH_KNOTS ( 'NONE', 3,
 ( #8748, #105847, #24965, #32532 ),
 .UNSPECIFIED., .F., .F.,
 ( 4, 4 ),
 ( 1.170938346284344789E-17, 0.003511374632863300226 ),
 .UNSPECIFIED. ) ;
#71863=EDGE_LOOP ( 'NONE', ( #4835, #40457, #42391, #29482 ) ) ;
#71871=CARTESIAN_POINT ( 'NONE',  ( -30.12932728364529922, 334.4140447340107585, 17.11298374841474867 ) ) ;
#71877=CIRCLE ( 'NONE', #73552, 0.9999999999999941158 ) ;
#71885=CARTESIAN_POINT ( 'NONE',  ( 43.75401118688382951, 486.3173572309547694, 5.908089951475070656 ) ) ;
#71900=VERTEX_POINT ( 'NONE', #77712 ) ;
#71902=AXIS2_PLACEMENT_3D ( 'NONE', #68787, #35915, #101668 ) ;
#71915=CARTESIAN_POINT ( 'NONE',  ( 15.66780019633566567, 294.5588774916458306, 1.874735905060328056 ) ) ;
#71923=ADVANCED_FACE ( 'NONE', ( #78748 ), #22385, .F. ) ;
#71929=CARTESIAN_POINT ( 'NONE',  ( -40.69416551809789695, 490.1135946711737006, 11.28307282940560086 ) ) ;
#71939=CARTESIAN_POINT ( 'NONE',  ( -39.83065760000179267, 436.5763539059782374, 5.509783410167077733 ) ) ;
#71940=CARTESIAN_POINT ( 'NONE',  ( -43.99399868446376871, 464.5851102538602504, 10.32278593049915649 ) ) ;
#71942=( BOUNDED_SURFACE ( )  B_SPLINE_SURFACE ( 3, 2, ( 
 ( #89894, #58048, #25190 ),
 ( #67229, #82328, #24655 ),
 ( #32207, #41339, #57507 ),
 ( #836, #99027, #25745 ),
 ( #26271, #33807, #66685 ),
 ( #99566, #9487, #17081 ),
 ( #42398, #75293, #16533 ),
 ( #82866, #59134, #73154 ),
 ( #90430, #92016, #49958 ),
 ( #91503, #56980, #65085 ) ),
 .UNSPECIFIED., .F., .F., .F. ) 
 B_SPLINE_SURFACE_WITH_KNOTS ( ( 4, 2, 2, 2, 4 ),
 ( 3, 3 ),
 ( 0.007286154432480726126, 0.008335500519281571763, 0.009384846606082415665, 0.01043419269288325957, 0.01148353877968410347 ),
 ( 0.1485529662656749350, 1.000000000000000000 ),
 .UNSPECIFIED. ) 
 GEOMETRIC_REPRESENTATION_ITEM ( )  RATIONAL_B_SPLINE_SURFACE ( (
 ( 0.9428520994613440731, 0.8076514324310039017, 1.000000000000000000),
 ( 0.9457545067941961481, 0.8174203633578406292, 1.000000000000000000),
 ( 0.9476060023041493752, 0.8236521322564903658, 1.000000000000000000),
 ( 0.9488932852697182785, 0.8279848729547364394, 1.000000000000000000),
 ( 0.9483224819758968582, 0.8260636615909705549, 1.000000000000000000),
 ( 0.9449873596068385506, 0.8148382971539733788, 1.000000000000000000),
 ( 0.9422359404858332566, 0.8055775627836994079, 1.000000000000000000),
 ( 0.9351232435981660096, 0.7816376271955178812, 1.000000000000000000),
 ( 0.9307673920762341568, 0.7669766896476877260, 1.000000000000000000),
 ( 0.9259068126999906445, 0.7506169376399400850, 1.000000000000000000) ) ) 
 REPRESENTATION_ITEM ( '' )  SURFACE ( )  );
#71953=CARTESIAN_POINT ( 'NONE',  ( -27.47093694407817210, 296.2799286419132727, -9.692114557243211692 ) ) ;
#71960=CARTESIAN_POINT ( 'NONE',  ( 36.68219968559907329, 426.6315103464384038, 5.464024069355958524 ) ) ;
#71963=CARTESIAN_POINT ( 'NONE',  ( -28.97859824875257218, 308.1531040660597682, -9.025514053728203478 ) ) ;
#71964=CARTESIAN_POINT ( 'NONE',  ( 41.74356089131816816, 489.2821409585033621, 10.50625248545157753 ) ) ;
#71965=CARTESIAN_POINT ( 'NONE',  ( -42.99999999999998579, 464.8825480873695710, 15.07585856869430607 ) ) ;
#71969=AXIS2_PLACEMENT_3D ( 'NONE', #21085, #37259, #37793 ) ;
#71970=FACE_OUTER_BOUND ( 'NONE', #50845, .T. ) ;
#71973=CARTESIAN_POINT ( 'NONE',  ( -33.70841932975964284, 485.0774894644218875, 1.934193826885682199 ) ) ;
#71981=CARTESIAN_POINT ( 'NONE',  ( 39.15257853886765105, 311.4970519361567654, 1.970299295586781962 ) ) ;
#71989=CARTESIAN_POINT ( 'NONE',  ( 43.09948196127356823, 484.9577458347779384, -0.8563396247094318126 ) ) ;
#71997=CARTESIAN_POINT ( 'NONE',  ( 43.75401118688384372, 486.3173572309546557, 5.908089951475091084 ) ) ;
#72009=CARTESIAN_POINT ( 'NONE',  ( -43.54570344706581153, 464.5919001249989719, 9.427857144823894586 ) ) ;
#72019=ADVANCED_FACE ( 'NONE', ( #45626 ), #43566, .F. ) ;
#72027=CARTESIAN_POINT ( 'NONE',  ( 44.12472801211155371, 485.7238370326410859, 3.975897585125152123 ) ) ;
#72030=CARTESIAN_POINT ( 'NONE',  ( -36.56870781681114835, 337.1622652273130711, -1.695314226153411763 ) ) ;
#72032=CARTESIAN_POINT ( 'NONE',  ( -46.00000000000000000, 486.2666530176200581, 2.948218630481520997 ) ) ;
#72035=ORIENTED_EDGE ( 'NONE', *, *, #85149, .F. ) ;
#72039=CARTESIAN_POINT ( 'NONE',  ( -39.14057804813676000, 485.8491723118624463, -4.975388520154326422 ) ) ;
#72041=CARTESIAN_POINT ( 'NONE',  ( 4.023876337984799711, 300.5161520203807299, -10.00978828653755315 ) ) ;
#72060=CARTESIAN_POINT ( 'NONE',  ( 13.27219118062621561, 304.5542594574499162, 9.873754632660967090 ) ) ;
#72072=CARTESIAN_POINT ( 'NONE',  ( -30.00000000000000711, 464.1495552126472148, 11.87789752000373156 ) ) ;
#72074=B_SPLINE_CURVE_WITH_KNOTS ( 'NONE', 3,
 ( #8416, #66124, #91482, #16511 ),
 .UNSPECIFIED., .F., .F.,
 ( 4, 4 ),
 ( 2.069507657746056223E-16, 0.001795780652478906267 ),
 .UNSPECIFIED. ) ;
#72085=CARTESIAN_POINT ( 'NONE',  ( 39.33042632267689953, 460.7392826591629387, 2.124562382290182239 ) ) ;
#72089=CARTESIAN_POINT ( 'NONE',  ( 43.63930228698950486, 486.5321682126036080, 6.480714085081864972 ) ) ;
#72091=( BOUNDED_SURFACE ( )  B_SPLINE_SURFACE ( 3, 2, ( 
 ( #50044, #73242, #90511 ),
 ( #48446, #49514, #7448 ),
 ( #106146, #16087, #66230 ),
 ( #25836, #81864, #65712 ) ),
 .UNSPECIFIED., .F., .F., .F. ) 
 B_SPLINE_SURFACE_WITH_KNOTS ( ( 4, 4 ),
 ( 3, 3 ),
 ( 1.084202172485504434E-17, 0.0008582108274410138026 ),
 ( 0.000000000000000000, 1.000000000000000000 ),
 .UNSPECIFIED. ) 
 GEOMETRIC_REPRESENTATION_ITEM ( )  RATIONAL_B_SPLINE_SURFACE ( (
 ( 1.000000000000000000, 0.7409272757993169423, 1.000000000000000000),
 ( 1.000000000000000000, 0.7386644886093517437, 1.000000000000000000),
 ( 1.000000000000000000, 0.7359402037277118502, 1.000000000000000000),
 ( 1.000000000000000000, 0.7328671738315170048, 1.000000000000000000) ) ) 
 REPRESENTATION_ITEM ( '' )  SURFACE ( )  );
#72092=CARTESIAN_POINT ( 'NONE',  ( 42.19179521601818550, 484.5286692029256983, -4.078961064719028862 ) ) ;
#72095=EDGE_LOOP ( 'NONE', ( #97827, #82214, #81437, #44234 ) ) ;
#72105=CARTESIAN_POINT ( 'NONE',  ( -23.79050601098939310, 306.1176470301992367, 9.215821030969554073 ) ) ;
#72108=CARTESIAN_POINT ( 'NONE',  ( 43.00000000000000000, 450.0000000000002274, 25.20242257375371864 ) ) ;
#72117=FACE_OUTER_BOUND ( 'NONE', #84070, .T. ) ;
#72131=CARTESIAN_POINT ( 'NONE',  ( 3.389930600490795420, 303.8518027742030085, -9.999999999492535707 ) ) ;
#72135=ORIENTED_EDGE ( 'NONE', *, *, #90324, .F. ) ;
#72161=CARTESIAN_POINT ( 'NONE',  ( 36.57269729962153093, 309.7540319447825823, 13.50089482657587503 ) ) ;
#72162=CARTESIAN_POINT ( 'NONE',  ( 42.36162206505731831, 485.1874691988857649, -2.398526663486076238 ) ) ;
#72166=CARTESIAN_POINT ( 'NONE',  ( -38.51502786940058343, 460.0233756673464427, 2.043034587342845043 ) ) ;
#72170=CARTESIAN_POINT ( 'NONE',  ( -35.57320956138945434, 461.3653195830025311, 3.400055647391269087 ) ) ;
#72173=CARTESIAN_POINT ( 'NONE',  ( -35.48605273723305942, 424.7888819862658352, 6.350197726503093776 ) ) ;
#72175=CARTESIAN_POINT ( 'NONE',  ( -25.99191122786077557, 305.5540186273516383, 10.54636674004932395 ) ) ;
#72192=CARTESIAN_POINT ( 'NONE',  ( 36.64823341582350480, 437.5392299810053487, 4.281405873620224511 ) ) ;
#72200=CARTESIAN_POINT ( 'NONE',  ( 37.49021716374312518, 468.5026615090375230, 18.51838214818229034 ) ) ;
#72215=CARTESIAN_POINT ( 'NONE',  ( 21.04247164025375483, 37.86482112153537116, -10.52123582012688097 ) ) ;
#72221=CIRCLE ( 'NONE', #89475, 7.025805963803935406 ) ;
#72234=CARTESIAN_POINT ( 'NONE',  ( 31.15871529744714863, 428.0462763543694109, 24.54283678189916884 ) ) ;
#72235=( BOUNDED_SURFACE ( )  B_SPLINE_SURFACE ( 3, 2, ( 
 ( #57915, #41745, #43349 ),
 ( #32625, #28264, #11489 ),
 ( #3425, #77842, #52486 ),
 ( #86494, #85405, #19116 ),
 ( #69752, #68705, #27200 ),
 ( #60616, #77310, #20726 ),
 ( #28806, #76766, #12552 ),
 ( #45490, #54065, #76234 ),
 ( #60090, #3955, #94024 ),
 ( #95101, #20185, #102105 ),
 ( #78357, #61134, #62217 ),
 ( #69236, #53036, #93506 ) ),
 .UNSPECIFIED., .F., .F., .F. ) 
 B_SPLINE_SURFACE_WITH_KNOTS ( ( 4, 2, 2, 2, 2, 4 ),
 ( 3, 3 ),
 ( -2.168404344971008868E-18, 0.001679904595664871237, 0.003359809191329744642, 0.004199761489162181019, 0.005039713786994618264, 0.006719618382659491018 ),
 ( 0.000000000000000000, 1.000000000000000000 ),
 .UNSPECIFIED. ) 
 GEOMETRIC_REPRESENTATION_ITEM ( )  RATIONAL_B_SPLINE_SURFACE ( (
 ( 1.000000000000000000, 0.8014084173415135792, 1.000000000000000000),
 ( 1.000000000000000000, 0.8133474198022304646, 1.000000000000000000),
 ( 1.000000000000000000, 0.8251589633861846629, 1.000000000000000000),
 ( 1.000000000000000000, 0.8478574907170124408, 1.000000000000000000),
 ( 1.000000000000000000, 0.8587488926553007440, 1.000000000000000000),
 ( 1.000000000000000000, 0.8739423948878513038, 1.000000000000000000),
 ( 1.000000000000000000, 0.8787956638559439870, 1.000000000000000000),
 ( 1.000000000000000000, 0.8878757020716585568, 1.000000000000000000),
 ( 1.000000000000000000, 0.8921241670188198025, 1.000000000000000000),
 ( 1.000000000000000000, 0.9038999154880622555, 1.000000000000000000),
 ( 1.000000000000000000, 0.9104653308040103754, 1.000000000000000000),
 ( 1.000000000000000000, 0.9153908114177993216, 1.000000000000000000) ) ) 
 REPRESENTATION_ITEM ( '' )  SURFACE ( )  );
#72238=ORIENTED_EDGE ( 'NONE', *, *, #70852, .F. ) ;
#72239=CARTESIAN_POINT ( 'NONE',  ( -32.83963058903137266, 487.9259900561239647, 4.912448545037069181 ) ) ;
#72254=DIRECTION ( 'NONE',  ( -0.000000000000000000, -0.5617366626182503930, -0.8273160954982743398 ) ) ;
#72263=CARTESIAN_POINT ( 'NONE',  ( 13.58964414657211073, 303.5476453198347144, -10.06465184102012955 ) ) ;
#72273=ADVANCED_FACE ( 'NONE', ( #98399 ), #69716, .T. ) ;
#72280=CARTESIAN_POINT ( 'NONE',  ( -42.69811214730272297, 434.9611672192513652, 18.34625614733208820 ) ) ;
#72284=CARTESIAN_POINT ( 'NONE',  ( -36.65515723092381251, 373.6298163844335249, 4.402904589519302192 ) ) ;
#72289=CARTESIAN_POINT ( 'NONE',  ( -33.62653946147953121, 300.0647574820262093, -8.836532605440917010 ) ) ;
#72293=ORIENTED_EDGE ( 'NONE', *, *, #91024, .F. ) ;
#72297=CARTESIAN_POINT ( 'NONE',  ( 30.86805345995181327, 345.9229254628596095, 18.50907901912128395 ) ) ;
#72309=ADVANCED_FACE ( 'NONE', ( #3437 ), #87687, .F. ) ;
#72312=CARTESIAN_POINT ( 'NONE',  ( -37.46459653829825953, 360.1626999571597594, 2.821112259843927994 ) ) ;
#72338=EDGE_CURVE ( 'NONE', #56970, #100861, #63356, .T. ) ;
#72351=CARTESIAN_POINT ( 'NONE',  ( 29.01988888469873018, 321.8047804620298393, 14.12772110426748284 ) ) ;
#72357=EDGE_CURVE ( 'NONE', #33657, #38940, #89139, .T. ) ;
#72375=CARTESIAN_POINT ( 'NONE',  ( 32.87491876136141400, 485.1684955304415894, 5.618973769036216481 ) ) ;
#72377=CARTESIAN_POINT ( 'NONE',  ( -33.00000000000000000, 450.0000000000002274, 13.20242257375370976 ) ) ;
#72386=CARTESIAN_POINT ( 'NONE',  ( -32.78741055188834963, 485.3331003366709524, 5.977022408746728743 ) ) ;
#72393=CARTESIAN_POINT ( 'NONE',  ( 29.60041846187245795, 307.3673858255965001, -8.977896531553003712 ) ) ;
#72407=CARTESIAN_POINT ( 'NONE',  ( -24.93816302196866275, 307.4233949143036284, 10.52291764336465008 ) ) ;
#72410=DIRECTION ( 'NONE',  ( 0.000000000000000000, 0.000000000000000000, -1.000000000000000000 ) ) ;
#72413=DIRECTION ( 'NONE',  ( -0.000000000000000000, 1.000000000000000000, -0.000000000000000000 ) ) ;
#72423=FACE_OUTER_BOUND ( 'NONE', #1951, .T. ) ;
#72451=DIRECTION ( 'NONE',  ( 0.000000000000000000, 0.1742756985702809125, 0.9846968979781752784 ) ) ;
#72457=CARTESIAN_POINT ( 'NONE',  ( 39.28547526272472368, 437.8764796837014046, 22.93021597682914248 ) ) ;
#72469=ORIENTED_EDGE ( 'NONE', *, *, #50660, .T. ) ;
#72483=CARTESIAN_POINT ( 'NONE',  ( 27.33006516600399038, 307.9308989645884367, -8.309468075633031248 ) ) ;
#72492=VERTEX_POINT ( 'NONE', #54083 ) ;
#72506=CARTESIAN_POINT ( 'NONE',  ( 30.76610509901443891, 309.0084209058028932, -8.583914624946309857 ) ) ;
#72514=CARTESIAN_POINT ( 'NONE',  ( 43.66784424859969960, 484.4037905981119820, 1.818048676808467823 ) ) ;
#72521=ORIENTED_EDGE ( 'NONE', *, *, #51014, .T. ) ;
#72547=CARTESIAN_POINT ( 'NONE',  ( -32.69883954133502613, 464.5926484747980112, 16.74362576150847204 ) ) ;
#72548=CARTESIAN_POINT ( 'NONE',  ( -33.21102376836597614, 438.9613914113129454, 23.92328486949907074 ) ) ;
#72549=CARTESIAN_POINT ( 'NONE',  ( 32.97893058398564392, 361.9919399545990473, 22.73043233383004846 ) ) ;
#72550=CARTESIAN_POINT ( 'NONE',  ( -43.56702065117462297, 370.0667959703745851, 13.88062581363111470 ) ) ;
#72553=CARTESIAN_POINT ( 'NONE',  ( -46.00000000000000000, 487.9838442367869220, -0.2095173675535702273 ) ) ;
#72559=ORIENTED_EDGE ( 'NONE', *, *, #84660, .T. ) ;
#72563=EDGE_CURVE ( 'NONE', #41040, #38837, #97900, .T. ) ;
#72567=CARTESIAN_POINT ( 'NONE',  ( 39.63576248123835910, 464.1159270358589879, 18.30995280209005927 ) ) ;
#72575=CARTESIAN_POINT ( 'NONE',  ( 0.000000000000000000, 274.9999999999999432, 0.000000000000000000 ) ) ;
#72589=ADVANCED_FACE ( 'NONE', ( #64337 ), #99301, .F. ) ;
#72597=CARTESIAN_POINT ( 'NONE',  ( -32.16294467543131930, 464.8250491768795882, 14.67690201923579352 ) ) ;
#72606=CARTESIAN_POINT ( 'NONE',  ( 34.12241045381283300, 439.1279507012955037, 24.06036799111038604 ) ) ;
#72612=CARTESIAN_POINT ( 'NONE',  ( 39.71334445446535000, 460.7040462571919193, 2.103363390004007627 ) ) ;
#72616=STYLED_ITEM ( 'NONE', ( #97715 ), #20124 ) ;
#72629=EDGE_LOOP ( 'NONE', ( #101864, #50957, #3314, #88380 ) ) ;
#72630=CARTESIAN_POINT ( 'NONE',  ( -28.38881774565038896, 318.1718324713938273, 13.21570572201404303 ) ) ;
#72632=CARTESIAN_POINT ( 'NONE',  ( 20.42551034609843086, 304.8951776613778861, 8.946191631382156118 ) ) ;
#72635=CARTESIAN_POINT ( 'NONE',  ( -30.00000000000000000, 500.0000000000002274, 0.000000000000000000 ) ) ;
#72652=CIRCLE ( 'NONE', #26205, 3.000000000000026645 ) ;
#72660=VERTEX_POINT ( 'NONE', #600 ) ;
#72669=B_SPLINE_CURVE_WITH_KNOTS ( 'NONE', 3,
 ( #104307, #47660, #23971, #56813 ),
 .UNSPECIFIED., .F., .F.,
 ( 4, 4 ),
 ( 6.871344576781776423E-17, 0.001856568542220787864 ),
 .UNSPECIFIED. ) ;
#72670=ORIENTED_EDGE ( 'NONE', *, *, #63763, .F. ) ;
#72672=CARTESIAN_POINT ( 'NONE',  ( -33.74271564777242816, 484.1802673187708592, 2.058285076122308155 ) ) ;
#72676=CARTESIAN_POINT ( 'NONE',  ( 43.21649601278002706, 436.3330504929571703, 19.41248623753888580 ) ) ;
#72683=CARTESIAN_POINT ( 'NONE',  ( 38.96347140373135431, 313.4333200668041854, 6.407657066588297035 ) ) ;
#72685=ADVANCED_FACE ( 'NONE', ( #19002 ), #91151, .F. ) ;
#72689=CARTESIAN_POINT ( 'NONE',  ( -40.26058501384667210, 460.2706387420201395, 2.258779328633529371 ) ) ;
#72697=CARTESIAN_POINT ( 'NONE',  ( -28.65514056416654398, 297.4037072407057281, 10.49742630379315322 ) ) ;
#72704=ORIENTED_EDGE ( 'NONE', *, *, #81, .T. ) ;
#72709=CARTESIAN_POINT ( 'NONE',  ( 35.72538317320631052, 438.1659592258356497, 3.984952432984858017 ) ) ;
#72715=DIRECTION ( 'NONE',  ( 0.000000000000000000, 0.000000000000000000, 1.000000000000000000 ) ) ;
#72719=CARTESIAN_POINT ( 'NONE',  ( 9.675290556392710073, 294.8809879903661226, -10.04271151416038954 ) ) ;
#72730=CARTESIAN_POINT ( 'NONE',  ( 40.73953790046563483, -18.92596047533412573, 20.36976895023281742 ) ) ;
#72758=CARTESIAN_POINT ( 'NONE',  ( -28.76346532419124458, 309.5219921958590135, -8.933260212751790164 ) ) ;
#72765=CARTESIAN_POINT ( 'NONE',  ( 43.41290683822506935, 487.0833545439620593, 7.569976829064905210 ) ) ;
#72766=VERTEX_POINT ( 'NONE', #40376 ) ;
#72769=CARTESIAN_POINT ( 'NONE',  ( -7.088826404115056157, 296.1964324881551534, -10.02186216631903370 ) ) ;
#72775=CARTESIAN_POINT ( 'NONE',  ( -13.70970213139414895, 294.5458219564956153, 9.871961192988456091 ) ) ;
#72779=CARTESIAN_POINT ( 'NONE',  ( 34.79468063551433232, 490.6633164237547930, 11.75004032468988235 ) ) ;
#72783=VERTEX_POINT ( 'NONE', #58705 ) ;
#72796=CARTESIAN_POINT ( 'NONE',  ( -42.74438300981208982, 419.2451651247366158, 19.59905343518640919 ) ) ;
#72799=CARTESIAN_POINT ( 'NONE',  ( -34.09307597759925557, 322.8769654760196772, -5.350189533808188180 ) ) ;
#72806=CARTESIAN_POINT ( 'NONE',  ( -29.28112164441576226, 307.0004567166486709, -9.064633347289211329 ) ) ;
#72809=VERTEX_POINT ( 'NONE', #106157 ) ;
#72813=CARTESIAN_POINT ( 'NONE',  ( 25.05494358412147449, 307.4491500886443305, 9.528491992859288828 ) ) ;
#72830=CARTESIAN_POINT ( 'NONE',  ( 38.82068856954457203, 477.2421094490886162, -1.707083602274671374 ) ) ;
#72847=DIRECTION ( 'NONE',  ( 0.000000000000000000, -0.07486943176531161981, 0.9971933454386564533 ) ) ;
#72849=CARTESIAN_POINT ( 'NONE',  ( 30.00000000000000000, 500.0000000000002274, 0.000000000000000000 ) ) ;
#72861=B_SPLINE_CURVE_WITH_KNOTS ( 'NONE', 3,
 ( #19618, #84833, #43311, #77807, #84301, #28769, #53529, #52448, #77275, #35244 ),
 .UNSPECIFIED., .F., .F.,
 ( 4, 2, 2, 2, 4 ),
 ( -5.999999997985845112E-08, 0.002353756740120384067, 0.004707573480240747829, 0.009415206960481474485, 0.01883047392096293127 ),
 .UNSPECIFIED. ) ;
#72871=VERTEX_POINT ( 'NONE', #1719 ) ;
#72875=DIRECTION ( 'NONE',  ( -0.000000000000000000, -1.000000000000000000, -0.000000000000000000 ) ) ;
#72891=ORIENTED_EDGE ( 'NONE', *, *, #19814, .F. ) ;
#72901=CARTESIAN_POINT ( 'NONE',  ( 37.83758010121639614, 485.6941950553124343, -4.518273513596184898 ) ) ;
#72907=CARTESIAN_POINT ( 'NONE',  ( -43.47452733440542261, 362.3092494624403912, 12.84014924004942415 ) ) ;
#72908=CARTESIAN_POINT ( 'NONE',  ( 21.24454331354147385, 302.9514041099373571, -9.978735210106369991 ) ) ;
#72918=CARTESIAN_POINT ( 'NONE',  ( 43.74855578046756222, 328.6220886837048170, -1.765109843966993441 ) ) ;
#72923=CARTESIAN_POINT ( 'NONE',  ( -31.37379325839373934, 432.3256879030839741, 23.18622107664128151 ) ) ;
#72951=CARTESIAN_POINT ( 'NONE',  ( 46.00000000000000000, 450.0000000000002274, 13.20242257375370976 ) ) ;
#72973=CARTESIAN_POINT ( 'NONE',  ( 33.66103144839009786, 439.0639482787724432, 24.00889586765897832 ) ) ;
#72984=CARTESIAN_POINT ( 'NONE',  ( -43.51330286016842308, 435.7669547662763989, 8.554287073375030914 ) ) ;
#72986=EDGE_CURVE ( 'NONE', #78613, #67620, #9050, .T. ) ;
#72987=CARTESIAN_POINT ( 'NONE',  ( 36.57468857844234122, 463.9816243198107486, 19.61678995109879864 ) ) ;
#72991=CARTESIAN_POINT ( 'NONE',  ( -45.48003679188781234, 379.8448106960472614, 7.220331889307936457 ) ) ;
#72993=CARTESIAN_POINT ( 'NONE',  ( -41.58649125062324003, 315.0454808444952732, -5.157136739135766312 ) ) ;
#72997=CARTESIAN_POINT ( 'NONE',  ( 29.35909118268796192, 310.5218271128537140, -8.690052357984560771 ) ) ;
#73004=FACE_OUTER_BOUND ( 'NONE', #68780, .T. ) ;
#73018=CARTESIAN_POINT ( 'NONE',  ( -30.00000000000000000, 461.8802764867013479, 14.89328939273681662 ) ) ;
#73040=CARTESIAN_POINT ( 'NONE',  ( -16.04053133235774808, 302.5635519178338768, -10.06124968053929436 ) ) ;
#73045=VERTEX_POINT ( 'NONE', #37860 ) ;
#73058=CARTESIAN_POINT ( 'NONE',  ( 44.30296249756166560, 485.3595172641092290, 2.292223182636803802 ) ) ;
#73059=CARTESIAN_POINT ( 'NONE',  ( -37.75731493300575181, 438.6148476127195863, 23.62858942192393386 ) ) ;
#73060=CARTESIAN_POINT ( 'NONE',  ( 24.83612219788692244, 304.4592009172700386, 10.29129484861557309 ) ) ;
#73061=CARTESIAN_POINT ( 'NONE',  ( -44.33586564007308795, 336.2641261982522565, -0.002537273210375349999 ) ) ;
#73063=CARTESIAN_POINT ( 'NONE',  ( -44.13666298176345038, 485.5987328015601179, 3.573899382266691127 ) ) ;
#73065=VERTEX_POINT ( 'NONE', #71759 ) ;
#73068=CARTESIAN_POINT ( 'NONE',  ( -46.00000000000000000, 500.0000000000002274, -5.000000000000001776 ) ) ;
#73069=CARTESIAN_POINT ( 'NONE',  ( -39.83118896912314000, 485.8577528566776209, -4.999724294280131431 ) ) ;
#73076=CARTESIAN_POINT ( 'NONE',  ( -32.94331731755182346, 463.6330061646623335, 6.942105804440992678 ) ) ;
#73083=CARTESIAN_POINT ( 'NONE',  ( -36.22417390465002285, 491.4095951024455076, 12.30556361669862042 ) ) ;
#73089=CARTESIAN_POINT ( 'NONE',  ( 18.20175014771579569, 303.6397678898111394, 9.891910565086597273 ) ) ;
#73090=VERTEX_POINT ( 'NONE', #45395 ) ;
#73102=CARTESIAN_POINT ( 'NONE',  ( -39.16821133293855439, 459.8632445465567571, 1.901232704179571575 ) ) ;
#73104=CARTESIAN_POINT ( 'NONE',  ( 44.00013453485157555, 465.7974093566498937, 11.65569858486426824 ) ) ;
#73127=CARTESIAN_POINT ( 'NONE',  ( 29.29475614497689762, 307.0157710316811404, -9.061019955416419691 ) ) ;
#73132=CARTESIAN_POINT ( 'NONE',  ( -45.29905483860081716, 480.9466865490944656, -2.171671249451534003 ) ) ;
#73133=VERTEX_POINT ( 'NONE', #49073 ) ;
#73142=CARTESIAN_POINT ( 'NONE',  ( -24.51502932331456108, 306.8928289099468998, 10.39682823628861108 ) ) ;
#73144=( BOUNDED_SURFACE ( )  B_SPLINE_SURFACE ( 3, 2, ( 
 ( #27657, #60530, #3336 ),
 ( #75620, #61052, #11943 ),
 ( #44872, #28709, #61591 ),
 ( #1724, #34675, #94487 ),
 ( #67547, #20642, #59461 ),
 ( #84252, #10349, #70191 ),
 ( #86925, #46962, #37865 ),
 ( #63711, #80388, #5968 ),
 ( #23251, #104674, #71242 ),
 ( #104140, #97109, #95020 ) ),
 .UNSPECIFIED., .F., .F., .T. ) 
 B_SPLINE_SURFACE_WITH_KNOTS ( ( 4, 2, 2, 2, 4 ),
 ( 3, 3 ),
 ( 0.006110147660070369691, 0.007140910106245465863, 0.008171672552420562036, 0.009202434998595659943, 0.01023319744477075612 ),
 ( 0.000000000000000000, 0.8503742053513317911 ),
 .UNSPECIFIED. ) 
 GEOMETRIC_REPRESENTATION_ITEM ( )  RATIONAL_B_SPLINE_SURFACE ( (
 ( 1.000000000000000000, 0.7509311617978130515, 0.9254657543235544903),
 ( 1.000000000000000000, 0.7661071201673247399, 0.9300071839847410260),
 ( 1.000000000000000000, 0.7795789861866246895, 0.9340386613018172302),
 ( 1.000000000000000000, 0.8013757198166023832, 0.9405613684820788301),
 ( 1.000000000000000000, 0.8096851085567824402, 0.9430479662686670483),
 ( 1.000000000000000000, 0.8194567880828296236, 0.9459721568969409189),
 ( 1.000000000000000000, 0.8208804111421099670, 0.9463981783599909603),
 ( 1.000000000000000000, 0.8160668081439683696, 0.9449577000125506387),
 ( 1.000000000000000000, 0.8098474096059313787, 0.9430965351155695675),
 ( 1.000000000000000000, 0.8002676374315798036, 0.9402297730672883880) ) ) 
 REPRESENTATION_ITEM ( '' )  SURFACE ( )  );
#73147=CARTESIAN_POINT ( 'NONE',  ( 31.22567349391626124, 439.6199880051409536, 23.21640098373832117 ) ) ;
#73154=CARTESIAN_POINT ( 'NONE',  ( 46.00000000000000000, 438.2642212955902323, 10.59429296198023707 ) ) ;
#73190=CARTESIAN_POINT ( 'NONE',  ( 42.69811214730273008, 434.9611672192513652, 18.34625614733207755 ) ) ;
#73196=COLOUR_RGB ( '', 0.72549020, 0.75294118, 0.79215686) ;
#73199=CARTESIAN_POINT ( 'NONE',  ( 38.54753914444563634, 311.7982143856372659, 5.994412429555442401 ) ) ;
#73202=EDGE_CURVE ( 'NONE', #88625, #75902, #7921, .T. ) ;
#73208=CARTESIAN_POINT ( 'NONE',  ( -40.53119313125447576, 460.3380581626501566, 2.322614769218545039 ) ) ;
#73215=CARTESIAN_POINT ( 'NONE',  ( -30.53534817441637017, 298.8129631075795487, 10.81987346015778328 ) ) ;
#73219=CARTESIAN_POINT ( 'NONE',  ( 5.281083960078516881, 298.2116408387686874, 8.506842287730004060 ) ) ;
#73226=FACE_OUTER_BOUND ( 'NONE', #10810, .T. ) ;
#73237=CARTESIAN_POINT ( 'NONE',  ( -31.35230430510937794, 438.7809062751878173, 22.96768963798378138 ) ) ;
#73242=CARTESIAN_POINT ( 'NONE',  ( 33.70841932975964994, 485.0774894644218875, 1.934193826885746814 ) ) ;
#73248=EDGE_CURVE ( 'NONE', #7327, #25681, #12197, .T. ) ;
#73251=CIRCLE ( 'NONE', #35511, 12.00000000000000711 ) ;
#73258=CIRCLE ( 'NONE', #6067, 0.9999999999999982236 ) ;
#73295=VERTEX_POINT ( 'NONE', #24839 ) ;
#73301=CARTESIAN_POINT ( 'NONE',  ( -9.614507834009854648, 294.6546879296599855, 9.895101348594113944 ) ) ;
#73307=CARTESIAN_POINT ( 'NONE',  ( -34.85314843810904506, 481.9552851365352808, 14.52865862526927643 ) ) ;
#73310=ORIENTED_EDGE ( 'NONE', *, *, #106544, .T. ) ;
#73312=CARTESIAN_POINT ( 'NONE',  ( -6.144719067894300224, 301.8764984594092198, -10.02047959687495826 ) ) ;
#73325=CARTESIAN_POINT ( 'NONE',  ( -30.98269412877740336, 314.5905989724842584, -6.678017073065344533 ) ) ;
#73334=CARTESIAN_POINT ( 'NONE',  ( -25.42905077590008744, 295.6753621798500262, -9.823388355175115549 ) ) ;
#73341=CARTESIAN_POINT ( 'NONE',  ( 29.36238239445474107, 323.3665426074553579, 13.50881304725993282 ) ) ;
#73344=DIRECTION ( 'NONE',  ( 0.000000000000000000, 0.000000000000000000, 1.000000000000000000 ) ) ;
#73353=FACE_BOUND ( 'NONE', #44570, .T. ) ;
#73372=DIRECTION ( 'NONE',  ( -1.000000000000000000, 0.000000000000000000, 0.000000000000000000 ) ) ;
#73388=CARTESIAN_POINT ( 'NONE',  ( 0.000000000000000000, 304.8518027762758038, -10.00000000000000355 ) ) ;
#73407=CARTESIAN_POINT ( 'NONE',  ( 30.00000000000000000, 462.0143252985375852, 13.78012569455009029 ) ) ;
#73414=AXIS2_PLACEMENT_3D ( 'NONE', #29343, #39533, #72410 ) ;
#73419=EDGE_LOOP ( 'NONE', ( #64819, #39785, #48994, #55804, #13932, #23369, #52073 ) ) ;
#73426=ORIENTED_EDGE ( 'NONE', *, *, #21549, .F. ) ;
#73447=CARTESIAN_POINT ( 'NONE',  ( 44.32955949053914679, 435.2565657989975421, 11.97827722465379097 ) ) ;
#73451=CARTESIAN_POINT ( 'NONE',  ( -30.87955015324946828, 351.7733141111877444, 20.67482462247657082 ) ) ;
#73453=CARTESIAN_POINT ( 'NONE',  ( -32.88333705524295425, 439.7317646416726689, 24.13381181826147781 ) ) ;
#73457=CARTESIAN_POINT ( 'NONE',  ( -30.50035377180213558, 337.4047871495883442, 16.76239630436412043 ) ) ;
#73463=CARTESIAN_POINT ( 'NONE',  ( -38.89974112662849137, 460.7404230935934493, 2.234279992752822963 ) ) ;
#73470=CARTESIAN_POINT ( 'NONE',  ( 32.10815921214906865, 435.9979227416979484, 24.01722067222687684 ) ) ;
#73502=CARTESIAN_POINT ( 'NONE',  ( -39.83282735953067544, 489.3954873304602415, 11.44298468960946025 ) ) ;
#73505=CARTESIAN_POINT ( 'NONE',  ( 32.99999999999999289, 439.7597899781498541, 24.16317522621305613 ) ) ;
#73518=CARTESIAN_POINT ( 'NONE',  ( 37.22405814379364841, 463.3230035706885701, 20.09439497145411124 ) ) ;
#73521=DIRECTION ( 'NONE',  ( 0.000000000000000000, 0.000000000000000000, -1.000000000000000000 ) ) ;
#73523=CARTESIAN_POINT ( 'NONE',  ( -35.76379064120181539, 307.0162303970107587, 12.81051142610679960 ) ) ;
#73525=CARTESIAN_POINT ( 'NONE',  ( -27.18908553330205180, 296.5274986157688772, 10.30015177545897842 ) ) ;
#73529=CARTESIAN_POINT ( 'NONE',  ( 30.20825430514037535, 310.0052099631511737, -8.578664711180536528 ) ) ;
#73537=CARTESIAN_POINT ( 'NONE',  ( 42.69811214730273718, 434.9611672192513652, 18.34625614733210242 ) ) ;
#73539=CARTESIAN_POINT ( 'NONE',  ( -33.49978038584191609, 465.4670364589441647, 16.54746596769432543 ) ) ;
#73543=CARTESIAN_POINT ( 'NONE',  ( -35.65219468668893654, 436.9652430364855036, 4.678245027582931925 ) ) ;
#73552=AXIS2_PLACEMENT_3D ( 'NONE', #14471, #61619, #44897 ) ;
#73571=CARTESIAN_POINT ( 'NONE',  ( 26.86604693904285668, 307.4841669554380701, -8.413536135732222476 ) ) ;
#73578=FACE_OUTER_BOUND ( 'NONE', #39023, .T. ) ;
#73583=CARTESIAN_POINT ( 'NONE',  ( -36.27064846733345860, 463.5381974806653602, 19.67843218035488562 ) ) ;
#73596=DIRECTION ( 'NONE',  ( 0.000000000000000000, 0.6935263888316357539, -0.7204312236391137159 ) ) ;
#73597=CARTESIAN_POINT ( 'NONE',  ( -43.74985542820371620, 435.5770091380364306, 16.96136490515579354 ) ) ;
#73598=CARTESIAN_POINT ( 'NONE',  ( -40.91188376428177520, 436.7570986683169281, 21.64372942866937422 ) ) ;
#73599=CARTESIAN_POINT ( 'NONE',  ( 32.54109659871799920, 344.3893346267446987, 19.67009027976686042 ) ) ;
#73600=CARTESIAN_POINT ( 'NONE',  ( -36.78952342955899724, 340.7883647611195670, -0.8934509747473148300 ) ) ;
#73602=CARTESIAN_POINT ( 'NONE',  ( -43.89153851290792829, 485.1215805105567824, -0.3742518171758901224 ) ) ;
#73608=AXIS2_PLACEMENT_3D ( 'NONE', #96181, #103205, #28286 ) ;
#73620=EDGE_CURVE ( 'NONE', #77744, #32226, #70870, .T. ) ;
#73624=CARTESIAN_POINT ( 'NONE',  ( -35.46673095357269290, 491.6344107835661816, 12.45081314981167786 ) ) ;
#73629=AXIS2_PLACEMENT_3D ( 'NONE', #69314, #51511, #52040 ) ;
#73642=CARTESIAN_POINT ( 'NONE',  ( -41.31945219041483597, 484.8187774037884878, -3.609221751577367243 ) ) ;
#73656=CARTESIAN_POINT ( 'NONE',  ( 36.19631612776407792, 463.3208255589806299, 20.09850791239177070 ) ) ;
#73671=CARTESIAN_POINT ( 'NONE',  ( 31.42582775662773642, 298.3612856942310145, -9.227187029712617061 ) ) ;
#73678=CARTESIAN_POINT ( 'NONE',  ( -21.23684446602553777, 304.9566545053270943, -9.977713076987676288 ) ) ;
#73689=CARTESIAN_POINT ( 'NONE',  ( -23.27911350275410030, 305.7949572072080286, 9.142907481312498419 ) ) ;
#73690=ORIENTED_EDGE ( 'NONE', *, *, #78838, .T. ) ;
#73714=CARTESIAN_POINT ( 'NONE',  ( 35.69739812508499455, 430.4862580793411553, 4.964222856391316441 ) ) ;
#73715=EDGE_LOOP ( 'NONE', ( #38694, #55291, #70877, #71705 ) ) ;
#73723=CARTESIAN_POINT ( 'NONE',  ( -30.00000000000000000, 500.0000000000002274, 0.000000000000000000 ) ) ;
#73733=CARTESIAN_POINT ( 'NONE',  ( -39.43334695255446576, 464.6962277817929134, 18.31103035469426388 ) ) ;
#73734=EDGE_CURVE ( 'NONE', #63037, #16979, #58089, .T. ) ;
#73738=ORIENTED_EDGE ( 'NONE', *, *, #43432, .F. ) ;
#73742=CARTESIAN_POINT ( 'NONE',  ( 28.87552933249129339, 311.5367771203828511, 12.02311567741501364 ) ) ;
#73744=CARTESIAN_POINT ( 'NONE',  ( 41.46910480218706851, 484.7338956289814860, -3.418960549715459596 ) ) ;
#73747=CARTESIAN_POINT ( 'NONE',  ( -41.54789589616743939, 460.8787123354538835, 2.862784844401427886 ) ) ;
#73750=EDGE_CURVE ( 'NONE', #54099, #17876, #99132, .T. ) ;
#73765=B_SPLINE_CURVE_WITH_KNOTS ( 'NONE', 3,
 ( #34072, #8689, #35130, #100356, #66945, #74479, #91750, #91231, #59392, #50212 ),
 .UNSPECIFIED., .F., .F.,
 ( 4, 2, 2, 2, 4 ),
 ( 0.000000000000000000, 0.001268689343002603895, 0.002537378686005207790, 0.003806068029007811902, 0.005074757372010415581 ),
 .UNSPECIFIED. ) ;
#73776=DIRECTION ( 'NONE',  ( 0.000000000000000000, -1.000000000000000000, 0.000000000000000000 ) ) ;
#73782=DIRECTION ( 'NONE',  ( 0.000000000000000000, 0.000000000000000000, -1.000000000000000000 ) ) ;
#73788=EDGE_LOOP ( 'NONE', ( #80291, #13213, #9902, #22653 ) ) ;
#73791=CARTESIAN_POINT ( 'NONE',  ( 32.85155332502863956, 463.8111683108725174, 7.359358840565810134 ) ) ;
#73792=CARTESIAN_POINT ( 'NONE',  ( -33.00000000000000000, 434.0826380246136296, 11.57835738278528659 ) ) ;
#73793=( BOUNDED_SURFACE ( )  B_SPLINE_SURFACE ( 3, 2, ( 
 ( #37752, #103504, #22628 ),
 ( #55981, #46337, #72200 ),
 ( #96484, #97002, #21554 ),
 ( #38784, #30711, #105104 ),
 ( #71651, #4816, #21045 ),
 ( #88392, #5352, #6385 ) ),
 .UNSPECIFIED., .F., .F., .F. ) 
 B_SPLINE_SURFACE_WITH_KNOTS ( ( 4, 2, 4 ),
 ( 3, 3 ),
 ( 0.06198440071626125369, 0.07559254306859702899, 0.08920068542093280428 ),
 ( 0.000000000000000000, 0.6299191188712893741 ),
 .UNSPECIFIED. ) 
 GEOMETRIC_REPRESENTATION_ITEM ( )  RATIONAL_B_SPLINE_SURFACE ( (
 ( 1.000000000000000000, 0.8155006202972323592, 0.8634406139837984551),
 ( 1.000000000000000000, 0.8155004682860759191, 0.8634405014709529702),
 ( 1.000000000000000000, 0.8155003797931379417, 0.8634404359718641508),
 ( 1.000000000000000000, 0.8155004189615391308, 0.8634404649628169004),
 ( 1.000000000000000000, 0.8155005447095090565, 0.8634405580366559807),
 ( 1.000000000000000000, 0.8155006922796284030, 0.8634406672624155288) ) ) 
 REPRESENTATION_ITEM ( '' )  SURFACE ( )  );
#73809=CARTESIAN_POINT ( 'NONE',  ( -2.256328376251533818, 294.8363286739503337, -9.758570717811821282 ) ) ;
#73818=ORIENTED_EDGE ( 'NONE', *, *, #86503, .T. ) ;
#73819=CARTESIAN_POINT ( 'NONE',  ( 32.16579691290905174, 416.1863149338369681, 25.51939566887129018 ) ) ;
#73840=CARTESIAN_POINT ( 'NONE',  ( -1.338640380347093206, 297.3185856424206008, -10.00123718159664321 ) ) ;
#73848=CARTESIAN_POINT ( 'NONE',  ( -12.23762156676873758, 302.5837270733004516, 9.880035066194738036 ) ) ;
#73870=CARTESIAN_POINT ( 'NONE',  ( -35.30859608300242058, 361.7926923559893453, 3.555634394399922904 ) ) ;
#73874=FACE_OUTER_BOUND ( 'NONE', #85986, .T. ) ;
#73877=CARTESIAN_POINT ( 'NONE',  ( -23.71817961469832525, 303.5093770010555545, -9.858623782581350525 ) ) ;
#73882=CARTESIAN_POINT ( 'NONE',  ( -39.95193705026029818, 335.6054456153876799, 19.72964827771248864 ) ) ;
#73893=FACE_OUTER_BOUND ( 'NONE', #103328, .T. ) ;
#73894=CARTESIAN_POINT ( 'NONE',  ( 33.74271564777244237, 484.1802673187708592, 2.058285076122321922 ) ) ;
#73908=CARTESIAN_POINT ( 'NONE',  ( 17.59729583105167094, 294.5991521133998390, -2.053319976387710799 ) ) ;
#73923=EDGE_CURVE ( 'NONE', #104224, #46568, #105272, .T. ) ;
#73925=AXIS2_PLACEMENT_3D ( 'NONE', #54723, #14268, #87658 ) ;
#73929=CARTESIAN_POINT ( 'NONE',  ( -12.08334041755991706, 304.5866437775407007, -10.05636128505472726 ) ) ;
#73930=CARTESIAN_POINT ( 'NONE',  ( 25.95507789760542039, 309.1386286255022924, 10.94030088463808070 ) ) ;
#73969=CARTESIAN_POINT ( 'NONE',  ( 44.25156094338286294, 463.6569123591601738, 7.442995203284897165 ) ) ;
#73973=CARTESIAN_POINT ( 'NONE',  ( -30.00000000000000355, 461.8163627757389236, 11.11111419090868857 ) ) ;
#73979=B_SPLINE_CURVE_WITH_KNOTS ( 'NONE', 3,
 ( #37854, #62120, #78789, #4922 ),
 .UNSPECIFIED., .F., .F.,
 ( 4, 4 ),
 ( 0.0007508562874606444218, 0.02095882498916069175 ),
 .UNSPECIFIED. ) ;
#73990=CARTESIAN_POINT ( 'NONE',  ( -42.52018344096930491, 435.0260445553154796, 8.239822296475871610 ) ) ;
#73993=CARTESIAN_POINT ( 'NONE',  ( -43.35041983548516953, 465.4837887082163093, 10.07799631915044358 ) ) ;
#74001=ADVANCED_FACE ( 'NONE', ( #26340 ), #25663, .T. ) ;
#74006=CIRCLE ( 'NONE', #84341, 15.00000000000000711 ) ;
#74008=CARTESIAN_POINT ( 'NONE',  ( 43.00000000000000711, 461.4080316921935605, 3.462976341553827719 ) ) ;
#74031=CARTESIAN_POINT ( 'NONE',  ( -33.07276483573667747, 438.9325140356154975, 23.89537236861306013 ) ) ;
#74041=CARTESIAN_POINT ( 'NONE',  ( -39.73996485276600055, 490.7364375727938750, 11.79908848420498302 ) ) ;
#74046=CARTESIAN_POINT ( 'NONE',  ( -36.59842210978563060, 438.2481675559515111, 3.880703544898892687 ) ) ;
#74054=CARTESIAN_POINT ( 'NONE',  ( 35.35823899438943840, 463.7178658455732148, 19.28807933140813446 ) ) ;
#74060=CARTESIAN_POINT ( 'NONE',  ( -40.17205142263708240, 310.2804317922712016, -6.358608209523628929 ) ) ;
#74063=CARTESIAN_POINT ( 'NONE',  ( 20.96800765626202789, 304.9222235596747623, -9.985031600492462189 ) ) ;
#74073=CARTESIAN_POINT ( 'NONE',  ( -43.43869229197127169, 464.9661605157749591, 13.42065392471462815 ) ) ;
#74074=CARTESIAN_POINT ( 'NONE',  ( 43.02621584241283870, 434.6128289108255558, 16.97888786058996402 ) ) ;
#74080=CARTESIAN_POINT ( 'NONE',  ( -36.22735294587202759, 437.9860357368660289, 4.211724321152335193 ) ) ;
#74100=ORIENTED_EDGE ( 'NONE', *, *, #78457, .F. ) ;
#74108=EDGE_CURVE ( 'NONE', #21702, #105760, #95055, .T. ) ;
#74112=CARTESIAN_POINT ( 'NONE',  ( 36.69990213913942512, 461.9654235716706694, 3.159576000644405358 ) ) ;
#74121=CARTESIAN_POINT ( 'NONE',  ( 30.00000000000155964, 464.1855333580207343, 13.92840612649013110 ) ) ;
#74134=CARTESIAN_POINT ( 'NONE',  ( 19.96162532426522773, 302.8116070918645164, 9.928455558879880627 ) ) ;
#74136=CARTESIAN_POINT ( 'NONE',  ( -37.00818793297098352, 345.1386355367852730, 0.03061739860943737609 ) ) ;
#74141=ORIENTED_EDGE ( 'NONE', *, *, #9619, .F. ) ;
#74144=CARTESIAN_POINT ( 'NONE',  ( 39.99565418590076860, 463.9333411592453444, 18.76875386499541776 ) ) ;
#74159=CARTESIAN_POINT ( 'NONE',  ( -35.43142158410745424, 491.1302584546127150, 12.10548931029582853 ) ) ;
#74161=B_SPLINE_CURVE_WITH_KNOTS ( 'NONE', 3,
 ( #29509, #37603, #47223, #38128, #69932, #21404, #102832, #86137, #54241, #45140 ),
 .UNSPECIFIED., .F., .F.,
 ( 4, 2, 2, 2, 4 ),
 ( 0.000000000000000000, 0.001637141140915473027, 0.003274282281830946054, 0.004911423422746419298, 0.006548564563661892109 ),
 .UNSPECIFIED. ) ;
#74171=EDGE_LOOP ( 'NONE', ( #72135, #60209, #106377, #48258, #89127, #70525 ) ) ;
#74202=CARTESIAN_POINT ( 'NONE',  ( 26.64323232996463631, 304.7933454163547253, -9.574263947122538809 ) ) ;
#74208=CARTESIAN_POINT ( 'NONE',  ( -35.44563196690202744, 355.0508310518326311, 1.542887188894044526 ) ) ;
#74209=ORIENTED_EDGE ( 'NONE', *, *, #58751, .T. ) ;
#74210=CARTESIAN_POINT ( 'NONE',  ( 44.11331465659122131, 485.7406967462466696, 4.043683577888340430 ) ) ;
#74214=CARTESIAN_POINT ( 'NONE',  ( -42.31104777394613592, 465.8656652864358421, 14.28483731023798065 ) ) ;
#74237=CARTESIAN_POINT ( 'NONE',  ( 38.26404824536036386, 461.1055978787671847, 2.389911169387158196 ) ) ;
#74246=CARTESIAN_POINT ( 'NONE',  ( 40.95420997525301487, 387.0967036739339164, 27.26945002580065136 ) ) ;
#74249=CARTESIAN_POINT ( 'NONE',  ( -38.51502786940007184, 460.0233756673457606, 2.043034587342192676 ) ) ;
#74261=EDGE_CURVE ( 'NONE', #46619, #1725, #82542, .T. ) ;
#74267=CARTESIAN_POINT ( 'NONE',  ( -41.59749957395938225, 465.5821881718248392, 15.80727685357802947 ) ) ;
#74268=CARTESIAN_POINT ( 'NONE',  ( -31.42024686275397727, 416.1372461024106428, 24.31832120901086469 ) ) ;
#74270=ORIENTED_EDGE ( 'NONE', *, *, #35028, .F. ) ;
#74274=DIRECTION ( 'NONE',  ( 0.000000000000000000, 0.000000000000000000, 1.000000000000000000 ) ) ;
#74277=CARTESIAN_POINT ( 'NONE',  ( 24.72051274681640010, 304.3800740200679797, 10.27342727648563603 ) ) ;
#74286=CARTESIAN_POINT ( 'NONE',  ( -22.02746468779565348, 303.1977850725832582, 10.01134046771178099 ) ) ;
#74294=CARTESIAN_POINT ( 'NONE',  ( 8.577352724654989657, 295.3685542829744008, 5.149687988174879827 ) ) ;
#74298=EDGE_LOOP ( 'NONE', ( #28106, #86923, #83943, #103651 ) ) ;
#74307=CIRCLE ( 'NONE', #58790, 5.000000000000001776 ) ;
#74316=FACE_OUTER_BOUND ( 'NONE', #93284, .T. ) ;
#74328=ORIENTED_EDGE ( 'NONE', *, *, #11277, .T. ) ;
#74339=CARTESIAN_POINT ( 'NONE',  ( -8.232252328884545278, 294.6936158193711321, -5.684270446938944232 ) ) ;
#74345=CARTESIAN_POINT ( 'NONE',  ( 31.22166362330205658, 392.4804080715629766, 25.19617774411732469 ) ) ;
#74348=EDGE_LOOP ( 'NONE', ( #10879, #40373, #4372, #13901 ) ) ;
#74356=DIRECTION ( 'NONE',  ( 0.000000000000000000, 0.000000000000000000, 1.000000000000000000 ) ) ;
#74363=CARTESIAN_POINT ( 'NONE',  ( -1.050160786985519401, 296.8373249700017595, -10.00076906402484056 ) ) ;
#74365=EDGE_LOOP ( 'NONE', ( #105607, #29474, #95926, #29402, #85940, #16981 ) ) ;
#74372=CARTESIAN_POINT ( 'NONE',  ( -17.24530556510137913, 294.5883485050384252, 1.881388368280897394 ) ) ;
#74376=CARTESIAN_POINT ( 'NONE',  ( -37.52432843440377042, 473.0043530063420576, 17.54905768162751656 ) ) ;
#74384=CIRCLE ( 'NONE', #55445, 8.000000000000014211 ) ;
#74394=CARTESIAN_POINT ( 'NONE',  ( -31.63428818830020006, 313.0192821382818806, -7.834016845888556624 ) ) ;
#74397=CARTESIAN_POINT ( 'NONE',  ( -43.99245308601258841, 435.4957624057696535, 9.973844990784979103 ) ) ;
#74400=CARTESIAN_POINT ( 'NONE',  ( -24.02662587718601728, 303.6064254585912181, -9.837495461294045285 ) ) ;
#74404=B_SPLINE_CURVE_WITH_KNOTS ( 'NONE', 3,
 ( #99538, #276, #15975, #1361 ),
 .UNSPECIFIED., .F., .F.,
 ( 4, 4 ),
 ( 0.000000000000000000, 0.001739938677309369732 ),
 .UNSPECIFIED. ) ;
#74407=CARTESIAN_POINT ( 'NONE',  ( -35.40631554953355931, 484.3223335191826777, -1.491095299259842077 ) ) ;
#74408=CARTESIAN_POINT ( 'NONE',  ( -39.77306975198764860, 332.5681192115835643, 19.05727885500202845 ) ) ;
#74419=CARTESIAN_POINT ( 'NONE',  ( 43.49684453862397504, 485.4584183652858655, 3.971660685822626213 ) ) ;
#74425=FACE_OUTER_BOUND ( 'NONE', #17647, .T. ) ;
#74436=CARTESIAN_POINT ( 'NONE',  ( 24.41215030396864449, 295.4555635972245682, -1.870474547456364878 ) ) ;
#74437=CARTESIAN_POINT ( 'NONE',  ( 0.000000000000000000, 0.000000000000000000, 0.000000000000000000 ) ) ;
#74458=CARTESIAN_POINT ( 'NONE',  ( -31.96671797320371766, 484.9925651024506692, 5.143045411170144909 ) ) ;
#74460=CARTESIAN_POINT ( 'NONE',  ( 35.76320840016588676, 388.4727839510825333, 5.610592865731860002 ) ) ;
#74471=VERTEX_POINT ( 'NONE', #47634 ) ;
#74473=STYLED_ITEM ( 'NONE', ( #14325 ), #31828 ) ;
#74479=CARTESIAN_POINT ( 'NONE',  ( 43.63014793319424456, 464.1804522840816389, 6.475900273557109621 ) ) ;
#74481=CARTESIAN_POINT ( 'NONE',  ( -43.86555507693260836, 486.1044689237326679, 5.341991804863218007 ) ) ;
#74489=ORIENTED_EDGE ( 'NONE', *, *, #84212, .F. ) ;
#74508=CARTESIAN_POINT ( 'NONE',  ( -35.38683386460204616, 303.0231846730247867, -0.1303635103169306364 ) ) ;
#74515=ORIENTED_EDGE ( 'NONE', *, *, #6512, .T. ) ;
#74516=CARTESIAN_POINT ( 'NONE',  ( 43.99245308600651327, 435.4957624057694261, 9.973844990776925101 ) ) ;
#74519=FACE_OUTER_BOUND ( 'NONE', #70601, .T. ) ;
#74520=CARTESIAN_POINT ( 'NONE',  ( 40.77380256327629837, 468.8478597483947965, 21.13608272249925690 ) ) ;
#74533=CARTESIAN_POINT ( 'NONE',  ( -38.85838710091159953, 485.2519636814003547, -4.251885899892715592 ) ) ;
#74535=ADVANCED_FACE ( 'NONE', ( #4812 ), #60566, .T. ) ;
#74548=B_SPLINE_CURVE_WITH_KNOTS ( 'NONE', 3,
 ( #79422, #64320, #37951, #15214, #81003, #79944, #89646, #23337, #103703, #105295, #72907, #63260, #22815, #14142, #64838, #105817, #46010, #5017, #13614, #5537, #71854, #29850, #88586, #62727, #6054, #38462, #104222, #30369, #96151, #22284, #55133, #16276, #74508, #25479, #57253, #15748, #32498, #98779, #34102, #83143, #16823, #24931, #24414, #57783, #585, #9240, #98261, #65368 ),
 .UNSPECIFIED., .F., .F.,
 ( 4, 2, 2, 2, 2, 2, 2, 2, 2, 2, 2, 2, 2, 2, 2, 2, 2, 2, 2, 2, 2, 2, 2, 4 ),
 ( 0.0007293822660806825427, 0.01952279057336408011, 0.03831619888064748125, 0.05710960718793087892, 0.06650631134157250490, 0.07590301549521411006, 0.08529971964885574298, 0.09469642380249734814, 0.1040931279561389672, 0.1134898321097805723, 0.1181881841866014582, 0.1228865362634223579, 0.1252357123018327245, 0.1275848883402430911, 0.1322832404170639631, 0.1334578284362692435, 0.1346324164554744685, 0.1369815924938849461, 0.1393307685322954514, 0.1405053565515007596, 0.1416799445707060401, 0.1440291206091167397, 0.1463782966475274394, 0.1510766487243488110 ),
 .UNSPECIFIED. ) ;
#74558=CARTESIAN_POINT ( 'NONE',  ( 0.000000000000000000, 0.000000000000000000, -4.999999999999999112 ) ) ;
#74561=CARTESIAN_POINT ( 'NONE',  ( -30.39986296867173365, 318.3104204385729190, 13.73210969081261013 ) ) ;
#74566=CARTESIAN_POINT ( 'NONE',  ( -1.128087032575124216, 302.6811185911183770, 9.936167251361171182 ) ) ;
#74571=DIRECTION ( 'NONE',  ( -0.000000000000000000, -1.000000000000000000, -0.000000000000000000 ) ) ;
#74573=CARTESIAN_POINT ( 'NONE',  ( 36.49542067541441526, 439.4713014004300362, 23.89653312818885311 ) ) ;
#74586=CARTESIAN_POINT ( 'NONE',  ( 35.72584807339057988, 463.6218724463090552, 19.50045127627888775 ) ) ;
#74589=CARTESIAN_POINT ( 'NONE',  ( 13.69035610859369889, 302.5483965847918739, 9.872518234831204609 ) ) ;
#74593=CARTESIAN_POINT ( 'NONE',  ( -40.88293604215247967, 432.5779639752643675, 26.56799667982232549 ) ) ;
#74597=CARTESIAN_POINT ( 'NONE',  ( 26.45606761501369064, 305.8501895426643387, -9.560627638420045926 ) ) ;
#74635=AXIS2_PLACEMENT_3D ( 'NONE', #10729, #52258, #18333 ) ;
#74638=CARTESIAN_POINT ( 'NONE',  ( 33.54694104246176778, 327.2920069512696273, -3.491838498529484802 ) ) ;
#74643=CARTESIAN_POINT ( 'NONE',  ( 18.75165323930665906, 302.6701165016055484, -10.03850434714902740 ) ) ;
#74644=CARTESIAN_POINT ( 'NONE',  ( -17.59839952628324511, 294.5991929880352700, -2.053311126443894352 ) ) ;
#74646=CARTESIAN_POINT ( 'NONE',  ( -36.98821436528694306, 463.5274861635123216, 19.70078135306431477 ) ) ;
#74657=CARTESIAN_POINT ( 'NONE',  ( 34.16642289233210050, 463.8422268500519863, 18.98106911353328385 ) ) ;
#74662=CARTESIAN_POINT ( 'NONE',  ( -39.28789537393542020, 311.9693088241641021, 2.089465571748127637 ) ) ;
#74665=FACE_OUTER_BOUND ( 'NONE', #19883, .T. ) ;
#74671=AXIS2_PLACEMENT_3D ( 'NONE', #43820, #76713, #12504 ) ;
#74683=VERTEX_POINT ( 'NONE', #66765 ) ;
#74686=CARTESIAN_POINT ( 'NONE',  ( -37.83989825151990516, 491.6297408768480750, 12.44743998624971759 ) ) ;
#74694=CARTESIAN_POINT ( 'NONE',  ( -19.07845090537422550, 294.6331628770684574, 9.890526070132905190 ) ) ;
#74723=B_SPLINE_SURFACE_WITH_KNOTS ( 'NONE', 1, 3, ( 
 ( #43745, #93371, #36762, #61550, #94443, #52358, #50749, #83654, #9768, #75578, #2743, #35698, #1674, #34633, #97455, #80744, #48898, #32767, #86361, #30641, #53439, #65639, #32222, #105041, #88855, #56996, #31182, #65102 ),
 ( #96427, #24152, #71588, #81793, #106617, #105558, #23611, #63529, #89911, #81270, #22562, #16019, #56463, #96942, #31697, #97999, #55400, #7918, #64584, #40296, #89394, #40821, #15488, #73714, #48376, #20602, #12425, #39784 ) ),
 .UNSPECIFIED., .F., .F., .F.,
 ( 2, 2 ),
 ( 4, 2, 2, 2, 2, 2, 2, 2, 2, 2, 2, 2, 2, 4 ),
 ( 0.000000000000000000, 1.000000000000000000 ),
 ( 0.08901491201581737678, 0.1032490540155679704, 0.1174831960153185778, 0.1317173380150691853, 0.1459514800148197788, 0.1744197640143299588, 0.2028880480138401388, 0.2598246160128514504, 0.3167611840118632616, 0.4306343200098861623, 0.5445074560079088410, 0.6583805920059359051, 0.7722537280039543095, 1.000000000000000000 ),
 .UNSPECIFIED. ) ;
#74731=CARTESIAN_POINT ( 'NONE',  ( 28.36261055972402190, 306.0659664076646891, -9.283380716933603338 ) ) ;
#74738=DIRECTION ( 'NONE',  ( -1.000000000000000000, -0.000000000000000000, -0.000000000000000000 ) ) ;
#74741=CARTESIAN_POINT ( 'NONE',  ( -36.41079454256560410, 485.4442866794553879, -3.629012552424295102 ) ) ;
#74744=CARTESIAN_POINT ( 'NONE',  ( 43.10371592040115019, 462.6168321841718125, 4.970041475426357991 ) ) ;
#74747=CIRCLE ( 'NONE', #12771, 0.9999999999999991118 ) ;
#74751=CARTESIAN_POINT ( 'NONE',  ( 31.00808149270786274, 439.2166318629403463, 22.50860008698266057 ) ) ;
#74756=FACE_OUTER_BOUND ( 'NONE', #85232, .T. ) ;
#74762=DIRECTION ( 'NONE',  ( 0.000000000000000000, 0.000000000000000000, 1.000000000000000000 ) ) ;
#74769=CARTESIAN_POINT ( 'NONE',  ( 31.21759734847655210, 387.2566916973277671, 24.99345285570965913 ) ) ;
#74772=CARTESIAN_POINT ( 'NONE',  ( -30.00000000000000355, 487.5660443506044999, 6.762394459359180487 ) ) ;
#74778=DIRECTION ( 'NONE',  ( -0.000000000000000000, -1.000000000000000000, -0.000000000000000000 ) ) ;
#74780=EDGE_CURVE ( 'NONE', #29420, #96657, #74384, .T. ) ;
#74792=CARTESIAN_POINT ( 'NONE',  ( -38.06223451516787293, 464.2386140055725718, 19.21930428800968471 ) ) ;
#74793=CARTESIAN_POINT ( 'NONE',  ( -31.36907691194473813, 433.8632848466868381, 23.03436070161451710 ) ) ;
#74800=CARTESIAN_POINT ( 'NONE',  ( 33.01607209031806178, 301.6304077285213907, 11.48551711194975766 ) ) ;
#74803=CARTESIAN_POINT ( 'NONE',  ( -41.50820411079211425, 461.5963371455321180, 2.703439750996433855 ) ) ;
#74805=EDGE_CURVE ( 'NONE', #89689, #234, #106783, .T. ) ;
#74809=CARTESIAN_POINT ( 'NONE',  ( -24.97007374329429652, 295.7209793996028111, 10.12394817307690786 ) ) ;
#74810=DIRECTION ( 'NONE',  ( 0.000000000000000000, 0.000000000000000000, 1.000000000000000000 ) ) ;
#74813=CARTESIAN_POINT ( 'NONE',  ( 33.67444716837015761, 489.3309112354451713, 10.55021651976789521 ) ) ;
#74815=CARTESIAN_POINT ( 'NONE',  ( 4.395101463923444918, 299.0276004806994479, 8.996626958117586170 ) ) ;
#74834=EDGE_CURVE ( 'NONE', #61960, #79974, #5187, .T. ) ;
#74854=CARTESIAN_POINT ( 'NONE',  ( 39.83456023769738863, 489.3941229067897325, 11.44194699760926603 ) ) ;
#74865=CARTESIAN_POINT ( 'NONE',  ( 31.22086979617878910, 398.3983149021029249, 25.40418687235769113 ) ) ;
#74873=CARTESIAN_POINT ( 'NONE',  ( 43.52075891743746894, 484.7805561108181109, 4.063293749111048569 ) ) ;
#74886=CARTESIAN_POINT ( 'NONE',  ( 35.68327731609498699, 437.0250969216240264, 4.635559385101182706 ) ) ;
#74888=CARTESIAN_POINT ( 'NONE',  ( -2.469322996728156472, 298.9266300818543414, -10.00398374146220171 ) ) ;
#74897=CARTESIAN_POINT ( 'NONE',  ( -17.64534493868312026, 294.6036102501091705, 9.884244339924812550 ) ) ;
#74898=CIRCLE ( 'NONE', #30138, 0.9999999999999997780 ) ;
#74901=CARTESIAN_POINT ( 'NONE',  ( 37.67950550371620722, 491.6872717898539236, 12.48612654750107964 ) ) ;
#74904=B_SPLINE_CURVE_WITH_KNOTS ( 'NONE', 3,
 ( #62820, #95713, #56130, #66926, #91731, #59372, #1075, #24883 ),
 .UNSPECIFIED., .F., .F.,
 ( 4, 2, 2, 4 ),
 ( 4.429863980152083197E-29, 0.01011967574619566934, 0.01517951361929350575, 0.02023935149239133868 ),
 .UNSPECIFIED. ) ;
#74906=ORIENTED_EDGE ( 'NONE', *, *, #65291, .F. ) ;
#74910=ORIENTED_EDGE ( 'NONE', *, *, #67614, .F. ) ;
#74917=CARTESIAN_POINT ( 'NONE',  ( -31.48659109300052350, 438.9656692063605306, 23.23080034282737927 ) ) ;
#74919=CARTESIAN_POINT ( 'NONE',  ( -31.19706370536868434, 315.2691834397311368, -6.507072380722979332 ) ) ;
#74921=( BOUNDED_SURFACE ( )  B_SPLINE_SURFACE ( 3, 2, ( 
 ( #22975, #56886, #31081 ),
 ( #6215, #96847, #73063 ),
 ( #15380, #72032, #89813 ),
 ( #47209, #14840, #97890 ),
 ( #13777, #81167, #80636 ),
 ( #23506, #63960, #40185 ),
 ( #56350, #15913, #96327 ),
 ( #72553, #22454, #73602 ),
 ( #48791, #62893, #14305 ),
 ( #80111, #104386, #30536 ) ),
 .UNSPECIFIED., .F., .F., .F. ) 
 B_SPLINE_SURFACE_WITH_KNOTS ( ( 4, 2, 2, 2, 4 ),
 ( 3, 3 ),
 ( 0.007162312563335121278, 0.008169815727932031035, 0.009177318892528939925, 0.01018482205712584882, 0.01119232522172275771 ),
 ( 0.000000000000000000, 0.8513194332817035637 ),
 .UNSPECIFIED. ) 
 GEOMETRIC_REPRESENTATION_ITEM ( )  RATIONAL_B_SPLINE_SURFACE ( (
 ( 1.000000000000000000, 0.7967391679699951101, 0.9395581286042928859),
 ( 1.000000000000000000, 0.8061132416517035049, 0.9423456137792036724),
 ( 1.000000000000000000, 0.8123079594501175782, 0.9441876820850600982),
 ( 1.000000000000000000, 0.8173936710915957748, 0.9456999750631016610),
 ( 1.000000000000000000, 0.8162642092137375460, 0.9453641169989284165),
 ( 1.000000000000000000, 0.8072284251113268638, 0.9426772259967470813),
 ( 1.000000000000000000, 0.7993563690608861405, 0.9403363824871115995),
 ( 1.000000000000000000, 0.7784392998177147582, 0.9341164590687904834),
 ( 1.000000000000000000, 0.7654114976929390357, 0.9302424970627795053),
 ( 1.000000000000000000, 0.7506543109476874198, 0.9258542832858760452) ) ) 
 REPRESENTATION_ITEM ( '' )  SURFACE ( )  );
#74928=CARTESIAN_POINT ( 'NONE',  ( -29.06849802192348875, 297.2210473627602028, -1.482792297568717776 ) ) ;
#74935=CARTESIAN_POINT ( 'NONE',  ( -31.72164027590077140, 329.7834567237236456, 16.51415323402584434 ) ) ;
#74946=AXIS2_PLACEMENT_3D ( 'NONE', #44626, #62399, #70485 ) ;
#74950=CARTESIAN_POINT ( 'NONE',  ( 42.80559098686211428, 434.8801202229377623, 8.726134940903639503 ) ) ;
#74973=CARTESIAN_POINT ( 'NONE',  ( 37.29743189577540363, 437.4067884073982100, 4.451016994670380811 ) ) ;
#74986=CARTESIAN_POINT ( 'NONE',  ( 41.70256300459691090, 461.0340457114389778, 3.032228049028132588 ) ) ;
#74993=VERTEX_POINT ( 'NONE', #65567 ) ;
#74995=EDGE_CURVE ( 'NONE', #94269, #45028, #1318, .T. ) ;
#74996=CARTESIAN_POINT ( 'NONE',  ( 42.19180677453719142, 462.2931784592651638, 3.389262873192005809 ) ) ;
#75005=CARTESIAN_POINT ( 'NONE',  ( 43.74985542820358830, 435.5770091380369422, 16.96136490515564788 ) ) ;
#75010=ORIENTED_EDGE ( 'NONE', *, *, #6744, .F. ) ;
#75024=ADVANCED_FACE ( 'NONE', ( #98454 ), #24545, .F. ) ;
#75025=CARTESIAN_POINT ( 'NONE',  ( -37.85084083633361018, 437.2249973798734004, 3.569182825063079711 ) ) ;
#75029=CARTESIAN_POINT ( 'NONE',  ( -30.00000000000000355, 461.8665156241398222, 11.40533150091695447 ) ) ;
#75036=DIRECTION ( 'NONE',  ( 0.2107607412267715197, 0.000000000000000000, 0.9775376770015271610 ) ) ;
#75038=CARTESIAN_POINT ( 'NONE',  ( 43.62838954006687686, 434.9736691849527688, 14.34345830637867891 ) ) ;
#75041=CARTESIAN_POINT ( 'NONE',  ( 0.000000000000000000, 300.0000000000000000, 0.000000000000000000 ) ) ;
#75042=CARTESIAN_POINT ( 'NONE',  ( 37.04388863813380794, 311.3287000699716032, 13.89786840526617517 ) ) ;
#75047=AXIS2_PLACEMENT_3D ( 'NONE', #64043, #23054, #56974 ) ;
#75057=CARTESIAN_POINT ( 'NONE',  ( -34.73928773455866548, 485.6865460664022294, -2.860109793110690912 ) ) ;
#75059=B_SPLINE_CURVE_WITH_KNOTS ( 'NONE', 3,
 ( #25760, #42418, #49974, #18168 ),
 .UNSPECIFIED., .F., .F.,
 ( 4, 4 ),
 ( 5.204170427930421283E-18, 0.0002767692171812351329 ),
 .UNSPECIFIED. ) ;
#75065=CARTESIAN_POINT ( 'NONE',  ( 24.60836828936892928, 305.5564293789130943, 10.31529206589142156 ) ) ;
#75081=CARTESIAN_POINT ( 'NONE',  ( -26.96904186675336490, 306.9427295668461397, 10.87987742757496612 ) ) ;
#75086=CARTESIAN_POINT ( 'NONE',  ( -1.918307803942188361, 301.4527163651389401, 9.816892514603376085 ) ) ;
#75091=CARTESIAN_POINT ( 'NONE',  ( 21.29975379448946171, 294.8969325209483259, -1.990407376643353210 ) ) ;
#75101=TOROIDAL_SURFACE ( 'NONE', #30332, 12.00000000000000711, 3.000000000000000000 ) ;
#75103=CARTESIAN_POINT ( 'NONE',  ( -30.00000000000001066, 464.2325109574570092, 15.22807244442123498 ) ) ;
#75108=CARTESIAN_POINT ( 'NONE',  ( 31.17406065558679629, 437.9984601485548978, 21.19262156861901403 ) ) ;
#75116=VECTOR ( 'NONE', #33259, 1000.000000000000000 ) ;
#75123=ORIENTED_EDGE ( 'NONE', *, *, #71088, .T. ) ;
#75130=CARTESIAN_POINT ( 'NONE',  ( 7.347880794884116778E-16, 70.00000000000000000, 5.999999999999998224 ) ) ;
#75133=EDGE_CURVE ( 'NONE', #55140, #34982, #105495, .T. ) ;
#75136=CARTESIAN_POINT ( 'NONE',  ( -35.45036406932465667, 436.3203772529668640, 5.179456583037453044 ) ) ;
#75146=ADVANCED_FACE ( 'NONE', ( #24081 ), #63470, .T. ) ;
#75147=DIRECTION ( 'NONE',  ( 0.000000000000000000, 0.000000000000000000, -1.000000000000000000 ) ) ;
#75161=DIRECTION ( 'NONE',  ( -0.9623543818480316814, 0.1986072300191289164, 0.1855511032627455981 ) ) ;
#75167=CARTESIAN_POINT ( 'NONE',  ( -32.67323224503967083, 485.6332095909901341, 6.597358449828222504 ) ) ;
#75168=ORIENTED_EDGE ( 'NONE', *, *, #40858, .F. ) ;
#75169=ORIENTED_EDGE ( 'NONE', *, *, #18587, .T. ) ;
#75173=CARTESIAN_POINT ( 'NONE',  ( -15.67167025678515913, 294.5587403484931883, -10.06229237371755048 ) ) ;
#75177=CARTESIAN_POINT ( 'NONE',  ( -37.56086443613940418, 463.3607749238124143, 20.02088289192456116 ) ) ;
#75195=CARTESIAN_POINT ( 'NONE',  ( -36.15856845288970334, 304.2561437961289244, 0.1683646767355131690 ) ) ;
#75196=DIRECTION ( 'NONE',  ( 1.000000000000000000, 0.000000000000000000, 0.000000000000000000 ) ) ;
#75199=CARTESIAN_POINT ( 'NONE',  ( -43.02621584241283870, 434.6128289108255558, 16.97888786058999244 ) ) ;
#75211=ORIENTED_EDGE ( 'NONE', *, *, #93690, .F. ) ;
#75217=CARTESIAN_POINT ( 'NONE',  ( -37.52420436161200712, 473.1127600448368185, 17.51444808554655097 ) ) ;
#75222=CARTESIAN_POINT ( 'NONE',  ( 43.18056654203890332, 485.1460802498596649, 5.477204712337894854 ) ) ;
#75227=CARTESIAN_POINT ( 'NONE',  ( -20.97754405179127346, 294.8763868968453608, 9.942224931492237516 ) ) ;
#75230=ORIENTED_EDGE ( 'NONE', *, *, #71198, .T. ) ;
#75234=CARTESIAN_POINT ( 'NONE',  ( 44.57115381837846257, 434.3516557708408641, 14.78613344168310562 ) ) ;
#75237=VERTEX_POINT ( 'NONE', #75785 ) ;
#75256=CARTESIAN_POINT ( 'NONE',  ( -42.47964311110575153, 356.5060619603087844, 15.81299726375038794 ) ) ;
#75258=ORIENTED_EDGE ( 'NONE', *, *, #5995, .F. ) ;
#75262=DIRECTION ( 'NONE',  ( 0.000000000000000000, -0.9137523047319339176, 0.4062717386147834953 ) ) ;
#75263=AXIS2_PLACEMENT_3D ( 'NONE', #72092, #13844, #45701 ) ;
#75266=CARTESIAN_POINT ( 'NONE',  ( 30.76801067634421116, 297.9428771719580027, -9.321789843264367548 ) ) ;
#75267=CARTESIAN_POINT ( 'NONE',  ( 40.17205142263708240, 310.2804317922712016, -6.358608209531249500 ) ) ;
#75283=CARTESIAN_POINT ( 'NONE',  ( -23.00081687371528716, 305.6505493688913475, 9.110661126385450004 ) ) ;
#75293=CARTESIAN_POINT ( 'NONE',  ( 46.00000000000000000, 436.1215487527605887, 10.84755050468337956 ) ) ;
#75299=CARTESIAN_POINT ( 'NONE',  ( 38.85446894546473828, 460.8903912184138676, 2.218456751109172398 ) ) ;
#75308=CARTESIAN_POINT ( 'NONE',  ( 31.00389226642222340, 485.8187364282109115, 14.27494812388583512 ) ) ;
#75323=EDGE_LOOP ( 'NONE', ( #49687, #5119, #103098, #32351 ) ) ;
#75327=CARTESIAN_POINT ( 'NONE',  ( -31.20656969146428139, 410.2463405114667125, 25.45169261709286701 ) ) ;
#75329=CIRCLE ( 'NONE', #82255, 1.000000000000003553 ) ;
#75330=ORIENTED_EDGE ( 'NONE', *, *, #60309, .T. ) ;
#75337=CARTESIAN_POINT ( 'NONE',  ( 27.19928665125400613, 307.3533174255223912, 10.98053163142592936 ) ) ;
#75347=CARTESIAN_POINT ( 'NONE',  ( -28.10757706655090260, 297.0759717083114992, 10.42362710127031455 ) ) ;
#75353=CARTESIAN_POINT ( 'NONE',  ( 34.26493447557741234, 490.0907185571251716, 11.27927472375406381 ) ) ;
#75354=CARTESIAN_POINT ( 'NONE',  ( 9.693872975896447031, 294.6517661903899352, 2.542797243357461046 ) ) ;
#75364=CARTESIAN_POINT ( 'NONE',  ( 41.50820411079202898, 461.5963371455317770, 2.703439750996501800 ) ) ;
#75379=CARTESIAN_POINT ( 'NONE',  ( -37.18119764942264283, 491.8021068614480669, 12.56169729800564561 ) ) ;
#75382=CARTESIAN_POINT ( 'NONE',  ( 43.51602118667805996, 463.0217781655570093, 9.924214466287779146 ) ) ;
#75384=AXIS2_PLACEMENT_3D ( 'NONE', #87019, #15226, #96166 ) ;
#75387=VERTEX_POINT ( 'NONE', #11568 ) ;
#75400=CARTESIAN_POINT ( 'NONE',  ( 43.00000000000000000, 461.4080316921935605, 3.462976341553837045 ) ) ;
#75405=CARTESIAN_POINT ( 'NONE',  ( -7.160168481740964985, 294.7244989119860747, -7.003737591215575264 ) ) ;
#75415=ORIENTED_EDGE ( 'NONE', *, *, #15126, .F. ) ;
#75416=CARTESIAN_POINT ( 'NONE',  ( 31.39562674014780796, 425.0116429153000581, 23.79458313699800698 ) ) ;
#75421=CARTESIAN_POINT ( 'NONE',  ( -43.41290683822509067, 487.0833545439620593, 7.569976829064873236 ) ) ;
#75426=CARTESIAN_POINT ( 'NONE',  ( -30.24427031855517711, 312.0196691915732004, -8.325478004009855937 ) ) ;
#75449=CARTESIAN_POINT ( 'NONE',  ( -35.97769258149595117, 482.2767054324580727, 15.66024800223706315 ) ) ;
#75451=ORIENTED_EDGE ( 'NONE', *, *, #29696, .F. ) ;
#75469=EDGE_CURVE ( 'NONE', #78207, #7327, #43725, .T. ) ;
#75477=CARTESIAN_POINT ( 'NONE',  ( -36.77630017244687366, 485.3194367660009902, -3.124714951674963270 ) ) ;
#75479=CARTESIAN_POINT ( 'NONE',  ( -40.24268529043574461, 341.6860726634804450, 21.00658913394816452 ) ) ;
#75485=COLOUR_RGB ( '', 0.08235294, 0.09019608, 0.10196078) ;
#75489=CARTESIAN_POINT ( 'NONE',  ( -38.53630335303979848, 439.2832101125267172, 23.70088186842717803 ) ) ;
#75507=CARTESIAN_POINT ( 'NONE',  ( 40.17205142263708240, 310.2804317922712016, -6.358608209523628929 ) ) ;
#75509=FACE_OUTER_BOUND ( 'NONE', #65527, .T. ) ;
#75517=CARTESIAN_POINT ( 'NONE',  ( 36.97266421100042066, 437.4722577376851973, 4.366281382753225415 ) ) ;
#75520=ORIENTED_EDGE ( 'NONE', *, *, #22484, .T. ) ;
#75524=ORIENTED_EDGE ( 'NONE', *, *, #86503, .F. ) ;
#75533=CARTESIAN_POINT ( 'NONE',  ( 37.54559764570182523, 464.1143081516207189, 19.43664670202678835 ) ) ;
#75534=CARTESIAN_POINT ( 'NONE',  ( 42.23079339798729848, 460.7352525929352964, 2.726051457480590745 ) ) ;
#75535=CARTESIAN_POINT ( 'NONE',  ( -33.97359119245064107, 434.1099241184709285, 11.80501937577160021 ) ) ;
#75548=CARTESIAN_POINT ( 'NONE',  ( 32.03352823755274414, 487.4857469360636060, 8.014200094826978926 ) ) ;
#75568=AXIS2_PLACEMENT_3D ( 'NONE', #8256, #49780, #51367 ) ;
#75577=CARTESIAN_POINT ( 'NONE',  ( -23.96375140441108442, 306.3052962357393199, 10.25885168886986243 ) ) ;
#75578=CARTESIAN_POINT ( 'NONE',  ( 25.95507789760542039, 309.1386286255022924, 10.94030088463808070 ) ) ;
#75588=CARTESIAN_POINT ( 'NONE',  ( 43.71217423904119670, 435.6632154632235938, 9.092528312217329045 ) ) ;
#75593=CARTESIAN_POINT ( 'NONE',  ( 39.13885763974980136, 324.4948203046521371, 17.18769520460729439 ) ) ;
#75600=CARTESIAN_POINT ( 'NONE',  ( -24.35993018935220533, 306.6204276456223852, 9.332123231157906318 ) ) ;
#75610=CARTESIAN_POINT ( 'NONE',  ( 42.36808196472509991, 461.6713445545159971, 3.771400599639967322 ) ) ;
#75611=CARTESIAN_POINT ( 'NONE',  ( 20.74847835458628964, 303.9423534201437747, 9.956307716536178631 ) ) ;
#75620=CARTESIAN_POINT ( 'NONE',  ( -46.00000000000000000, 460.1242873147282353, 6.750975842490332113 ) ) ;
#75625=CARTESIAN_POINT ( 'NONE',  ( 32.16914446836155861, 486.0693400665549007, 5.247150504716460162 ) ) ;
#75627=CARTESIAN_POINT ( 'NONE',  ( -33.13214351254949719, 379.6169617581111879, 24.74988620700858633 ) ) ;
#75628=CARTESIAN_POINT ( 'NONE',  ( -31.73507068214536631, 436.7267398747721359, 21.10082163792574406 ) ) ;
#75644=ADVANCED_FACE ( 'NONE', ( #33105 ), #52, .F. ) ;
#75645=FACE_OUTER_BOUND ( 'NONE', #70726, .T. ) ;
#75651=CARTESIAN_POINT ( 'NONE',  ( 32.42201911889981858, 435.8451540523121821, 18.25951462285809868 ) ) ;
#75656=AXIS2_PLACEMENT_3D ( 'NONE', #86436, #35229, #12500 ) ;
#75660=FACE_OUTER_BOUND ( 'NONE', #69172, .T. ) ;
#75664=ORIENTED_EDGE ( 'NONE', *, *, #24718, .T. ) ;
#75677=CARTESIAN_POINT ( 'NONE',  ( 32.09911992168216699, 438.9232547152094526, 23.66653216045977359 ) ) ;
#75683=VERTEX_POINT ( 'NONE', #41700 ) ;
#75687=VERTEX_POINT ( 'NONE', #90252 ) ;
#75696=CARTESIAN_POINT ( 'NONE',  ( 24.00188669994001600, 304.6317240716171000, -9.832141748992357932 ) ) ;
#75711=CARTESIAN_POINT ( 'NONE',  ( 35.41856067487186976, 369.9239349834528525, 4.703027911095471580 ) ) ;
#75722=CARTESIAN_POINT ( 'NONE',  ( 32.66167952490037152, 465.7843590037583112, 12.50185730157094888 ) ) ;
#75724=ORIENTED_EDGE ( 'NONE', *, *, #65298, .T. ) ;
#75729=CARTESIAN_POINT ( 'NONE',  ( 38.02740175684945001, 490.5688714813351226, 12.25042287455591428 ) ) ;
#75736=( NAMED_UNIT ( * ) SI_UNIT ( $, .STERADIAN. ) SOLID_ANGLE_UNIT ( ) );
#75737=DIRECTION ( 'NONE',  ( 0.000000000000000000, -0.9846968979781746123, 0.1742756985702836880 ) ) ;
#75740=CARTESIAN_POINT ( 'NONE',  ( -40.90488780024449511, 312.7491308540076602, -5.736144956087439795 ) ) ;
#75741=CARTESIAN_POINT ( 'NONE',  ( -6.812116597003051943, 304.7372916636546165, -10.02434008908077345 ) ) ;
#75744=EDGE_LOOP ( 'NONE', ( #79448, #72293, #29258, #13963, #22924 ) ) ;
#75754=CARTESIAN_POINT ( 'NONE',  ( 20.97754405179121662, 294.8763868968453608, 9.942224931492262385 ) ) ;
#75761=B_SPLINE_CURVE_WITH_KNOTS ( 'NONE', 3,
 ( #28078, #21055, #93838, #83213, #53893, #86824, #11839, #25556, #36705, #101400 ),
 .UNSPECIFIED., .F., .F.,
 ( 4, 2, 2, 2, 4 ),
 ( 0.000000000000000000, 0.001010458115798221809, 0.002020916231596442750, 0.003031374347394663257, 0.004041832463192884632 ),
 .UNSPECIFIED. ) ;
#75778=ADVANCED_FACE ( 'NONE', ( #94523 ), #32569, .F. ) ;
#75781=AXIS2_PLACEMENT_3D ( 'NONE', #19918, #103440, #78616 ) ;
#75785=CARTESIAN_POINT ( 'NONE',  ( -32.82691535583477105, 485.1045372766795367, 1.724905475514941999 ) ) ;
#75792=CARTESIAN_POINT ( 'NONE',  ( -43.21893375682410010, 435.1753267429568268, 16.08377476667729766 ) ) ;
#75794=CARTESIAN_POINT ( 'NONE',  ( -31.18468355460609942, 439.5714648327614782, 23.11716509955518006 ) ) ;
#75802=CARTESIAN_POINT ( 'NONE',  ( -40.93241935747697369, 325.6791013269530026, 9.457466926974674948 ) ) ;
#75806=CARTESIAN_POINT ( 'NONE',  ( -36.64884602963550009, 372.9174138272855998, 4.319931451223398611 ) ) ;
#75808=CARTESIAN_POINT ( 'NONE',  ( 43.50377727019363050, 435.9167426301696082, 18.24083946424737590 ) ) ;
#75810=CARTESIAN_POINT ( 'NONE',  ( 24.71680885386722792, 295.5449029855087701, -1.851325031251247699 ) ) ;
#75811=CARTESIAN_POINT ( 'NONE',  ( 35.59667163540026280, 463.9592197885497171, -0.04846191499040426731 ) ) ;
#75825=CARTESIAN_POINT ( 'NONE',  ( -20.05499119796240137, 304.8398979948669876, 9.934468975907650545 ) ) ;
#75829=CARTESIAN_POINT ( 'NONE',  ( 32.11826742321338202, 487.8588087913172444, 8.620620385260318486 ) ) ;
#75835=ORIENTED_EDGE ( 'NONE', *, *, #99395, .F. ) ;
#75854=CARTESIAN_POINT ( 'NONE',  ( -32.00531707493602340, 486.9465202150305458, 7.099108550606821666 ) ) ;
#75855=VERTEX_POINT ( 'NONE', #47526 ) ;
#75864=CARTESIAN_POINT ( 'NONE',  ( -31.21769207662248391, 336.6603772009976865, 17.83294671529322173 ) ) ;
#75870=CARTESIAN_POINT ( 'NONE',  ( -13.22953023205303857, 303.5546567990938343, 9.873837419613719746 ) ) ;
#75878=CARTESIAN_POINT ( 'NONE',  ( 33.00000000000000000, 435.0774731480752280, 11.67986145722084501 ) ) ;
#75879=CARTESIAN_POINT ( 'NONE',  ( 32.00486866709039901, 300.3058852649511437, 11.16929972234588853 ) ) ;
#75883=DIRECTION ( 'NONE',  ( 1.000000000000000000, 0.000000000000000000, 0.000000000000000000 ) ) ;
#75884=CARTESIAN_POINT ( 'NONE',  ( 27.28205084651333223, 296.4635464116785215, 2.286800737873711853 ) ) ;
#75888=ORIENTED_EDGE ( 'NONE', *, *, #52695, .T. ) ;
#75893=CARTESIAN_POINT ( 'NONE',  ( 34.84618260875178208, 489.9833681528626812, 11.97975507378821725 ) ) ;
#75899=CARTESIAN_POINT ( 'NONE',  ( 46.00000000000000000, 461.9428920847516906, 12.03309428281970206 ) ) ;
#75902=VERTEX_POINT ( 'NONE', #88537 ) ;
#75918=CARTESIAN_POINT ( 'NONE',  ( -34.59893540551257018, 491.2022546151288793, 12.15065315885553865 ) ) ;
#75935=CARTESIAN_POINT ( 'NONE',  ( -36.28675805325661230, 437.5816793914590903, 4.254145058677060831 ) ) ;
#75950=CARTESIAN_POINT ( 'NONE',  ( 27.54067839420761388, 314.0233244279185669, 12.16855529173855821 ) ) ;
#75960=CARTESIAN_POINT ( 'NONE',  ( -36.64823341582351901, 437.5392299810053487, 4.281405873620232505 ) ) ;
#75961=CARTESIAN_POINT ( 'NONE',  ( -27.97565635352651015, 315.9216507687758053, 12.64980990155120999 ) ) ;
#75969=ORIENTED_EDGE ( 'NONE', *, *, #17028, .T. ) ;
#75971=CARTESIAN_POINT ( 'NONE',  ( -9.371250387818031768, 295.2890354896795770, -10.04040834969037199 ) ) ;
#75972=EDGE_CURVE ( 'NONE', #9067, #81556, #51369, .T. ) ;
#75987=CARTESIAN_POINT ( 'NONE',  ( -46.00000000000000711, 435.9998667017527509, 13.49155791609234711 ) ) ;
#75996=CARTESIAN_POINT ( 'NONE',  ( 35.34137816767491103, 436.0137577674745444, 5.688536468115818145 ) ) ;
#75997=CARTESIAN_POINT ( 'NONE',  ( -20.98870079052705861, 304.9248738074109610, -9.984468272890918428 ) ) ;
#76007=CARTESIAN_POINT ( 'NONE',  ( -38.08476327432922659, 485.5431326501830540, -4.039650833747947978 ) ) ;
#76008=CARTESIAN_POINT ( 'NONE',  ( -40.91643043736473118, 378.4535619638084540, 26.47871939907729200 ) ) ;
#76021=CARTESIAN_POINT ( 'NONE',  ( -33.00000000000000000, 500.0000000000002274, 0.000000000000000000 ) ) ;
#76038=CARTESIAN_POINT ( 'NONE',  ( 28.84964340243799441, 297.0390576586646603, -1.524508641439632051 ) ) ;
#76059=CARTESIAN_POINT ( 'NONE',  ( 26.27902093981875709, 306.9027577142574614, -9.548073367147230428 ) ) ;
#76063=ORIENTED_EDGE ( 'NONE', *, *, #29696, .T. ) ;
#76067=CARTESIAN_POINT ( 'NONE',  ( -16.98784884574818577, 303.5779498825697829, -10.05824724361832168 ) ) ;
#76078=CARTESIAN_POINT ( 'NONE',  ( 36.87655955837855259, 438.2068510013161813, 3.933030107424693167 ) ) ;
#76083=AXIS2_PLACEMENT_3D ( 'NONE', #5348, #104554, #71129 ) ;
#76120=CARTESIAN_POINT ( 'NONE',  ( -43.04469050570867239, 434.7734435962895532, 9.248231035232469921 ) ) ;
#76137=CARTESIAN_POINT ( 'NONE',  ( 31.21850725759788503, 336.6757834771444777, 17.83627441276912151 ) ) ;
#76159=DIRECTION ( 'NONE',  ( -1.000000000000000000, -0.000000000000000000, -0.000000000000000000 ) ) ;
#76174=ADVANCED_FACE ( 'NONE', ( #103000 ), #36686, .T. ) ;
#76181=CARTESIAN_POINT ( 'NONE',  ( 32.65674990438940739, 434.9893739305006193, 13.53244902892662438 ) ) ;
#76189=AXIS2_PLACEMENT_3D ( 'NONE', #32656, #40708, #57411 ) ;
#76199=CARTESIAN_POINT ( 'NONE',  ( -45.40507512465600115, 439.2794387026467575, 6.273370203490043373 ) ) ;
#76204=CARTESIAN_POINT ( 'NONE',  ( -43.59756234217317683, 434.3244621007142996, 14.55946156040369921 ) ) ;
#76209=ORIENTED_EDGE ( 'NONE', *, *, #41219, .T. ) ;
#76222=AXIS2_PLACEMENT_3D ( 'NONE', #19446, #12350, #12877 ) ;
#76225=CARTESIAN_POINT ( 'NONE',  ( 32.54608566124238678, 315.7613049388691593, -7.144893715508695564 ) ) ;
#76234=CARTESIAN_POINT ( 'NONE',  ( 39.41219261697651177, 436.7611714244556538, 5.258763975274515445 ) ) ;
#76257=CARTESIAN_POINT ( 'NONE',  ( 39.41275501334703080, 489.7121233615675919, 11.67778311875517971 ) ) ;
#76268=CIRCLE ( 'NONE', #81403, 1.000000000000000888 ) ;
#76269=CARTESIAN_POINT ( 'NONE',  ( -37.17800977877799085, 306.1414503807761207, 0.6316131526643408156 ) ) ;
#76270=CARTESIAN_POINT ( 'NONE',  ( -13.56845119367292263, 303.5479323376442835, -10.06459098692300280 ) ) ;
#76273=CARTESIAN_POINT ( 'NONE',  ( -42.93430011344045738, 435.4574193744091986, 17.27214342660893465 ) ) ;
#76297=CARTESIAN_POINT ( 'NONE',  ( -36.64823341582350480, 437.5392299810052350, 4.281405873620236946 ) ) ;
#76300=DIRECTION ( 'NONE',  ( 1.000000000000000000, 0.000000000000000000, 0.000000000000000000 ) ) ;
#76302=FACE_OUTER_BOUND ( 'NONE', #56879, .T. ) ;
#76306=ORIENTED_EDGE ( 'NONE', *, *, #61923, .T. ) ;
#76307=DIRECTION ( 'NONE',  ( 0.000000000000000000, 0.000000000000000000, -1.000000000000000000 ) ) ;
#76311=CARTESIAN_POINT ( 'NONE',  ( 43.70848695378473536, 435.5669781845215311, 16.96397918787648607 ) ) ;
#76312=ORIENTED_EDGE ( 'NONE', *, *, #103018, .T. ) ;
#76315=CARTESIAN_POINT ( 'NONE',  ( -44.17836536378455037, 435.2619773020561524, 14.65562696767985074 ) ) ;
#76317=CARTESIAN_POINT ( 'NONE',  ( -32.03584064644572749, 439.7197644807975507, 23.90968771023494455 ) ) ;
#76323=( BOUNDED_SURFACE ( )  B_SPLINE_SURFACE ( 3, 2, ( 
 ( #689, #49812, #49269 ),
 ( #16382, #7750, #16934 ),
 ( #42787, #58447, #1778 ),
 ( #41195, #82716, #1232 ),
 ( #67607, #74080, #66533 ),
 ( #65476, #34202, #40660 ),
 ( #33653, #99407, #57894 ),
 ( #25589, #9336, #26130 ),
 ( #73543, #17470, #100486 ),
 ( #89758, #32605, #98366 ),
 ( #56834, #67074, #66000 ),
 ( #75136, #50859, #165 ) ),
 .UNSPECIFIED., .F., .F., .F. ) 
 B_SPLINE_SURFACE_WITH_KNOTS ( ( 4, 2, 2, 2, 2, 4 ),
 ( 3, 3 ),
 ( 5.421010862427522170E-19, 0.0004396180695635565935, 0.0008792361391271126449, 0.001758472278254224856, 0.002637708417381336851, 0.003516944556508449279 ),
 ( 0.000000000000000000, 1.000000000000000000 ),
 .UNSPECIFIED. ) 
 GEOMETRIC_REPRESENTATION_ITEM ( )  RATIONAL_B_SPLINE_SURFACE ( (
 ( 1.000000000000000000, 0.9193453746270702220, 1.000000000000000000),
 ( 1.000000000000000000, 0.9231392589453282227, 1.000000000000000000),
 ( 1.000000000000000000, 0.9252300355217707439, 1.000000000000000000),
 ( 1.000000000000000000, 0.9257136340830524057, 1.000000000000000000),
 ( 1.000000000000000000, 0.9240662039546210238, 1.000000000000000000),
 ( 1.000000000000000000, 0.9140412217422946295, 1.000000000000000000),
 ( 1.000000000000000000, 0.9005671153104095605, 1.000000000000000000),
 ( 1.000000000000000000, 0.8672639112272950701, 1.000000000000000000),
 ( 1.000000000000000000, 0.8470036231255452241, 1.000000000000000000),
 ( 1.000000000000000000, 0.8036658034632763181, 1.000000000000000000),
 ( 1.000000000000000000, 0.7801896332603067696, 1.000000000000000000),
 ( 1.000000000000000000, 0.7557288854856922811, 1.000000000000000000) ) ) 
 REPRESENTATION_ITEM ( '' )  SURFACE ( )  );
#76332=CARTESIAN_POINT ( 'NONE',  ( 23.66085433736493471, 295.2283149760944525, -9.919964171137618081 ) ) ;
#76333=CARTESIAN_POINT ( 'NONE',  ( 45.43339346675878687, 430.7348383325900727, 7.234598910837349628 ) ) ;
#76347=CARTESIAN_POINT ( 'NONE',  ( 31.30845532010006949, 439.0134050661394554, 22.67842551736903189 ) ) ;
#76355=ORIENTED_EDGE ( 'NONE', *, *, #78794, .T. ) ;
#76366=SURFACE_STYLE_FILL_AREA ( #8975 ) ;
#76372=CARTESIAN_POINT ( 'NONE',  ( -30.00000000000000355, 486.7182699440880356, 5.240683647336917161 ) ) ;
#76384=ORIENTED_EDGE ( 'NONE', *, *, #41028, .T. ) ;
#76385=ORIENTED_EDGE ( 'NONE', *, *, #94376, .T. ) ;
#76386=CARTESIAN_POINT ( 'NONE',  ( -32.81992448453854649, 465.7192846569213884, 11.17271167765305506 ) ) ;
#76390=CARTESIAN_POINT ( 'NONE',  ( -19.83463548332447601, 303.8035096162418540, 9.926734387303332241 ) ) ;
#76392=CARTESIAN_POINT ( 'NONE',  ( -31.22086652946737217, 398.4027782038555756, 25.40425845524832482 ) ) ;
#76399=CARTESIAN_POINT ( 'NONE',  ( 25.28412188507380165, 304.8344537246382515, 10.37783159469212357 ) ) ;
#76404=DIRECTION ( 'NONE',  ( 0.000000000000000000, 0.000000000000000000, -1.000000000000000000 ) ) ;
#76425=VERTEX_POINT ( 'NONE', #13432 ) ;
#76428=CARTESIAN_POINT ( 'NONE',  ( -46.00000000000000000, 459.9277931459707247, 6.461582622321701663 ) ) ;
#76440=CARTESIAN_POINT ( 'NONE',  ( -42.89416851001919895, 486.3091028888858887, 6.394136786226152225 ) ) ;
#76441=FACE_OUTER_BOUND ( 'NONE', #26424, .T. ) ;
#76454=CARTESIAN_POINT ( 'NONE',  ( 39.67350626972746142, 485.2175160376946224, -4.383017744911751556 ) ) ;
#76456=CARTESIAN_POINT ( 'NONE',  ( -36.19868307047016742, 437.5496401283068622, 4.275188479071593939 ) ) ;
#76463=SURFACE_STYLE_FILL_AREA ( #51657 ) ;
#76471=CARTESIAN_POINT ( 'NONE',  ( 25.69418243244179934, 306.7938479978786859, 10.60760969656614172 ) ) ;
#76475=EDGE_LOOP ( 'NONE', ( #106524, #49305, #42159, #72704, #101032 ) ) ;
#76489=CARTESIAN_POINT ( 'NONE',  ( -44.14911905790362567, 464.3766534541991291, 9.623404994943159707 ) ) ;
#76499=VERTEX_POINT ( 'NONE', #2967 ) ;
#76517=EDGE_LOOP ( 'NONE', ( #20290, #51480, #14253, #4645, #11673 ) ) ;
#76535=CARTESIAN_POINT ( 'NONE',  ( -34.82075917463970427, 344.3979323805427839, 0.4374665251995884518 ) ) ;
#76536=CARTESIAN_POINT ( 'NONE',  ( -34.73046204960461836, 304.6187811521189701, 12.21458540402294091 ) ) ;
#76563=CARTESIAN_POINT ( 'NONE',  ( 0.6295717893779785301, 294.8518027745081440, -10.00000000019932855 ) ) ;
#76564=CARTESIAN_POINT ( 'NONE',  ( 45.17824257314219949, 354.4244853104167987, 3.762393652172960845 ) ) ;
#76566=DIRECTION ( 'NONE',  ( 0.000000000000000000, 0.000000000000000000, -1.000000000000000000 ) ) ;
#76569=CARTESIAN_POINT ( 'NONE',  ( -11.82165952410163356, 294.5900423753296309, -10.05563889079273210 ) ) ;
#76573=B_SPLINE_CURVE_WITH_KNOTS ( 'NONE', 3,
 ( #27664, #77766, #86932, #44882 ),
 .UNSPECIFIED., .F., .F.,
 ( 4, 4 ),
 ( 0.0009266594673085438907, 0.02188556764208124394 ),
 .UNSPECIFIED. ) ;
#76599=CARTESIAN_POINT ( 'NONE',  ( -44.21332904831280075, 435.2494715644501753, 14.45449769377407101 ) ) ;
#76635=ADVANCED_FACE ( 'NONE', ( #16871 ), #8759, .T. ) ;
#76657=B_SPLINE_CURVE_WITH_KNOTS ( 'NONE', 3,
 ( #87518, #23321, #14127, #62712 ),
 .UNSPECIFIED., .F., .F.,
 ( 4, 4 ),
 ( 0.000000000000000000, 0.0007558628827966600407 ),
 .UNSPECIFIED. ) ;
#76660=ORIENTED_EDGE ( 'NONE', *, *, #41026, .T. ) ;
#76667=CARTESIAN_POINT ( 'NONE',  ( 31.59878246649166300, 345.3114421961439007, 19.61614401236478145 ) ) ;
#76677=FACE_OUTER_BOUND ( 'NONE', #11236, .T. ) ;
#76678=ORIENTED_EDGE ( 'NONE', *, *, #50717, .T. ) ;
#76683=ORIENTED_EDGE ( 'NONE', *, *, #79954, .T. ) ;
#76691=ORIENTED_EDGE ( 'NONE', *, *, #22998, .T. ) ;
#76692=B_SPLINE_CURVE_WITH_KNOTS ( 'NONE', 3,
 ( #33937, #100749, #51132, #26916, #51669, #44669, #3672, #53798, #38189, #52736, #95870, #86201, #29568, #62968, #21997, #54849 ),
 .UNSPECIFIED., .F., .F.,
 ( 4, 2, 2, 2, 2, 2, 2, 4 ),
 ( 4.213851856174009611E-17, 0.0003803734300660355032, 0.0007607468601320289394, 0.001141120290198022105, 0.001521493720264015595, 0.001901867150330008869, 0.002282240580396002142, 0.003042987440528005169 ),
 .UNSPECIFIED. ) ;
#76711=CARTESIAN_POINT ( 'NONE',  ( -33.33807306172103324, 464.2324349908527665, 17.97546588382418875 ) ) ;
#76713=DIRECTION ( 'NONE',  ( 1.081159191512680572E-15, -0.07486943176528189359, 0.9971933454386585627 ) ) ;
#76722=EDGE_CURVE ( 'NONE', #3187, #94269, #47531, .T. ) ;
#76746=ORIENTED_EDGE ( 'NONE', *, *, #106429, .F. ) ;
#76749=AXIS2_PLACEMENT_3D ( 'NONE', #45974, #71295, #39481 ) ;
#76766=CARTESIAN_POINT ( 'NONE',  ( 39.99946440396829672, 437.0919103049818091, 5.547728658186661832 ) ) ;
#76774=EDGE_LOOP ( 'NONE', ( #97592, #34994, #63952, #11098, #48473 ) ) ;
#76779=CARTESIAN_POINT ( 'NONE',  ( -43.35553785604018628, 484.2706869242194898, -0.02741892262543544484 ) ) ;
#76780=CARTESIAN_POINT ( 'NONE',  ( -33.76105693399936314, 471.3091059247023509, 5.717665057388538585 ) ) ;
#76781=CARTESIAN_POINT ( 'NONE',  ( 32.84088564781233543, 464.9638558180852215, 11.24476942535933155 ) ) ;
#76786=CARTESIAN_POINT ( 'NONE',  ( -35.53807395028670868, 391.2493183892675006, 6.679337639029564677 ) ) ;
#76797=CARTESIAN_POINT ( 'NONE',  ( -38.86455081257312116, 307.2518422178578703, -7.111262733053415275 ) ) ;
#76798=CARTESIAN_POINT ( 'NONE',  ( -3.416845212125001030, 304.8518027757642699, -9.000000000435770531 ) ) ;
#76813=LINE ( 'NONE', #75754, #57864 ) ;
#76832=FACE_BOUND ( 'NONE', #64200, .T. ) ;
#76836=CARTESIAN_POINT ( 'NONE',  ( 44.21332904831252364, 435.2494715644490952, 14.45449769377161253 ) ) ;
#76847=CARTESIAN_POINT ( 'NONE',  ( 44.19868099429156416, 435.2430970659377749, 14.45534906870892655 ) ) ;
#76848=ADVANCED_FACE ( 'NONE', ( #68621 ), #73144, .T. ) ;
#76851=CARTESIAN_POINT ( 'NONE',  ( -40.62042009610185289, 488.7249922674023992, 10.90475042733557309 ) ) ;
#76861=CARTESIAN_POINT ( 'NONE',  ( -42.58368830533729721, 480.4992008869074311, 9.550881666320744756 ) ) ;
#76862=CARTESIAN_POINT ( 'NONE',  ( -27.30328935667969859, 296.4063755745402204, 2.273684783268656417 ) ) ;
#76863=ORIENTED_EDGE ( 'NONE', *, *, #14725, .F. ) ;
#76864=CARTESIAN_POINT ( 'NONE',  ( -36.37334183242405317, 355.3971063992966037, 1.747594907370741524 ) ) ;
#76868=CARTESIAN_POINT ( 'NONE',  ( 24.99721807548662866, 295.6203948953991585, -1.835103857512845105 ) ) ;
#76869=CARTESIAN_POINT ( 'NONE',  ( 20.24579557674108088, 304.8297271373347144, -10.00469232190996927 ) ) ;
#76880=CARTESIAN_POINT ( 'NONE',  ( 44.48086712839104706, 338.5312796060234177, 0.5033553857222125005 ) ) ;
#76884=CARTESIAN_POINT ( 'NONE',  ( 31.38018240640768397, 439.2446336569565233, 22.99622140208172993 ) ) ;
#76909=CARTESIAN_POINT ( 'NONE',  ( -43.77569424703144563, 434.3726356145336922, 11.96512969951308847 ) ) ;
#76913=CARTESIAN_POINT ( 'NONE',  ( 46.00000000000000000, 500.0000000000002274, 15.00000000000000711 ) ) ;
#76916=ORIENTED_EDGE ( 'NONE', *, *, #54593, .T. ) ;
#76925=CARTESIAN_POINT ( 'NONE',  ( -32.16765682584846786, 415.4409746963033854, 25.54514402344307555 ) ) ;
#76926=ORIENTED_EDGE ( 'NONE', *, *, #14563, .F. ) ;
#76933=CARTESIAN_POINT ( 'NONE',  ( 38.45073040354913729, 439.3073909824421435, 23.72287809797798630 ) ) ;
#76934=CARTESIAN_POINT ( 'NONE',  ( -31.42031127665597623, 438.9001181076657758, 23.11845042760961988 ) ) ;
#76942=CARTESIAN_POINT ( 'NONE',  ( 21.31062199470357044, 303.0145930226796622, 9.972157899344148646 ) ) ;
#76949=CARTESIAN_POINT ( 'NONE',  ( 32.43844611059790850, 299.9187617745382113, 3.072456096697431693 ) ) ;
#76956=CARTESIAN_POINT ( 'NONE',  ( 4.061773079301143952, 294.8078983759118614, 9.927667266017472514 ) ) ;
#76962=CIRCLE ( 'NONE', #23638, 0.9999999999999991118 ) ;
#76967=CARTESIAN_POINT ( 'NONE',  ( 35.22510507712048167, 436.7812103362905987, 6.088528189192170537 ) ) ;
#76980=CARTESIAN_POINT ( 'NONE',  ( -35.97836163551201594, 491.7764920885232414, 12.54497382757487323 ) ) ;
#76985=EDGE_CURVE ( 'NONE', #79406, #337, #47336, .T. ) ;
#76991=CARTESIAN_POINT ( 'NONE',  ( 42.19179521601819260, 485.4956273777428919, -3.824025998174083618 ) ) ;
#77013=CARTESIAN_POINT ( 'NONE',  ( 22.98868130639473861, 305.6447374718524657, 9.109369938318858217 ) ) ;
#77016=ORIENTED_EDGE ( 'NONE', *, *, #20361, .F. ) ;
#77017=EDGE_CURVE ( 'NONE', #84046, #15159, #58393, .T. ) ;
#77023=CARTESIAN_POINT ( 'NONE',  ( -34.06332199976886699, 330.0526646846329299, -3.810096259360388427 ) ) ;
#77036=CARTESIAN_POINT ( 'NONE',  ( -9.148737761767405274, 294.6669993733668775, -4.042064116724770173 ) ) ;
#77050=ORIENTED_EDGE ( 'NONE', *, *, #56319, .T. ) ;
#77054=CARTESIAN_POINT ( 'NONE',  ( -43.27801297234302780, 485.1608390498441850, -2.258185464243190221 ) ) ;
#77055=ADVANCED_FACE ( 'NONE', ( #73893 ), #28481, .F. ) ;
#77059=DIRECTION ( 'NONE',  ( -0.3900125511322734551, -0.5465874153436415250, -0.7410346870067915370 ) ) ;
#77065=CARTESIAN_POINT ( 'NONE',  ( 39.95479119095725906, 335.6566949496817642, 19.74082504813667782 ) ) ;
#77076=CARTESIAN_POINT ( 'NONE',  ( -32.15310320217081852, 439.7024266304582625, 23.94087012106557566 ) ) ;
#77079=CARTESIAN_POINT ( 'NONE',  ( -38.42297841453999752, 318.8661547594436456, 15.79363851032234045 ) ) ;
#77099=B_SPLINE_CURVE_WITH_KNOTS ( 'NONE', 3,
 ( #75533, #100868, #92780, #33503, #43700, #17320, #2703, #35651, #82567, #101419, #57737, #8671 ),
 .UNSPECIFIED., .F., .F.,
 ( 4, 2, 2, 2, 2, 4 ),
 ( 5.282959581270353437E-15, 0.001731416251740865511, 0.003462832503476448356, 0.004328540629344262980, 0.005194248755212077170, 0.006925665006947724633 ),
 .UNSPECIFIED. ) ;
#77107=CARTESIAN_POINT ( 'NONE',  ( 34.25382146508943748, 436.5998831423237334, 6.438976971928319415 ) ) ;
#77110=CARTESIAN_POINT ( 'NONE',  ( 5.645355559246219457, 301.6283892719084179, -10.01771515668981039 ) ) ;
#77112=CARTESIAN_POINT ( 'NONE',  ( 43.66598739136852458, 384.2106680610543208, 15.34735960979999980 ) ) ;
#77136=CIRCLE ( 'NONE', #29008, 15.00000000000001421 ) ;
#77137=CARTESIAN_POINT ( 'NONE',  ( 39.08187240373737126, 460.7913535929789077, 2.155912156265418655 ) ) ;
#77138=CARTESIAN_POINT ( 'NONE',  ( -34.42712901035238815, 435.4031854876006378, 9.698380883803752184 ) ) ;
#77141=CARTESIAN_POINT ( 'NONE',  ( -43.58619280597381618, 434.9882623928566545, 14.52865984557642065 ) ) ;
#77169=DIRECTION ( 'NONE',  ( 0.9746329792208491272, 0.000000000000000000, -0.2238091951084492937 ) ) ;
#77193=CARTESIAN_POINT ( 'NONE',  ( -37.88504238421052861, 464.3115779013460269, 20.35635421822102131 ) ) ;
#77210=CARTESIAN_POINT ( 'NONE',  ( 46.00000000000000711, 438.0199209727295511, 11.62474111259973775 ) ) ;
#77220=CARTESIAN_POINT ( 'NONE',  ( -33.49627437238255112, 465.2401082457186590, 8.307162268441771857 ) ) ;
#77226=CARTESIAN_POINT ( 'NONE',  ( -9.970195021759442611, 302.6460196488377505, -10.04373974541436887 ) ) ;
#77234=AXIS2_PLACEMENT_3D ( 'NONE', #11298, #27551, #60431 ) ;
#77239=CARTESIAN_POINT ( 'NONE',  ( 43.58525199863880317, 435.7810069860513522, 17.82023302324629199 ) ) ;
#77247=CARTESIAN_POINT ( 'NONE',  ( 41.18601555923955715, 436.5297812499078987, 21.34108204767431616 ) ) ;
#77249=CARTESIAN_POINT ( 'NONE',  ( 41.12904442321167409, 485.7386261246315939, -4.649563818470188181 ) ) ;
#77260=CARTESIAN_POINT ( 'NONE',  ( 33.06682630402978873, 435.0798260220875591, 15.58372260938782539 ) ) ;
#77262=CARTESIAN_POINT ( 'NONE',  ( 32.82269234420716231, 485.2607240917815830, 5.823166218282061379 ) ) ;
#77270=CARTESIAN_POINT ( 'NONE',  ( -45.43339346675878687, 430.7348383325900727, 7.234598910837349628 ) ) ;
#77275=CARTESIAN_POINT ( 'NONE',  ( -4.269529794339158357, 302.8261475903860855, 9.931633466322995929 ) ) ;
#77289=ORIENTED_EDGE ( 'NONE', *, *, #70424, .F. ) ;
#77293=AXIS2_PLACEMENT_3D ( 'NONE', #3097, #52698, #2019 ) ;
#77310=CARTESIAN_POINT ( 'NONE',  ( 40.20451861284013262, 437.0088225241108262, 5.689194366316798757 ) ) ;
#77318=CARTESIAN_POINT ( 'NONE',  ( 35.40902385155721532, 484.3229957183398824, -1.494454771037330376 ) ) ;
#77320=B_SPLINE_CURVE_WITH_KNOTS ( 'NONE', 3,
 ( #12698, #69894, #53183, #70950 ),
 .UNSPECIFIED., .F., .F.,
 ( 4, 4 ),
 ( 0.000000000000000000, 0.003677212860670048700 ),
 .UNSPECIFIED. ) ;
#77332=PRESENTATION_STYLE_ASSIGNMENT (( #19138 ) ) ;
#77333=CARTESIAN_POINT ( 'NONE',  ( -36.72880825614078759, 408.9631818827540997, 6.288650551464858296 ) ) ;
#77366=AXIS2_PLACEMENT_3D ( 'NONE', #36542, #38129, #78021 ) ;
#77367=CARTESIAN_POINT ( 'NONE',  ( -37.83989825151947173, 491.0717236019712573, 13.27726931866635596 ) ) ;
#77396=CARTESIAN_POINT ( 'NONE',  ( -31.92502370130780065, 439.7300840721472923, 23.86368504749432518 ) ) ;
#77399=CARTESIAN_POINT ( 'NONE',  ( -42.19180677453721273, 462.2931784592651638, 3.389262873192026682 ) ) ;
#77412=CARTESIAN_POINT ( 'NONE',  ( 30.24427031855517711, 312.0196691915732004, -8.325478004009855937 ) ) ;
#77415=EDGE_CURVE ( 'NONE', #45384, #4872, #80853, .T. ) ;
#77420=CARTESIAN_POINT ( 'NONE',  ( 43.71297783477850629, 485.1278128289774827, -1.116606130290134002 ) ) ;
#77424=CARTESIAN_POINT ( 'NONE',  ( 33.59630659472934866, 315.8721021973062193, -6.875841742740135487 ) ) ;
#77426=CARTESIAN_POINT ( 'NONE',  ( 43.71335306921149311, 464.5235014653563894, 7.258763594095269056 ) ) ;
#77429=CARTESIAN_POINT ( 'NONE',  ( -33.00000000000000000, 489.5971041675261404, 10.80646835458718868 ) ) ;
#77467=CARTESIAN_POINT ( 'NONE',  ( -31.59843708504450532, 345.3014512875046194, 19.61421373405919510 ) ) ;
#77484=CARTESIAN_POINT ( 'NONE',  ( -41.46910480219017359, 484.7338956289797238, -3.418960549711475672 ) ) ;
#77486=CARTESIAN_POINT ( 'NONE',  ( 26.59919547731570333, 296.3152804941264549, 10.25407297267763873 ) ) ;
#77492=CARTESIAN_POINT ( 'NONE',  ( -33.00000000000000000, 450.0000000000002274, 25.20242257375371864 ) ) ;
#77493=CARTESIAN_POINT ( 'NONE',  ( 31.56956794793236298, 299.1326689194955861, 2.890017757335089144 ) ) ;
#77501=CARTESIAN_POINT ( 'NONE',  ( 12.23754451682550481, 302.5837290440147171, 9.880035480020872285 ) ) ;
#77514=CARTESIAN_POINT ( 'NONE',  ( 34.36795306836310715, 436.8606731934561367, 5.945192215386652990 ) ) ;
#77524=CARTESIAN_POINT ( 'NONE',  ( -37.00811329507524761, 491.8246567885113336, 12.57632236122367431 ) ) ;
#77553=CARTESIAN_POINT ( 'NONE',  ( 25.61036159288622471, 308.3346455602268747, 9.743090724280190074 ) ) ;
#77557=ORIENTED_EDGE ( 'NONE', *, *, #35028, .T. ) ;
#77585=DIRECTION ( 'NONE',  ( 0.000000000000000000, -1.000000000000000000, 0.000000000000000000 ) ) ;
#77589=CARTESIAN_POINT ( 'NONE',  ( 0.000000000000000000, 0.000000000000000000, 0.000000000000000000 ) ) ;
#77592=ORIENTED_EDGE ( 'NONE', *, *, #77415, .T. ) ;
#77605=CARTESIAN_POINT ( 'NONE',  ( 33.14123094351160859, 415.5030858634154356, 25.77660549537051082 ) ) ;
#77609=CARTESIAN_POINT ( 'NONE',  ( -44.32955949054232292, 435.2565657989985652, 11.97827722465822475 ) ) ;
#77618=CARTESIAN_POINT ( 'NONE',  ( -21.70127168875638546, 305.0664967217661001, -8.954259079442119074 ) ) ;
#77619=CARTESIAN_POINT ( 'NONE',  ( -36.73440919039663299, 310.3360335768772416, 13.64782109026154977 ) ) ;
#77637=B_SPLINE_CURVE_WITH_KNOTS ( 'NONE', 3,
 ( #31015, #40654, #63893, #14777 ),
 .UNSPECIFIED., .F., .F.,
 ( 4, 4 ),
 ( 0.000000000000000000, 0.003416952886430368354 ),
 .UNSPECIFIED. ) ;
#77645=CARTESIAN_POINT ( 'NONE',  ( 33.00000000000000000, 435.0774731480752280, 11.67986145722084501 ) ) ;
#77648=CARTESIAN_POINT ( 'NONE',  ( 7.416584036454647588, 294.7171783682853743, -6.719350101588912771 ) ) ;
#77649=CARTESIAN_POINT ( 'NONE',  ( 27.47093694407817210, 296.2799286419132727, -9.692114557243211692 ) ) ;
#77650=CARTESIAN_POINT ( 'NONE',  ( 37.75894927425606085, 307.4551686108193849, 0.9580216366009680629 ) ) ;
#77663=EDGE_CURVE ( 'NONE', #55140, #41735, #74006, .T. ) ;
#77680=DIRECTION ( 'NONE',  ( 0.000000000000000000, 0.000000000000000000, 1.000000000000000000 ) ) ;
#77712=CARTESIAN_POINT ( 'NONE',  ( -1.128077836147719282, 302.8478239976500390, 9.936168295454388399 ) ) ;
#77714=CARTESIAN_POINT ( 'NONE',  ( -20.97754405179121662, 294.8763868968453608, 9.942224931492262385 ) ) ;
#77726=CARTESIAN_POINT ( 'NONE',  ( -32.62589942841216128, 485.9514140855798132, 7.203752716014093060 ) ) ;
#77738=CARTESIAN_POINT ( 'NONE',  ( -31.03678703374864156, 438.6650838204933507, 21.86890379898568426 ) ) ;
#77744=VERTEX_POINT ( 'NONE', #71381 ) ;
#77756=CARTESIAN_POINT ( 'NONE',  ( -32.95589646111131543, 464.8957215206405067, 10.75300444715554171 ) ) ;
#77762=CARTESIAN_POINT ( 'NONE',  ( -20.87150057907853551, 302.8935307529103511, -9.991130529295787710 ) ) ;
#77766=CARTESIAN_POINT ( 'NONE',  ( -42.59614121018025656, 472.7198067255875458, 11.67823714611271768 ) ) ;
#77767=ORIENTED_EDGE ( 'NONE', *, *, #36452, .T. ) ;
#77777=CARTESIAN_POINT ( 'NONE',  ( -43.55054245096678756, 486.2288135416363275, 8.070792277557934824 ) ) ;
#77779=CARTESIAN_POINT ( 'NONE',  ( -30.00000000000000000, 488.8442721620238558, 4.433647275927475206 ) ) ;
#77807=CARTESIAN_POINT ( 'NONE',  ( -16.83213846691014126, 302.5742749712027262, 9.878299602143622238 ) ) ;
#77811=B_SPLINE_CURVE_WITH_KNOTS ( 'NONE', 3,
 ( #20089, #29758, #69137, #95520 ),
 .UNSPECIFIED., .F., .F.,
 ( 4, 4 ),
 ( 0.000000000000000000, 0.002118337988235547299 ),
 .UNSPECIFIED. ) ;
#77812=CARTESIAN_POINT ( 'NONE',  ( -32.10528697966012857, 486.1671898930081852, 5.449875171704860577 ) ) ;
#77842=CARTESIAN_POINT ( 'NONE',  ( 41.81614247337357426, 436.2534677952791640, 7.171297734017413106 ) ) ;
#77843=EDGE_CURVE ( 'NONE', #21702, #73045, #24080, .T. ) ;
#77866=CARTESIAN_POINT ( 'NONE',  ( -35.73766838807912904, 382.4801828565075539, 5.056470275602615416 ) ) ;
#77907=DIRECTION ( 'NONE',  ( 0.000000000000000000, 0.9349068334195446139, -0.3548932414479595843 ) ) ;
#77910=CARTESIAN_POINT ( 'NONE',  ( 32.22503847990217452, 485.9064490506207790, 4.829857536092636572 ) ) ;
#77915=( BOUNDED_SURFACE ( )  B_SPLINE_SURFACE ( 3, 2, ( 
 ( #33206, #15934, #90897 ),
 ( #89832, #91436, #81706 ),
 ( #57977, #17014, #99495 ),
 ( #7829, #41271, #66077 ),
 ( #8897, #74159, #7297 ),
 ( #97912, #24064, #73624 ),
 ( #41798, #106529, #40208 ),
 ( #24587, #17550, #32684 ),
 ( #8369, #73083, #98956 ),
 ( #80659, #105992, #25670 ),
 ( #48287, #81186, #89307 ),
 ( #58535, #49349, #32141 ),
 ( #65019, #66612, #40739 ),
 ( #6780, #15402, #64506 ),
 ( #49889, #31618, #48813 ),
 ( #98441, #82796, #74686 ) ),
 .UNSPECIFIED., .F., .F., .F. ) 
 B_SPLINE_SURFACE_WITH_KNOTS ( ( 4, 2, 2, 2, 2, 2, 2, 4 ),
 ( 3, 3 ),
 ( 0.000000000000000000, 0.001044086800741871740, 0.001566130201112807610, 0.002088173601483743480, 0.002610217001854679350, 0.003132260402225615220, 0.003654303802596551090, 0.004176347202967486960 ),
 ( 0.000000000000000000, 1.000000000000000000 ),
 .UNSPECIFIED. ) 
 GEOMETRIC_REPRESENTATION_ITEM ( )  RATIONAL_B_SPLINE_SURFACE ( (
 ( 1.000000000000000000, 0.8350736500408202367, 1.000000000000000000),
 ( 1.000000000000000000, 0.8489954227501540496, 1.000000000000000000),
 ( 1.000000000000000000, 0.8615675893696067567, 1.000000000000000000),
 ( 1.000000000000000000, 0.8776574663916940633, 1.000000000000000000),
 ( 1.000000000000000000, 0.8825492266237192629, 1.000000000000000000),
 ( 1.000000000000000000, 0.8909252284700192037, 1.000000000000000000),
 ( 1.000000000000000000, 0.8944578560793419175, 1.000000000000000000),
 ( 1.000000000000000000, 0.9000429021727629486, 1.000000000000000000),
 ( 1.000000000000000000, 0.9020681612884537959, 1.000000000000000000),
 ( 1.000000000000000000, 0.9043430709037243442, 1.000000000000000000),
 ( 1.000000000000000000, 0.9046293304020756043, 1.000000000000000000),
 ( 1.000000000000000000, 0.9034445554302654724, 1.000000000000000000),
 ( 1.000000000000000000, 0.9019515008116110177, 1.000000000000000000),
 ( 1.000000000000000000, 0.8973842636247786331, 1.000000000000000000),
 ( 1.000000000000000000, 0.8943059481781706621, 1.000000000000000000),
 ( 1.000000000000000000, 0.8904848454314516770, 1.000000000000000000) ) ) 
 REPRESENTATION_ITEM ( '' )  SURFACE ( )  );
#77935=CARTESIAN_POINT ( 'NONE',  ( -41.75349605900994021, 461.8279235811434660, 2.915883750441013333 ) ) ;
#77940=CARTESIAN_POINT ( 'NONE',  ( -36.49890972612865880, 361.2193401986697836, 2.712660087864745329 ) ) ;
#77941=CARTESIAN_POINT ( 'NONE',  ( 38.02420928480272977, 490.5701994133388553, 12.25121054170005941 ) ) ;
#77942=CARTESIAN_POINT ( 'NONE',  ( -33.00000000000000000, 500.0000000000002274, 15.00000000000000711 ) ) ;
#77945=CARTESIAN_POINT ( 'NONE',  ( 22.10266876167072425, 303.0855146123441273, -9.950096580394351520 ) ) ;
#77955=CARTESIAN_POINT ( 'NONE',  ( 36.36099827879255741, 334.2868656930699558, -2.351449576734861324 ) ) ;
#77959=CARTESIAN_POINT ( 'NONE',  ( 31.94980155458579318, 439.7324857888989982, 23.88680823179080903 ) ) ;
#77961=ORIENTED_EDGE ( 'NONE', *, *, #81, .F. ) ;
#77968=ORIENTED_EDGE ( 'NONE', *, *, #39336, .F. ) ;
#77970=AXIS2_PLACEMENT_3D ( 'NONE', #86128, #95790, #13255 ) ;
#77980=CARTESIAN_POINT ( 'NONE',  ( -43.36987996248237209, 463.6266071970522376, 5.362859981238893070 ) ) ;
#77993=DIRECTION ( 'NONE',  ( 9.251858538543008510E-15, -0.9911985061125712093, 0.1323839925376438520 ) ) ;
#78010=CARTESIAN_POINT ( 'NONE',  ( 25.00873914691374367, 295.6585831474191082, 2.110237673684152604 ) ) ;
#78020=LINE ( 'NONE', #5714, #28259 ) ;
#78021=DIRECTION ( 'NONE',  ( 0.000000000000000000, -0.6886991506762676352, 0.7250472259499980421 ) ) ;
#78026=AXIS2_PLACEMENT_3D ( 'NONE', #38480, #57808, #41644 ) ;
#78029=CARTESIAN_POINT ( 'NONE',  ( -2.204364238465237794E-15, -20.00000000000001776, -9.000000000000007105 ) ) ;
#78043=CARTESIAN_POINT ( 'NONE',  ( 0.000000000000000000, 80.00000000000000000, 0.000000000000000000 ) ) ;
#78059=CARTESIAN_POINT ( 'NONE',  ( 38.92819510383412762, 485.1409701397173535, -4.243468885292519310 ) ) ;
#78063=CARTESIAN_POINT ( 'NONE',  ( -32.28552837373656814, 464.7648866755938570, 15.30384310834764428 ) ) ;
#78075=ADVANCED_FACE ( 'NONE', ( #102036 ), #8562, .T. ) ;
#78076=ORIENTED_EDGE ( 'NONE', *, *, #65291, .T. ) ;
#78079=CARTESIAN_POINT ( 'NONE',  ( 25.89392128340153576, 307.0924142446438054, 10.67957798942343217 ) ) ;
#78102=ORIENTED_EDGE ( 'NONE', *, *, #106374, .T. ) ;
#78117=CARTESIAN_POINT ( 'NONE',  ( 43.03880698781972569, 435.3545807224048190, 16.83573131045119098 ) ) ;
#78119=CARTESIAN_POINT ( 'NONE',  ( -46.00000000000000711, 460.6827615371018965, 7.624057330649156583 ) ) ;
#78126=CARTESIAN_POINT ( 'NONE',  ( 42.72191162735155245, 427.3218109763436132, 19.12685808572960511 ) ) ;
#78127=CARTESIAN_POINT ( 'NONE',  ( -43.02661387979790675, 465.7449615347597387, 11.43319743843397696 ) ) ;
#78129=CARTESIAN_POINT ( 'NONE',  ( -43.62838954006684844, 434.9736691849526551, 14.34345830637900576 ) ) ;
#78139=CARTESIAN_POINT ( 'NONE',  ( -29.70730338703692652, 314.7332412851916956, 12.83056961409002916 ) ) ;
#78144=CARTESIAN_POINT ( 'NONE',  ( 42.33268550343510839, 436.4462712439766960, 6.764016893796107155 ) ) ;
#78165=CARTESIAN_POINT ( 'NONE',  ( 0.7515601774665998658, 295.1017350046088268, -10.00017833058526584 ) ) ;
#78166=CARTESIAN_POINT ( 'NONE',  ( 40.75641113481592726, 360.0948485545300741, 24.37153223514695100 ) ) ;
#78167=CARTESIAN_POINT ( 'NONE',  ( 36.78140055146844389, 305.3596551341470331, 0.4383668257698736803 ) ) ;
#78171=CARTESIAN_POINT ( 'NONE',  ( -46.00000000000003553, 464.2883104330369974, 11.80345442596980199 ) ) ;
#78185=CARTESIAN_POINT ( 'NONE',  ( -43.49712701248153479, 471.1120579834711748, 8.168005033297315975 ) ) ;
#78196=CARTESIAN_POINT ( 'NONE',  ( 44.12589798587349321, 464.4133173135357424, 9.756011010161726560 ) ) ;
#78200=CARTESIAN_POINT ( 'NONE',  ( -38.95242300085207177, 491.1731620564949026, 12.13306966136735099 ) ) ;
#78203=ORIENTED_EDGE ( 'NONE', *, *, #70117, .F. ) ;
#78207=VERTEX_POINT ( 'NONE', #44344 ) ;
#78208=CIRCLE ( 'NONE', #40328, 5.000000000000001776 ) ;
#78213=CARTESIAN_POINT ( 'NONE',  ( 43.54570344706466756, 464.5919001250003930, 9.427857144828900360 ) ) ;
#78220=CARTESIAN_POINT ( 'NONE',  ( 44.11327388758692081, 464.4313852428372797, 9.822198357557351045 ) ) ;
#78255=CARTESIAN_POINT ( 'NONE',  ( -33.84761347220317873, 488.7471039746334327, 11.01988148152523550 ) ) ;
#78265=ORIENTED_EDGE ( 'NONE', *, *, #96576, .T. ) ;
#78270=CARTESIAN_POINT ( 'NONE',  ( 41.92281291883664096, 435.4200907145704491, 7.396891011706831165 ) ) ;
#78273=CARTESIAN_POINT ( 'NONE',  ( -42.91610780537345704, 434.7038292309375720, 17.44089711044167856 ) ) ;
#78274=CARTESIAN_POINT ( 'NONE',  ( -32.93513049338658760, 465.6726574193327224, 10.66039033145138504 ) ) ;
#78293=FACE_OUTER_BOUND ( 'NONE', #9112, .T. ) ;
#78294=CIRCLE ( 'NONE', #16313, 1.000000000000020872 ) ;
#78309=ADVANCED_FACE ( 'NONE', ( #84803 ), #51748, .F. ) ;
#78316=EDGE_CURVE ( 'NONE', #48464, #41735, #60338, .T. ) ;
#78318=DIRECTION ( 'NONE',  ( -1.000000000000000000, 0.000000000000000000, 0.000000000000000000 ) ) ;
#78328=CARTESIAN_POINT ( 'NONE',  ( 33.77559172535807619, 464.7834715296606305, 7.192701217093271815 ) ) ;
#78342=CARTESIAN_POINT ( 'NONE',  ( -30.00000000000000000, 450.0000000000002274, 18.20242257375371153 ) ) ;
#78351=CARTESIAN_POINT ( 'NONE',  ( 36.49551160402948113, 361.0291929650597353, 2.682884907252832463 ) ) ;
#78357=CARTESIAN_POINT ( 'NONE',  ( 38.39281685574057690, 437.9237591976291810, 4.303444208756668665 ) ) ;
#78361=B_SPLINE_CURVE_WITH_KNOTS ( 'NONE', 3,
 ( #41560, #99245, #84682, #59358, #9708, #33485, #67445, #92220, #100322, #1610, #35096, #49643, #50684, #42084 ),
 .UNSPECIFIED., .F., .F.,
 ( 4, 2, 2, 2, 2, 2, 4 ),
 ( 0.000000000000000000, 0.0008623664466435473864, 0.001724732893287094773, 0.003449465786574139672, 0.004311832233217661146, 0.005174198679861184355, 0.006898931573148161384 ),
 .UNSPECIFIED. ) ;
#78372=CARTESIAN_POINT ( 'NONE',  ( 32.46316046841738512, 488.6793347432256382, 9.801212136610072179 ) ) ;
#78376=CIRCLE ( 'NONE', #50789, 15.00000000000000711 ) ;
#78378=CARTESIAN_POINT ( 'NONE',  ( -40.54863160047752046, 437.2386745228059794, 5.317148167338432430 ) ) ;
#78381=CARTESIAN_POINT ( 'NONE',  ( -35.02700494599118031, 463.8298975055874962, 19.03023931479493314 ) ) ;
#78403=ORIENTED_EDGE ( 'NONE', *, *, #78316, .T. ) ;
#78405=EDGE_CURVE ( 'NONE', #34141, #26380, #18915, .T. ) ;
#78425=DIRECTION ( 'NONE',  ( 0.000000000000000000, 0.000000000000000000, -1.000000000000000000 ) ) ;
#78429=CARTESIAN_POINT ( 'NONE',  ( -41.92281291883663386, 435.4200907145705060, 7.396891011706863139 ) ) ;
#78433=EDGE_CURVE ( 'NONE', #71046, #87574, #87468, .T. ) ;
#78455=CARTESIAN_POINT ( 'NONE',  ( 34.03884506130833643, 322.5454401300060567, -5.433161704552694538 ) ) ;
#78457=EDGE_CURVE ( 'NONE', #95757, #20727, #21578, .T. ) ;
#78462=CARTESIAN_POINT ( 'NONE',  ( -24.08998881576893680, 304.6612033203863348, -9.825736866731734409 ) ) ;
#78463=DIRECTION ( 'NONE',  ( 0.000000000000000000, 0.000000000000000000, 1.000000000000000000 ) ) ;
#78465=CARTESIAN_POINT ( 'NONE',  ( -43.51084452654468748, 465.2903130129606666, 9.421687747985890482 ) ) ;
#78477=CARTESIAN_POINT ( 'NONE',  ( 37.59065068584150282, 369.8620417756742995, 4.163880029477669886 ) ) ;
#78490=CARTESIAN_POINT ( 'NONE',  ( 33.00000000000000000, 489.5971041675262541, 10.80646835458729349 ) ) ;
#78500=CARTESIAN_POINT ( 'NONE',  ( -44.27172743694714541, 463.5980762766266707, 7.352902973895489858 ) ) ;
#78501=CARTESIAN_POINT ( 'NONE',  ( 1.128238012697730275, 300.0000000000000000, 9.936150108905557943 ) ) ;
#78503=ORIENTED_EDGE ( 'NONE', *, *, #78457, .T. ) ;
#78525=VERTEX_POINT ( 'NONE', #95414 ) ;
#78528=CARTESIAN_POINT ( 'NONE',  ( 31.17288985937226542, 438.0041457322897713, 21.19838952990721026 ) ) ;
#78530=CARTESIAN_POINT ( 'NONE',  ( 24.23803912011595685, 304.0757452244806700, 10.20472470771674622 ) ) ;
#78547=CARTESIAN_POINT ( 'NONE',  ( 43.75010090113893568, 464.8337800386751724, 11.75004750935173448 ) ) ;
#78550=ADVANCED_FACE ( 'NONE', ( #64133 ), #73793, .T. ) ;
#78551=CARTESIAN_POINT ( 'NONE',  ( -21.04247164025375483, 37.86482112153537116, 10.52123582012688274 ) ) ;
#78565=CARTESIAN_POINT ( 'NONE',  ( -38.81358894280271699, 485.1131561813180042, -4.191378885296423995 ) ) ;
#78568=CARTESIAN_POINT ( 'NONE',  ( 43.97892253342649127, 485.8746234538170938, 4.637105959624745033 ) ) ;
#78597=CARTESIAN_POINT ( 'NONE',  ( 19.70764564238373495, 304.7954121406194190, 9.925013215726725235 ) ) ;
#78604=FACE_OUTER_BOUND ( 'NONE', #3127, .T. ) ;
#78613=VERTEX_POINT ( 'NONE', #22080 ) ;
#78616=DIRECTION ( 'NONE',  ( 0.000000000000000000, 0.000000000000000000, -1.000000000000000000 ) ) ;
#78622=CARTESIAN_POINT ( 'NONE',  ( 33.00000000000000000, 500.0000000000002274, 12.00000000000000711 ) ) ;
#78629=VERTEX_POINT ( 'NONE', #54935 ) ;
#78631=CARTESIAN_POINT ( 'NONE',  ( -46.00000000000001421, 436.1447960644705404, 9.230581956296642687 ) ) ;
#78641=CARTESIAN_POINT ( 'NONE',  ( 40.94500826520420134, 409.4144549123020056, 27.74959626577850713 ) ) ;
#78649=CARTESIAN_POINT ( 'NONE',  ( -35.25431541795652635, 462.2816602437375764, 4.574345776432286570 ) ) ;
#78653=CARTESIAN_POINT ( 'NONE',  ( -38.13184040399831787, 310.3448107234241888, 5.627667502867490512 ) ) ;
#78660=MECHANICAL_DESIGN_GEOMETRIC_PRESENTATION_REPRESENTATION('',(#21818),#80428);
#78684=CARTESIAN_POINT ( 'NONE',  ( 1.338640380261408858, 297.3185856422899178, -10.00123718159648689 ) ) ;
#78685=CARTESIAN_POINT ( 'NONE',  ( 40.85254446136673323, 441.7500193615117610, 25.53625856138344474 ) ) ;
#78686=CARTESIAN_POINT ( 'NONE',  ( 40.86653802755286335, 319.2575511279100056, 3.927576133266500680 ) ) ;
#78696=CARTESIAN_POINT ( 'NONE',  ( 0.000000000000000000, -0.1944580884125578779, -19.78098730681987405 ) ) ;
#78710=TOROIDAL_SURFACE ( 'NONE', #6343, 12.00000000000000711, 3.000000000000000000 ) ;
#78722=CARTESIAN_POINT ( 'NONE',  ( -31.84025840404170182, 489.2001951420293722, 8.970820463101537356 ) ) ;
#78729=AXIS2_PLACEMENT_3D ( 'NONE', #40003, #57221, #30335 ) ;
#78748=FACE_OUTER_BOUND ( 'NONE', #10417, .T. ) ;
#78761=ORIENTED_EDGE ( 'NONE', *, *, #19418, .F. ) ;
#78773=CARTESIAN_POINT ( 'NONE',  ( -31.63765798398162588, 436.4483132331570800, 18.85061845559700444 ) ) ;
#78774=CARTESIAN_POINT ( 'NONE',  ( -33.21459943997732722, 487.8270262908587256, 10.08789160144731056 ) ) ;
#78782=CARTESIAN_POINT ( 'NONE',  ( -28.94221336919291332, 306.6375891257424087, -9.149909065943708342 ) ) ;
#78789=CARTESIAN_POINT ( 'NONE',  ( 43.48483803624226596, 478.3762783859503429, 6.210097532619577088 ) ) ;
#78794=EDGE_CURVE ( 'NONE', #36676, #4725, #67789, .T. ) ;
#78795=CARTESIAN_POINT ( 'NONE',  ( -42.80674739067558221, 434.8200538645568827, 17.89665983759107704 ) ) ;
#78796=CIRCLE ( 'NONE', #106356, 0.9999999999999987788 ) ;
#78802=CARTESIAN_POINT ( 'NONE',  ( -36.41468026840615124, 439.0114751707915843, 23.96625823804127720 ) ) ;
#78804=CARTESIAN_POINT ( 'NONE',  ( -37.01956797474046823, 345.4690947806042232, 0.09929204855550027853 ) ) ;
#78811=EDGE_LOOP ( 'NONE', ( #31319, #54357, #25069, #13253 ) ) ;
#78821=CARTESIAN_POINT ( 'NONE',  ( -30.00000000000000000, 488.6481008951269587, 3.890293910847615333 ) ) ;
#78838=EDGE_CURVE ( 'NONE', #17636, #26380, #93384, .T. ) ;
#78844=CARTESIAN_POINT ( 'NONE',  ( 6.744163421200966901, 304.7396475197473364, -9.023845328246613562 ) ) ;
#78850=EDGE_LOOP ( 'NONE', ( #26816, #46051, #26829, #57535 ) ) ;
#78852=( BOUNDED_SURFACE ( )  B_SPLINE_SURFACE ( 3, 2, ( 
 ( #58508, #35863, #11523 ),
 ( #42846, #101083, #76798 ),
 ( #91929, #75741, #67129 ),
 ( #67663, #27779, #43387 ),
 ( #76270, #68739, #66590 ),
 ( #9939, #50389, #2376 ),
 ( #26707, #101623, #83301 ),
 ( #34258, #1837, #748 ) ),
 .UNSPECIFIED., .F., .F., .F. ) 
 B_SPLINE_SURFACE_WITH_KNOTS ( ( 4, 2, 2, 4 ),
 ( 3, 3 ),
 ( 0.009810586775086673275, 0.01999416116298580876, 0.02508594835693537736, 0.03017773555088494597 ),
 ( 0.000000000000000000, 1.000000000000000000 ),
 .UNSPECIFIED. ) 
 GEOMETRIC_REPRESENTATION_ITEM ( )  RATIONAL_B_SPLINE_SURFACE ( (
 ( 1.000000000000000000, 0.7071067811865475727, 1.000000000000000000),
 ( 1.000000000000000000, 0.7071067811865475727, 1.000000000000000000),
 ( 1.000000000000000000, 0.7071080532031980281, 1.000000000000000000),
 ( 1.000000000000000000, 0.7071061932061152300, 1.000000000000000000),
 ( 1.000000000000000000, 0.7071074416953658792, 1.000000000000000000),
 ( 1.000000000000000000, 0.7071061820943852494, 1.000000000000000000),
 ( 1.000000000000000000, 0.7071482300333765680, 1.000000000000000000),
 ( 1.000000000000000000, 0.7071067811865450192, 1.000000000000000000) ) ) 
 REPRESENTATION_ITEM ( '' )  SURFACE ( )  );
#78871=EDGE_LOOP ( 'NONE', ( #29643, #61922, #92786, #30684 ) ) ;
#78891=CARTESIAN_POINT ( 'NONE',  ( 23.08332880300597978, 303.3267438324617160, -9.898176362637144621 ) ) ;
#78899=CIRCLE ( 'NONE', #103004, 3.000000000000006661 ) ;
#78903=CARTESIAN_POINT ( 'NONE',  ( -34.94338628507543376, 342.5355909536760350, -0.9693026116843473927 ) ) ;
#78928=CARTESIAN_POINT ( 'NONE',  ( -44.12472801210821416, 485.7238370326489871, 3.975897585127424527 ) ) ;
#78930=CARTESIAN_POINT ( 'NONE',  ( 34.87911814363040719, 490.1439009131577791, 11.96539503908413415 ) ) ;
#78935=CARTESIAN_POINT ( 'NONE',  ( 32.84444940698777771, 439.0476299206099497, 24.86213004146451766 ) ) ;
#78944=ORIENTED_EDGE ( 'NONE', *, *, #25505, .F. ) ;
#78972=AXIS2_PLACEMENT_3D ( 'NONE', #90279, #99955, #81627 ) ;
#78976=CARTESIAN_POINT ( 'NONE',  ( 33.49615637169857507, 465.2403011571852289, 8.307633084691127934 ) ) ;
#78985=CARTESIAN_POINT ( 'NONE',  ( 32.01721732537988885, 318.3378566774296701, -5.732130415166460047 ) ) ;
#78991=CARTESIAN_POINT ( 'NONE',  ( -20.56310269357972587, 303.8628971230333491, -9.997642691052938346 ) ) ;
#79003=CARTESIAN_POINT ( 'NONE',  ( -33.47662383462841262, 484.3276029200706603, 3.198141044746298789 ) ) ;
#79013=CARTESIAN_POINT ( 'NONE',  ( 30.98142344576083573, 309.3658521538144441, -8.497048073299385607 ) ) ;
#79018=CARTESIAN_POINT ( 'NONE',  ( 31.32516044773268149, 438.3824493690776762, 22.69256374299771295 ) ) ;
#79024=CARTESIAN_POINT ( 'NONE',  ( -44.28929576524119227, 435.2229490444834141, 14.00215079178472166 ) ) ;
#79028=CARTESIAN_POINT ( 'NONE',  ( -35.53321744913902336, 463.4104023594616706, 19.92304894059135023 ) ) ;
#79063=CARTESIAN_POINT ( 'NONE',  ( -33.50421398922254923, 488.2600042842250332, 10.59612602189812414 ) ) ;
#79070=CARTESIAN_POINT ( 'NONE',  ( -41.13328595189528158, 484.9084785457653197, -3.795084846866993988 ) ) ;
#79076=CARTESIAN_POINT ( 'NONE',  ( 40.02527844605699414, 463.9419950688768495, 18.74737584574104332 ) ) ;
#79089=CARTESIAN_POINT ( 'NONE',  ( 44.26781960101214963, 464.1284203585717592, 8.781346234564500364 ) ) ;
#79092=CARTESIAN_POINT ( 'NONE',  ( -43.51595707228967314, 485.1238408984097532, -1.707557185901023677 ) ) ;
#79094=CARTESIAN_POINT ( 'NONE',  ( 35.11649460235492626, 436.5236565062589875, 6.589765443822644286 ) ) ;
#79112=ORIENTED_EDGE ( 'NONE', *, *, #90788, .F. ) ;
#79113=CARTESIAN_POINT ( 'NONE',  ( 40.98863139543689726, 485.5630605922963809, -4.100416933092245309 ) ) ;
#79134=CARTESIAN_POINT ( 'NONE',  ( -29.49192533388955084, 326.6740820537864920, 15.30567695811878970 ) ) ;
#79136=CARTESIAN_POINT ( 'NONE',  ( 21.38648923915819466, 305.0940074287001380, 9.988878310497041113 ) ) ;
#79144=CARTESIAN_POINT ( 'NONE',  ( 46.00000000000000000, 487.9838442367869220, -0.2095173675547508108 ) ) ;
#79146=DIRECTION ( 'NONE',  ( -0.9605097441496667221, 0.000000000000000000, -0.2782463501890758972 ) ) ;
#79176=CARTESIAN_POINT ( 'NONE',  ( -46.00000000000000000, 438.0166301925364110, 11.64259471675216950 ) ) ;
#79183=ORIENTED_EDGE ( 'NONE', *, *, #46973, .T. ) ;
#79190=CARTESIAN_POINT ( 'NONE',  ( 40.89635135780635977, 427.9313666579921573, 26.89375439067753959 ) ) ;
#79199=CARTESIAN_POINT ( 'NONE',  ( -34.87421981230464496, 463.4384841829531183, 4.864009048391830348 ) ) ;
#79201=VERTEX_POINT ( 'NONE', #23827 ) ;
#79203=CARTESIAN_POINT ( 'NONE',  ( -32.35864103015216386, 300.7401528847129271, 11.27243207037040484 ) ) ;
#79216=CARTESIAN_POINT ( 'NONE',  ( 33.50185725305296103, 488.2566613463520184, 10.59321780396354029 ) ) ;
#79229=CARTESIAN_POINT ( 'NONE',  ( 40.93292669599463096, 378.0706848361106722, 26.55786848468904537 ) ) ;
#79231=CARTESIAN_POINT ( 'NONE',  ( 32.65228357897255052, 299.7864930558274068, -0.8975401584249106390 ) ) ;
#79239=ADVANCED_FACE ( 'NONE', ( #64266, #89591 ), #21701, .T. ) ;
#79248=CARTESIAN_POINT ( 'NONE',  ( -44.11327388758650159, 464.4313852428384735, 9.822198357558047377 ) ) ;
#79261=ORIENTED_EDGE ( 'NONE', *, *, #67207, .F. ) ;
#79263=CARTESIAN_POINT ( 'NONE',  ( 32.10523163092994992, 436.9431439331139586, 23.91259324438140510 ) ) ;
#79265=B_SPLINE_CURVE_WITH_KNOTS ( 'NONE', 3,
 ( #41249, #35723, #3315, #10853, #36262, #11926, #52928, #85854, #43249, #92311, #69130, #84237 ),
 .UNSPECIFIED., .F., .F.,
 ( 4, 2, 2, 2, 2, 4 ),
 ( 0.000000000000000000, 0.0004272229515409421198, 0.0008544459030818842395, 0.001708891806163794283, 0.002563337709245704001, 0.003417783612327614153 ),
 .UNSPECIFIED. ) ;
#79268=DIRECTION ( 'NONE',  ( 0.7663137714224784736, 0.000000000000000000, 0.6424665000825005023 ) ) ;
#79271=CARTESIAN_POINT ( 'NONE',  ( -17.47333451427476447, 294.5877965850818327, -2.055689352271495629 ) ) ;
#79295=CARTESIAN_POINT ( 'NONE',  ( -32.82691535583477815, 485.1045372766794799, 1.724905475514949771 ) ) ;
#79311=CARTESIAN_POINT ( 'NONE',  ( -31.35596682365697419, 438.0939828603714545, 22.55458131664454768 ) ) ;
#79315=AXIS2_PLACEMENT_3D ( 'NONE', #1289, #67126, #33711 ) ;
#79321=CARTESIAN_POINT ( 'NONE',  ( -28.34102358861306570, 306.0549377924973555, -9.285773497043622982 ) ) ;
#79329=CARTESIAN_POINT ( 'NONE',  ( 31.42312417694817483, 414.9735925968759602, 24.35715672292620582 ) ) ;
#79334=CARTESIAN_POINT ( 'NONE',  ( -33.49051768689264463, 464.3918346587479959, 8.532988796677324572 ) ) ;
#79352=DIRECTION ( 'NONE',  ( -0.02699252395738975518, 0.001721171576548164101, -0.9996341536876447442 ) ) ;
#79357=CARTESIAN_POINT ( 'NONE',  ( 46.00000000000000000, 438.3878896346935790, 16.22878885428537998 ) ) ;
#79359=EDGE_LOOP ( 'NONE', ( #29461, #53906, #46246, #60662 ) ) ;
#79379=CARTESIAN_POINT ( 'NONE',  ( 43.74985542820358830, 435.5770091380369422, 16.96136490515564788 ) ) ;
#79406=VERTEX_POINT ( 'NONE', #1612 ) ;
#79407=FACE_OUTER_BOUND ( 'NONE', #105676, .T. ) ;
#79409=CARTESIAN_POINT ( 'NONE',  ( 32.84237740334681632, 485.2251842821273158, 5.746442123022902138 ) ) ;
#79414=CARTESIAN_POINT ( 'NONE',  ( -43.03185303983481447, 485.3613526602391062, 6.073233449168579767 ) ) ;
#79421=CARTESIAN_POINT ( 'NONE',  ( -46.00000000000000000, 438.4646224975039672, 9.895601460523739235 ) ) ;
#79422=CARTESIAN_POINT ( 'NONE',  ( -43.59756234217317683, 434.3244621007142996, 14.55946156040369921 ) ) ;
#79426=DIRECTION ( 'NONE',  ( 0.000000000000000000, 1.000000000000000000, 1.224646799147353207E-16 ) ) ;
#79436=CARTESIAN_POINT ( 'NONE',  ( 45.40507512465600115, 439.2794387026467575, 6.273370203490043373 ) ) ;
#79437=CARTESIAN_POINT ( 'NONE',  ( 43.00000000000000000, 500.0000000000002274, 0.000000000000000000 ) ) ;
#79440=CARTESIAN_POINT ( 'NONE',  ( -42.37751841893198446, 435.9440627571723326, 7.948837343527305421 ) ) ;
#79445=CARTESIAN_POINT ( 'NONE',  ( -43.48220711419978812, 485.4752262574868951, 4.033700225028757025 ) ) ;
#79448=ORIENTED_EDGE ( 'NONE', *, *, #94369, .F. ) ;
#79449=EDGE_CURVE ( 'NONE', #23052, #2708, #34639, .T. ) ;
#79458=DIRECTION ( 'NONE',  ( 0.1269898409407502204, -0.9919025243773941236, 0.001721171576547747550 ) ) ;
#79475=CARTESIAN_POINT ( 'NONE',  ( 19.22276103763711319, 302.7169779577087070, 9.908341515297090396 ) ) ;
#79477=VERTEX_POINT ( 'NONE', #8654 ) ;
#79489=CARTESIAN_POINT ( 'NONE',  ( 42.48192783572675779, 485.4100919824720677, -3.499593777788684523 ) ) ;
#79517=CARTESIAN_POINT ( 'NONE',  ( 31.90221457330017785, 317.1353150898008266, -7.038899609007000180 ) ) ;
#79518=DIRECTION ( 'NONE',  ( 0.4753313241820203983, -0.2469313775204406425, 0.8444436198155712558 ) ) ;
#79520=CARTESIAN_POINT ( 'NONE',  ( -27.94623540071386003, 307.0441435012233455, -9.286149966824948976 ) ) ;
#79537=CARTESIAN_POINT ( 'NONE',  ( 40.66390020119442283, 311.9487095737082427, -5.937893087732901698 ) ) ;
#79556=COLOUR_RGB ( '', 0.31764706, 0.68627451, 0.89019608) ;
#79599=CARTESIAN_POINT ( 'NONE',  ( 41.15051831715039299, 464.6037346866244775, 16.66306381442320372 ) ) ;
#79616=EDGE_LOOP ( 'NONE', ( #90137, #97512, #810, #89586, #62715 ) ) ;
#79625=CARTESIAN_POINT ( 'NONE',  ( 43.34642793389308935, 464.8022470463094464, 10.25621957614987956 ) ) ;
#79630=CARTESIAN_POINT ( 'NONE',  ( 43.84752573847596580, 486.0721194390229698, 5.282948175099586585 ) ) ;
#79653=CARTESIAN_POINT ( 'NONE',  ( -21.51569398614858031, 294.9107018935607130, -9.987480606144492512 ) ) ;
#79655=FACE_OUTER_BOUND ( 'NONE', #82316, .T. ) ;
#79656=CARTESIAN_POINT ( 'NONE',  ( -34.24139198049589794, 434.2621489448225134, 10.63631919729165887 ) ) ;
#79664=ADVANCED_FACE ( 'NONE', ( #97015 ), #54561, .T. ) ;
#79666=CARTESIAN_POINT ( 'NONE',  ( -28.61750315445088333, 319.5788945160356320, 13.56838495107838760 ) ) ;
#79710=ORIENTED_EDGE ( 'NONE', *, *, #25287, .T. ) ;
#79718=CARTESIAN_POINT ( 'NONE',  ( 38.13456177595863750, 310.3538162346446825, 5.629934070714594618 ) ) ;
#79722=CARTESIAN_POINT ( 'NONE',  ( -39.69476719266030074, 459.8381870091886867, 1.879428691193028467 ) ) ;
#79732=CARTESIAN_POINT ( 'NONE',  ( -24.72181951469942973, 304.3809629507088630, 10.27362881536904382 ) ) ;
#79746=CARTESIAN_POINT ( 'NONE',  ( 35.30457612794975120, 437.1674308734191072, 5.430039551426535382 ) ) ;
#79754=CARTESIAN_POINT ( 'NONE',  ( 9.970195021754667764, 302.6460196488380916, -10.04373974541434045 ) ) ;
#79766=CARTESIAN_POINT ( 'NONE',  ( 20.05074616892822448, 67.05096163904791240, 10.02537308446411224 ) ) ;
#79817=CARTESIAN_POINT ( 'NONE',  ( -10.01915592506624897, 302.6453132215667097, -2.043889601136170686 ) ) ;
#79819=CARTESIAN_POINT ( 'NONE',  ( 32.64200203778431586, 464.2416672416183019, 8.403568186820924879 ) ) ;
#79830=ORIENTED_EDGE ( 'NONE', *, *, #86004, .T. ) ;
#79834=CARTESIAN_POINT ( 'NONE',  ( 32.21797308369555424, 464.6987731533820352, 10.77720717743793344 ) ) ;
#79835=CARTESIAN_POINT ( 'NONE',  ( -32.03156805414178621, 438.9467387518307646, 23.64778041155028276 ) ) ;
#79837=CARTESIAN_POINT ( 'NONE',  ( 33.74271564777241394, 484.1802673187709729, 2.058285076122400081 ) ) ;
#79839=CARTESIAN_POINT ( 'NONE',  ( -33.00540147334749008, 487.4196752801198613, 9.523982417603866324 ) ) ;
#79843=AXIS2_PLACEMENT_3D ( 'NONE', #81889, #56553, #47928 ) ;
#79847=CARTESIAN_POINT ( 'NONE',  ( -31.38357374201002870, 298.3332731590748494, -9.233538704492573856 ) ) ;
#79862=CARTESIAN_POINT ( 'NONE',  ( -33.21102376836598324, 438.9613914113128317, 23.92328486949907074 ) ) ;
#79864=CARTESIAN_POINT ( 'NONE',  ( -37.62251730745840916, 437.3427388312646258, 4.535622330043208805 ) ) ;
#79894=VERTEX_POINT ( 'NONE', #58145 ) ;
#79899=B_SPLINE_CURVE_WITH_KNOTS ( 'NONE', 3,
 ( #58685, #84013, #19340, #75379, #77524, #18789, #52169, #91587, #76980, #10119, #43029, #66771, #1478, #75918, #51637, #36042 ),
 .UNSPECIFIED., .F., .F.,
 ( 4, 2, 2, 2, 2, 2, 2, 4 ),
 ( 7.152448122690996019E-18, 0.0005173708498437065446, 0.001034741699687405933, 0.001552112549531105322, 0.002069483399374804494, 0.002586854249218503883, 0.003104225099062203272, 0.004138966798749600315 ),
 .UNSPECIFIED. ) ;
#79904=B_SPLINE_CURVE_WITH_KNOTS ( 'NONE', 3,
 ( #63440, #22461, #96333, #45131 ),
 .UNSPECIFIED., .F., .F.,
 ( 4, 4 ),
 ( 0.000000000000000000, 0.0002629889189352557668 ),
 .UNSPECIFIED. ) ;
#79930=FACE_OUTER_BOUND ( 'NONE', #15000, .T. ) ;
#79944=CARTESIAN_POINT ( 'NONE',  ( -43.67631032990321671, 390.4612520042348365, 15.75310585023781407 ) ) ;
#79949=CARTESIAN_POINT ( 'NONE',  ( -35.61930400255787532, 462.7723509827301314, 4.024879462734057611 ) ) ;
#79954=EDGE_CURVE ( 'NONE', #57189, #48471, #99657, .T. ) ;
#79956=ORIENTED_EDGE ( 'NONE', *, *, #19731, .F. ) ;
#79958=CARTESIAN_POINT ( 'NONE',  ( 45.43339346675878687, 430.7348383325900727, 7.234598910837349628 ) ) ;
#79960=CARTESIAN_POINT ( 'NONE',  ( -33.88469969133009840, 464.6054137899091074, 6.797944932417651742 ) ) ;
#79965=CARTESIAN_POINT ( 'NONE',  ( 0.000000000000000000, 0.000000000000000000, 0.000000000000000000 ) ) ;
#79972=CIRCLE ( 'NONE', #67897, 1.000000000000001110 ) ;
#79974=VERTEX_POINT ( 'NONE', #43567 ) ;
#79999=CARTESIAN_POINT ( 'NONE',  ( 15.86539410927191440, 294.5609640058206082, 9.875179453861520074 ) ) ;
#80018=CARTESIAN_POINT ( 'NONE',  ( -46.00000000000000000, 463.6369139993306021, 9.775485381098368620 ) ) ;
#80035=CARTESIAN_POINT ( 'NONE',  ( 34.99329892478774440, 329.7144367575227193, -3.662448773238903055 ) ) ;
#80050=CARTESIAN_POINT ( 'NONE',  ( -33.74271564777242105, 484.1802673187710297, 2.058285076122328139 ) ) ;
#80061=CARTESIAN_POINT ( 'NONE',  ( 32.45330468351755826, 312.3793289830200592, -7.753281021820742858 ) ) ;
#80077=CARTESIAN_POINT ( 'NONE',  ( 43.03987588564147160, 486.0760633267551611, 5.817066388975991487 ) ) ;
#80098=( BOUNDED_SURFACE ( )  B_SPLINE_SURFACE ( 3, 2, ( 
 ( #63919, #71989, #45610 ),
 ( #31039, #96806, #22937 ),
 ( #88710, #80597, #6718 ),
 ( #72514, #105420, #94700 ),
 ( #53679, #86613, #12678 ),
 ( #33147, #106463, #24533 ),
 ( #40674, #64443, #182 ),
 ( #89773, #24007, #15875 ),
 ( #7770, #42263, #32621 ),
 ( #82733, #8835, #50348 ) ),
 .UNSPECIFIED., .F., .F., .F. ) 
 B_SPLINE_SURFACE_WITH_KNOTS ( ( 4, 2, 2, 2, 4 ),
 ( 3, 3 ),
 ( 9.697104230710351658E-16, 0.002793818337083670434, 0.003492272921354345507, 0.004190727505625021013, 0.005587636674166371158 ),
 ( 0.000000000000000000, 1.000000000000000000 ),
 .UNSPECIFIED. ) 
 GEOMETRIC_REPRESENTATION_ITEM ( )  RATIONAL_B_SPLINE_SURFACE ( (
 ( 1.000000000000000000, 0.8239349643288951253, 1.000000000000000000),
 ( 1.000000000000000000, 0.8395566633234762266, 1.000000000000000000),
 ( 1.000000000000000000, 0.8448327636285400954, 1.000000000000000000),
 ( 1.000000000000000000, 0.8449253468988903171, 1.000000000000000000),
 ( 1.000000000000000000, 0.8445754865264456512, 1.000000000000000000),
 ( 1.000000000000000000, 0.8431693930248722602, 1.000000000000000000),
 ( 1.000000000000000000, 0.8421154100732993752, 1.000000000000000000),
 ( 1.000000000000000000, 0.8378581409665019075, 1.000000000000000000),
 ( 1.000000000000000000, 0.8335888548700695067, 1.000000000000000000),
 ( 1.000000000000000000, 0.8273155905870500648, 1.000000000000000000) ) ) 
 REPRESENTATION_ITEM ( '' )  SURFACE ( )  );
#80099=CARTESIAN_POINT ( 'NONE',  ( -43.00000000000000000, 437.9690125970932399, 14.09127711025710639 ) ) ;
#80103=VERTEX_POINT ( 'NONE', #48850 ) ;
#80108=CARTESIAN_POINT ( 'NONE',  ( 26.15315386302562928, 305.7446874650615882, 10.59157493570054775 ) ) ;
#80110=DIRECTION ( 'NONE',  ( 0.2266275398148295539, 0.09415776302337237891, 0.9694195551255979648 ) ) ;
#80111=CARTESIAN_POINT ( 'NONE',  ( -46.00000000000000000, 488.0336798547362491, -0.8984331811837963366 ) ) ;
#80117=CARTESIAN_POINT ( 'NONE',  ( 0.000000000000000000, 294.8518027762758038, 9.936999415352289589 ) ) ;
#80118=CARTESIAN_POINT ( 'NONE',  ( -40.38854417759198157, 485.1419806746749828, -4.245955111568370022 ) ) ;
#80119=CARTESIAN_POINT ( 'NONE',  ( 0.000000000000000000, 294.8518027762758038, -10.00000000000000178 ) ) ;
#80123=CARTESIAN_POINT ( 'NONE',  ( 40.62716977365077042, 464.4319289640043849, 17.32222667058900001 ) ) ;
#80124=CARTESIAN_POINT ( 'NONE',  ( -33.00000000000000000, 450.0000000000002274, 28.20242257375372219 ) ) ;
#80144=CARTESIAN_POINT ( 'NONE',  ( 15.72108712621133186, 304.5560400716026379, 9.874133111316416134 ) ) ;
#80151=CARTESIAN_POINT ( 'NONE',  ( 0.000000000000000000, 273.9999999999999432, 0.000000000000000000 ) ) ;
#80154=CARTESIAN_POINT ( 'NONE',  ( 43.35041983546129529, 465.4837887079268057, 10.07799631932362239 ) ) ;
#80163=CARTESIAN_POINT ( 'NONE',  ( 35.05202888951401263, 439.1669932502342135, 24.09215602862335004 ) ) ;
#80186=CARTESIAN_POINT ( 'NONE',  ( -25.89661693312760349, 307.0966920204201642, 10.68061420533875250 ) ) ;
#80188=CARTESIAN_POINT ( 'NONE',  ( 20.08142311587312179, 304.8415473682318861, 8.934819560836576358 ) ) ;
#80191=ORIENTED_EDGE ( 'NONE', *, *, #73202, .T. ) ;
#80211=CARTESIAN_POINT ( 'NONE',  ( 1.262177448353618889E-25, 303.8518027762758038, -10.00000000000000533 ) ) ;
#80221=CARTESIAN_POINT ( 'NONE',  ( 38.47428897412612514, 484.8307741943459632, -5.088672563358043632 ) ) ;
#80237=CARTESIAN_POINT ( 'NONE',  ( 37.52740353635520165, 308.4545598930066035, 5.153891583661067699 ) ) ;
#80242=CARTESIAN_POINT ( 'NONE',  ( 32.62396605173337605, 486.1273723460453766, 7.520682129464227650 ) ) ;
#80243=EDGE_CURVE ( 'NONE', #101726, #1493, #53451, .T. ) ;
#80244=CARTESIAN_POINT ( 'NONE',  ( -33.21566647566201880, 463.2601667903500129, 6.161217084504481356 ) ) ;
#80247=CARTESIAN_POINT ( 'NONE',  ( -42.10086803841213765, 435.6552064019012960, 19.95582312411055881 ) ) ;
#80248=CARTESIAN_POINT ( 'NONE',  ( -31.40680613098830420, 299.6578337794886124, 11.01686700637052674 ) ) ;
#80254=CARTESIAN_POINT ( 'NONE',  ( 13.22944098689769632, 303.5546580367862930, 9.873837682497947910 ) ) ;
#80262=EDGE_CURVE ( 'NONE', #71046, #78613, #48270, .T. ) ;
#80263=CARTESIAN_POINT ( 'NONE',  ( 35.52295374289817431, 436.6489517640840177, 4.915275271775414012 ) ) ;
#80273=CARTESIAN_POINT ( 'NONE',  ( 9.297673743008640912, 295.3592874400322899, -10.03978397955114588 ) ) ;
#80286=CARTESIAN_POINT ( 'NONE',  ( 0.000000000000000000, -19.99999999999998934, 0.000000000000000000 ) ) ;
#80291=ORIENTED_EDGE ( 'NONE', *, *, #86004, .F. ) ;
#80307=CARTESIAN_POINT ( 'NONE',  ( 34.15310232806822910, 465.0579147271382681, 17.72315479633545010 ) ) ;
#80319=ADVANCED_FACE ( 'NONE', ( #63681 ), #46403, .T. ) ;
#80324=ORIENTED_EDGE ( 'NONE', *, *, #26573, .T. ) ;
#80330=B_SPLINE_CURVE_WITH_KNOTS ( 'NONE', 3,
 ( #4278, #55596, #88532, #14611 ),
 .UNSPECIFIED., .F., .F.,
 ( 4, 4 ),
 ( 3.469446951953614189E-18, 0.001900242520396275888 ),
 .UNSPECIFIED. ) ;
#80335=CARTESIAN_POINT ( 'NONE',  ( -9.047684060188633026, 302.6745968392543205, 9.899357598522687596 ) ) ;
#80342=CARTESIAN_POINT ( 'NONE',  ( -33.80014854764822019, 484.1533675815112474, 1.810747741428984314 ) ) ;
#80348=CARTESIAN_POINT ( 'NONE',  ( -0.4977218462097728335, 295.8604035916879980, -9.999999999979417353 ) ) ;
#80355=CARTESIAN_POINT ( 'NONE',  ( 30.00000000000000355, 461.8423776372148950, 11.25810401088899759 ) ) ;
#80360=FACE_OUTER_BOUND ( 'NONE', #84960, .T. ) ;
#80363=CARTESIAN_POINT ( 'NONE',  ( -32.12566262182737375, 486.1613120233242284, 5.452106427430423174 ) ) ;
#80370=CARTESIAN_POINT ( 'NONE',  ( -33.30612659720004132, 300.4521844812165341, -0.7417152064293228708 ) ) ;
#80379=CARTESIAN_POINT ( 'NONE',  ( 22.22078930644830308, 305.3250122787871987, 9.038968116793329344 ) ) ;
#80388=CARTESIAN_POINT ( 'NONE',  ( -46.00000000001166711, 463.3768225339526907, 8.978553580135045564 ) ) ;
#80389=CARTESIAN_POINT ( 'NONE',  ( -35.05548986855151838, 439.9462388155539543, 24.33445361994856526 ) ) ;
#80391=CARTESIAN_POINT ( 'NONE',  ( -26.21429215707765792, 304.5182411030272078, -9.636487232772985578 ) ) ;
#80392=EDGE_CURVE ( 'NONE', #17876, #73295, #85549, .T. ) ;
#80407=ORIENTED_EDGE ( 'NONE', *, *, #45975, .T. ) ;
#80408=DIRECTION ( 'NONE',  ( 0.000000000000000000, 0.000000000000000000, 1.000000000000000000 ) ) ;
#80428=( GEOMETRIC_REPRESENTATION_CONTEXT ( 3 ) GLOBAL_UNCERTAINTY_ASSIGNED_CONTEXT ( ( #53696 ) ) GLOBAL_UNIT_ASSIGNED_CONTEXT ( ( #57945, #18055, #75736 ) ) REPRESENTATION_CONTEXT ( 'NONE', 'WORKASPACE' ) );
#80442=CARTESIAN_POINT ( 'NONE',  ( -15.72336466908044095, 304.5560426036738022, 8.874135081214639342 ) ) ;
#80444=CARTESIAN_POINT ( 'NONE',  ( 30.00000000000000000, 462.0217650461267453, 12.66663979486846081 ) ) ;
#80446=CARTESIAN_POINT ( 'NONE',  ( -43.03987588564145028, 486.0760633267551611, 5.817066388976097180 ) ) ;
#80466=CARTESIAN_POINT ( 'NONE',  ( 43.77599596716764552, 462.5271020414195391, 5.125623680081139888 ) ) ;
#80472=CARTESIAN_POINT ( 'NONE',  ( 37.02012750797187124, 345.4824561708261399, 0.1020140138803038443 ) ) ;
#80483=CARTESIAN_POINT ( 'NONE',  ( -26.54817876223620488, 310.6276912632132507, 11.31208242866018132 ) ) ;
#80488=LINE ( 'NONE', #13099, #101659 ) ;
#80492=CARTESIAN_POINT ( 'NONE',  ( -44.10116655607205871, 485.7577240482563070, 4.111541829922503943 ) ) ;
#80530=CARTESIAN_POINT ( 'NONE',  ( 0.000000000000000000, 0.000000000000000000, 0.000000000000000000 ) ) ;
#80548=DIRECTION ( 'NONE',  ( 0.000000000000000000, -1.000000000000000000, 0.000000000000000000 ) ) ;
#80549=ORIENTED_EDGE ( 'NONE', *, *, #84641, .T. ) ;
#80558=CARTESIAN_POINT ( 'NONE',  ( -40.93435977689158989, 414.3154843149413296, 27.72243992809649527 ) ) ;
#80564=CARTESIAN_POINT ( 'NONE',  ( 33.72097909745567534, 327.0062835497062110, -4.563092033313610685 ) ) ;
#80568=CARTESIAN_POINT ( 'NONE',  ( -22.25702730880545843, 304.1569973802309619, -9.934833947929556430 ) ) ;
#80570=CARTESIAN_POINT ( 'NONE',  ( -43.18591170618147146, 464.9496799542819190, 14.54256400180418218 ) ) ;
#80578=CARTESIAN_POINT ( 'NONE',  ( -35.03620922308809327, 464.5070590296365367, 18.87187099903851717 ) ) ;
#80588=CARTESIAN_POINT ( 'NONE',  ( 37.02242109889342458, 304.0242369042755968, -7.899015950623281768 ) ) ;
#80597=CARTESIAN_POINT ( 'NONE',  ( 43.58530483652910448, 484.9293427334628177, 0.7222135195755269299 ) ) ;
#80604=FACE_OUTER_BOUND ( 'NONE', #59123, .T. ) ;
#80611=PRESENTATION_STYLE_ASSIGNMENT (( #47712 ) ) ;
#80614=CARTESIAN_POINT ( 'NONE',  ( -44.28408485723331722, 463.6816916292610813, 7.557853517639972374 ) ) ;
#80615=CARTESIAN_POINT ( 'NONE',  ( 43.00000000000000000, 461.4080316921935605, 3.462976341553817949 ) ) ;
#80619=ORIENTED_EDGE ( 'NONE', *, *, #106052, .F. ) ;
#80633=CARTESIAN_POINT ( 'NONE',  ( -44.47935674825744456, 338.5055569983761643, 0.4977047367126199995 ) ) ;
#80636=CARTESIAN_POINT ( 'NONE',  ( -44.22863636901156070, 485.2832843285482909, 1.778997975940832310 ) ) ;
#80637=CARTESIAN_POINT ( 'NONE',  ( -33.84761347220299399, 488.7471039746336032, 11.01988148152527103 ) ) ;
#80640=DIRECTION ( 'NONE',  ( 0.000000000000000000, 0.000000000000000000, -1.000000000000000000 ) ) ;
#80643=CARTESIAN_POINT ( 'NONE',  ( 3.364021409948656505, 294.8518027753228807, 9.936999415087239385 ) ) ;
#80649=CARTESIAN_POINT ( 'NONE',  ( 40.97311670756442226, 465.3163554148249546, 16.72191547249029853 ) ) ;
#80654=VERTEX_POINT ( 'NONE', #95781 ) ;
#80658=( GEOMETRIC_REPRESENTATION_CONTEXT ( 3 ) GLOBAL_UNCERTAINTY_ASSIGNED_CONTEXT ( ( #38419 ) ) GLOBAL_UNIT_ASSIGNED_CONTEXT ( ( #31035, #7767, #39640 ) ) REPRESENTATION_CONTEXT ( 'NONE', 'WORKASPACE' ) );
#80659=CARTESIAN_POINT ( 'NONE',  ( -36.52797673978124493, 490.9928046865521196, 12.47113835538635129 ) ) ;
#80668=CARTESIAN_POINT ( 'NONE',  ( 3.339334701221695401, 304.8518027741603191, 9.936999414964258648 ) ) ;
#80669=ORIENTED_EDGE ( 'NONE', *, *, #39336, .T. ) ;
#80690=CARTESIAN_POINT ( 'NONE',  ( 36.88942319598261577, 438.8974264175596431, 23.87252030258318669 ) ) ;
#80693=CARTESIAN_POINT ( 'NONE',  ( 40.21603221112102489, 460.7694907478772848, 2.143794914364641535 ) ) ;
#80695=B_SPLINE_CURVE_WITH_KNOTS ( 'NONE', 3,
 ( #66397, #17339, #50214, #75005 ),
 .UNSPECIFIED., .F., .F.,
 ( 4, 4 ),
 ( 0.000000000000000000, 0.001346487449956073213 ),
 .UNSPECIFIED. ) ;
#80706=CARTESIAN_POINT ( 'NONE',  ( -42.80417301746779657, 434.8807528697725502, 8.723038671918009967 ) ) ;
#80709=CARTESIAN_POINT ( 'NONE',  ( -38.47428897412184767, 485.7788508071988645, -4.770630528146724281 ) ) ;
#80715=CARTESIAN_POINT ( 'NONE',  ( -30.15664824853507398, 323.6649206493684687, 14.81758955126313637 ) ) ;
#80724=CARTESIAN_POINT ( 'NONE',  ( 44.08482021419140295, 485.1618240760802792, 0.4493778471356573712 ) ) ;
#80742=CYLINDRICAL_SURFACE ( 'NONE', #35279, 15.00000000000000711 ) ;
#80743=CARTESIAN_POINT ( 'NONE',  ( 11.86977464456163922, 303.5920060571866088, -10.05522031238126424 ) ) ;
#80744=CARTESIAN_POINT ( 'NONE',  ( 30.12932728364529922, 334.4140447340107585, 17.11298374841474867 ) ) ;
#80754=CARTESIAN_POINT ( 'NONE',  ( -21.64906249285503392, 304.1279031160725026, 9.996121053679246415 ) ) ;
#80756=( GEOMETRIC_REPRESENTATION_CONTEXT ( 3 ) GLOBAL_UNCERTAINTY_ASSIGNED_CONTEXT ( ( #100166 ) ) GLOBAL_UNIT_ASSIGNED_CONTEXT ( ( #51119, #3120, #36064 ) ) REPRESENTATION_CONTEXT ( 'NONE', 'WORKASPACE' ) );
#80767=VERTEX_POINT ( 'NONE', #21388 ) ;
#80768=DIRECTION ( 'NONE',  ( 0.000000000000000000, 0.000000000000000000, 1.000000000000000000 ) ) ;
#80773=CARTESIAN_POINT ( 'NONE',  ( 38.82779737621938665, 321.9597977506067537, 16.55577433839140156 ) ) ;
#80784=CARTESIAN_POINT ( 'NONE',  ( -43.21649601278601693, 436.3330504929538165, 19.41248623753216407 ) ) ;
#80786=CARTESIAN_POINT ( 'NONE',  ( -31.43357885710805633, 299.6859785502570048, 11.02347074399675186 ) ) ;
#80802=DIRECTION ( 'NONE',  ( -0.000000000000000000, -1.000000000000000000, -0.000000000000000000 ) ) ;
#80811=EDGE_CURVE ( 'NONE', #56333, #97465, #8351, .T. ) ;
#80821=DIRECTION ( 'NONE',  ( 0.000000000000000000, 0.000000000000000000, -1.000000000000000000 ) ) ;
#80853=CIRCLE ( 'NONE', #32626, 5.000000000000000888 ) ;
#80865=CARTESIAN_POINT ( 'NONE',  ( -3.010187908185308903, 299.5653876365528845, -10.00571708631421686 ) ) ;
#80869=B_SPLINE_CURVE_WITH_KNOTS ( 'NONE', 3,
 ( #79248, #64150, #4839, #95976 ),
 .UNSPECIFIED., .F., .F.,
 ( 4, 4 ),
 ( 0.000000000000000000, 0.0002092826938412524983 ),
 .UNSPECIFIED. ) ;
#80874=CARTESIAN_POINT ( 'NONE',  ( -11.99473552897978124, 294.5867349183714623, 1.880683768558506719 ) ) ;
#80877=CARTESIAN_POINT ( 'NONE',  ( 20.37278541768183615, 303.8378246129572631, -10.00297115033342266 ) ) ;
#80878=CARTESIAN_POINT ( 'NONE',  ( 37.83989825151484609, 491.6297408768497803, 12.44743998625087933 ) ) ;
#80895=CARTESIAN_POINT ( 'NONE',  ( -32.17889379758943846, 439.3695696554026426, 23.63219374846804044 ) ) ;
#80898=CARTESIAN_POINT ( 'NONE',  ( -30.72294868208370744, 313.4051624346869289, -7.977499477794275151 ) ) ;
#80900=CARTESIAN_POINT ( 'NONE',  ( -29.99999999999997158, 486.7667864837128491, 5.222266633581357453 ) ) ;
#80905=CARTESIAN_POINT ( 'NONE',  ( -33.52989424313292233, 300.6882358251922369, -0.6863093620646967263 ) ) ;
#80912=DIRECTION ( 'NONE',  ( -1.000000000000000000, 0.000000000000000000, 0.000000000000000000 ) ) ;
#80913=DIRECTION ( 'NONE',  ( 0.1270361284032104077, 0.9918980905719715357, 0.000000000000000000 ) ) ;
#80914=CARTESIAN_POINT ( 'NONE',  ( 30.13443748760208862, 331.7808586020135522, 15.50310796814377845 ) ) ;
#80925=CARTESIAN_POINT ( 'NONE',  ( -34.07401144359369738, 439.5803311721820705, 24.00237084771177010 ) ) ;
#80932=CARTESIAN_POINT ( 'NONE',  ( -33.00000000000000000, 450.0000000000002274, -1.797577426246302013 ) ) ;
#80933=EDGE_CURVE ( 'NONE', #37996, #79894, #63864, .T. ) ;
#80938=DIRECTION ( 'NONE',  ( 0.000000000000000000, 0.000000000000000000, 1.000000000000000000 ) ) ;
#80944=AXIS2_PLACEMENT_3D ( 'NONE', #47674, #14778, #6691 ) ;
#80945=B_SPLINE_CURVE_WITH_KNOTS ( 'NONE', 3,
 ( #8784, #49233, #82138, #25000, #67573, #99918, #9837, #49777, #32568, #74046, #1194, #66491 ),
 .UNSPECIFIED., .F., .F.,
 ( 4, 2, 2, 2, 2, 4 ),
 ( 0.000000000000000000, 0.0008601990320054680138, 0.001720398064010936028, 0.002580597096016404041, 0.003010696612019150842, 0.003440796128021898076 ),
 .UNSPECIFIED. ) ;
#80951=ORIENTED_EDGE ( 'NONE', *, *, #58298, .F. ) ;
#80962=CARTESIAN_POINT ( 'NONE',  ( 35.48628994100678824, 491.6413678155948332, 12.45547902532423379 ) ) ;
#80969=CARTESIAN_POINT ( 'NONE',  ( 33.21587117940961775, 465.5376284999449581, 9.463823683337858839 ) ) ;
#80975=FACE_OUTER_BOUND ( 'NONE', #59622, .T. ) ;
#80981=ORIENTED_EDGE ( 'NONE', *, *, #23819, .F. ) ;
#80988=CARTESIAN_POINT ( 'NONE',  ( 36.54984892593326151, 463.9827100737089722, 19.61538121061435547 ) ) ;
#80990=FACE_OUTER_BOUND ( 'NONE', #73419, .T. ) ;
#80997=CARTESIAN_POINT ( 'NONE',  ( 45.99999999999997158, 463.0783855722254430, 8.172228418139317441 ) ) ;
#81003=CARTESIAN_POINT ( 'NONE',  ( -43.67706251530178463, 402.9872697375532766, 16.14665223012086415 ) ) ;
#81006=CARTESIAN_POINT ( 'NONE',  ( -37.72161557782784058, 461.3708194167276702, 2.611246763486743117 ) ) ;
#81020=CARTESIAN_POINT ( 'NONE',  ( -31.42312704992726680, 414.9721857482184646, 24.35715877706864774 ) ) ;
#81030=ORIENTED_EDGE ( 'NONE', *, *, #22619, .F. ) ;
#81054=( BOUNDED_SURFACE ( )  B_SPLINE_SURFACE ( 3, 2, ( 
 ( #67647, #16972, #50900 ),
 ( #82213, #100526, #57400 ),
 ( #92427, #50371, #75177 ),
 ( #26687, #59023, #203 ),
 ( #34240, #74646, #83282 ),
 ( #33167, #59560, #91910 ),
 ( #18583, #51444, #7788 ),
 ( #40694, #73583, #106486 ),
 ( #32643, #65514, #98402 ),
 ( #24554, #25076, #57934 ),
 ( #58489, #90856, #49848 ),
 ( #730, #33696, #66570 ),
 ( #35843, #12045, #61153 ),
 ( #60634, #78381, #19668 ),
 ( #52505, #95118, #44977 ),
 ( #53581, #94039, #2885 ) ),
 .UNSPECIFIED., .F., .F., .T. ) 
 B_SPLINE_SURFACE_WITH_KNOTS ( ( 4, 2, 2, 2, 2, 2, 2, 4 ),
 ( 3, 3 ),
 ( 2.630274470449833757E-16, 0.0005221599045739626225, 0.001044319809147662217, 0.001566479713721361921, 0.002088639618295061624, 0.002610799522868761328, 0.003132959427442461031, 0.004177279236589860438 ),
 ( 0.000000000000000000, 1.000000000000000000 ),
 .UNSPECIFIED. ) 
 GEOMETRIC_REPRESENTATION_ITEM ( )  RATIONAL_B_SPLINE_SURFACE ( (
 ( 1.000000000000000000, 0.8909749942926979971, 1.000000000000000000),
 ( 1.000000000000000000, 0.8947619310247098001, 1.000000000000000000),
 ( 1.000000000000000000, 0.8978044232673220160, 1.000000000000000000),
 ( 1.000000000000000000, 0.9023043032728860213, 1.000000000000000000),
 ( 1.000000000000000000, 0.9037672509134783150, 1.000000000000000000),
 ( 1.000000000000000000, 0.9049062503963291038, 1.000000000000000000),
 ( 1.000000000000000000, 0.9045936109743369924, 1.000000000000000000),
 ( 1.000000000000000000, 0.9022616022707382610, 1.000000000000000000),
 ( 1.000000000000000000, 0.9002067130764697112, 1.000000000000000000),
 ( 1.000000000000000000, 0.8945795303826531431, 1.000000000000000000),
 ( 1.000000000000000000, 0.8910211780037325946, 1.000000000000000000),
 ( 1.000000000000000000, 0.8825640046898904911, 1.000000000000000000),
 ( 1.000000000000000000, 0.8776492255290634370, 1.000000000000000000),
 ( 1.000000000000000000, 0.8615337984044251218, 1.000000000000000000),
 ( 1.000000000000000000, 0.8487841387214820621, 1.000000000000000000),
 ( 1.000000000000000000, 0.8347624811021875368, 1.000000000000000000) ) ) 
 REPRESENTATION_ITEM ( '' )  SURFACE ( )  );
#81056=CARTESIAN_POINT ( 'NONE',  ( 16.33222328768405163, 294.5674815784677776, 1.876697781737655779 ) ) ;
#81059=CIRCLE ( 'NONE', #3553, 2.999999999999981792 ) ;
#81068=CARTESIAN_POINT ( 'NONE',  ( -37.83989825152028885, 491.6297408768477339, 12.44743998624950798 ) ) ;
#81069=CARTESIAN_POINT ( 'NONE',  ( 32.83703342409250325, 465.7129651006319477, 11.08653443108778092 ) ) ;
#81084=ORIENTED_EDGE ( 'NONE', *, *, #38504, .T. ) ;
#81090=CARTESIAN_POINT ( 'NONE',  ( 35.51382444471309441, 463.4141161792265962, 19.91564417027522538 ) ) ;
#81094=CARTESIAN_POINT ( 'NONE',  ( -45.31383884518383098, 362.9196860876334085, 5.161789940898600548 ) ) ;
#81096=CARTESIAN_POINT ( 'NONE',  ( -40.73878143178837519, 486.4834083601638213, 16.46716573231486436 ) ) ;
#81099=CARTESIAN_POINT ( 'NONE',  ( 28.97004836423603535, 308.1417733683699112, -9.028218307027925604 ) ) ;
#81102=ADVANCED_FACE ( 'NONE', ( #31990, #7670 ), #56211, .T. ) ;
#81109=VECTOR ( 'NONE', #42261, 1000.000000000000000 ) ;
#81122=CARTESIAN_POINT ( 'NONE',  ( 38.87647009787237806, 310.5762796638829855, 1.738341351311467387 ) ) ;
#81144=DIRECTION ( 'NONE',  ( 0.000000000000000000, 0.000000000000000000, -1.000000000000000000 ) ) ;
#81159=EDGE_LOOP ( 'NONE', ( #34784, #40629, #87691, #9559 ) ) ;
#81164=CARTESIAN_POINT ( 'NONE',  ( -43.06478785906146811, 345.9681365877381154, 10.01537130693817623 ) ) ;
#81165=CIRCLE ( 'NONE', #57056, 1.000000000000000222 ) ;
#81167=CARTESIAN_POINT ( 'NONE',  ( -46.00000000000572697, 486.0748346210346540, 1.693312618872886866 ) ) ;
#81180=CARTESIAN_POINT ( 'NONE',  ( 41.13675135394154836, 465.3862164892198052, 16.49847611935184943 ) ) ;
#81186=CARTESIAN_POINT ( 'NONE',  ( -36.65209206386415275, 491.4469928998125852, 12.33162904370220225 ) ) ;
#81200=CARTESIAN_POINT ( 'NONE',  ( -40.85715431133397146, 485.0116719597020847, -3.999197217707391339 ) ) ;
#81211=AXIS2_PLACEMENT_3D ( 'NONE', #6900, #15522, #48414 ) ;
#81212=EDGE_LOOP ( 'NONE', ( #86711, #103539, #97, #88991 ) ) ;
#81219=CARTESIAN_POINT ( 'NONE',  ( 41.35836404316623316, 461.4284568614619388, 2.579347946915451217 ) ) ;
#81220=ORIENTED_EDGE ( 'NONE', *, *, #61740, .T. ) ;
#81224=MECHANICAL_DESIGN_GEOMETRIC_PRESENTATION_REPRESENTATION('',(#64112),#8940);
#81225=CARTESIAN_POINT ( 'NONE',  ( 34.61135223818107676, 301.0186358733434986, -8.614137653301380482 ) ) ;
#81231=CARTESIAN_POINT ( 'NONE',  ( -33.63427961064055438, 325.9154870834976236, -4.827994974213513757 ) ) ;
#81240=CARTESIAN_POINT ( 'NONE',  ( -25.26650806423123896, 307.7638625427180727, 9.604356516990046444 ) ) ;
#81241=EDGE_CURVE ( 'NONE', #26579, #54099, #37915, .T. ) ;
#81242=ORIENTED_EDGE ( 'NONE', *, *, #7944, .T. ) ;
#81254=DIRECTION ( 'NONE',  ( 1.000000000000000000, 0.000000000000000000, 0.000000000000000000 ) ) ;
#81260=CARTESIAN_POINT ( 'NONE',  ( 37.88504238421471371, 463.4171042825133213, 19.90923349043903556 ) ) ;
#81270=CARTESIAN_POINT ( 'NONE',  ( 30.24427031855517711, 312.0196691915732004, -8.325478004009855937 ) ) ;
#81271=EDGE_LOOP ( 'NONE', ( #64781, #61578, #85281, #68966 ) ) ;
#81282=CARTESIAN_POINT ( 'NONE',  ( 33.07276483573664905, 438.9325140356084489, 23.89537236861388081 ) ) ;
#81284=CARTESIAN_POINT ( 'NONE',  ( -40.63205167635505433, 465.1703340539525016, 17.16604311417211548 ) ) ;
#81286=CARTESIAN_POINT ( 'NONE',  ( 42.35751940687331540, 435.3789575402772130, 19.45706151681951823 ) ) ;
#81293=CARTESIAN_POINT ( 'NONE',  ( 40.84703668878825766, 325.1337667956213977, 9.320964315343294615 ) ) ;
#81295=B_SPLINE_CURVE_WITH_KNOTS ( 'NONE', 3,
 ( #62938, #95832, #5746, #30051 ),
 .UNSPECIFIED., .F., .F.,
 ( 4, 4 ),
 ( 0.0007494527726711166030, 0.02469145274879585433 ),
 .UNSPECIFIED. ) ;
#81303=CARTESIAN_POINT ( 'NONE',  ( 32.14400760092454590, 464.7181002246658181, 11.03224828307627980 ) ) ;
#81305=CARTESIAN_POINT ( 'NONE',  ( -25.59654319921001075, 305.1310134180918112, 10.44692895254650900 ) ) ;
#81307=CARTESIAN_POINT ( 'NONE',  ( 37.85084083633365282, 438.0234350436313093, 4.171260309356235929 ) ) ;
#81310=VECTOR ( 'NONE', #102123, 1000.000000000000114 ) ;
#81312=CARTESIAN_POINT ( 'NONE',  ( 6.560339683636790653, 297.0608611330067674, 7.566031652892246662 ) ) ;
#81313=CARTESIAN_POINT ( 'NONE',  ( 16.53805850995897941, 303.5675046017279897, 9.876558242819349687 ) ) ;
#81331=AXIS2_PLACEMENT_3D ( 'NONE', #95060, #44916, #103139 ) ;
#81367=EDGE_CURVE ( 'NONE', #14964, #57174, #77811, .T. ) ;
#81375=CARTESIAN_POINT ( 'NONE',  ( -9.881511277310785601, 294.6462811792092680, 1.569873444576042942 ) ) ;
#81387=CARTESIAN_POINT ( 'NONE',  ( -6.618938675458717391, 296.2345938570451267, -10.01875627916766121 ) ) ;
#81397=CARTESIAN_POINT ( 'NONE',  ( 0.000000000000000000, 67.05096163904791240, 0.000000000000000000 ) ) ;
#81403=AXIS2_PLACEMENT_3D ( 'NONE', #56356, #229, #15386 ) ;
#81414=CARTESIAN_POINT ( 'NONE',  ( -31.76669557235910091, 439.7354465714767571, 23.77638826982954967 ) ) ;
#81416=CARTESIAN_POINT ( 'NONE',  ( -36.31305047672606179, 353.1205851602086341, 1.341197250394855489 ) ) ;
#81420=CARTESIAN_POINT ( 'NONE',  ( -43.61263226029857520, 434.4864728595579209, 10.89080223165826133 ) ) ;
#81421=ORIENTED_EDGE ( 'NONE', *, *, #103082, .F. ) ;
#81423=CARTESIAN_POINT ( 'NONE',  ( -27.29321646936245926, 296.3890529966017766, -1.667088702040937065 ) ) ;
#81437=ORIENTED_EDGE ( 'NONE', *, *, #43057, .F. ) ;
#81445=CARTESIAN_POINT ( 'NONE',  ( 41.46829321581945749, 485.6036604809296477, -3.691894868447965550 ) ) ;
#81449=EDGE_CURVE ( 'NONE', #57174, #46619, #73979, .T. ) ;
#81462=CARTESIAN_POINT ( 'NONE',  ( 36.64823341582351190, 437.5392299810055192, 4.281405873620245828 ) ) ;
#81472=CARTESIAN_POINT ( 'NONE',  ( 46.00000000000000000, 500.0000000000002274, 0.000000000000000000 ) ) ;
#81475=CARTESIAN_POINT ( 'NONE',  ( 43.65900554256388233, 484.6127093603670914, 3.254021613880305974 ) ) ;
#81476=FACE_OUTER_BOUND ( 'NONE', #42691, .T. ) ;
#81477=CARTESIAN_POINT ( 'NONE',  ( -32.81992448453853939, 465.7192846569224685, 11.17271167765295559 ) ) ;
#81489=CARTESIAN_POINT ( 'NONE',  ( 30.00000000000000355, 461.9594878872943582, 14.33673855775172079 ) ) ;
#81510=CARTESIAN_POINT ( 'NONE',  ( 46.00000000000000000, 462.4524393752382139, 6.584174932629923482 ) ) ;
#81523=ORIENTED_EDGE ( 'NONE', *, *, #66561, .F. ) ;
#81527=DIRECTION ( 'NONE',  ( -1.000000000000000000, 0.000000000000000000, 0.000000000000000000 ) ) ;
#81529=CARTESIAN_POINT ( 'NONE',  ( -33.16497501406121984, 438.9508968883769171, 23.91452439717005873 ) ) ;
#81532=CARTESIAN_POINT ( 'NONE',  ( -39.57869015843257898, 437.2512761492686195, 5.285341955748192433 ) ) ;
#81537=CIRCLE ( 'NONE', #35094, 0.9999999999999988898 ) ;
#81544=ORIENTED_EDGE ( 'NONE', *, *, #59875, .F. ) ;
#81556=VERTEX_POINT ( 'NONE', #89023 ) ;
#81567=B_SPLINE_SURFACE_WITH_KNOTS ( 'NONE', 1, 3, ( 
 ( #79653, #39220, #5249, #4717, #5764, #70515, #94805, #37654, #38178, #54836, #6281, #21981, #29558, #62429, #71034, #38686, #103925, #71552, #63494, #89877, #81755, #15445, #23574, #41318, #76199, #49399, #73132, #15985 ),
 ( #43317, #73678, #64548, #56422, #82308, #2301, #89355, #8418, #48336, #68116, #97414, #24113, #32183, #81231, #10402, #106036, #57485, #74208, #287, #35250, #101013, #33253, #7348, #48862, #106580, #40257, #65066, #66126 ) ),
 .UNSPECIFIED., .F., .F., .F.,
 ( 2, 2 ),
 ( 4, 2, 2, 2, 2, 2, 2, 2, 2, 2, 2, 2, 2, 4 ),
 ( 0.000000000000000000, 1.000000000000000000 ),
 ( 0.08901491201581737678, 0.1032490540155679704, 0.1174831960153185778, 0.1317173380150691853, 0.1459514800148197788, 0.1744197640143299588, 0.2028880480138401388, 0.2598246160128514504, 0.3167611840118632616, 0.4306343200098861623, 0.5445074560079088410, 0.6583805920059359051, 0.7722537280039543095, 1.000000000000000000 ),
 .UNSPECIFIED. ) ;
#81569=EDGE_CURVE ( 'NONE', #4842, #58946, #28967, .T. ) ;
#81580=CARTESIAN_POINT ( 'NONE',  ( -39.59091745083550506, 490.2217143383006714, 11.38611456561468316 ) ) ;
#81584=CARTESIAN_POINT ( 'NONE',  ( 35.03794650530581123, 439.1670263218123864, 24.09217910952948216 ) ) ;
#81605=CARTESIAN_POINT ( 'NONE',  ( -33.08751701378358945, 301.6823158026044780, 11.49690784967660662 ) ) ;
#81607=CARTESIAN_POINT ( 'NONE',  ( -32.16694665535142406, 298.7751107022914425, -9.134474995491629556 ) ) ;
#81611=CARTESIAN_POINT ( 'NONE',  ( 30.56684744126956232, 310.6574340941369314, -8.419107643419287967 ) ) ;
#81622=CARTESIAN_POINT ( 'NONE',  ( -32.45893998669878044, 464.7013998967537418, 16.05169235329088195 ) ) ;
#81627=DIRECTION ( 'NONE',  ( 0.000000000000000000, 0.9024170203239317845, -0.4308636924012935743 ) ) ;
#81662=CARTESIAN_POINT ( 'NONE',  ( -11.68525014344062818, 302.5966531034369496, -10.05424063234815613 ) ) ;
#81671=CARTESIAN_POINT ( 'NONE',  ( 30.00000000000000355, 461.9311049912211047, 11.83317730145386015 ) ) ;
#81681=CARTESIAN_POINT ( 'NONE',  ( 23.89727872382834661, 303.8791563162774310, 10.16063969049587712 ) ) ;
#81682=CARTESIAN_POINT ( 'NONE',  ( -37.68702322361429680, 382.9563223952199564, 5.553542584039877994 ) ) ;
#81705=ADVANCED_FACE ( 'NONE', ( #59315 ), #32128, .F. ) ;
#81706=CARTESIAN_POINT ( 'NONE',  ( -34.34094660029732182, 491.0078558915762983, 12.00869558947848859 ) ) ;
#81734=CARTESIAN_POINT ( 'NONE',  ( 36.71005241817402975, 463.3006260613077529, 20.13736821485172612 ) ) ;
#81749=CARTESIAN_POINT ( 'NONE',  ( 28.93681320501227106, 306.6321427781763873, -9.151182930968348117 ) ) ;
#81755=CARTESIAN_POINT ( 'NONE',  ( -45.49982102694234953, 388.3127959276886827, 7.886590035822850453 ) ) ;
#81762=CARTESIAN_POINT ( 'NONE',  ( 43.41041896048977833, 463.0441421627334080, 5.626145546387755658 ) ) ;
#81789=CARTESIAN_POINT ( 'NONE',  ( 29.01988888469873018, 321.8047804620298393, 14.12772110426748284 ) ) ;
#81793=CARTESIAN_POINT ( 'NONE',  ( 23.95564068939877345, 305.6666757346319514, -9.824255363917307804 ) ) ;
#81804=ORIENTED_EDGE ( 'NONE', *, *, #89010, .F. ) ;
#81813=EDGE_LOOP ( 'NONE', ( #38506, #69595, #63152, #47266, #30680 ) ) ;
#81816=CARTESIAN_POINT ( 'NONE',  ( 33.50421398922629379, 488.2600042842303196, 10.59612602190272312 ) ) ;
#81817=( GEOMETRIC_REPRESENTATION_CONTEXT ( 3 ) GLOBAL_UNCERTAINTY_ASSIGNED_CONTEXT ( ( #83266 ) ) GLOBAL_UNIT_ASSIGNED_CONTEXT ( ( #35376, #11579, #94108 ) ) REPRESENTATION_CONTEXT ( 'NONE', 'WORKASPACE' ) );
#81819=CARTESIAN_POINT ( 'NONE',  ( 30.50659871040408078, 318.9590941947862461, 13.89418334184498427 ) ) ;
#81820=CIRCLE ( 'NONE', #102557, 10.00000000000000000 ) ;
#81825=CARTESIAN_POINT ( 'NONE',  ( -41.35951450184050771, 460.7308729162644454, 2.709719765164665617 ) ) ;
#81827=CARTESIAN_POINT ( 'NONE',  ( 32.71902930631058837, 485.4797908183053323, 6.287473911065069920 ) ) ;
#81830=CARTESIAN_POINT ( 'NONE',  ( -28.24278080084331322, 297.1537272779650607, 10.44109103508797887 ) ) ;
#81837=( BOUNDED_SURFACE ( )  B_SPLINE_SURFACE ( 3, 2, ( 
 ( #81445, #38905, #97115 ),
 ( #31366, #14063, #72830 ),
 ( #64242, #16195, #81978 ),
 ( #30831, #56647, #22736 ) ),
 .UNSPECIFIED., .F., .F., .F. ) 
 B_SPLINE_SURFACE_WITH_KNOTS ( ( 4, 4 ),
 ( 3, 3 ),
 ( 0.007093323349943533689, 0.03301372383216878009 ),
 ( 0.000000000000000000, 1.000000000000000000 ),
 .UNSPECIFIED. ) 
 GEOMETRIC_REPRESENTATION_ITEM ( )  RATIONAL_B_SPLINE_SURFACE ( (
 ( 1.000000000000000000, 0.8381405729291011575, 1.000000000000000000),
 ( 1.000000000000000000, 0.8381407632135386976, 1.000000000000000000),
 ( 1.000000000000000000, 0.8381408010577027223, 1.000000000000000000),
 ( 1.000000000000000000, 0.8381406085692050256, 1.000000000000000000) ) ) 
 REPRESENTATION_ITEM ( '' )  SURFACE ( )  );
#81841=CARTESIAN_POINT ( 'NONE',  ( 0.000000000000000000, 303.8518027762758038, 9.936999415352289589 ) ) ;
#81847=CARTESIAN_POINT ( 'NONE',  ( 42.58433969240391548, 479.4768267386956495, 9.887265036232028237 ) ) ;
#81850=AXIS2_PLACEMENT_3D ( 'NONE', #67568, #19589, #85337 ) ;
#81855=LINE ( 'NONE', #88391, #15318 ) ;
#81864=CARTESIAN_POINT ( 'NONE',  ( 33.88237199998285121, 485.0486819176492759, 1.241522336454517594 ) ) ;
#81880=CIRCLE ( 'NONE', #19977, 0.9999999999999875655 ) ;
#81884=AXIS2_PLACEMENT_3D ( 'NONE', #44789, #11859, #77680 ) ;
#81889=CARTESIAN_POINT ( 'NONE',  ( 0.000000000000000000, 81.00000000000000000, 0.000000000000000000 ) ) ;
#81899=CARTESIAN_POINT ( 'NONE',  ( 28.85163153077909115, 319.8032021574594523, 12.62209958446642588 ) ) ;
#81906=CARTESIAN_POINT ( 'NONE',  ( -33.00496812084397646, 465.6658704666172639, 15.15901827095664522 ) ) ;
#81916=ORIENTED_EDGE ( 'NONE', *, *, #11892, .T. ) ;
#81918=CARTESIAN_POINT ( 'NONE',  ( -7.653149674035952366, 294.7103690674142626, -6.445128602722142830 ) ) ;
#81926=CARTESIAN_POINT ( 'NONE',  ( -9.846553493373482624, 302.6513161806682888, 9.894388782117784942 ) ) ;
#81931=CARTESIAN_POINT ( 'NONE',  ( 37.00151214921998388, 491.8254423329678957, 12.57683263657896688 ) ) ;
#81932=CARTESIAN_POINT ( 'NONE',  ( -32.13004029922196736, 464.8241378157327404, 14.61694575657911166 ) ) ;
#81934=ORIENTED_EDGE ( 'NONE', *, *, #99693, .F. ) ;
#81948=CARTESIAN_POINT ( 'NONE',  ( -28.34990703596096395, 308.9679587906881579, -9.065518352637484512 ) ) ;
#81956=CARTESIAN_POINT ( 'NONE',  ( -24.54082342953966034, 303.7793720978580723, -9.799731773458871587 ) ) ;
#81962=CARTESIAN_POINT ( 'NONE',  ( -42.47047798398502749, 355.1276945667507334, 15.62095130985220059 ) ) ;
#81975=CARTESIAN_POINT ( 'NONE',  ( -39.46184362519017697, 438.4175760117823870, 22.75062681417281496 ) ) ;
#81976=VERTEX_POINT ( 'NONE', #38249 ) ;
#81978=CARTESIAN_POINT ( 'NONE',  ( 38.83535783861245250, 468.9533400912722527, 0.4924304409069520938 ) ) ;
#81980=DIRECTION ( 'NONE',  ( -1.000000000000000000, 0.000000000000000000, 0.000000000000000000 ) ) ;
#81992=B_SPLINE_CURVE_WITH_KNOTS ( 'NONE', 3,
 ( #16082, #58684, #7442, #48962, #73237, #917, #58135, #91061, #25830, #7983, #100192, #32296, #50040, #67311 ),
 .UNSPECIFIED., .F., .F.,
 ( 4, 2, 2, 2, 2, 2, 4 ),
 ( 6.938893903907228378E-18, 0.0004833252911870726618, 0.0009666505823741383847, 0.001208313227967711253, 0.001449975873561284339, 0.001691638519154857207, 0.001933301164748430293 ),
 .UNSPECIFIED. ) ;
#82007=ORIENTED_EDGE ( 'NONE', *, *, #53088, .F. ) ;
#82014=CARTESIAN_POINT ( 'NONE',  ( -13.63130828375568981, 294.5445729804733901, -10.06530370901874250 ) ) ;
#82015=CARTESIAN_POINT ( 'NONE',  ( -19.70764564238371719, 304.7954121406193622, 9.925013215726785631 ) ) ;
#82018=CARTESIAN_POINT ( 'NONE',  ( 30.00000000000000355, 490.2049413361779671, 6.956578744621319643 ) ) ;
#82026=EDGE_CURVE ( 'NONE', #101726, #65472, #46744, .T. ) ;
#82031=CARTESIAN_POINT ( 'NONE',  ( 2.019483917365790222E-25, 304.8518027762758038, 8.936999415352287812 ) ) ;
#82041=EDGE_LOOP ( 'NONE', ( #44671, #26574, #5752, #18839 ) ) ;
#82050=DIRECTION ( 'NONE',  ( 0.000000000000000000, 0.8813945903473795473, -0.4723807533191579089 ) ) ;
#82054=EDGE_LOOP ( 'NONE', ( #76660, #37060, #9059, #63183 ) ) ;
#82060=CARTESIAN_POINT ( 'NONE',  ( 35.37498230280639433, 485.2520700389516151, -2.749549059028474129 ) ) ;
#82065=CARTESIAN_POINT ( 'NONE',  ( 51.01037695545453232, 450.0000000000002274, 13.20242257375370976 ) ) ;
#82075=CARTESIAN_POINT ( 'NONE',  ( 43.69860345152648051, 434.4324800463855922, 11.31831452735614008 ) ) ;
#82108=DIRECTION ( 'NONE',  ( 0.000000000000000000, 0.000000000000000000, 1.000000000000000000 ) ) ;
#82131=AXIS2_PLACEMENT_3D ( 'NONE', #46260, #103948, #79146 ) ;
#82133=CARTESIAN_POINT ( 'NONE',  ( 40.17576961386068746, 438.0154178803811647, 22.24081819228610613 ) ) ;
#82138=CARTESIAN_POINT ( 'NONE',  ( -34.62919541716505023, 437.4394979580210361, 4.999019296795436773 ) ) ;
#82148=CARTESIAN_POINT ( 'NONE',  ( 35.22347075582237608, 464.3861918352842508, 19.05313339797742600 ) ) ;
#82154=CARTESIAN_POINT ( 'NONE',  ( -27.18908553330205180, 296.5274986157688772, 10.30015177545897842 ) ) ;
#82156=CARTESIAN_POINT ( 'NONE',  ( -40.85254446136673323, 441.7500193615117610, 25.53625856138344474 ) ) ;
#82160=CARTESIAN_POINT ( 'NONE',  ( 21.64331233096206475, 305.0431391404469537, -8.959384353494732167 ) ) ;
#82166=CARTESIAN_POINT ( 'NONE',  ( -42.61140200160145497, 465.9030374194823594, 13.21253569360412783 ) ) ;
#82172=CIRCLE ( 'NONE', #90817, 5.000000000000000000 ) ;
#82191=EDGE_CURVE ( 'NONE', #4872, #45384, #64017, .T. ) ;
#82213=CARTESIAN_POINT ( 'NONE',  ( -37.43130592801911405, 464.0780360861290319, 19.48660943767402998 ) ) ;
#82214=ORIENTED_EDGE ( 'NONE', *, *, #987, .F. ) ;
#82218=CARTESIAN_POINT ( 'NONE',  ( 32.03945371335148451, 464.8492019110282740, 12.52442169461163246 ) ) ;
#82225=EDGE_LOOP ( 'NONE', ( #11662, #26740, #46905, #2412 ) ) ;
#82230=CARTESIAN_POINT ( 'NONE',  ( -36.06456757113840439, 330.6367415789401321, -3.201966090863014536 ) ) ;
#82241=CIRCLE ( 'NONE', #16807, 0.9999999999999984457 ) ;
#82255=AXIS2_PLACEMENT_3D ( 'NONE', #93894, #21624, #28661 ) ;
#82264=CARTESIAN_POINT ( 'NONE',  ( 0.000000000000000000, 294.8518027762758038, 9.936999415352289589 ) ) ;
#82273=CARTESIAN_POINT ( 'NONE',  ( -39.80234998357077103, 485.2146942042872979, -4.378040023498154021 ) ) ;
#82281=CARTESIAN_POINT ( 'NONE',  ( -46.00000000000000000, 436.0345727778312721, 16.01583062807923596 ) ) ;
#82286=CARTESIAN_POINT ( 'NONE',  ( 35.53321744913674252, 463.4104023594617843, 19.92304894059051890 ) ) ;
#82292=( BOUNDED_SURFACE ( )  B_SPLINE_SURFACE ( 3, 2, ( 
 ( #36432, #52026, #60682 ),
 ( #102176, #61748, #69302 ),
 ( #2943, #93025, #11026 ),
 ( #19187, #53624, #84937 ) ),
 .UNSPECIFIED., .F., .F., .F. ) 
 B_SPLINE_SURFACE_WITH_KNOTS ( ( 4, 4 ),
 ( 3, 3 ),
 ( -3.903127820947815962E-18, 0.0007499009164755671619 ),
 ( 0.000000000000000000, 1.000000000000000000 ),
 .UNSPECIFIED. ) 
 GEOMETRIC_REPRESENTATION_ITEM ( )  RATIONAL_B_SPLINE_SURFACE ( (
 ( 1.000000000000000000, 0.7301269460247310494, 1.000000000000000000),
 ( 1.000000000000000000, 0.7327382575064720349, 1.000000000000000000),
 ( 1.000000000000000000, 0.7350727526496287911, 1.000000000000000000),
 ( 1.000000000000000000, 0.7370557512816016121, 1.000000000000000000) ) ) 
 REPRESENTATION_ITEM ( '' )  SURFACE ( )  );
#82294=STYLED_ITEM ( 'NONE', ( #2479 ), #9074 ) ;
#82302=CARTESIAN_POINT ( 'NONE',  ( 30.12025201962617160, 308.0360787568225760, -8.818471063241863916 ) ) ;
#82308=CARTESIAN_POINT ( 'NONE',  ( -24.80105969489321893, 306.0237540681346218, -9.745911707962003234 ) ) ;
#82312=DIRECTION ( 'NONE',  ( -0.5356766697699745228, 0.1574227122301985193, -0.8296195484306273515 ) ) ;
#82316=EDGE_LOOP ( 'NONE', ( #81523, #14420, #3995, #60947 ) ) ;
#82317=CARTESIAN_POINT ( 'NONE',  ( -20.43433360646712416, 304.8965913596235850, 8.946491893676210339 ) ) ;
#82319=CARTESIAN_POINT ( 'NONE',  ( 34.63713372481439023, 485.1220453274884221, -1.973566398568655123 ) ) ;
#82321=CARTESIAN_POINT ( 'NONE',  ( 32.04854177564008211, 486.3112398708905175, 5.779390795271076797 ) ) ;
#82328=CARTESIAN_POINT ( 'NONE',  ( 46.00000000000000000, 435.9962990437406916, 13.93498389398033410 ) ) ;
#82344=CARTESIAN_POINT ( 'NONE',  ( 40.88293604215247967, 432.5779639752643675, 26.56799667982232549 ) ) ;
#82346=CARTESIAN_POINT ( 'NONE',  ( 13.56846521071778255, 303.5479320962715519, -10.06459103807807587 ) ) ;
#82347=CARTESIAN_POINT ( 'NONE',  ( -30.00000000000558487, 487.3958844382141251, 6.449680606608591660 ) ) ;
#82348=ORIENTED_EDGE ( 'NONE', *, *, #86828, .T. ) ;
#82353=DIRECTION ( 'NONE',  ( 0.000000000000000000, -0.9676758637755515924, 0.2521971900442986914 ) ) ;
#82363=CARTESIAN_POINT ( 'NONE',  ( 33.21102376836596193, 438.9613914113129454, 23.92328486949907784 ) ) ;
#82365=CIRCLE ( 'NONE', #13435, 1.000000000000014433 ) ;
#82367=CARTESIAN_POINT ( 'NONE',  ( -30.24422310998454577, 336.7236929599040991, 17.61079458025261602 ) ) ;
#82373=CARTESIAN_POINT ( 'NONE',  ( 32.65560599211094939, 434.9894379982545729, 13.53857720042920043 ) ) ;
#82374=CARTESIAN_POINT ( 'NONE',  ( 34.18266571248467045, 303.5689682991300060, 11.95674675998675518 ) ) ;
#82381=B_SPLINE_CURVE_WITH_KNOTS ( 'NONE', 3,
 ( #98393, #57392, #75167, #90304, #8845, #1260, #99439, #34227 ),
 .UNSPECIFIED., .F., .F.,
 ( 4, 2, 2, 4 ),
 ( 0.000000000000000000, 0.001046156454241313960, 0.002092312908482627919, 0.004184625816965175174 ),
 .UNSPECIFIED. ) ;
#82385=CARTESIAN_POINT ( 'NONE',  ( -24.57118404873822826, 295.6022528646752221, 10.09816379703451616 ) ) ;
#82392=CARTESIAN_POINT ( 'NONE',  ( 9.150944205135592924, 294.9553539103914659, 4.044928260314501145 ) ) ;
#82400=CARTESIAN_POINT ( 'NONE',  ( 1.288479777019286333E-15, 37.86482112153536406, 10.52123582012688274 ) ) ;
#82425=B_SPLINE_CURVE_WITH_KNOTS ( 'NONE', 3,
 ( #28700, #86914, #27643, #44316, #103088, #77210, #3322, #21144, #11932, #54496 ),
 .UNSPECIFIED., .F., .F.,
 ( 4, 2, 2, 2, 4 ),
 ( 0.000000000000000000, 0.001057229007211967810, 0.002114458014423935620, 0.003171687021635903429, 0.004228916028847871239 ),
 .UNSPECIFIED. ) ;
#82426=ORIENTED_EDGE ( 'NONE', *, *, #26185, .F. ) ;
#82436=CARTESIAN_POINT ( 'NONE',  ( 42.76313255034848737, 461.1833584523197374, 3.199811539391409720 ) ) ;
#82448=CARTESIAN_POINT ( 'NONE',  ( 30.24426401564364753, 336.7248776613420205, 17.61103644359287301 ) ) ;
#82451=VERTEX_POINT ( 'NONE', #22864 ) ;
#82481=EDGE_CURVE ( 'NONE', #97550, #26330, #51345, .T. ) ;
#82485=CARTESIAN_POINT ( 'NONE',  ( 35.80547854523823759, 490.7930927354842652, 12.38248481219585884 ) ) ;
#82496=ORIENTED_EDGE ( 'NONE', *, *, #80392, .F. ) ;
#82503=CARTESIAN_POINT ( 'NONE',  ( -34.54824451023232257, 338.5131454125937012, -0.8343175004005460860 ) ) ;
#82508=ORIENTED_EDGE ( 'NONE', *, *, #105197, .T. ) ;
#82510=CARTESIAN_POINT ( 'NONE',  ( -26.70424429299868763, 296.1616889006899669, -1.717105780328246567 ) ) ;
#82514=CARTESIAN_POINT ( 'NONE',  ( -35.23448287039504834, 485.0606775613101718, -1.508972397133680143 ) ) ;
#82515=CARTESIAN_POINT ( 'NONE',  ( -32.00452718204254410, 333.4532925135374626, 17.36126857274863156 ) ) ;
#82527=CARTESIAN_POINT ( 'NONE',  ( 43.48224507221030422, 485.4751843846681254, 4.033548163687394883 ) ) ;
#82532=CARTESIAN_POINT ( 'NONE',  ( -32.20627048526868208, 464.6794164287650801, 10.68709986547766988 ) ) ;
#82542=B_SPLINE_CURVE_WITH_KNOTS ( 'NONE', 3,
 ( #66081, #33741, #75222, #66615 ),
 .UNSPECIFIED., .F., .F.,
 ( 4, 4 ),
 ( 1.001051563156762085E-15, 0.001949579373385036327 ),
 .UNSPECIFIED. ) ;
#82544=CARTESIAN_POINT ( 'NONE',  ( 0.000000000000000000, 80.00000000000000000, -8.000000000000014211 ) ) ;
#82567=CARTESIAN_POINT ( 'NONE',  ( 41.13640268182594184, 465.3860676345191791, 16.49894919583628905 ) ) ;
#82568=CARTESIAN_POINT ( 'NONE',  ( -32.87806366422623228, 464.9425629022531439, 11.07779413895617004 ) ) ;
#82570=CARTESIAN_POINT ( 'NONE',  ( 32.11606453551802787, 486.2854634841322650, 5.773331070944215604 ) ) ;
#82584=CARTESIAN_POINT ( 'NONE',  ( -20.24579557674108088, 304.8297271373347144, -10.00469232190996927 ) ) ;
#82607=CARTESIAN_POINT ( 'NONE',  ( 32.28552837373269568, 464.7648866755952213, 15.30384310833107975 ) ) ;
#82611=CARTESIAN_POINT ( 'NONE',  ( 32.81992448453858913, 465.7192846569213316, 11.17271167765314388 ) ) ;
#82622=CARTESIAN_POINT ( 'NONE',  ( 43.86611073477487821, 435.5752409525302937, 9.535927547466386045 ) ) ;
#82627=CARTESIAN_POINT ( 'NONE',  ( 40.07586470527510158, 337.7832441655235129, 20.21182470898328631 ) ) ;
#82633=CARTESIAN_POINT ( 'NONE',  ( -31.27146333409443812, 363.0590912728651460, 21.43603929113760387 ) ) ;
#82643=AXIS2_PLACEMENT_3D ( 'NONE', #37348, #85887, #93963 ) ;
#82647=CARTESIAN_POINT ( 'NONE',  ( 25.98780635108152737, 307.2400872882208773, 10.71531891313127183 ) ) ;
#82664=CARTESIAN_POINT ( 'NONE',  ( -33.09102985894170246, 433.0213902170605138, 24.60354821821731264 ) ) ;
#82666=ORIENTED_EDGE ( 'NONE', *, *, #101926, .F. ) ;
#82675=CARTESIAN_POINT ( 'NONE',  ( 41.66068395357901011, 437.6580662123523098, 21.73548463238672923 ) ) ;
#82685=EDGE_LOOP ( 'NONE', ( #20465, #73738, #26493, #63220 ) ) ;
#82687=CARTESIAN_POINT ( 'NONE',  ( -42.51410301899422706, 462.6487061729604306, 3.764838390874527541 ) ) ;
#82689=ADVANCED_FACE ( 'NONE', ( #1172 ), #43130, .T. ) ;
#82691=CARTESIAN_POINT ( 'NONE',  ( 34.16642289233192287, 463.8422268500521000, 18.98106911353298187 ) ) ;
#82697=CARTESIAN_POINT ( 'NONE',  ( -40.93292669599463096, 378.0706848361106722, 26.55786848468904537 ) ) ;
#82701=CARTESIAN_POINT ( 'NONE',  ( 25.78481569285033714, 306.6490176242861025, -8.604953696922189366 ) ) ;
#82713=CARTESIAN_POINT ( 'NONE',  ( -33.68177706158878237, 464.5004658938952389, 17.05886715805492670 ) ) ;
#82716=CARTESIAN_POINT ( 'NONE',  ( -36.33173443512122702, 437.9974107914313208, 4.196572296727017815 ) ) ;
#82730=FILL_AREA_STYLE ('',( #57374 ) ) ;
#82733=CARTESIAN_POINT ( 'NONE',  ( 43.52075891743749736, 484.7805561108179973, 4.063293749110879816 ) ) ;
#82742=CARTESIAN_POINT ( 'NONE',  ( 35.45927743045602654, 433.4366494758652948, 5.520752814291649102 ) ) ;
#82752=CARTESIAN_POINT ( 'NONE',  ( 32.94994279514025948, 464.9549361168423047, 15.12478419437806210 ) ) ;
#82772=CARTESIAN_POINT ( 'NONE',  ( -45.47616038644186176, 382.7747991321946301, 7.369568083445501294 ) ) ;
#82777=ORIENTED_EDGE ( 'NONE', *, *, #20423, .F. ) ;
#82781=CARTESIAN_POINT ( 'NONE',  ( 43.00000000000000000, 464.8825480873695710, 15.07585856869435936 ) ) ;
#82796=CARTESIAN_POINT ( 'NONE',  ( -37.62595466100607666, 491.2446780561959372, 12.18850516984483612 ) ) ;
#82812=EDGE_CURVE ( 'NONE', #80103, #51980, #41736, .T. ) ;
#82832=CARTESIAN_POINT ( 'NONE',  ( -41.60913992197761502, 468.1836805815477192, 17.09491368641011633 ) ) ;
#82837=CARTESIAN_POINT ( 'NONE',  ( -37.88504238421052861, 463.4171042825119002, 19.90923349044181379 ) ) ;
#82839=CARTESIAN_POINT ( 'NONE',  ( 29.01392623672715132, 306.7126468544000772, -9.132303470068400486 ) ) ;
#82848=CARTESIAN_POINT ( 'NONE',  ( -33.71029056097432886, 485.0094969250626491, -0.6083101643363590938 ) ) ;
#82850=CARTESIAN_POINT ( 'NONE',  ( 43.60687476841235366, 374.6170328897057402, 14.40570227514321466 ) ) ;
#82866=CARTESIAN_POINT ( 'NONE',  ( 43.91914608742546733, 435.5074579457412938, 9.837368328701776576 ) ) ;
#82867=ORIENTED_EDGE ( 'NONE', *, *, #14177, .T. ) ;
#82871=CARTESIAN_POINT ( 'NONE',  ( 37.71869766778865340, 461.3719613792328573, 2.612049572453471136 ) ) ;
#82876=CARTESIAN_POINT ( 'NONE',  ( 0.000000000000000000, 81.00000000000000000, 0.000000000000000000 ) ) ;
#82881=CARTESIAN_POINT ( 'NONE',  ( 16.94582768995435984, 304.5649027789814909, -10.06098247776249188 ) ) ;
#82882=CARTESIAN_POINT ( 'NONE',  ( -34.26359294763754093, 462.2983250974768339, 4.610187765825797257 ) ) ;
#82902=CARTESIAN_POINT ( 'NONE',  ( -42.44404385065663377, 464.7189401834564819, 16.13499420399455175 ) ) ;
#82903=CARTESIAN_POINT ( 'NONE',  ( -31.22166591873284958, 392.4860439548177169, 25.19642211891369499 ) ) ;
#82911=CARTESIAN_POINT ( 'NONE',  ( 28.65390007077115797, 297.4029314509076016, 10.49725111039197145 ) ) ;
#82913=CARTESIAN_POINT ( 'NONE',  ( -41.33517203638642457, 460.1869644147454892, 2.191757750720012776 ) ) ;
#82914=CARTESIAN_POINT ( 'NONE',  ( 42.48134374264972735, 356.5879242656516226, 15.82646805172678661 ) ) ;
#82918=ORIENTED_EDGE ( 'NONE', *, *, #11952, .T. ) ;
#82919=CARTESIAN_POINT ( 'NONE',  ( -21.19348424345033521, 294.8901562694577478, 1.945151701991107540 ) ) ;
#82963=DIRECTION ( 'NONE',  ( 0.000000000000000000, 0.000000000000000000, -1.000000000000000000 ) ) ;
#82964=EDGE_LOOP ( 'NONE', ( #20412, #48240, #23300, #36412 ) ) ;
#82965=AXIS2_PLACEMENT_3D ( 'NONE', #56147, #89090, #57227 ) ;
#82970=CARTESIAN_POINT ( 'NONE',  ( 38.50925662097987612, 490.3066386719625598, 12.08729337933079862 ) ) ;
#82982=CARTESIAN_POINT ( 'NONE',  ( 30.85676804175761845, 345.5934757462927109, 18.44563300946912321 ) ) ;
#82993=CARTESIAN_POINT ( 'NONE',  ( -26.54817876223620488, 310.6276912632132507, 11.31208242866018132 ) ) ;
#83003=CARTESIAN_POINT ( 'NONE',  ( -5.833922283738917969, 294.7609306416122195, -8.134666899072025004 ) ) ;
#83016=CARTESIAN_POINT ( 'NONE',  ( 35.31256682049291840, 491.0612481437107704, 12.05460915451404880 ) ) ;
#83036=CARTESIAN_POINT ( 'NONE',  ( -28.16657779764221203, 308.8746777916272777, -8.086782216783561239 ) ) ;
#83042=CARTESIAN_POINT ( 'NONE',  ( -20.49977525862255945, 302.8459220885800960, -10.00124997875688670 ) ) ;
#83047=CARTESIAN_POINT ( 'NONE',  ( -36.10664099193432719, 485.3877008568640008, -3.396001134007734290 ) ) ;
#83048=CARTESIAN_POINT ( 'NONE',  ( -31.66192239831772071, 329.0498789714471854, 16.34307995493717769 ) ) ;
#83049=CARTESIAN_POINT ( 'NONE',  ( -32.82334337205544017, 485.9852583078038606, 5.593860717071749811 ) ) ;
#83059=CARTESIAN_POINT ( 'NONE',  ( 30.00000000000000000, 490.5636507777048791, 7.413185101890151785 ) ) ;
#83066=EDGE_CURVE ( 'NONE', #35120, #96476, #64160, .T. ) ;
#83068=CARTESIAN_POINT ( 'NONE',  ( 46.00000000000000000, 488.3725375423206287, 3.127739281036224117 ) ) ;
#83070=EDGE_CURVE ( 'NONE', #457, #73090, #64802, .T. ) ;
#83096=CARTESIAN_POINT ( 'NONE',  ( -43.74985542820371620, 435.5770091380364306, 16.96136490515579354 ) ) ;
#83097=CARTESIAN_POINT ( 'NONE',  ( 31.21759734847655210, 387.2566916973277671, 24.99345285570965913 ) ) ;
#83098=CARTESIAN_POINT ( 'NONE',  ( -34.05377138046417684, 435.1042973066813033, 11.34048742922945685 ) ) ;
#83103=ORIENTED_EDGE ( 'NONE', *, *, #68476, .T. ) ;
#83108=CARTESIAN_POINT ( 'NONE',  ( -16.53376292628442812, 304.5679863953762947, 9.876672385353252537 ) ) ;
#83117=( BOUNDED_SURFACE ( )  B_SPLINE_SURFACE ( 3, 2, ( 
 ( #88135, #80018, #31512 ),
 ( #6129, #39060, #71940 ),
 ( #104844, #64394, #27548 ),
 ( #37221, #78171, #59890 ) ),
 .UNSPECIFIED., .F., .F., .F. ) 
 B_SPLINE_SURFACE_WITH_KNOTS ( ( 4, 4 ),
 ( 3, 3 ),
 ( 0.01114851999725509704, 0.01303042415393934096 ),
 ( 0.000000000000000000, 0.8381935999574059437 ),
 .UNSPECIFIED. ) 
 GEOMETRIC_REPRESENTATION_ITEM ( )  RATIONAL_B_SPLINE_SURFACE ( (
 ( 1.000000000000000000, 0.8031285674522142815, 0.9362898844564289114),
 ( 1.000000000000000000, 0.7874857493404847641, 0.9312276682860687327),
 ( 1.000000000000000000, 0.7712021973814140452, 0.9259581024412611994),
 ( 1.000000000000000000, 0.7544987785202109665, 0.9205526622925915836) ) ) 
 REPRESENTATION_ITEM ( '' )  SURFACE ( )  );
#83143=CARTESIAN_POINT ( 'NONE',  ( -30.81186653459094416, 298.3092085573109671, -1.237150650991206025 ) ) ;
#83150=CARTESIAN_POINT ( 'NONE',  ( 43.80952869898890611, 434.9438303799720984, 12.65470026211498400 ) ) ;
#83151=ADVANCED_FACE ( 'NONE', ( #73226 ), #38848, .F. ) ;
#83159=CARTESIAN_POINT ( 'NONE',  ( 38.51502786939645517, 460.0233756673477501, 2.043034587343977027 ) ) ;
#83162=CARTESIAN_POINT ( 'NONE',  ( -29.50104258278691205, 324.7387376422711895, 13.83862620216122075 ) ) ;
#83168=EDGE_LOOP ( 'NONE', ( #46681, #2174, #98486, #56786, #11870 ) ) ;
#83189=CARTESIAN_POINT ( 'NONE',  ( -28.34860985744511908, 309.9008460147075539, 11.61304566638001390 ) ) ;
#83198=EDGE_CURVE ( 'NONE', #20836, #10763, #382, .T. ) ;
#83203=CARTESIAN_POINT ( 'NONE',  ( 33.59806029755767298, 439.5207550827159366, 23.94543542408109005 ) ) ;
#83207=DIRECTION ( 'NONE',  ( -1.000000000000000000, 0.000000000000000000, 0.000000000000000000 ) ) ;
#83213=CARTESIAN_POINT ( 'NONE',  ( 46.00000000000000000, 488.0491671480462514, 1.813224401588382717 ) ) ;
#83217=CARTESIAN_POINT ( 'NONE',  ( 33.72113281714197797, 434.9249850380938369, 12.79200524501336034 ) ) ;
#83225=CARTESIAN_POINT ( 'NONE',  ( -39.24156521425334176, 307.7088117867400001, -7.003459073692002157 ) ) ;
#83227=CIRCLE ( 'NONE', #102174, 1.000000000000009326 ) ;
#83239=CARTESIAN_POINT ( 'NONE',  ( -33.38752815995437828, 464.7252609253681612, 16.46839106284949494 ) ) ;
#83241=CARTESIAN_POINT ( 'NONE',  ( 9.797174393178835518E-16, 81.00000000000000000, 8.000000000000007105 ) ) ;
#83246=ORIENTED_EDGE ( 'NONE', *, *, #15844, .F. ) ;
#83256=CARTESIAN_POINT ( 'NONE',  ( 32.05241217997335212, 487.5077369494006803, 9.813907492612683470 ) ) ;
#83260=( BOUNDED_SURFACE ( )  B_SPLINE_SURFACE ( 3, 3, ( 
 ( #42593, #37074, #86148, #67421 ),
 ( #45667, #37612, #43137, #78029 ),
 ( #102838, #70476, #100298, #29005 ),
 ( #61331, #94219, #59325, #102302 ),
 ( #92198, #78551, #50658, #4679 ),
 ( #103372, #12218, #18351, #99771 ) ),
 .UNSPECIFIED., .F., .F., .T. ) 
 B_SPLINE_SURFACE_WITH_KNOTS ( ( 4, 1, 1, 4 ),
 ( 4, 4 ),
 ( 0.000000000000000000, 0.4213833399777465738, 0.5213833399777465516, 0.9843640123765011740 ),
 ( 0.000000000000000000, 1.000000000000000000 ),
 .UNSPECIFIED. ) 
 GEOMETRIC_REPRESENTATION_ITEM ( )  RATIONAL_B_SPLINE_SURFACE ( (
 ( 1.000000000000000000, 0.3333333333333334259, 0.3333333333333334259, 1.000000000000000000),
 ( 1.000000000000000000, 0.3333333333333334259, 0.3333333333333334259, 1.000000000000000000),
 ( 1.000000000000000000, 0.3333333333333334259, 0.3333333333333334259, 1.000000000000000000),
 ( 1.000000000000000000, 0.3333333333333334259, 0.3333333333333334259, 1.000000000000000000),
 ( 1.000000000000000000, 0.3333333333333334259, 0.3333333333333334259, 1.000000000000000000),
 ( 1.000000000000000000, 0.3333333333333334259, 0.3333333333333334259, 1.000000000000000000) ) ) 
 REPRESENTATION_ITEM ( '' )  SURFACE ( )  );
#83264=SURFACE_SIDE_STYLE ('',( #98898 ) ) ;
#83266=UNCERTAINTY_MEASURE_WITH_UNIT (LENGTH_MEASURE( 1.000000000000000082E-05 ), #35376, 'distance_accuracy_value', 'NONE');
#83269=ORIENTED_EDGE ( 'NONE', *, *, #32719, .T. ) ;
#83273=CARTESIAN_POINT ( 'NONE',  ( 32.70880207180495347, 321.7209935153538254, -4.878524035375318313 ) ) ;
#83280=CARTESIAN_POINT ( 'NONE',  ( -17.36371387429518975, 302.5953826724242504, -10.05438065605093456 ) ) ;
#83282=CARTESIAN_POINT ( 'NONE',  ( -37.04971407824218943, 463.3105192861251567, 20.11836016812711492 ) ) ;
#83286=CARTESIAN_POINT ( 'NONE',  ( 32.87547266101578458, 465.6993878536675879, 10.91512469976459343 ) ) ;
#83287=CARTESIAN_POINT ( 'NONE',  ( 29.99999999999923972, 464.1662643419747951, 12.90481041407959673 ) ) ;
#83300=CARTESIAN_POINT ( 'NONE',  ( -40.81016822426350643, 312.4315563144064072, -5.816209787523243691 ) ) ;
#83301=CARTESIAN_POINT ( 'NONE',  ( -18.59880227178827994, 304.6205263575372442, -9.049159319796237000 ) ) ;
#83303=ORIENTED_EDGE ( 'NONE', *, *, #94304, .T. ) ;
#83313=ADVANCED_FACE ( 'NONE', ( #50028, #18225 ), #42468, .T. ) ;
#83328=CARTESIAN_POINT ( 'NONE',  ( -7.093721425956736049, 304.7303285792975771, 9.911179277710184365 ) ) ;
#83332=CARTESIAN_POINT ( 'NONE',  ( 44.19067352157695439, 435.2576879214440169, 14.58866310346203576 ) ) ;
#83337=EDGE_CURVE ( 'NONE', #64798, #48477, #46654, .T. ) ;
#83348=CARTESIAN_POINT ( 'NONE',  ( 32.28552837373269568, 464.7648866755952213, 15.30384310833107975 ) ) ;
#83358=CARTESIAN_POINT ( 'NONE',  ( -39.62985215079022083, 316.5869118491702920, 7.204194025685374037 ) ) ;
#83365=CARTESIAN_POINT ( 'NONE',  ( 36.07978899617289414, 302.6969447429428897, -8.217629260179846185 ) ) ;
#83378=CARTESIAN_POINT ( 'NONE',  ( 43.60048099680660272, 433.3730128036348219, 14.72755969045772950 ) ) ;
#83381=ORIENTED_EDGE ( 'NONE', *, *, #54906, .T. ) ;
#83382=CARTESIAN_POINT ( 'NONE',  ( -23.80680574697089469, 304.9792048259543549, 10.18372908566200330 ) ) ;
#83386=CARTESIAN_POINT ( 'NONE',  ( 32.01581173012298365, 487.4782005592953738, 8.020290309139436857 ) ) ;
#83389=CARTESIAN_POINT ( 'NONE',  ( 30.00000000000000000, 500.0000000000002274, 0.000000000000000000 ) ) ;
#83404=CARTESIAN_POINT ( 'NONE',  ( 31.21933008645656926, 405.2090764464551853, 25.56980379099173817 ) ) ;
#83405=LINE ( 'NONE', #93643, #95694 ) ;
#83407=CARTESIAN_POINT ( 'NONE',  ( -34.06603414617824654, 462.4608636921087736, 4.846872666268491336 ) ) ;
#83419=CARTESIAN_POINT ( 'NONE',  ( -23.38206103562286486, 304.7406344060533456, 10.13027383527492731 ) ) ;
#83428=CARTESIAN_POINT ( 'NONE',  ( -31.38693051204033324, 427.9638760193610665, 23.57266965543569270 ) ) ;
#83433=CARTESIAN_POINT ( 'NONE',  ( 33.08902662345825973, 439.4144565034923744, 23.84226355454061874 ) ) ;
#83436=CARTESIAN_POINT ( 'NONE',  ( 27.04196716693042646, 307.0757598473238090, 10.91257262733961753 ) ) ;
#83445=CARTESIAN_POINT ( 'NONE',  ( -20.97754405179131254, 294.8763868968453608, 9.942224931492253504 ) ) ;
#83449=CARTESIAN_POINT ( 'NONE',  ( 34.47176506789151063, 489.5748983164542096, 11.69726377703232778 ) ) ;
#83470=CARTESIAN_POINT ( 'NONE',  ( 35.77017041476860015, 490.7753167606494458, 12.37440192957616070 ) ) ;
#83471=CARTESIAN_POINT ( 'NONE',  ( 34.88900972249397370, 464.6206820655982028, 18.69027339340997784 ) ) ;
#83495=ORIENTED_EDGE ( 'NONE', *, *, #27851, .T. ) ;
#83498=CARTESIAN_POINT ( 'NONE',  ( 9.789044728060087408, 294.6486233851415477, -2.043184600578025201 ) ) ;
#83503=CARTESIAN_POINT ( 'NONE',  ( 29.35230083617101116, 317.9833937185579202, 13.40910235493362634 ) ) ;
#83536=DIRECTION ( 'NONE',  ( -0.000000000000000000, -1.000000000000000000, -0.000000000000000000 ) ) ;
#83559=CARTESIAN_POINT ( 'NONE',  ( -43.63911886418856767, 435.1012159695318360, 10.95008075558104110 ) ) ;
#83563=CARTESIAN_POINT ( 'NONE',  ( -38.47428897412110160, 485.7788508071988076, -4.770630528146475591 ) ) ;
#83564=CARTESIAN_POINT ( 'NONE',  ( -42.74672710594789748, 418.3108395146689418, 19.64234251677965659 ) ) ;
#83591=CARTESIAN_POINT ( 'NONE',  ( 45.29905483467455696, 497.0732240353902398, -8.041250874568902418 ) ) ;
#83605=ADVANCED_FACE ( 'NONE', ( #11688 ), #54126, .F. ) ;
#83616=CARTESIAN_POINT ( 'NONE',  ( 31.00389226642222340, 485.8187364282109115, 14.27494812388583512 ) ) ;
#83617=CARTESIAN_POINT ( 'NONE',  ( 41.18500240986835337, 460.1236783698127510, 2.133705300515011061 ) ) ;
#83618=CARTESIAN_POINT ( 'NONE',  ( -35.12011055360168399, 436.4929263758896809, 6.579006402756536254 ) ) ;
#83622=B_SPLINE_CURVE_WITH_KNOTS ( 'NONE', 3,
 ( #26613, #41166, #16348, #41689 ),
 .UNSPECIFIED., .F., .F.,
 ( 4, 4 ),
 ( 1.734723475976806902E-18, 0.0001919544104626820578 ),
 .UNSPECIFIED. ) ;
#83640=CARTESIAN_POINT ( 'NONE',  ( -0.7521598668867096604, 300.0000000000000000, 9.936704142777553983 ) ) ;
#83642=ORIENTED_EDGE ( 'NONE', *, *, #88658, .F. ) ;
#83646=CARTESIAN_POINT ( 'NONE',  ( -46.00000000000000711, 488.2671786690042950, 2.798715677624241671 ) ) ;
#83653=FACE_OUTER_BOUND ( 'NONE', #78811, .T. ) ;
#83654=CARTESIAN_POINT ( 'NONE',  ( 24.60488647473181345, 306.9835580411500473, 10.41807558718820914 ) ) ;
#83657=ADVANCED_FACE ( 'NONE', ( #14335 ), #60904, .T. ) ;
#83667=CARTESIAN_POINT ( 'NONE',  ( 43.71789550056999474, 434.9437403290091879, 13.92762231526894112 ) ) ;
#83671=ORIENTED_EDGE ( 'NONE', *, *, #17733, .T. ) ;
#83672=CARTESIAN_POINT ( 'NONE',  ( 42.55893460000645234, 435.1566242046030766, 18.92048169488380083 ) ) ;
#83673=CARTESIAN_POINT ( 'NONE',  ( 40.95595929481465447, 405.2208686710653183, 27.85131585683114963 ) ) ;
#83678=CARTESIAN_POINT ( 'NONE',  ( 34.67805467039151779, 461.9798124557175356, 4.171311676497361454 ) ) ;
#83686=AXIS2_PLACEMENT_3D ( 'NONE', #40107, #89194, #41692 ) ;
#83691=ORIENTED_EDGE ( 'NONE', *, *, #94481, .T. ) ;
#83708=CARTESIAN_POINT ( 'NONE',  ( 32.21290004233850368, 485.9817488811997350, 5.040586218672359564 ) ) ;
#83713=EDGE_LOOP ( 'NONE', ( #10351, #25368, #47088, #40715 ) ) ;
#83719=ADVANCED_FACE ( 'NONE', ( #101116 ), #82292, .F. ) ;
#83722=CARTESIAN_POINT ( 'NONE',  ( 17.47322663601547177, 294.5877948852590293, -2.055689749307683112 ) ) ;
#83731=AXIS2_PLACEMENT_3D ( 'NONE', #65155, #80802, #8508 ) ;
#83736=CARTESIAN_POINT ( 'NONE',  ( 31.61469319755823193, 437.7834757340932583, 21.48356015851413048 ) ) ;
#83746=CARTESIAN_POINT ( 'NONE',  ( 44.17836536378482748, 435.2619773020558682, 14.65562696767865170 ) ) ;
#83747=ADVANCED_FACE ( 'NONE', ( #45555 ), #19717, .T. ) ;
#83757=B_SPLINE_CURVE_WITH_KNOTS ( 'NONE', 3,
 ( #68611, #102554, #51328, #35190 ),
 .UNSPECIFIED., .F., .F.,
 ( 4, 4 ),
 ( 5.791482857413889982E-16, 0.0001919544104619767843 ),
 .UNSPECIFIED. ) ;
#83768=ORIENTED_EDGE ( 'NONE', *, *, #40564, .T. ) ;
#83781=CARTESIAN_POINT ( 'NONE',  ( 31.40588807316546038, 312.3426313771107061, -8.004124503849919137 ) ) ;
#83795=CARTESIAN_POINT ( 'NONE',  ( 35.49387599962324202, 421.8708178829924691, 6.500313947379569690 ) ) ;
#83797=EDGE_CURVE ( 'NONE', #45699, #75687, #83227, .T. ) ;
#83801=ORIENTED_EDGE ( 'NONE', *, *, #88658, .T. ) ;
#83805=CARTESIAN_POINT ( 'NONE',  ( -43.68959978692321044, 484.5138553196954376, 2.648407630516707023 ) ) ;
#83808=CARTESIAN_POINT ( 'NONE',  ( 33.00000000000000000, 450.0000000000002274, 28.20242257375372219 ) ) ;
#83813=CARTESIAN_POINT ( 'NONE',  ( 32.89532852795907303, 465.6911463857187528, 10.83018753746880236 ) ) ;
#83816=CARTESIAN_POINT ( 'NONE',  ( 39.19378338565743292, 489.8656698032318104, 11.78649807965894603 ) ) ;
#83826=AXIS2_PLACEMENT_3D ( 'NONE', #88416, #6406, #104049 ) ;
#83829=CARTESIAN_POINT ( 'NONE',  ( -41.09174544714365851, 313.3976221602537180, -5.572537511513111497 ) ) ;
#83851=CARTESIAN_POINT ( 'NONE',  ( -37.50059943756144776, 490.7879993827797307, 12.38039871356719246 ) ) ;
#83853=CARTESIAN_POINT ( 'NONE',  ( -32.84237740334621236, 485.2251842821281116, 5.746442123025396143 ) ) ;
#83861=CARTESIAN_POINT ( 'NONE',  ( -36.97266421102955292, 437.4722577378113328, 4.366281382744582551 ) ) ;
#83872=ORIENTED_EDGE ( 'NONE', *, *, #31727, .F. ) ;
#83891=CARTESIAN_POINT ( 'NONE',  ( 33.74271564777244237, 484.1802673187708592, 2.058285076122321922 ) ) ;
#83894=CARTESIAN_POINT ( 'NONE',  ( -36.29465277445844151, 352.4908535429611902, 1.226005505992772804 ) ) ;
#83898=CARTESIAN_POINT ( 'NONE',  ( 23.63566405412713323, 303.4845845294884725, -9.864010225974007895 ) ) ;
#83899=CARTESIAN_POINT ( 'NONE',  ( 30.95643954367146833, 313.8918926584737505, -7.857037206977866006 ) ) ;
#83908=CARTESIAN_POINT ( 'NONE',  ( 43.00000000000000000, 484.2804969086081996, -2.982821241663323075 ) ) ;
#83916=CARTESIAN_POINT ( 'NONE',  ( -23.29322033388968904, 305.8372712004871801, 10.15257527089631751 ) ) ;
#83922=CARTESIAN_POINT ( 'NONE',  ( 31.96903519139344141, 486.7815514870802076, 6.755070114929473846 ) ) ;
#83939=CARTESIAN_POINT ( 'NONE',  ( 37.04388863813380794, 311.3287000699716032, 13.89786840526617517 ) ) ;
#83940=LINE ( 'NONE', #76913, #52647 ) ;
#83942=DIRECTION ( 'NONE',  ( -0.000000000000000000, -1.000000000000000000, -0.000000000000000000 ) ) ;
#83943=ORIENTED_EDGE ( 'NONE', *, *, #10236, .F. ) ;
#83954=CARTESIAN_POINT ( 'NONE',  ( -30.00226090868998696, 322.3790423074855198, 14.50231502595238453 ) ) ;
#83957=ORIENTED_EDGE ( 'NONE', *, *, #102543, .T. ) ;
#83960=CARTESIAN_POINT ( 'NONE',  ( -3.308895880083044805, 303.8518027751322848, 9.936999415074330599 ) ) ;
#83961=DIRECTION ( 'NONE',  ( 1.000000000000000000, -0.000000000000000000, -0.000000000000000000 ) ) ;
#83962=CARTESIAN_POINT ( 'NONE',  ( -31.15872997657971410, 428.0413696779457382, 24.54324983164422136 ) ) ;
#83968=CARTESIAN_POINT ( 'NONE',  ( 33.07276483573531323, 438.9325140356083921, 23.89537236861360014 ) ) ;
#83971=CARTESIAN_POINT ( 'NONE',  ( 35.82669496149354416, 304.5988386916886839, 4.195970393794294928 ) ) ;
#83981=CARTESIAN_POINT ( 'NONE',  ( -21.88255344520474921, 294.9922948560505915, 9.966861928665570858 ) ) ;
#83985=CARTESIAN_POINT ( 'NONE',  ( -43.94956565205965404, 434.7294131184608545, 8.824837262795423243 ) ) ;
#83987=FACE_OUTER_BOUND ( 'NONE', #27912, .T. ) ;
#84005=CIRCLE ( 'NONE', #27231, 0.9999999999999992228 ) ;
#84008=CARTESIAN_POINT ( 'NONE',  ( 36.12276851866623417, 490.9183493301041494, 12.43853037509677151 ) ) ;
#84009=CARTESIAN_POINT ( 'NONE',  ( -32.87494462546125362, 485.1684504739463932, 5.618872456255630254 ) ) ;
#84013=CARTESIAN_POINT ( 'NONE',  ( -37.67992928263237218, 491.6871197847713688, 12.48602433195068073 ) ) ;
#84046=VERTEX_POINT ( 'NONE', #95308 ) ;
#84047=CARTESIAN_POINT ( 'NONE',  ( 30.95817488778657989, 357.0893258606180893, 21.51345825778299314 ) ) ;
#84057=CARTESIAN_POINT ( 'NONE',  ( -35.76320840016588676, 388.4727839510825333, 5.610592865731860002 ) ) ;
#84070=EDGE_LOOP ( 'NONE', ( #28299, #46964, #72670, #64414, #19892, #96197 ) ) ;
#84075=CARTESIAN_POINT ( 'NONE',  ( -42.48296590551735363, 485.4097859441482683, -3.498432987069644895 ) ) ;
#84077=CARTESIAN_POINT ( 'NONE',  ( 43.72966438978044579, 434.3041953058477702, 13.93761445528211596 ) ) ;
#84090=AXIS2_PLACEMENT_3D ( 'NONE', #103575, #47448, #29723 ) ;
#84097=CARTESIAN_POINT ( 'NONE',  ( -25.74409405560901476, 306.5801223853982833, -9.620750498333789480 ) ) ;
#84105=EDGE_CURVE ( 'NONE', #23997, #60854, #37727, .T. ) ;
#84109=CARTESIAN_POINT ( 'NONE',  ( -36.24643790419225553, 484.5338396111271777, -2.428444667542725810 ) ) ;
#84111=CARTESIAN_POINT ( 'NONE',  ( -40.94836816866144602, 406.2627700906166979, 27.72596324573498805 ) ) ;
#84124=ORIENTED_EDGE ( 'NONE', *, *, #99395, .T. ) ;
#84132=B_SPLINE_CURVE_WITH_KNOTS ( 'NONE', 3,
 ( #18516, #1756, #51375, #34713, #74589, #665, #67587, #91849, #34177, #67055 ),
 .UNSPECIFIED., .F., .F.,
 ( 4, 2, 2, 2, 4 ),
 ( 0.001128025973688894868, 0.01055240993440221230, 0.01526460191475887199, 0.01762069790493720617, 0.01997679389511553688 ),
 .UNSPECIFIED. ) ;
#84150=CARTESIAN_POINT ( 'NONE',  ( 37.85084083633361729, 438.0234350436310820, 4.171260309356161322 ) ) ;
#84160=ADVANCED_FACE ( 'NONE', ( #56682 ), #46458, .F. ) ;
#84169=CARTESIAN_POINT ( 'NONE',  ( 35.74483125092430669, 413.6409941285803598, 6.029078300230034770 ) ) ;
#84170=CARTESIAN_POINT ( 'NONE',  ( 41.17144925627759022, 461.2585203975962713, 2.461466063511514424 ) ) ;
#84180=DIRECTION ( 'NONE',  ( 0.9736964118521804767, 0.000000000000000000, -0.2278492869117413333 ) ) ;
#84185=AXIS2_PLACEMENT_3D ( 'NONE', #72951, #49209, #82108 ) ;
#84200=ORIENTED_EDGE ( 'NONE', *, *, #15042, .T. ) ;
#84212=EDGE_CURVE ( 'NONE', #52196, #22409, #74904, .T. ) ;
#84213=CARTESIAN_POINT ( 'NONE',  ( 37.85084083633365282, 438.0234350436313093, 4.171260309356235929 ) ) ;
#84217=CARTESIAN_POINT ( 'NONE',  ( -32.72014288347608613, 485.4774019869826134, 6.282418260599838433 ) ) ;
#84224=CARTESIAN_POINT ( 'NONE',  ( 40.73878143178837519, 486.4834083601638213, 16.46716573231486436 ) ) ;
#84228=CIRCLE ( 'NONE', #4998, 15.00000000000000711 ) ;
#84231=CARTESIAN_POINT ( 'NONE',  ( 43.18591170615831487, 464.9496799542843064, 14.54256400178507747 ) ) ;
#84237=CARTESIAN_POINT ( 'NONE',  ( 34.47678062874019389, 437.1474145881098821, 5.468662283308706407 ) ) ;
#84252=CARTESIAN_POINT ( 'NONE',  ( -46.00000000000000000, 461.1597079622330284, 8.544206286659692395 ) ) ;
#84260=CARTESIAN_POINT ( 'NONE',  ( -25.40129139438734285, 304.9292372608223900, 10.39962324656867843 ) ) ;
#84261=B_SPLINE_SURFACE_WITH_KNOTS ( 'NONE', 1, 3, ( 
 ( #76869, #102216, #86061, #27315, #50985, #34329, #52590, #11059, #44525, #77412, #83899, #1365, #51529, #28363, #2445, #42919, #27847, #93603, #10538, #60718, #2981, #84446, #68808, #52060, #100613, #75811, #43455, #85516 ),
 ( #1906, #60197, #59113, #68262, #18129, #35935, #34860, #101153, #53142, #12134, #75267, #67728, #19755, #59645, #19230, #11595, #93064, #84975, #26775, #3529, #92521, #101688, #18675, #76333, #36468, #35393, #69336, #61241 ) ),
 .UNSPECIFIED., .F., .F., .F.,
 ( 2, 2 ),
 ( 4, 2, 2, 2, 2, 2, 2, 2, 2, 2, 2, 2, 2, 4 ),
 ( 0.000000000000000000, 1.000000000000000000 ),
 ( 0.08901491201581737678, 0.1032490540155679704, 0.1174831960153185778, 0.1317173380150691853, 0.1459514800148197788, 0.1744197640143299588, 0.2028880480138401388, 0.2598246160128514504, 0.3167611840118632616, 0.4306343200098861623, 0.5445074560079088410, 0.6583805920059359051, 0.7722537280039543095, 1.000000000000000000 ),
 .UNSPECIFIED. ) ;
#84270=CARTESIAN_POINT ( 'NONE',  ( -42.19618372163272113, 487.7264399052817794, 8.629926728125361990 ) ) ;
#84287=CARTESIAN_POINT ( 'NONE',  ( 32.04707041935533596, 435.9091500956466234, 19.86198171785667554 ) ) ;
#84301=CARTESIAN_POINT ( 'NONE',  ( -16.04671841158817358, 302.5605069650110863, 9.875078356356782550 ) ) ;
#84331=CARTESIAN_POINT ( 'NONE',  ( 27.24240537402066309, 306.4001577942659651, -9.435465325163482575 ) ) ;
#84333=CARTESIAN_POINT ( 'NONE',  ( -32.15166163075724626, 486.0589784586660471, 5.199393881400879103 ) ) ;
#84341=AXIS2_PLACEMENT_3D ( 'NONE', #11018, #21287, #53616 ) ;
#84348=EDGE_CURVE ( 'NONE', #79201, #23775, #13211, .T. ) ;
#84363=FILL_AREA_STYLE_COLOUR ( '', #75485 ) ;
#84366=EDGE_LOOP ( 'NONE', ( #55508, #6790, #87272, #55355, #64657, #104279 ) ) ;
#84368=CARTESIAN_POINT ( 'NONE',  ( -43.03357534758885095, 463.2291678140052227, 4.675918524150252331 ) ) ;
#84369=ORIENTED_EDGE ( 'NONE', *, *, #35845, .T. ) ;
#84370=ORIENTED_EDGE ( 'NONE', *, *, #59475, .F. ) ;
#84376=CARTESIAN_POINT ( 'NONE',  ( -38.72759624817576452, 310.1070778200068503, 1.620604754975068174 ) ) ;
#84380=VERTEX_POINT ( 'NONE', #18940 ) ;
#84399=AXIS2_PLACEMENT_3D ( 'NONE', #17166, #1474, #50037 ) ;
#84400=CARTESIAN_POINT ( 'NONE',  ( -32.87547266101557852, 465.6993878536674742, 10.91512469976539279 ) ) ;
#84414=CIRCLE ( 'NONE', #75781, 5.000000000000003553 ) ;
#84427=CARTESIAN_POINT ( 'NONE',  ( 38.81358894280276672, 485.1131561813238591, -4.191378885298274959 ) ) ;
#84438=CARTESIAN_POINT ( 'NONE',  ( -42.60801251486928720, 467.2312078438266099, 12.94848564814438419 ) ) ;
#84439=CARTESIAN_POINT ( 'NONE',  ( -21.19348424345033521, 294.8901562694577478, 1.945151701991089332 ) ) ;
#84446=CARTESIAN_POINT ( 'NONE',  ( 35.76482652855951017, 405.2378813769876729, 6.148826621638260548 ) ) ;
#84451=ORIENTED_EDGE ( 'NONE', *, *, #96728, .T. ) ;
#84456=CARTESIAN_POINT ( 'NONE',  ( -32.88333705524179607, 439.7317646416724415, 24.13381181826117583 ) ) ;
#84457=CARTESIAN_POINT ( 'NONE',  ( 45.47623700953192127, 382.7937029844407562, 7.371119132332191626 ) ) ;
#84458=CARTESIAN_POINT ( 'NONE',  ( 43.72734063489998846, 464.0947689350302880, 7.873621169229567229 ) ) ;
#84460=CARTESIAN_POINT ( 'NONE',  ( 31.43086057969960478, 439.6979630470218581, 23.48915592383433193 ) ) ;
#84473=CARTESIAN_POINT ( 'NONE',  ( 33.95156263172584943, 464.5083255208626838, 6.608064661821377861 ) ) ;
#84474=CARTESIAN_POINT ( 'NONE',  ( 37.46478434938782698, 360.1732274943323659, 2.822779564172262390 ) ) ;
#84486=CARTESIAN_POINT ( 'NONE',  ( -36.14398083585128774, 461.0280587598256261, 3.026911855274814656 ) ) ;
#84496=EDGE_CURVE ( 'NONE', #84500, #79406, #31012, .T. ) ;
#84497=CARTESIAN_POINT ( 'NONE',  ( -32.13416116311759652, 374.4058483644059265, 24.05691306682159336 ) ) ;
#84500=VERTEX_POINT ( 'NONE', #20012 ) ;
#84506=CARTESIAN_POINT ( 'NONE',  ( 39.75151623530055645, 438.7665981957342751, 23.14798673880785529 ) ) ;
#84507=CARTESIAN_POINT ( 'NONE',  ( -31.18704516878236177, 357.2439419286618545, 20.55224204967724688 ) ) ;
#84516=CARTESIAN_POINT ( 'NONE',  ( 25.67326358033849942, 305.2097782842129732, 10.46538467574003839 ) ) ;
#84524=CARTESIAN_POINT ( 'NONE',  ( 27.63977025857940717, 296.6218385434618767, 2.321776652389909490 ) ) ;
#84532=CARTESIAN_POINT ( 'NONE',  ( 6.646227138586374927, 302.7439599329172779, 9.914178426197896243 ) ) ;
#84535=CIRCLE ( 'NONE', #55174, 0.9999999999999996669 ) ;
#84545=( BOUNDED_SURFACE ( )  B_SPLINE_SURFACE ( 3, 2, ( 
 ( #59657, #74744, #92537 ),
 ( #48871, #81762, #32739 ),
 ( #65607, #98492, #24644 ),
 ( #57492, #99012, #90417 ),
 ( #16520, #53157, #77426 ),
 ( #29447, #84458, #3542 ),
 ( #52072, #11608, #101700 ),
 ( #62319, #86074, #36480 ),
 ( #93075, #20842, #68272 ),
 ( #103301, #102227, #20309 ) ),
 .UNSPECIFIED., .F., .F., .F. ) 
 B_SPLINE_SURFACE_WITH_KNOTS ( ( 4, 2, 2, 2, 4 ),
 ( 3, 3 ),
 ( 6.505213034913026604E-19, 0.002844712610137182639, 0.003555890762671477974, 0.004267068915205773742, 0.005689425220274364411 ),
 ( 0.000000000000000000, 1.000000000000000000 ),
 .UNSPECIFIED. ) 
 GEOMETRIC_REPRESENTATION_ITEM ( )  RATIONAL_B_SPLINE_SURFACE ( (
 ( 1.000000000000000000, 0.8258027051680146835, 1.000000000000000000),
 ( 1.000000000000000000, 0.8423184768582745452, 1.000000000000000000),
 ( 1.000000000000000000, 0.8479189272860049309, 1.000000000000000000),
 ( 1.000000000000000000, 0.8482780919516984541, 1.000000000000000000),
 ( 1.000000000000000000, 0.8479712937334785705, 1.000000000000000000),
 ( 1.000000000000000000, 0.8466356411039382968, 1.000000000000000000),
 ( 1.000000000000000000, 0.8456087446180271527, 1.000000000000000000),
 ( 1.000000000000000000, 0.8414089630397959541, 1.000000000000000000),
 ( 1.000000000000000000, 0.8371477558891856630, 1.000000000000000000),
 ( 1.000000000000000000, 0.8308329163120958816, 1.000000000000000000) ) ) 
 REPRESENTATION_ITEM ( '' )  SURFACE ( )  );
#84553=DIRECTION ( 'NONE',  ( 0.000000000000000000, 0.000000000000000000, 1.000000000000000000 ) ) ;
#84556=CARTESIAN_POINT ( 'NONE',  ( -43.52560348121802747, 486.7876442849098453, 7.034435017230201481 ) ) ;
#84558=B_SPLINE_CURVE_WITH_KNOTS ( 'NONE', 3,
 ( #64023, #81219, #7336, #71543, #63486, #88806, #88283, #80693, #40245, #104445, #72612, #103916, #72085, #104992, #30597, #6270 ),
 .UNSPECIFIED., .F., .F.,
 ( 4, 2, 2, 2, 2, 2, 2, 4 ),
 ( 2.478060227011367563E-17, 0.0007707015628690528459, 0.001156052344303514163, 0.001541403125737975371, 0.001926753907172436579, 0.002312104688606898221, 0.002697455470041359212, 0.003082806251475820637 ),
 .UNSPECIFIED. ) ;
#84563=ORIENTED_EDGE ( 'NONE', *, *, #84496, .F. ) ;
#84575=CARTESIAN_POINT ( 'NONE',  ( -35.86608289195888233, 437.2866345698543569, 4.452337163522260610 ) ) ;
#84588=CARTESIAN_POINT ( 'NONE',  ( 27.67623204030578421, 310.9913909337609539, 11.64485516987953240 ) ) ;
#84598=CARTESIAN_POINT ( 'NONE',  ( -32.54922218626916930, 319.8023524069591303, -6.363686095274232457 ) ) ;
#84608=CARTESIAN_POINT ( 'NONE',  ( -9.407137736701065123, 302.6622268194199705, -10.04029227552683068 ) ) ;
#84613=CARTESIAN_POINT ( 'NONE',  ( -19.15465222815915070, 294.6774222264219247, 1.900466129964910378 ) ) ;
#84623=CARTESIAN_POINT ( 'NONE',  ( -46.00000000000000000, 437.9173578870133952, 12.34179081168478298 ) ) ;
#84632=CARTESIAN_POINT ( 'NONE',  ( -20.95526673416674868, 304.9223276462623744, -8.985009476610910539 ) ) ;
#84641=EDGE_CURVE ( 'NONE', #68930, #4192, #88486, .T. ) ;
#84644=LINE ( 'NONE', #53339, #28195 ) ;
#84647=CARTESIAN_POINT ( 'NONE',  ( -34.55934088217597377, 338.7551446543786824, -0.7819439798765525085 ) ) ;
#84648=CARTESIAN_POINT ( 'NONE',  ( -37.13583097524582399, 311.9121134930005610, 14.04606923393727058 ) ) ;
#84655=VERTEX_POINT ( 'NONE', #95980 ) ;
#84660=EDGE_CURVE ( 'NONE', #65653, #18077, #52273, .T. ) ;
#84664=CARTESIAN_POINT ( 'NONE',  ( 46.00000000000000000, 450.0000000000002274, 13.20242257375370976 ) ) ;
#84674=CARTESIAN_POINT ( 'NONE',  ( 2.435618412119228804, 294.8338784867337381, -9.717600221945083661 ) ) ;
#84675=CARTESIAN_POINT ( 'NONE',  ( 37.51854390953261742, 313.5286481325095451, 14.45587837336505999 ) ) ;
#84677=DIRECTION ( 'NONE',  ( 1.000000000000000000, 0.000000000000000000, 0.000000000000000000 ) ) ;
#84682=CARTESIAN_POINT ( 'NONE',  ( -41.85455215201762513, 465.6883253721317146, 15.30917575692330246 ) ) ;
#84686=CARTESIAN_POINT ( 'NONE',  ( 0.000000000000000000, 300.0000000000000000, 0.000000000000000000 ) ) ;
#84695=DIRECTION ( 'NONE',  ( 0.000000000000000000, -3.700743415417185576E-15, -1.000000000000000000 ) ) ;
#84697=CARTESIAN_POINT ( 'NONE',  ( 21.23684446602550935, 304.9566545053270943, -9.977713076987674512 ) ) ;
#84698=CARTESIAN_POINT ( 'NONE',  ( 40.53119313125029066, 460.3380581626494745, 2.322614769220080699 ) ) ;
#84723=EDGE_LOOP ( 'NONE', ( #46230, #67989 ) ) ;
#84739=CARTESIAN_POINT ( 'NONE',  ( -23.61963550967466574, 306.0340374937824777, 10.19690224617928287 ) ) ;
#84745=B_SPLINE_CURVE_WITH_KNOTS ( 'NONE', 3,
 ( #30049, #12763, #64009, #96373, #4698, #54814, #13824, #8392, #16490, #65039, #32159, #73102, #56928, #42356 ),
 .UNSPECIFIED., .F., .F.,
 ( 4, 2, 2, 2, 2, 2, 4 ),
 ( 2.602085213965210642E-18, 0.001035928240051109178, 0.001553892360076662574, 0.002071856480102215754, 0.002589820600127769150, 0.003107784720153322546, 0.004143712960204457528 ),
 .UNSPECIFIED. ) ;
#84750=CARTESIAN_POINT ( 'NONE',  ( -32.78741055188836384, 485.3331003366710092, 5.977022408746766047 ) ) ;
#84761=CARTESIAN_POINT ( 'NONE',  ( -23.95966359935239609, 306.2573737793246664, 9.247948789945837689 ) ) ;
#84767=EDGE_CURVE ( 'NONE', #67620, #23775, #28224, .T. ) ;
#84778=EDGE_CURVE ( 'NONE', #89053, #96664, #14342, .T. ) ;
#84784=B_SPLINE_CURVE_WITH_KNOTS ( 'NONE', 3,
 ( #101526, #37356, #69697, #4418, #52426, #2272, #43812, #3895, #69175, #70220, #103121, #53505, #29272, #62152, #102043, #27143 ),
 .UNSPECIFIED., .F., .F.,
 ( 4, 2, 2, 2, 2, 2, 2, 4 ),
 ( 7.196489415735148522E-17, 0.0007700875212649647061, 0.001155131281897411009, 0.001540175042529857421, 0.001925218803162303833, 0.002310262563794750028, 0.002695306324427196656, 0.003080350085059642851 ),
 .UNSPECIFIED. ) ;
#84803=FACE_OUTER_BOUND ( 'NONE', #78871, .T. ) ;
#84805=CARTESIAN_POINT ( 'NONE',  ( -41.59000009475712289, 487.6876459975654825, 9.910902919395237376 ) ) ;
#84816=CARTESIAN_POINT ( 'NONE',  ( 34.85314611530805706, 481.9558839989245485, 14.52857051749963091 ) ) ;
#84833=CARTESIAN_POINT ( 'NONE',  ( -19.18365999306769609, 302.7119710974035343, 9.907277072326611034 ) ) ;
#84870=CARTESIAN_POINT ( 'NONE',  ( -32.85155332502864667, 463.8111683108725174, 7.359358840565846549 ) ) ;
#84880=CARTESIAN_POINT ( 'NONE',  ( 32.28930913498017929, 488.2717154064768579, 9.213726894932253941 ) ) ;
#84882=CARTESIAN_POINT ( 'NONE',  ( 0.000000000000000000, 303.8518027762758038, -10.00000000000000355 ) ) ;
#84886=CARTESIAN_POINT ( 'NONE',  ( -19.70764564238371719, 304.7954121406193622, 9.925013215726785631 ) ) ;
#84890=FILL_AREA_STYLE ('',( #84363 ) ) ;
#84891=FACE_OUTER_BOUND ( 'NONE', #104908, .T. ) ;
#84902=CYLINDRICAL_SURFACE ( 'NONE', #71807, 5.000000000000001776 ) ;
#84907=CARTESIAN_POINT ( 'NONE',  ( -39.04768082253571748, 311.1420226168212366, 1.880774019654843254 ) ) ;
#84919=ORIENTED_EDGE ( 'NONE', *, *, #85517, .F. ) ;
#84929=CARTESIAN_POINT ( 'NONE',  ( -32.84951609414347473, 478.7804999730025202, 7.701738758140129093 ) ) ;
#84937=CARTESIAN_POINT ( 'NONE',  ( 32.85155332502866798, 463.8111683108725174, 7.359358840565819904 ) ) ;
#84939=CARTESIAN_POINT ( 'NONE',  ( 43.61214829175436591, 434.3223057887385608, 14.49707129802061800 ) ) ;
#84960=EDGE_LOOP ( 'NONE', ( #11267, #42977, #62502, #36174 ) ) ;
#84966=CARTESIAN_POINT ( 'NONE',  ( -42.69336147150778515, 372.1122575306994236, 17.99588274971726420 ) ) ;
#84974=CARTESIAN_POINT ( 'NONE',  ( 23.94432778666880068, 303.5797213061153457, -9.843316957413865254 ) ) ;
#84975=CARTESIAN_POINT ( 'NONE',  ( 45.17824257314219949, 354.4244853104167987, 3.762393652172960845 ) ) ;
#84986=CARTESIAN_POINT ( 'NONE',  ( 41.00553391478180032, 320.1856813797184600, 4.158943489448629904 ) ) ;
#84987=FACE_OUTER_BOUND ( 'NONE', #89746, .T. ) ;
#85027=ORIENTED_EDGE ( 'NONE', *, *, #90517, .T. ) ;
#85029=CARTESIAN_POINT ( 'NONE',  ( -32.77384846114340888, 465.0024891621177403, 11.55799621384033671 ) ) ;
#85031=AXIS2_PLACEMENT_3D ( 'NONE', #102683, #95137, #94613 ) ;
#85033=CARTESIAN_POINT ( 'NONE',  ( 38.67540923711027290, 439.2245545847551398, 23.63822418690137539 ) ) ;
#85034=CARTESIAN_POINT ( 'NONE',  ( -31.01628821198604768, 439.2628560410439604, 22.57312827278326495 ) ) ;
#85036=EDGE_CURVE ( 'NONE', #98784, #53610, #96707, .T. ) ;
#85044=CARTESIAN_POINT ( 'NONE',  ( 24.47931459791210429, 295.5124831337354863, 2.078786121475366677 ) ) ;
#85058=CARTESIAN_POINT ( 'NONE',  ( 30.00000000000000000, 461.8887775513396150, 11.55279652844105698 ) ) ;
#85061=CARTESIAN_POINT ( 'NONE',  ( 42.64966854229459869, 465.0854819100619011, 13.23715615004964086 ) ) ;
#85083=CARTESIAN_POINT ( 'NONE',  ( -42.72730916064396212, 485.8496625310939976, 7.279181987618908778 ) ) ;
#85084=CARTESIAN_POINT ( 'NONE',  ( 44.49616249768619269, 470.0858613617913306, 4.037852223137175400 ) ) ;
#85092=CARTESIAN_POINT ( 'NONE',  ( 39.29343254467229940, 485.1983557762937949, -4.348408391708091791 ) ) ;
#85094=CARTESIAN_POINT ( 'NONE',  ( -36.60690515392210642, 437.5575915073889632, 4.269387481551378372 ) ) ;
#85097=EDGE_CURVE ( 'NONE', #49781, #22579, #74747, .T. ) ;
#85103=CARTESIAN_POINT ( 'NONE',  ( 7.904834542844216827, 294.7031450397155368, -6.150931456888534044 ) ) ;
#85109=ORIENTED_EDGE ( 'NONE', *, *, #56945, .F. ) ;
#85110=CARTESIAN_POINT ( 'NONE',  ( 23.64531383863861436, 306.0645085318336100, 10.20398222576348957 ) ) ;
#85122=CARTESIAN_POINT ( 'NONE',  ( -30.12932728364529922, 334.4140447340107585, 17.11298374841474867 ) ) ;
#85131=CARTESIAN_POINT ( 'NONE',  ( -9.218636978381848479, 294.6649786875596533, -3.878494680342783774 ) ) ;
#85133=ORIENTED_EDGE ( 'NONE', *, *, #36116, .F. ) ;
#85149=EDGE_CURVE ( 'NONE', #78613, #9645, #61005, .T. ) ;
#85157=CIRCLE ( 'NONE', #61069, 12.00000000000001066 ) ;
#85160=CARTESIAN_POINT ( 'NONE',  ( -26.60412269428898924, 307.1936361343147155, -9.480968390364807874 ) ) ;
#85174=CARTESIAN_POINT ( 'NONE',  ( -30.05061994666513314, 312.1672957118879026, -7.283488774298362500 ) ) ;
#85175=CARTESIAN_POINT ( 'NONE',  ( -38.82405594768357560, 321.9282899208834579, 16.54806888951848265 ) ) ;
#85190=DIRECTION ( 'NONE',  ( 1.000000000000000000, -0.000000000000000000, -0.000000000000000000 ) ) ;
#85201=CARTESIAN_POINT ( 'NONE',  ( 5.515535885521446247, 296.1986775320684728, -10.01281319186619001 ) ) ;
#85203=CARTESIAN_POINT ( 'NONE',  ( 35.62336637792430594, 303.3604247956168365, -0.04934908291839113642 ) ) ;
#85205=ORIENTED_EDGE ( 'NONE', *, *, #38258, .T. ) ;
#85207=VERTEX_POINT ( 'NONE', #78490 ) ;
#85218=ORIENTED_EDGE ( 'NONE', *, *, #54768, .T. ) ;
#85227=CIRCLE ( 'NONE', #36999, 12.00000000000000711 ) ;
#85232=EDGE_LOOP ( 'NONE', ( #77289, #41967, #19469, #101174 ) ) ;
#85234=CARTESIAN_POINT ( 'NONE',  ( -43.61209369432236826, 434.3223138618526491, 14.49730483407481785 ) ) ;
#85278=CARTESIAN_POINT ( 'NONE',  ( -32.67430661331354713, 485.6291057174253751, 6.589190333393256438 ) ) ;
#85281=ORIENTED_EDGE ( 'NONE', *, *, #70058, .F. ) ;
#85289=CARTESIAN_POINT ( 'NONE',  ( 42.19180677453719142, 462.2931784592651638, 3.389262873192005809 ) ) ;
#85293=CIRCLE ( 'NONE', #90674, 5.000000000000000888 ) ;
#85303=CARTESIAN_POINT ( 'NONE',  ( 32.03491031660919219, 464.8549693818604851, 13.92556383226224526 ) ) ;
#85314=FACE_OUTER_BOUND ( 'NONE', #55401, .T. ) ;
#85321=CARTESIAN_POINT ( 'NONE',  ( 42.51086551946173131, 484.3281707585954905, -1.915972276551562548 ) ) ;
#85330=CARTESIAN_POINT ( 'NONE',  ( -7.152384844127436025, 296.5444182697836482, 6.994491946633746515 ) ) ;
#85337=DIRECTION ( 'NONE',  ( 0.9735618822052786170, 0.000000000000000000, -0.2284234259372612819 ) ) ;
#85341=CARTESIAN_POINT ( 'NONE',  ( 40.66024587926714418, 485.8034863302610233, -4.843677042987392767 ) ) ;
#85344=ADVANCED_FACE ( 'NONE', ( #80604 ), #9838, .F. ) ;
#85353=CARTESIAN_POINT ( 'NONE',  ( 32.78741055188847042, 485.3331003366707819, 5.977022408747033388 ) ) ;
#85359=CYLINDRICAL_SURFACE ( 'NONE', #40487, 5.000000000000000000 ) ;
#85387=CIRCLE ( 'NONE', #68132, 10.00000000000000000 ) ;
#85397=CARTESIAN_POINT ( 'NONE',  ( 28.56029514625197052, 307.6844803076128869, -9.136023263255507842 ) ) ;
#85405=CARTESIAN_POINT ( 'NONE',  ( 41.15811204217011010, 436.5847606186501366, 6.466625614333893601 ) ) ;
#85406=B_SPLINE_CURVE_WITH_KNOTS ( 'NONE', 3,
 ( #32083, #54195, #95222, #87134, #46137, #104349, #79024, #5142 ),
 .UNSPECIFIED., .F., .F.,
 ( 4, 2, 2, 4 ),
 ( 1.734723475976807094E-18, 0.002725205121551986433, 0.004087807682327984637, 0.005450410243103983275 ),
 .UNSPECIFIED. ) ;
#85425=DIRECTION ( 'NONE',  ( -1.000000000000000000, -0.000000000000000000, -0.000000000000000000 ) ) ;
#85426=CARTESIAN_POINT ( 'NONE',  ( -35.48030077899827006, 426.7164938744821825, 6.204872843841080510 ) ) ;
#85427=AXIS2_PLACEMENT_3D ( 'NONE', #42610, #2676, #1055 ) ;
#85439=CARTESIAN_POINT ( 'NONE',  ( -30.80797925829203976, 309.0763670535902179, -8.567432199028438333 ) ) ;
#85445=CARTESIAN_POINT ( 'NONE',  ( -43.58525199864187272, 435.7810069860521480, 17.82023302324694569 ) ) ;
#85473=CARTESIAN_POINT ( 'NONE',  ( -46.00000000000000000, 488.7535717825852544, 4.225312566738604225 ) ) ;
#85487=ORIENTED_EDGE ( 'NONE', *, *, #96766, .T. ) ;
#85506=CARTESIAN_POINT ( 'NONE',  ( -30.64820813098222985, 298.3937798550618936, 2.720202561658572105 ) ) ;
#85510=CARTESIAN_POINT ( 'NONE',  ( -36.64823341582351901, 437.5392299810053487, 4.281405873620232505 ) ) ;
#85515=CARTESIAN_POINT ( 'NONE',  ( 27.33779175179976662, 296.2809847081317685, -9.691540634816723454 ) ) ;
#85516=CARTESIAN_POINT ( 'NONE',  ( 35.56416567029047116, 496.2909070316903239, -10.19064917708978335 ) ) ;
#85517=EDGE_CURVE ( 'NONE', #38940, #29831, #16852, .T. ) ;
#85519=CARTESIAN_POINT ( 'NONE',  ( 19.86162800728184763, 303.8052307878185729, 8.927100233615687941 ) ) ;
#85523=CARTESIAN_POINT ( 'NONE',  ( 43.09948196127323428, 484.9577458347781089, -0.8563396247083570056 ) ) ;
#85526=CARTESIAN_POINT ( 'NONE',  ( 35.15748201403830109, 323.3744436496217531, -4.986382573361860082 ) ) ;
#85527=CARTESIAN_POINT ( 'NONE',  ( 38.86575227086510154, 477.1840224093098186, -1.710886565985892505 ) ) ;
#85531=CARTESIAN_POINT ( 'NONE',  ( -18.41162169223098033, 304.6294254666754568, 9.889731659030220001 ) ) ;
#85549=B_SPLINE_CURVE_WITH_KNOTS ( 'NONE', 3,
 ( #8067, #83960, #24295, #44039, #75870, #52646, #52117, #59705, #101216, #76390 ),
 .UNSPECIFIED., .F., .F.,
 ( 4, 2, 2, 2, 4 ),
 ( 1.498769063644528192E-28, 0.009926681031335791300, 0.01489002154700368868, 0.01737169180483764605, 0.01985336206267160342 ),
 .UNSPECIFIED. ) ;
#85555=DIRECTION ( 'NONE',  ( 0.000000000000000000, 0.000000000000000000, -1.000000000000000000 ) ) ;
#85556=CARTESIAN_POINT ( 'NONE',  ( -43.41041896072598405, 463.0441421612069917, 5.626145547246294676 ) ) ;
#85568=AXIS2_PLACEMENT_3D ( 'NONE', #5254, #12268, #94811 ) ;
#85572=CARTESIAN_POINT ( 'NONE',  ( -28.53018783420407445, 313.9245910824191697, 12.38472899747105949 ) ) ;
#85586=EDGE_LOOP ( 'NONE', ( #100991, #15586, #75888, #30923, #43234, #81242 ) ) ;
#85590=CARTESIAN_POINT ( 'NONE',  ( 24.36825887693873227, 295.5443735985305125, 10.08561002281235197 ) ) ;
#85600=ORIENTED_EDGE ( 'NONE', *, *, #40940, .T. ) ;
#85606=CARTESIAN_POINT ( 'NONE',  ( 2.627664075538336252, 302.8385117092220185, 9.934221049389936553 ) ) ;
#85615=FACE_OUTER_BOUND ( 'NONE', #106314, .T. ) ;
#85620=CARTESIAN_POINT ( 'NONE',  ( 37.02114271195448225, 490.9588991526813970, 12.45652432424409461 ) ) ;
#85624=CARTESIAN_POINT ( 'NONE',  ( 40.66415791351412423, 490.1350948120814337, 11.30186264364121662 ) ) ;
#85626=CARTESIAN_POINT ( 'NONE',  ( 44.10862079528723001, 485.7176850333829634, 3.977867558414246663 ) ) ;
#85634=CARTESIAN_POINT ( 'NONE',  ( 41.31161337382093279, 484.8232235214512684, -3.619187650536324519 ) ) ;
#85639=CARTESIAN_POINT ( 'NONE',  ( -37.99667718823692297, 439.4681409270056065, 23.88471372786844071 ) ) ;
#85643=EDGE_LOOP ( 'NONE', ( #37863, #66757, #86034, #71602, #76916 ) ) ;
#85653=AXIS2_PLACEMENT_3D ( 'NONE', #23736, #41476, #49565 ) ;
#85659=CARTESIAN_POINT ( 'NONE',  ( 22.31591624825033549, 305.3790487442428798, 10.05087283592891545 ) ) ;
#85677=CARTESIAN_POINT ( 'NONE',  ( 35.47319904751531539, 436.4618060951635243, 5.062631899564591365 ) ) ;
#85693=B_SPLINE_CURVE_WITH_KNOTS ( 'NONE', 3,
 ( #3766, #46342, #4819, #21051, #38278, #4288, #37215, #22085 ),
 .UNSPECIFIED., .F., .F.,
 ( 4, 2, 2, 4 ),
 ( 5.204170427930421283E-18, 0.005696202229710471167, 0.008544303344565708919, 0.01139240445942094754 ),
 .UNSPECIFIED. ) ;
#85705=VERTEX_POINT ( 'NONE', #20060 ) ;
#85725=AXIS2_PLACEMENT_3D ( 'NONE', #32435, #73372, #66360 ) ;
#85727=CARTESIAN_POINT ( 'NONE',  ( -30.50310125412890372, 318.9373365299751981, 13.88874147237046763 ) ) ;
#85737=EDGE_CURVE ( 'NONE', #97120, #65472, #28334, .T. ) ;
#85756=CARTESIAN_POINT ( 'NONE',  ( 1.050160786911071398, 296.8373249698643122, -10.00076906402473043 ) ) ;
#85757=CARTESIAN_POINT ( 'NONE',  ( 43.74855578046756222, 328.6220886837048170, -1.765109843966993441 ) ) ;
#85758=CARTESIAN_POINT ( 'NONE',  ( 43.35947070037873630, 356.1039901738380991, 11.86182662173998814 ) ) ;
#85788=DIRECTION ( 'NONE',  ( -0.3573389821873162453, -0.9339747597281914393, 0.000000000000000000 ) ) ;
#85790=VERTEX_POINT ( 'NONE', #73791 ) ;
#85810=EDGE_LOOP ( 'NONE', ( #9430, #4377, #41071, #3746 ) ) ;
#85811=ORIENTED_EDGE ( 'NONE', *, *, #43835, .T. ) ;
#85821=DIRECTION ( 'NONE',  ( -0.9508028509851098597, -0.1865215626109695546, 0.2473532802283995025 ) ) ;
#85823=CARTESIAN_POINT ( 'NONE',  ( -30.35537264529554946, 338.7115663565144246, 18.05293407820170515 ) ) ;
#85825=( BOUNDED_SURFACE ( )  B_SPLINE_SURFACE ( 3, 2, ( 
 ( #40278, #55899, #30625 ),
 ( #22001, #6842, #13867 ),
 ( #56443, #23060, #64049 ),
 ( #63513, #96411, #71571 ),
 ( #5785, #87783, #54854 ),
 ( #38707, #22543, #13332 ),
 ( #80724, #46257, #88314 ),
 ( #97434, #103946, #79144 ),
 ( #5270, #14389, #96924 ),
 ( #88834, #39766, #46781 ) ),
 .UNSPECIFIED., .F., .F., .F. ) 
 B_SPLINE_SURFACE_WITH_KNOTS ( ( 4, 2, 2, 2, 4 ),
 ( 3, 3 ),
 ( 0.007162312563338129288, 0.008169815727934513425, 0.009177318892530896693, 0.01018482205712727996, 0.01119232522172366323 ),
 ( 0.1508783416922580001, 1.000000000000000000 ),
 .UNSPECIFIED. ) 
 GEOMETRIC_REPRESENTATION_ITEM ( )  RATIONAL_B_SPLINE_SURFACE ( (
 ( 0.9388230293412898053, 0.7972639082172212621, 1.000000000000000000),
 ( 0.9416444161515592493, 0.8066137816935087246, 1.000000000000000000),
 ( 0.9435088878518229638, 0.8127925071465851303, 1.000000000000000000),
 ( 0.9450395734671753756, 0.8178650894608657795, 1.000000000000000000),
 ( 0.9446996306686668010, 0.8167385434149065926, 1.000000000000000000),
 ( 0.9419800614655553517, 0.8077260861841054629, 1.000000000000000000),
 ( 0.9396107484148550348, 0.7998743527141916054, 1.000000000000000000),
 ( 0.9333151777508156277, 0.7790112831926551129, 1.000000000000000000),
 ( 0.9293941002835721665, 0.7660171137735573010, 1.000000000000000000),
 ( 0.9249525166718545188, 0.7512980243340108277, 1.000000000000000000) ) ) 
 REPRESENTATION_ITEM ( '' )  SURFACE ( )  );
#85828=CARTESIAN_POINT ( 'NONE',  ( 37.20102314025923107, 438.1443282426988617, 4.012575796191242716 ) ) ;
#85834=CARTESIAN_POINT ( 'NONE',  ( -32.62376965138169993, 486.1221409277068801, 7.511474791651365557 ) ) ;
#85845=CARTESIAN_POINT ( 'NONE',  ( -32.37479440661866192, 435.2079318469511691, 18.54001184198767760 ) ) ;
#85846=CARTESIAN_POINT ( 'NONE',  ( 42.09158233638503077, 465.7816406625409513, 14.79318349170028668 ) ) ;
#85854=CARTESIAN_POINT ( 'NONE',  ( 35.07439070120019409, 437.8544070495369738, 4.397851634058062231 ) ) ;
#85862=STYLED_ITEM ( 'NONE', ( #89770 ), #61133 ) ;
#85875=CARTESIAN_POINT ( 'NONE',  ( -32.90753060623204362, 485.1134061475200951, 5.490696813865477921 ) ) ;
#85884=CARTESIAN_POINT ( 'NONE',  ( -8.573043381437493338, 295.3718485560969498, 5.156920410645950525 ) ) ;
#85885=DIRECTION ( 'NONE',  ( -0.000000000000000000, -1.000000000000000000, -0.000000000000000000 ) ) ;
#85887=DIRECTION ( 'NONE',  ( 1.000000000000000000, 0.000000000000000000, 0.000000000000000000 ) ) ;
#85914=CARTESIAN_POINT ( 'NONE',  ( -45.33180403702434091, 464.4945808635454227, 2.178908857919817699 ) ) ;
#85940=ORIENTED_EDGE ( 'NONE', *, *, #15394, .T. ) ;
#85970=CARTESIAN_POINT ( 'NONE',  ( -30.24427031855517711, 312.0196691915732004, -8.325478004009855937 ) ) ;
#85977=VERTEX_POINT ( 'NONE', #11329 ) ;
#85980=CARTESIAN_POINT ( 'NONE',  ( -35.76697723764162617, 397.1839565823023577, 5.954605915834287444 ) ) ;
#85986=EDGE_LOOP ( 'NONE', ( #70981, #72891, #97742, #91223 ) ) ;
#85994=CARTESIAN_POINT ( 'NONE',  ( -18.91950813577646784, 304.6927365361660804, 8.903189087522576983 ) ) ;
#85996=( BOUNDED_SURFACE ( )  B_SPLINE_SURFACE ( 3, 2, ( 
 ( #23679, #47384, #6387 ),
 ( #97005, #38275, #71135 ),
 ( #89456, #62530, #103507 ),
 ( #95416, #104026, #54392 ) ),
 .UNSPECIFIED., .F., .F., .F. ) 
 B_SPLINE_SURFACE_WITH_KNOTS ( ( 4, 4 ),
 ( 3, 3 ),
 ( 4.770489558936219510E-18, 0.001771883439662679666 ),
 ( 0.000000000000000000, 1.000000000000000000 ),
 .UNSPECIFIED. ) 
 GEOMETRIC_REPRESENTATION_ITEM ( )  RATIONAL_B_SPLINE_SURFACE ( (
 ( 1.000000000000000000, 0.7699558187665703768, 1.000000000000000000),
 ( 1.000000000000000000, 0.7661160612245745405, 1.000000000000000000),
 ( 1.000000000000000000, 0.7602452393655095841, 1.000000000000000000),
 ( 1.000000000000000000, 0.7533433155455017127, 1.000000000000000000) ) ) 
 REPRESENTATION_ITEM ( '' )  SURFACE ( )  );
#86004=EDGE_CURVE ( 'NONE', #105451, #89053, #5201, .T. ) ;
#86011=B_SPLINE_CURVE_WITH_KNOTS ( 'NONE', 3,
 ( #37055, #51596, #68876, #10604 ),
 .UNSPECIFIED., .F., .F.,
 ( 4, 4 ),
 ( 0.000000000000000000, 0.0007940539003707024418 ),
 .UNSPECIFIED. ) ;
#86021=CARTESIAN_POINT ( 'NONE',  ( 43.00000000000000000, 485.2629658518202405, -2.796394914059364911 ) ) ;
#86024=EDGE_CURVE ( 'NONE', #105963, #30899, #64419, .T. ) ;
#86034=ORIENTED_EDGE ( 'NONE', *, *, #29783, .T. ) ;
#86054=FACE_OUTER_BOUND ( 'NONE', #94812, .T. ) ;
#86059=CARTESIAN_POINT ( 'NONE',  ( 26.14799737485564890, 295.8871012151415130, -9.777418602662287128 ) ) ;
#86061=CARTESIAN_POINT ( 'NONE',  ( 22.18906107735381283, 305.1406206946286943, -9.938500898755204815 ) ) ;
#86072=CARTESIAN_POINT ( 'NONE',  ( 42.72237582395932520, 338.4720114372719308, 8.457513108131092139 ) ) ;
#86074=CARTESIAN_POINT ( 'NONE',  ( 43.68737779332730753, 464.3703856682132027, 8.648249337468564946 ) ) ;
#86075=ORIENTED_EDGE ( 'NONE', *, *, #77017, .T. ) ;
#86077=CARTESIAN_POINT ( 'NONE',  ( 31.61743702809175716, 439.0120537715812929, 23.38841530320140549 ) ) ;
#86080=CARTESIAN_POINT ( 'NONE',  ( -8.034710196240776243E-11, 303.8518027762758038, -9.000000000000005329 ) ) ;
#86085=B_SPLINE_CURVE_WITH_KNOTS ( 'NONE', 3,
 ( #56153, #9217, #89627, #65876, #64815, #97696, #89097, #49141, #40535, #98238 ),
 .UNSPECIFIED., .F., .F.,
 ( 4, 2, 2, 2, 4 ),
 ( 0.000000000000000000, 0.001247095126357080329, 0.002494190252714160658, 0.003741285379071240987, 0.004988380505428321315 ),
 .UNSPECIFIED. ) ;
#86120=CARTESIAN_POINT ( 'NONE',  ( -37.63787431931454819, 432.3637935970024273, 5.163396886644006756 ) ) ;
#86128=CARTESIAN_POINT ( 'NONE',  ( 33.00000000000000000, 450.0000000000002274, 25.20242257375371864 ) ) ;
#86130=CARTESIAN_POINT ( 'NONE',  ( 26.68501260228623906, 296.2122705307798469, 2.231322931648561880 ) ) ;
#86131=COLOUR_RGB ( '', 0.09019608, 0.27058824, 0.51372549) ;
#86137=CARTESIAN_POINT ( 'NONE',  ( -42.33268550343508707, 436.4462712439766960, 6.764016893796111596 ) ) ;
#86140=CARTESIAN_POINT ( 'NONE',  ( 46.00000000000000000, 461.6622277975422435, 10.18145404766785589 ) ) ;
#86148=CARTESIAN_POINT ( 'NONE',  ( 0.000000000000000000, -19.99999999999998934, 0.000000000000000000 ) ) ;
#86154=ORIENTED_EDGE ( 'NONE', *, *, #61367, .T. ) ;
#86163=CARTESIAN_POINT ( 'NONE',  ( -32.12958771267418712, 464.7275665249413805, 11.12424126545828784 ) ) ;
#86167=CARTESIAN_POINT ( 'NONE',  ( 12.19423397773156736, 304.5852035401753710, 9.880331998383338643 ) ) ;
#86170=CARTESIAN_POINT ( 'NONE',  ( -32.22120753352784561, 464.6691781026584636, 10.60621122532581140 ) ) ;
#86175=CARTESIAN_POINT ( 'NONE',  ( 40.62309488084314779, 485.6251729596485234, -4.313937499023156263 ) ) ;
#86187=AXIS2_PLACEMENT_3D ( 'NONE', #50568, #92645, #82963 ) ;
#86189=ORIENTED_EDGE ( 'NONE', *, *, #71855, .T. ) ;
#86190=CARTESIAN_POINT ( 'NONE',  ( 33.00795325653295009, 439.3958174160654835, 23.82489859418973666 ) ) ;
#86195=VERTEX_POINT ( 'NONE', #39382 ) ;
#86199=CARTESIAN_POINT ( 'NONE',  ( 22.46479421738874649, 305.4359882429142772, 10.06336503754929801 ) ) ;
#86201=CARTESIAN_POINT ( 'NONE',  ( -40.78808449138670511, 461.0038402359688234, 2.292482253616661581 ) ) ;
#86209=DIRECTION ( 'NONE',  ( -0.6621791990579699583, 0.000000000000000000, -0.7493455199939116351 ) ) ;
#86238=CARTESIAN_POINT ( 'NONE',  ( -44.12456444187882454, 435.3734385797342270, 10.68335876406171181 ) ) ;
#86240=CARTESIAN_POINT ( 'NONE',  ( -43.75401118688380819, 486.3173572309548263, 5.908089951475163915 ) ) ;
#86248=B_SPLINE_CURVE_WITH_KNOTS ( 'NONE', 3,
 ( #19470, #44777, #36712, #52307, #86307, #35104, #18931, #44235 ),
 .UNSPECIFIED., .F., .F.,
 ( 4, 2, 2, 4 ),
 ( 0.01358597261296601820, 0.01555715282820523473, 0.01654274293582484387, 0.01752833304344444953 ),
 .UNSPECIFIED. ) ;
#86250=CARTESIAN_POINT ( 'NONE',  ( 33.06122231440979675, 369.6080732779042819, 23.70317340430991493 ) ) ;
#86251=CARTESIAN_POINT ( 'NONE',  ( 42.48296590554126340, 485.4097859441455398, -3.498432987059889587 ) ) ;
#86252=CARTESIAN_POINT ( 'NONE',  ( -44.35776761200799001, 435.2162786697447814, 12.88191835534828478 ) ) ;
#86258=CARTESIAN_POINT ( 'NONE',  ( -32.42385571103915964, 438.8717992898766624, 23.74935544307452062 ) ) ;
#86261=CARTESIAN_POINT ( 'NONE',  ( -20.40408973000767290, 304.8517363292163509, -9.000014075294032523 ) ) ;
#86262=CARTESIAN_POINT ( 'NONE',  ( -41.06716693784987626, 327.3805982724676369, 9.858883544215990113 ) ) ;
#86268=DIRECTION ( 'NONE',  ( 0.000000000000000000, -0.9523642049634558626, 0.3049629831706212046 ) ) ;
#86290=CARTESIAN_POINT ( 'NONE',  ( 2.295593195821269195, 298.7070635966626355, -10.00347380708956635 ) ) ;
#86307=CARTESIAN_POINT ( 'NONE',  ( 9.988791316060179781, 294.6431201125005828, 0.5781485321568775593 ) ) ;
#86308=CARTESIAN_POINT ( 'NONE',  ( -41.47545032233811924, 461.4488778950835126, 2.700315249222962954 ) ) ;
#86323=ORIENTED_EDGE ( 'NONE', *, *, #80262, .T. ) ;
#86329=ORIENTED_EDGE ( 'NONE', *, *, #16463, .F. ) ;
#86351=ORIENTED_EDGE ( 'NONE', *, *, #54383, .T. ) ;
#86361=CARTESIAN_POINT ( 'NONE',  ( 31.02212611900126760, 360.5725590293961318, 22.12937154125974715 ) ) ;
#86379=CARTESIAN_POINT ( 'NONE',  ( -32.74248746529113419, 435.3839305082926785, 16.93970874907590840 ) ) ;
#86381=CARTESIAN_POINT ( 'NONE',  ( 32.37370863962282641, 435.2098570401744837, 18.54444254976758799 ) ) ;
#86393=CARTESIAN_POINT ( 'NONE',  ( 41.61957457421982554, 435.6113505990638828, 7.035653009325279150 ) ) ;
#86415=ORIENTED_EDGE ( 'NONE', *, *, #90788, .T. ) ;
#86436=CARTESIAN_POINT ( 'NONE',  ( -33.00000000000000000, 500.0000000000002274, -12.00000000000000711 ) ) ;
#86446=B_SPLINE_CURVE_WITH_KNOTS ( 'NONE', 3,
 ( #77226, #59465, #11407, #68625, #10352, #17940 ),
 .UNSPECIFIED., .F., .F.,
 ( 4, 2, 4 ),
 ( 0.000000000000000000, 0.005272480446829030769, 0.01054496089365805633 ),
 .UNSPECIFIED. ) ;
#86458=( BOUNDED_SURFACE ( )  B_SPLINE_SURFACE ( 3, 2, ( 
 ( #13224, #61274, #54207 ),
 ( #46152, #94164, #87146 ),
 ( #20333, #11631, #53179 ),
 ( #44563, #12167, #45099 ),
 ( #61822, #20865, #64458 ),
 ( #40689, #48242, #56864 ),
 ( #22432, #24022, #74112 ),
 ( #97330, #48768, #55789 ),
 ( #57396, #24549, #40164 ),
 ( #97866, #15890, #23485 ) ),
 .UNSPECIFIED., .F., .F., .F. ) 
 B_SPLINE_SURFACE_WITH_KNOTS ( ( 4, 2, 2, 2, 4 ),
 ( 3, 3 ),
 ( 9.107298248878237246E-18, 0.002138704226848488731, 0.004277408453696967920, 0.006416112680545447977, 0.008554816907393927167 ),
 ( 0.000000000000000000, 1.000000000000000000 ),
 .UNSPECIFIED. ) 
 GEOMETRIC_REPRESENTATION_ITEM ( )  RATIONAL_B_SPLINE_SURFACE ( (
 ( 1.000000000000000000, 0.7301269460247288290, 1.000000000000000000),
 ( 1.000000000000000000, 0.7403364392953195594, 1.000000000000000000),
 ( 1.000000000000000000, 0.7528282336556595400, 1.000000000000000000),
 ( 1.000000000000000000, 0.7798877127538836884, 1.000000000000000000),
 ( 1.000000000000000000, 0.7945789861789882558, 1.000000000000000000),
 ( 1.000000000000000000, 0.8227729472765989982, 1.000000000000000000),
 ( 1.000000000000000000, 0.8364472417785102643, 1.000000000000000000),
 ( 1.000000000000000000, 0.8612666947766824954, 1.000000000000000000),
 ( 1.000000000000000000, 0.8720837947351824937, 1.000000000000000000),
 ( 1.000000000000000000, 0.8806660624989743891, 1.000000000000000000) ) ) 
 REPRESENTATION_ITEM ( '' )  SURFACE ( )  );
#86489=CARTESIAN_POINT ( 'NONE',  ( 32.13501140704661196, 486.0946583834067383, 5.282944113654357565 ) ) ;
#86494=CARTESIAN_POINT ( 'NONE',  ( 41.60090381918656277, 436.7951626062907735, 6.075960697884984718 ) ) ;
#86503=EDGE_CURVE ( 'NONE', #55309, #90133, #66892, .T. ) ;
#86506=CARTESIAN_POINT ( 'NONE',  ( -21.23684446602550935, 304.9566545053270943, -9.977713076987674512 ) ) ;
#86510=CARTESIAN_POINT ( 'NONE',  ( -40.02090011478443898, 436.4865077410172489, 5.635628130756175302 ) ) ;
#86530=CARTESIAN_POINT ( 'NONE',  ( -11.51741314084194734, 304.6035749955722167, 8.884240740051277285 ) ) ;
#86543=EDGE_CURVE ( 'NONE', #6978, #59047, #64673, .T. ) ;
#86546=AXIS2_PLACEMENT_3D ( 'NONE', #91106, #17214, #74356 ) ;
#86547=EDGE_CURVE ( 'NONE', #96778, #23775, #21433, .T. ) ;
#86560=EDGE_LOOP ( 'NONE', ( #13089, #93836, #96943, #100518, #27359, #105044, #78503, #39528, #45117, #24722 ) ) ;
#86563=CARTESIAN_POINT ( 'NONE',  ( -39.42238789698101442, 436.7568662985884771, 5.264481638451546708 ) ) ;
#86581=CARTESIAN_POINT ( 'NONE',  ( 35.54351702707027272, 361.7442709301026298, 2.606710528293841644 ) ) ;
#86582=CARTESIAN_POINT ( 'NONE',  ( 43.68078092307730032, 484.4268836469389612, 2.016138049968958512 ) ) ;
#86605=CARTESIAN_POINT ( 'NONE',  ( 42.94916902413876159, 342.9903042650141742, 9.416962103331693257 ) ) ;
#86613=CARTESIAN_POINT ( 'NONE',  ( 43.68566140667488895, 485.0560336449399870, 1.938913452013092842 ) ) ;
#86623=VECTOR ( 'NONE', #482, 1000.000000000000000 ) ;
#86636=EDGE_LOOP ( 'NONE', ( #59991, #24648, #105154, #42324 ) ) ;
#86650=CARTESIAN_POINT ( 'NONE',  ( 33.32951764101204617, 490.0033476588131975, 11.19754049617962721 ) ) ;
#86659=CARTESIAN_POINT ( 'NONE',  ( 31.03678703375144821, 438.6650838204807314, 21.86890379897223013 ) ) ;
#86660=CARTESIAN_POINT ( 'NONE',  ( 28.21269487252221708, 296.8969659935266918, 2.382781577419921248 ) ) ;
#86673=CARTESIAN_POINT ( 'NONE',  ( 43.02661387979757279, 465.7449615347597955, 11.43319743843537850 ) ) ;
#86690=AXIS2_PLACEMENT_3D ( 'NONE', #104529, #70587, #23115 ) ;
#86693=CARTESIAN_POINT ( 'NONE',  ( 7.093721425956736049, 304.7303285792975771, 9.911179277710184365 ) ) ;
#86703=CARTESIAN_POINT ( 'NONE',  ( 40.15309039158240267, 485.1828724906196157, -4.320808352507255812 ) ) ;
#86711=ORIENTED_EDGE ( 'NONE', *, *, #40482, .F. ) ;
#86712=CARTESIAN_POINT ( 'NONE',  ( 42.87890743752956979, 485.5827513099150110, 6.686224016671874715 ) ) ;
#86718=AXIS2_PLACEMENT_3D ( 'NONE', #82876, #8973, #92558 ) ;
#86723=CIRCLE ( 'NONE', #19616, 15.00000000000001243 ) ;
#86725=CARTESIAN_POINT ( 'NONE',  ( 26.26255647543327143, 307.7041406114180973, 10.82825725285463925 ) ) ;
#86747=CARTESIAN_POINT ( 'NONE',  ( 36.19807994336332513, 437.5493722796938982, 4.275365344036610615 ) ) ;
#86763=ORIENTED_EDGE ( 'NONE', *, *, #78405, .T. ) ;
#86766=EDGE_LOOP ( 'NONE', ( #70971, #53103, #30173, #36538, #66301, #42821 ) ) ;
#86768=AXIS2_PLACEMENT_3D ( 'NONE', #16872, #59463, #65940 ) ;
#86769=CARTESIAN_POINT ( 'NONE',  ( 43.89370568762518587, 435.4157859806081206, 16.19551141317264253 ) ) ;
#86779=CARTESIAN_POINT ( 'NONE',  ( 40.95762649053725113, 390.9034865917477646, 27.40818397757877634 ) ) ;
#86780=CARTESIAN_POINT ( 'NONE',  ( -42.77633007792896791, 465.0956601421924006, 12.68100826425808414 ) ) ;
#86781=CARTESIAN_POINT ( 'NONE',  ( -42.08762648273019380, 487.0030674539066808, 9.106351919860241395 ) ) ;
#86789=CARTESIAN_POINT ( 'NONE',  ( -29.40856938088932182, 310.8503673664380358, -7.608145749800559798 ) ) ;
#86790=CARTESIAN_POINT ( 'NONE',  ( -38.31345439580793055, 310.9608064124970497, 5.782998304085245067 ) ) ;
#86815=CARTESIAN_POINT ( 'NONE',  ( 1.798224084799555200, 298.0247695551061042, -10.00218504963162758 ) ) ;
#86816=CARTESIAN_POINT ( 'NONE',  ( 40.07586470527510158, 337.7832441655235129, 20.21182470898328631 ) ) ;
#86824=CARTESIAN_POINT ( 'NONE',  ( 46.00000000000000000, 487.9624651068497201, 0.8047872055790837864 ) ) ;
#86825=CARTESIAN_POINT ( 'NONE',  ( -42.23079339798738374, 460.7352525929354101, 2.726051457480726636 ) ) ;
#86826=CARTESIAN_POINT ( 'NONE',  ( 18.00000000000001421, -20.00000000000001776, -9.000000000000008882 ) ) ;
#86828=EDGE_CURVE ( 'NONE', #72809, #90326, #66683, .T. ) ;
#86831=CARTESIAN_POINT ( 'NONE',  ( -43.71037717921252863, 462.3391554988666599, 4.824299547746595529 ) ) ;
#86846=EDGE_LOOP ( 'NONE', ( #83801, #106297, #81934, #95788, #99145, #10531, #104100 ) ) ;
#86856=CARTESIAN_POINT ( 'NONE',  ( 43.53200981659315971, 464.6079291498570001, 9.489543392920072762 ) ) ;
#86864=ORIENTED_EDGE ( 'NONE', *, *, #73248, .F. ) ;
#86870=ORIENTED_EDGE ( 'NONE', *, *, #102114, .F. ) ;
#86873=FACE_OUTER_BOUND ( 'NONE', #75744, .T. ) ;
#86875=EDGE_CURVE ( 'NONE', #20727, #12676, #39762, .T. ) ;
#86879=CARTESIAN_POINT ( 'NONE',  ( -34.95237279327285762, 304.8277712208536627, 12.26231981495593537 ) ) ;
#86882=CARTESIAN_POINT ( 'NONE',  ( -33.70841932975971389, 485.0774894644218307, 1.934193826885679313 ) ) ;
#86898=CARTESIAN_POINT ( 'NONE',  ( -32.65708775173074230, 434.9895743886469859, 13.53061570434023153 ) ) ;
#86899=CARTESIAN_POINT ( 'NONE',  ( -31.17290040000586515, 438.0040945452082042, 21.19833760118956789 ) ) ;
#86914=CARTESIAN_POINT ( 'NONE',  ( 46.00000000000000000, 437.9217094256704854, 13.73710413246956641 ) ) ;
#86923=ORIENTED_EDGE ( 'NONE', *, *, #86828, .F. ) ;
#86925=CARTESIAN_POINT ( 'NONE',  ( -46.00000000000000000, 461.2902899409307338, 8.859728897578733608 ) ) ;
#86928=CARTESIAN_POINT ( 'NONE',  ( -29.12616872298675474, 306.7985789502500893, -9.112683410444441634 ) ) ;
#86932=CARTESIAN_POINT ( 'NONE',  ( -42.58433969240390127, 479.4768267386957632, 9.887265036231987381 ) ) ;
#86938=CARTESIAN_POINT ( 'NONE',  ( -9.492026425949987356, 294.7525273391970586, 3.163606944373883234 ) ) ;
#86941=EDGE_CURVE ( 'NONE', #75237, #2439, #86011, .T. ) ;
#86946=CARTESIAN_POINT ( 'NONE',  ( 46.00000000000000000, 438.0652200859153140, 14.81161132415559578 ) ) ;
#86953=CARTESIAN_POINT ( 'NONE',  ( 41.71039089155822666, 485.6269440496952825, -4.295528331870388072 ) ) ;
#86958=ORIENTED_EDGE ( 'NONE', *, *, #9971, .F. ) ;
#86969=CARTESIAN_POINT ( 'NONE',  ( 38.47428897412579119, 485.7788508071993760, -4.770630528148342542 ) ) ;
#86987=B_SPLINE_CURVE_WITH_KNOTS ( 'NONE', 3,
 ( #33864, #33324, #15516, #66195, #48407, #31730, #99079, #64617, #91030, #17133, #50010, #82914, #9012, #96975, #23109, #55951, #88885, #14976, #11131, #10087, #2518, #44061, #34932, #27925, #100159, #18754, #3062, #100684, #52135, #67281, #58653, #60792, #25800, #51603, #76949, #77493, #93139, #27390, #91554, #36010, #17663, #84524, #75884, #92598, #11670, #26326, #19832, #10610 ),
 .UNSPECIFIED., .F., .F.,
 ( 4, 2, 2, 2, 2, 2, 2, 2, 2, 2, 2, 2, 2, 2, 2, 2, 2, 2, 2, 2, 2, 2, 2, 4 ),
 ( 0.0009115642548457684189, 0.01973540046764989814, 0.03855923668045402319, 0.05738307289325814825, 0.06679499099966014486, 0.07620690910606212065, 0.08561882721246411032, 0.09503074531886608611, 0.1044426634252680758, 0.1138545815316700377, 0.1185605405848710187, 0.1232664996380720135, 0.1256194791646725040, 0.1279724586912729944, 0.1326784177444739754, 0.1350313972710744659, 0.1373843767976749564, 0.1397373563242754191, 0.1409138460875756782, 0.1420903358508759096, 0.1444433153774764000, 0.1456198051407766314, 0.1467962949040768905, 0.1515022539572777605 ),
 .UNSPECIFIED. ) ;
#86993=CARTESIAN_POINT ( 'NONE',  ( -33.77559172535806908, 464.7834715296606873, 7.192701217093215860 ) ) ;
#86995=DIRECTION ( 'NONE',  ( 0.000000000000000000, 0.000000000000000000, -1.000000000000000000 ) ) ;
#86996=ORIENTED_EDGE ( 'NONE', *, *, #39965, .F. ) ;
#87005=CARTESIAN_POINT ( 'NONE',  ( -32.10528697966012857, 486.1671898930081852, 5.449875171704860577 ) ) ;
#87009=CARTESIAN_POINT ( 'NONE',  ( 32.92227116393141984, 439.7404285724723536, 24.14402898922816476 ) ) ;
#87012=CARTESIAN_POINT ( 'NONE',  ( 34.46660312962831796, 319.4207929304380968, -5.979192388231528987 ) ) ;
#87019=CARTESIAN_POINT ( 'NONE',  ( 0.000000000000000000, 81.00000000000000000, 0.000000000000000000 ) ) ;
#87022=CARTESIAN_POINT ( 'NONE',  ( -24.80105969489321893, 306.0237540681346218, -9.745911707960095427 ) ) ;
#87025=VECTOR ( 'NONE', #64581, 1000.000000000000000 ) ;
#87040=EDGE_CURVE ( 'NONE', #26937, #51023, #85157, .T. ) ;
#87048=CARTESIAN_POINT ( 'NONE',  ( 20.24579557674108088, 304.8297271373347144, -10.00469232190996927 ) ) ;
#87051=ADVANCED_FACE ( 'NONE', ( #11663 ), #56962, .F. ) ;
#87079=CARTESIAN_POINT ( 'NONE',  ( -42.20041562234357002, 435.2369744135583574, 7.788607701745487333 ) ) ;
#87088=CARTESIAN_POINT ( 'NONE',  ( 33.21599328327231149, 465.5375697722676591, 9.463303254740063508 ) ) ;
#87090=DIRECTION ( 'NONE',  ( 1.000000000000000000, 0.000000000000000000, 0.000000000000000000 ) ) ;
#87092=TOROIDAL_SURFACE ( 'NONE', #61221, 12.00000000000000711, 3.000000000000000000 ) ;
#87099=CARTESIAN_POINT ( 'NONE',  ( 32.17347608656518787, 319.0370483936366668, -5.555387326066758114 ) ) ;
#87103=CARTESIAN_POINT ( 'NONE',  ( 35.97836163550933009, 491.7764920885226161, 12.54497382757449131 ) ) ;
#87111=CARTESIAN_POINT ( 'NONE',  ( 32.93513049338658760, 465.6726574193327792, 10.66039033145146142 ) ) ;
#87114=EDGE_CURVE ( 'NONE', #1378, #46291, #59059, .T. ) ;
#87122=CARTESIAN_POINT ( 'NONE',  ( 42.59298759914230459, 320.2223789555831104, -3.850798572401481934 ) ) ;
#87126=CARTESIAN_POINT ( 'NONE',  ( 31.81284829423740135, 439.0025894409650959, 23.54372111369165310 ) ) ;
#87132=AXIS2_PLACEMENT_3D ( 'NONE', #82544, #43677, #1603 ) ;
#87134=CARTESIAN_POINT ( 'NONE',  ( -44.35014475220779673, 435.2396861789843001, 12.17836948353843596 ) ) ;
#87146=CARTESIAN_POINT ( 'NONE',  ( 34.14532928921329358, 464.2269668280595738, 6.057797726091872725 ) ) ;
#87149=DIRECTION ( 'NONE',  ( 0.000000000000000000, -0.8568390274594179790, -0.5155840193628955515 ) ) ;
#87165=CARTESIAN_POINT ( 'NONE',  ( -37.61995194924682551, 438.1737809428368564, 4.432418093030975115 ) ) ;
#87170=CARTESIAN_POINT ( 'NONE',  ( 42.72731753109084707, 485.8496451746399316, 7.279150061871429322 ) ) ;
#87175=CARTESIAN_POINT ( 'NONE',  ( -39.80120353649695630, 485.6913716985619658, -4.529092486723600430 ) ) ;
#87179=CARTESIAN_POINT ( 'NONE',  ( 5.644640995548282802, 301.6279895259619366, -10.01771135672319879 ) ) ;
#87182=CARTESIAN_POINT ( 'NONE',  ( 41.14212900119734684, 464.2935350810450359, 17.75680570235805078 ) ) ;
#87203=CARTESIAN_POINT ( 'NONE',  ( -43.00000000000000711, 485.2629658518202973, -2.796394914059372905 ) ) ;
#87205=CARTESIAN_POINT ( 'NONE',  ( 33.52756498066074187, 435.4194806154983439, 9.514010192928232357 ) ) ;
#87220=CARTESIAN_POINT ( 'NONE',  ( 41.97131279570576368, 485.5606288621858653, -4.070573943143920737 ) ) ;
#87221=CARTESIAN_POINT ( 'NONE',  ( 40.31754836868392289, 437.2079761516864664, 22.20092987877936608 ) ) ;
#87224=CARTESIAN_POINT ( 'NONE',  ( -40.92146453211002921, 438.1322861037302800, 22.38370651923338173 ) ) ;
#87226=CARTESIAN_POINT ( 'NONE',  ( -43.69780420584740455, 464.4352583045362621, 7.050850226778779373 ) ) ;
#87228=CARTESIAN_POINT ( 'NONE',  ( 43.03987588564152844, 486.0760633267547632, 5.817066388976027902 ) ) ;
#87244=CARTESIAN_POINT ( 'NONE',  ( -28.07965516020418306, 315.5842071114037708, 11.56093435300535965 ) ) ;
#87248=CARTESIAN_POINT ( 'NONE',  ( 21.43726646001635672, 305.0999692234804002, 8.990123627463036726 ) ) ;
#87272=ORIENTED_EDGE ( 'NONE', *, *, #83070, .T. ) ;
#87275=DIRECTION ( 'NONE',  ( 0.000000000000000000, 0.000000000000000000, -1.000000000000000000 ) ) ;
#87276=AXIS2_PLACEMENT_3D ( 'NONE', #66411, #32487, #98249 ) ;
#87284=CARTESIAN_POINT ( 'NONE',  ( 43.51517875624352172, 462.0595338174632047, 4.327785711310748518 ) ) ;
#87295=CARTESIAN_POINT ( 'NONE',  ( -43.03894652950386757, 464.9992092536282939, 11.55502599540882791 ) ) ;
#87301=EDGE_CURVE ( 'NONE', #35905, #37591, #7677, .T. ) ;
#87307=CARTESIAN_POINT ( 'NONE',  ( -25.77050100732808602, 305.3127693512194583, 10.48956834842311459 ) ) ;
#87311=VECTOR ( 'NONE', #97665, 1000.000000000000000 ) ;
#87341=CARTESIAN_POINT ( 'NONE',  ( 34.24477232042282537, 301.4776311158785802, -0.5002871126718249073 ) ) ;
#87351=CARTESIAN_POINT ( 'NONE',  ( 0.000000000000000000, -19.99999999999998934, 0.000000000000000000 ) ) ;
#87360=ORIENTED_EDGE ( 'NONE', *, *, #35335, .F. ) ;
#87365=DIRECTION ( 'NONE',  ( -0.3900125511318229821, 0.5465874153434815419, 0.7410346870071464753 ) ) ;
#87371=ORIENTED_EDGE ( 'NONE', *, *, #40103, .T. ) ;
#87373=CARTESIAN_POINT ( 'NONE',  ( 31.35993874404257298, 436.8062917347268694, 22.71845294991138786 ) ) ;
#87380=CARTESIAN_POINT ( 'NONE',  ( -42.19179521602437433, 484.5286692029248456, -4.078961064713001683 ) ) ;
#87388=DIRECTION ( 'NONE',  ( 9.251858538543049530E-15, 0.9349068334195396179, -0.3548932414479730180 ) ) ;
#87407=CARTESIAN_POINT ( 'NONE',  ( 32.85155332502863956, 463.8111683108725174, 7.359358840565810134 ) ) ;
#87428=CARTESIAN_POINT ( 'NONE',  ( -31.73514475001178781, 436.7265089541918996, 21.10053246029738006 ) ) ;
#87429=CARTESIAN_POINT ( 'NONE',  ( -32.28930913497472943, 488.2717154064631586, 9.213726894912662502 ) ) ;
#87434=CARTESIAN_POINT ( 'NONE',  ( -29.80964876741045444, 297.6586656248026657, -1.384360942660989746 ) ) ;
#87453=CARTESIAN_POINT ( 'NONE',  ( -41.75331920095275251, 461.8277566036530288, 2.915730576367146831 ) ) ;
#87454=ORIENTED_EDGE ( 'NONE', *, *, #88242, .F. ) ;
#87455=CARTESIAN_POINT ( 'NONE',  ( -37.70494463962872089, 407.6443545989597510, 6.531502666333342866 ) ) ;
#87464=CARTESIAN_POINT ( 'NONE',  ( -8.728354254914082233, 295.2541512756494058, 4.889958989508364162 ) ) ;
#87468=LINE ( 'NONE', #46465, #37953 ) ;
#87470=CARTESIAN_POINT ( 'NONE',  ( 11.51004862373886262, 294.5990991804076202, -2.053735195510829836 ) ) ;
#87476=DIRECTION ( 'NONE',  ( -1.000000000000000000, 0.000000000000000000, 0.000000000000000000 ) ) ;
#87478=( GEOMETRIC_REPRESENTATION_CONTEXT ( 3 ) GLOBAL_UNCERTAINTY_ASSIGNED_CONTEXT ( ( #43747 ) ) GLOBAL_UNIT_ASSIGNED_CONTEXT ( ( #67761, #35427, #10049 ) ) REPRESENTATION_CONTEXT ( 'NONE', 'WORKASPACE' ) );
#87483=CARTESIAN_POINT ( 'NONE',  ( 44.36529472639534788, 435.1964152669797841, 13.54961189024334267 ) ) ;
#87484=DIRECTION ( 'NONE',  ( 0.000000000000000000, 0.000000000000000000, 1.000000000000000000 ) ) ;
#87492=CARTESIAN_POINT ( 'NONE',  ( 16.85921514102166796, 304.5746142243267514, -9.058973955187422433 ) ) ;
#87502=CARTESIAN_POINT ( 'NONE',  ( -32.04841611708074112, 486.3115588597283363, 5.780120484955278748 ) ) ;
#87505=DIRECTION ( 'NONE',  ( -0.2529971249647445797, 0.000000000000000000, 0.9674670303217436373 ) ) ;
#87518=CARTESIAN_POINT ( 'NONE',  ( -32.88333705524179607, 439.7317646416724415, 24.13381181826117583 ) ) ;
#87523=CARTESIAN_POINT ( 'NONE',  ( -41.96546066671912456, 485.5623541565421988, -4.077117913357734658 ) ) ;
#87530=CARTESIAN_POINT ( 'NONE',  ( -46.00000000000001421, 437.8931063572202333, 13.37370747421774730 ) ) ;
#87546=CARTESIAN_POINT ( 'NONE',  ( -35.74363442581862671, 380.1068966271811860, 4.951945592532029927 ) ) ;
#87550=CARTESIAN_POINT ( 'NONE',  ( -42.20041562234358423, 435.2369744135583574, 7.788607701745487333 ) ) ;
#87551=DIRECTION ( 'NONE',  ( 0.000000000000000000, 0.000000000000000000, -1.000000000000000000 ) ) ;
#87574=VERTEX_POINT ( 'NONE', #552 ) ;
#87579=DIRECTION ( 'NONE',  ( -0.2237693372482013887, 0.01887181578571871243, 0.9744594082240937150 ) ) ;
#87588=MANIFOLD_SOLID_BREP ( '<13. Handle Knob>-<Fillet1>', #92802 ) ;
#87599=B_SPLINE_CURVE_WITH_KNOTS ( 'NONE', 3,
 ( #15374, #57412, #72547, #39673 ),
 .UNSPECIFIED., .F., .F.,
 ( 4, 4 ),
 ( 3.469446951953614189E-18, 0.002256496660487678635 ),
 .UNSPECIFIED. ) ;
#87600=CARTESIAN_POINT ( 'NONE',  ( -31.87080426956102031, 439.0384429942135398, 24.63328115755084013 ) ) ;
#87605=ADVANCED_FACE ( 'NONE', ( #98858 ), #28350, .F. ) ;
#87607=CARTESIAN_POINT ( 'NONE',  ( -40.03012460245057724, 436.4820657380744251, 5.641945619390483557 ) ) ;
#87622=CARTESIAN_POINT ( 'NONE',  ( -32.20054824794776493, 485.9557913861499969, 4.953638954091799995 ) ) ;
#87626=CARTESIAN_POINT ( 'NONE',  ( 35.50900462289761350, 382.2641358326593490, 6.015446932962731807 ) ) ;
#87645=ORIENTED_EDGE ( 'NONE', *, *, #42854, .F. ) ;
#87646=CARTESIAN_POINT ( 'NONE',  ( 42.99999999999999289, 485.2629658518202973, -2.796394914059370240 ) ) ;
#87650=CARTESIAN_POINT ( 'NONE',  ( 38.38704938250420184, 306.2898962380254488, -7.348315413633529580 ) ) ;
#87652=VERTEX_POINT ( 'NONE', #1213 ) ;
#87658=DIRECTION ( 'NONE',  ( 0.000000000000000000, 0.7863624351922580136, -0.6177654251562657572 ) ) ;
#87659=EDGE_CURVE ( 'NONE', #23322, #70575, #9438, .T. ) ;
#87666=CARTESIAN_POINT ( 'NONE',  ( -35.07179216366830588, 463.5162043426217338, 19.70794395571720159 ) ) ;
#87668=CARTESIAN_POINT ( 'NONE',  ( 43.32251133975108814, 485.6545735287631942, 4.688172406453896990 ) ) ;
#87674=EDGE_LOOP ( 'NONE', ( #20007, #69916, #9529, #33008 ) ) ;
#87680=CARTESIAN_POINT ( 'NONE',  ( -30.00000000000000355, 489.0503989117699462, 4.976653691326955453 ) ) ;
#87687=( BOUNDED_SURFACE ( )  B_SPLINE_SURFACE ( 3, 2, ( 
 ( #68165, #19666, #68719 ),
 ( #3967, #20196, #76779 ),
 ( #61698, #12042, #101602 ),
 ( #60107, #10448, #53052 ),
 ( #42824, #69767, #35839 ),
 ( #59556, #27757, #94592 ),
 ( #34771, #94035, #83805 ),
 ( #36382, #50897, #2355 ),
 ( #100523, #18579, #51441 ),
 ( #69246, #102661, #51967 ) ),
 .UNSPECIFIED., .F., .F., .F. ) 
 B_SPLINE_SURFACE_WITH_KNOTS ( ( 4, 2, 2, 2, 4 ),
 ( 3, 3 ),
 ( 1.647987302177966740E-17, 0.002793818337085216940, 0.003492272921356517380, 0.004190727505627817387, 0.005587636674170417400 ),
 ( 0.000000000000000000, 1.000000000000000000 ),
 .UNSPECIFIED. ) 
 GEOMETRIC_REPRESENTATION_ITEM ( )  RATIONAL_B_SPLINE_SURFACE ( (
 ( 1.000000000000000000, 0.8239349643288649272, 1.000000000000000000),
 ( 1.000000000000000000, 0.8395566633290327818, 1.000000000000000000),
 ( 1.000000000000000000, 0.8448327636212329406, 1.000000000000000000),
 ( 1.000000000000000000, 0.8449253469007168560, 1.000000000000000000),
 ( 1.000000000000000000, 0.8445754865294070601, 1.000000000000000000),
 ( 1.000000000000000000, 0.8431693930219159583, 1.000000000000000000),
 ( 1.000000000000000000, 0.8421154100742880289, 1.000000000000000000),
 ( 1.000000000000000000, 0.8378581409644991762, 1.000000000000000000),
 ( 1.000000000000000000, 0.8335888548715134627, 1.000000000000000000),
 ( 1.000000000000000000, 0.8273155905869840065, 1.000000000000000000) ) ) 
 REPRESENTATION_ITEM ( '' )  SURFACE ( )  );
#87691=ORIENTED_EDGE ( 'NONE', *, *, #1396, .F. ) ;
#87696=DIRECTION ( 'NONE',  ( 0.9737456255364647095, 0.000000000000000000, -0.2276388735444786204 ) ) ;
#87710=CARTESIAN_POINT ( 'NONE',  ( 40.62545454912861942, 465.1696752979974576, 17.15421908636345449 ) ) ;
#87716=AXIS2_PLACEMENT_3D ( 'NONE', #43054, #50066, #44117 ) ;
#87717=DIRECTION ( 'NONE',  ( -0.9915366780650374245, 0.1269898409407624329, 0.02699252395739039703 ) ) ;
#87719=ADVANCED_FACE ( 'NONE', ( #75660 ), #85359, .F. ) ;
#87727=AXIS2_PLACEMENT_3D ( 'NONE', #86080, #12152, #103309 ) ;
#87735=EDGE_CURVE ( 'NONE', #51428, #1378, #7435, .T. ) ;
#87739=CARTESIAN_POINT ( 'NONE',  ( -37.85084083633361729, 438.0234350436313093, 4.171260309356228824 ) ) ;
#87746=CARTESIAN_POINT ( 'NONE',  ( -46.00000000000000000, 461.7880546943549689, 10.79349299898142789 ) ) ;
#87754=CARTESIAN_POINT ( 'NONE',  ( 33.00496812083888898, 465.6658704666191966, 15.15901827093884258 ) ) ;
#87766=ORIENTED_EDGE ( 'NONE', *, *, #87929, .F. ) ;
#87768=CARTESIAN_POINT ( 'NONE',  ( -34.99928578097298981, 435.2191065300279433, 7.261429118812875672 ) ) ;
#87775=CARTESIAN_POINT ( 'NONE',  ( -24.24905399839806464, 305.2659941753802286, 10.24863818738177024 ) ) ;
#87777=CARTESIAN_POINT ( 'NONE',  ( 22.01171728258022853, 305.2737328247270625, 10.02785900982430256 ) ) ;
#87783=CARTESIAN_POINT ( 'NONE',  ( 45.99999999999428013, 486.0809427139465697, 1.692663251875475394 ) ) ;
#87790=DIRECTION ( 'NONE',  ( 1.000000000000000000, 0.000000000000000000, 0.000000000000000000 ) ) ;
#87795=CARTESIAN_POINT ( 'NONE',  ( 41.31850805822517714, 460.1795573263356118, 2.184907985913608908 ) ) ;
#87802=B_SPLINE_CURVE_WITH_KNOTS ( 'NONE', 3,
 ( #89112, #72901, #15208, #90706, #105290, #8711, #82060, #64314, #48096, #16815, #31951, #97711, #89642, #7631 ),
 .UNSPECIFIED., .F., .F.,
 ( 4, 2, 2, 2, 2, 2, 4 ),
 ( 7.410741937918042371E-18, 0.002039551581737956108, 0.003059327372606909443, 0.004079103163475863644, 0.006118654745213768578, 0.007138430536082721913, 0.008158206326951673512 ),
 .UNSPECIFIED. ) ;
#87814=ORIENTED_EDGE ( 'NONE', *, *, #10407, .F. ) ;
#87815=ORIENTED_EDGE ( 'NONE', *, *, #52061, .F. ) ;
#87818=CARTESIAN_POINT ( 'NONE',  ( 11.82165952410163356, 294.5900423753296309, -10.05563889079273210 ) ) ;
#87828=CARTESIAN_POINT ( 'NONE',  ( 36.34158003242083623, 308.9628109182459639, 13.30132686757931459 ) ) ;
#87830=CIRCLE ( 'NONE', #49916, 1.000000000000000888 ) ;
#87832=CARTESIAN_POINT ( 'NONE',  ( -39.82070819426019170, 460.7076632888579866, 2.105638695486015344 ) ) ;
#87835=CARTESIAN_POINT ( 'NONE',  ( -37.85256771641471829, 460.2291302834033218, 2.227843630145174725 ) ) ;
#87839=CARTESIAN_POINT ( 'NONE',  ( -32.36878476726423060, 299.8745122917198387, 3.062535334108964946 ) ) ;
#87847=ORIENTED_EDGE ( 'NONE', *, *, #18572, .F. ) ;
#87851=ORIENTED_EDGE ( 'NONE', *, *, #105370, .T. ) ;
#87855=ADVANCED_FACE ( 'NONE', ( #1080 ), #101092, .F. ) ;
#87867=DIRECTION ( 'NONE',  ( -0.000000000000000000, 1.000000000000000000, -0.000000000000000000 ) ) ;
#87891=CARTESIAN_POINT ( 'NONE',  ( 21.19348424345033521, 294.8901562694577478, 1.945151701991110205 ) ) ;
#87896=CARTESIAN_POINT ( 'NONE',  ( -39.95753117817366729, 490.6049172992401850, 11.69497456421621528 ) ) ;
#87928=CARTESIAN_POINT ( 'NONE',  ( -40.61216075948964033, 351.1469683695276558, 22.89433108575548914 ) ) ;
#87929=EDGE_CURVE ( 'NONE', #100942, #100925, #24103, .T. ) ;
#87935=TOROIDAL_SURFACE ( 'NONE', #12157, 12.00000000000000711, 3.000000000000000000 ) ;
#87951=CARTESIAN_POINT ( 'NONE',  ( -35.67189472734460054, 438.4023653113565047, 3.943223222944094886 ) ) ;
#87961=CARTESIAN_POINT ( 'NONE',  ( -27.28250412859145868, 305.2104144000636552, -9.479816361705919903 ) ) ;
#87968=CYLINDRICAL_SURFACE ( 'NONE', #8134, 15.00000000000000711 ) ;
#87969=CARTESIAN_POINT ( 'NONE',  ( 30.50103796836107861, 337.4180749914852981, 16.76525021871696097 ) ) ;
#87979=CARTESIAN_POINT ( 'NONE',  ( -33.65893543312866143, 439.0634705965974263, 24.00849711452648805 ) ) ;
#87980=ORIENTED_EDGE ( 'NONE', *, *, #53413, .F. ) ;
#87981=CARTESIAN_POINT ( 'NONE',  ( -37.66149909514062699, 377.9508026867375179, 5.097312388780781411 ) ) ;
#87990=EDGE_CURVE ( 'NONE', #82451, #68326, #73258, .T. ) ;
#88002=( BOUNDED_SURFACE ( )  B_SPLINE_SURFACE ( 3, 2, ( 
 ( #22185, #67926, #99757 ),
 ( #67409, #41521, #33454 ),
 ( #58785, #66329, #25928 ),
 ( #83564, #34535, #58233 ),
 ( #16719, #1021, #43123 ),
 ( #18336, #34001, #50646 ),
 ( #51191, #84111, #90610 ),
 ( #91680, #91162, #17796 ),
 ( #10210, #100811, #49067 ),
 ( #16181, #26972, #100285 ),
 ( #50140, #76008, #99212 ),
 ( #25376, #57687, #92186 ),
 ( #2108, #90074, #66871 ),
 ( #24833, #35058, #42579 ),
 ( #81962, #9666, #17267 ),
 ( #26447, #49608, #8088 ),
 ( #59314, #75479, #1572 ),
 ( #40994, #73882, #106777 ),
 ( #32928, #74408, #82515 ),
 ( #8618, #65802, #74935 ),
 ( #98679, #485, #83048 ),
 ( #9140, #42051, #60392 ),
 ( #86262, #20505, #45261 ),
 ( #19959, #93802, #101883 ),
 ( #44191, #85175, #92727 ),
 ( #12335, #77079, #27515 ),
 ( #102423, #37731, #85727 ),
 ( #21021, #69008, #11260 ),
 ( #3736, #36666, #53861 ),
 ( #94343, #11799, #78139 ),
 ( #4260, #84648, #44731 ),
 ( #53342, #37189, #28043 ),
 ( #93269, #77619, #12861 ),
 ( #94881, #69531, #70051 ),
 ( #86790, #45779, #19431 ),
 ( #28564, #60915, #102957 ),
 ( #78653, #70590, #18886 ),
 ( #51731, #103481, #29121 ),
 ( #52801, #4791, #61448 ),
 ( #61989, #59856, #10732 ),
 ( #43647, #76536, #2647 ),
 ( #101362, #35594, #68471 ),
 ( #52261, #3196, #36139 ),
 ( #22055, #5326, #31737 ),
 ( #15521, #105593, #64623 ),
 ( #13921, #14447, #23119 ),
 ( #38248, #47360, #30687 ),
 ( #5837, #48413, #39296 ),
 ( #64106, #63574, #46832 ),
 ( #30147, #79203, #55438 ),
 ( #54364, #7418, #72175 ),
 ( #88372, #88892, #87307 ),
 ( #105082, #38762, #31222 ),
 ( #55960, #80786, #104532 ),
 ( #63031, #80248, #89431 ),
 ( #97489, #6354, #96984 ),
 ( #23646, #56501, #95928 ),
 ( #71111, #103999, #81305 ),
 ( #87839, #14984, #47879 ),
 ( #71629, #40333, #96466 ),
 ( #22601, #73215, #6899 ),
 ( #29630, #39820, #54913 ),
 ( #46312, #62505, #79732 ),
 ( #13391, #72697, #95392 ),
 ( #21532, #91560, #106111 ),
 ( #98560, #81830, #1449 ),
 ( #92070, #75347, #34412 ),
 ( #90483, #91035, #99628 ),
 ( #7956, #17139, #363 ),
 ( #89948, #106652, #18213 ),
 ( #98038, #42456, #16590 ),
 ( #33332, #41396, #9547 ),
 ( #25805, #74809, #67284 ),
 ( #32803, #58658, #66200 ),
 ( #24710, #82385, #100164 ),
 ( #32262, #17667, #66740 ),
 ( #99085, #25248, #58102 ),
 ( #26332, #49479, #57557 ),
 ( #8492, #50533, #74286 ),
 ( #65675, #48937, #50015 ),
 ( #24188, #83981, #9017 ),
 ( #82919, #83445, #57034 ) ),
 .UNSPECIFIED., .F., .F., .T. ) 
 B_SPLINE_SURFACE_WITH_KNOTS ( ( 4, 2, 2, 2, 2, 2, 2, 2, 2, 2, 2, 2, 2, 2, 2, 2, 2, 2, 2, 2, 2, 2, 2, 2, 2, 2, 2, 2, 2, 2, 2, 2, 2, 2, 2, 2, 2, 2, 2, 2, 4 ),
 ( 3, 3 ),
 ( 0.05188019136508568302, 0.06984908127900800456, 0.07883352623596917574, 0.08781797119293033305, 0.1057868611068526477, 0.1147713060638138050, 0.1237557510207749761, 0.1417246409346973046, 0.1507090858916584619, 0.1596935308486196192, 0.1619396420878599363, 0.1641857533271002256, 0.1686779758055808043, 0.1731701982840613829, 0.1754163095233016723, 0.1776624207625419616, 0.1787854763821621062, 0.1793470041919721925, 0.1799085320017822509, 0.1821546432410225402, 0.1844007544802628296, 0.1849622822900728880, 0.1852430461949779450, 0.1855238100998829742, 0.1866468657195031189, 0.1877699213391232635, 0.1879103032915757643, 0.1879804942678020285, 0.1880506852440282928, 0.1883314491489333498, 0.1888929769587434082, 0.1900160325783635529, 0.1902967964832685821, 0.1905775603881736391, 0.1911390881979836975, 0.1922621438176038422, 0.1928236716274139284, 0.1929640535798664569, 0.1931044355323189576, 0.1933851994372239869, 0.1956313106764642762 ),
 ( 0.000000000000000000, 1.000000000000000000 ),
 .UNSPECIFIED. ) 
 GEOMETRIC_REPRESENTATION_ITEM ( )  RATIONAL_B_SPLINE_SURFACE ( (
 ( 1.000000000000000000, 0.7071066915981665257, 1.000000000000000000),
 ( 1.000000000000000000, 0.7071066382886482815, 1.000000000000000000),
 ( 1.000000000000000000, 0.7071067819013748812, 1.000000000000000000),
 ( 1.000000000000000000, 0.7071067819013748812, 1.000000000000000000),
 ( 1.000000000000000000, 0.7071067881452209880, 1.000000000000000000),
 ( 1.000000000000000000, 0.7071067881452209880, 1.000000000000000000),
 ( 1.000000000000000000, 0.7071067820841906437, 1.000000000000000000),
 ( 1.000000000000000000, 0.7071067820841906437, 1.000000000000000000),
 ( 1.000000000000000000, 0.7071082744393792918, 1.000000000000000000),
 ( 1.000000000000000000, 0.7071090812208852272, 1.000000000000000000),
 ( 1.000000000000000000, 0.7071085750256929092, 1.000000000000000000),
 ( 1.000000000000000000, 0.7071071111271418630, 1.000000000000000000),
 ( 1.000000000000000000, 0.7071064681235214033, 1.000000000000000000),
 ( 1.000000000000000000, 0.7071084972331730389, 1.000000000000000000),
 ( 1.000000000000000000, 0.7071099221851442351, 1.000000000000000000),
 ( 1.000000000000000000, 0.7071070408053770073, 1.000000000000000000),
 ( 1.000000000000000000, 0.7071068064871738335, 1.000000000000000000),
 ( 1.000000000000000000, 0.7071095048012291384, 1.000000000000000000),
 ( 1.000000000000000000, 0.7071073154889575552, 1.000000000000000000),
 ( 1.000000000000000000, 0.7071067115369314982, 1.000000000000000000),
 ( 1.000000000000000000, 0.7071075951519679714, 1.000000000000000000),
 ( 1.000000000000000000, 0.7071139925282480254, 1.000000000000000000),
 ( 1.000000000000000000, 0.7071183661598045012, 1.000000000000000000),
 ( 1.000000000000000000, 0.7071289949713209788, 1.000000000000000000),
 ( 1.000000000000000000, 0.7071314560732923082, 1.000000000000000000),
 ( 1.000000000000000000, 0.7071209471556917370, 1.000000000000000000),
 ( 1.000000000000000000, 0.7071073686105321388, 1.000000000000000000),
 ( 1.000000000000000000, 0.7071065108360928830, 1.000000000000000000),
 ( 1.000000000000000000, 0.7071095461198974030, 1.000000000000000000),
 ( 1.000000000000000000, 0.7071118034369724414, 1.000000000000000000),
 ( 1.000000000000000000, 0.7071112127294267857, 1.000000000000000000),
 ( 1.000000000000000000, 0.7071089568612387577, 1.000000000000000000),
 ( 1.000000000000000000, 0.7071080543739914903, 1.000000000000000000),
 ( 1.000000000000000000, 0.7071071383726338366, 1.000000000000000000),
 ( 1.000000000000000000, 0.7071069085306952440, 1.000000000000000000),
 ( 1.000000000000000000, 0.7071067322179039882, 1.000000000000000000),
 ( 1.000000000000000000, 0.7071073362163841081, 1.000000000000000000),
 ( 1.000000000000000000, 0.7071285152900517179, 1.000000000000000000),
 ( 1.000000000000000000, 0.7071790023132530356, 1.000000000000000000),
 ( 1.000000000000000000, 0.7072040895942260930, 1.000000000000000000),
 ( 1.000000000000000000, 0.7071723949973123258, 1.000000000000000000),
 ( 1.000000000000000000, 0.7071267374085528079, 1.000000000000000000),
 ( 1.000000000000000000, 0.7071181237617968351, 1.000000000000000000),
 ( 1.000000000000000000, 0.7071098451417374697, 1.000000000000000000),
 ( 1.000000000000000000, 0.7071078748714980655, 1.000000000000000000),
 ( 1.000000000000000000, 0.7071063635215881771, 1.000000000000000000),
 ( 1.000000000000000000, 0.7071068237248464561, 1.000000000000000000),
 ( 1.000000000000000000, 0.7071083882213404781, 1.000000000000000000),
 ( 1.000000000000000000, 0.7071118710946099339, 1.000000000000000000),
 ( 1.000000000000000000, 0.7071122098397134570, 1.000000000000000000),
 ( 1.000000000000000000, 0.7071084160890762638, 1.000000000000000000),
 ( 1.000000000000000000, 0.7071068976071489542, 1.000000000000000000),
 ( 1.000000000000000000, 0.7071067909637599458, 1.000000000000000000),
 ( 1.000000000000000000, 0.7071067772271979468, 1.000000000000000000),
 ( 1.000000000000000000, 0.7071067571163546228, 1.000000000000000000),
 ( 1.000000000000000000, 0.7071066487236993270, 1.000000000000000000),
 ( 1.000000000000000000, 0.7071065680923671604, 1.000000000000000000),
 ( 1.000000000000000000, 0.7071060580930246253, 1.000000000000000000),
 ( 1.000000000000000000, 0.7071053146948335089, 1.000000000000000000),
 ( 1.000000000000000000, 0.7071028930956892999, 1.000000000000000000),
 ( 1.000000000000000000, 0.7071011043164672216, 1.000000000000000000),
 ( 1.000000000000000000, 0.7070987825526636739, 1.000000000000000000),
 ( 1.000000000000000000, 0.7071026651449159317, 1.000000000000000000),
 ( 1.000000000000000000, 0.7071061651848329355, 1.000000000000000000),
 ( 1.000000000000000000, 0.7071066975805828658, 1.000000000000000000),
 ( 1.000000000000000000, 0.7071068470435215580, 1.000000000000000000),
 ( 1.000000000000000000, 0.7071077911912049263, 1.000000000000000000),
 ( 1.000000000000000000, 0.7071127756005890497, 1.000000000000000000),
 ( 1.000000000000000000, 0.7071176452039118487, 1.000000000000000000),
 ( 1.000000000000000000, 0.7071257956655977450, 1.000000000000000000),
 ( 1.000000000000000000, 0.7071209011550627643, 1.000000000000000000),
 ( 1.000000000000000000, 0.7071103648264748243, 1.000000000000000000),
 ( 1.000000000000000000, 0.7071068888656230067, 1.000000000000000000),
 ( 1.000000000000000000, 0.7071067572802584023, 1.000000000000000000),
 ( 1.000000000000000000, 0.7071071039850833628, 1.000000000000000000),
 ( 1.000000000000000000, 0.7071084011956232374, 1.000000000000000000),
 ( 1.000000000000000000, 0.7071093283064042723, 1.000000000000000000),
 ( 1.000000000000000000, 0.7071125871578549660, 1.000000000000000000),
 ( 1.000000000000000000, 0.7071153771953387901, 1.000000000000000000),
 ( 1.000000000000000000, 0.7071397769056843030, 1.000000000000000000),
 ( 1.000000000000000000, 0.7071225043649866926, 1.000000000000000000),
 ( 1.000000000000000000, 0.7071067811865480168, 1.000000000000000000) ) ) 
 REPRESENTATION_ITEM ( '' )  SURFACE ( )  );
#88018=FACE_OUTER_BOUND ( 'NONE', #34914, .T. ) ;
#88020=EDGE_CURVE ( 'NONE', #103578, #47564, #2674, .T. ) ;
#88024=AXIS2_PLACEMENT_3D ( 'NONE', #64865, #97224, #40589 ) ;
#88031=FACE_OUTER_BOUND ( 'NONE', #11433, .T. ) ;
#88041=ORIENTED_EDGE ( 'NONE', *, *, #90079, .F. ) ;
#88051=DIRECTION ( 'NONE',  ( 0.000000000000000000, 0.000000000000000000, -1.000000000000000000 ) ) ;
#88061=CARTESIAN_POINT ( 'NONE',  ( 32.96117425224227304, 439.7497740807306172, 24.15381775812835130 ) ) ;
#88067=CARTESIAN_POINT ( 'NONE',  ( -35.05484418697486149, 463.2659305983892750, 4.633372620823961618 ) ) ;
#88070=ORIENTED_EDGE ( 'NONE', *, *, #87114, .F. ) ;
#88076=CARTESIAN_POINT ( 'NONE',  ( -27.57151080649627417, 314.0751515626058676, 12.18133379269485239 ) ) ;
#88082=CARTESIAN_POINT ( 'NONE',  ( 42.57704743493908950, 486.1612337113410263, 7.852296464539637810 ) ) ;
#88086=CARTESIAN_POINT ( 'NONE',  ( -34.12349128637494289, 490.8027302422244134, 11.84948222508913318 ) ) ;
#88099=CARTESIAN_POINT ( 'NONE',  ( 31.84025839850067996, 489.2002011298899333, 8.970818581732807218 ) ) ;
#88108=CARTESIAN_POINT ( 'NONE',  ( 43.58492305596168137, 465.9553058690736407, 13.43507729846636245 ) ) ;
#88112=CARTESIAN_POINT ( 'NONE',  ( 15.65208535197129613, 294.5588103013598129, 9.874721941290198757 ) ) ;
#88134=CARTESIAN_POINT ( 'NONE',  ( -41.61957457421983975, 435.6113505990639396, 7.035653009325270268 ) ) ;
#88135=CARTESIAN_POINT ( 'NONE',  ( -46.00000000000000000, 461.6622277975412203, 10.18145404766301709 ) ) ;
#88154=CARTESIAN_POINT ( 'NONE',  ( 35.46172211909674843, 432.6321351846624452, 5.657271128263613669 ) ) ;
#88158=CARTESIAN_POINT ( 'NONE',  ( 40.81102101573196705, 489.2883016990687111, 10.51949396897182787 ) ) ;
#88166=CARTESIAN_POINT ( 'NONE',  ( -34.88900972249400212, 464.6206820655984870, 18.69027339340994232 ) ) ;
#88174=CARTESIAN_POINT ( 'NONE',  ( 35.85994258077860053, 303.7596300888440624, 0.04768371627283522762 ) ) ;
#88175=DIRECTION ( 'NONE',  ( 0.2472079847635547389, 0.000000000000000000, -0.9689624411034424289 ) ) ;
#88227=VERTEX_POINT ( 'NONE', #34990 ) ;
#88231=CARTESIAN_POINT ( 'NONE',  ( -43.71037717921252863, 462.3391554988666599, 4.824299547746595529 ) ) ;
#88233=CARTESIAN_POINT ( 'NONE',  ( -41.14690903223496576, 485.7356601713278224, -4.640470638255251856 ) ) ;
#88242=EDGE_CURVE ( 'NONE', #96664, #44923, #102593, .T. ) ;
#88279=CARTESIAN_POINT ( 'NONE',  ( 33.50220463782144265, 465.4655183566888468, 16.55182854115482272 ) ) ;
#88283=CARTESIAN_POINT ( 'NONE',  ( 40.45545246860639566, 460.8457769820566909, 2.191470225627300206 ) ) ;
#88285=CARTESIAN_POINT ( 'NONE',  ( -43.72400580963713423, 464.7562747155352554, 7.841095524562895491 ) ) ;
#88294=FACE_OUTER_BOUND ( 'NONE', #38967, .T. ) ;
#88305=CARTESIAN_POINT ( 'NONE',  ( -25.56687214313617318, 308.5055938668078284, 10.78667975285395286 ) ) ;
#88307=CARTESIAN_POINT ( 'NONE',  ( 22.31815708081593641, 304.3216620908660275, 10.03816277198476037 ) ) ;
#88308=( BOUNDED_SURFACE ( )  B_SPLINE_SURFACE ( 3, 2, ( 
 ( #21450, #54287, #6275 ),
 ( #104996, #47274, #53781 ),
 ( #72089, #61909, #86712 ),
 ( #45700, #87228, #46234 ) ),
 .UNSPECIFIED., .F., .F., .F. ) 
 B_SPLINE_SURFACE_WITH_KNOTS ( ( 4, 4 ),
 ( 3, 3 ),
 ( -3.469446951953614189E-18, 0.002002951328326270462 ),
 ( 0.000000000000000000, 1.000000000000000000 ),
 .UNSPECIFIED. ) 
 GEOMETRIC_REPRESENTATION_ITEM ( )  RATIONAL_B_SPLINE_SURFACE ( (
 ( 1.000000000000000000, 0.7699558187665878073, 1.000000000000000000),
 ( 1.000000000000000000, 0.7788467038584422353, 1.000000000000000000),
 ( 1.000000000000000000, 0.7876570642905440511, 1.000000000000000000),
 ( 1.000000000000000000, 0.7964405967476624326, 1.000000000000000000) ) ) 
 REPRESENTATION_ITEM ( '' )  SURFACE ( )  );
#88309=DIRECTION ( 'NONE',  ( 0.000000000000000000, 0.000000000000000000, -1.000000000000000000 ) ) ;
#88310=EDGE_LOOP ( 'NONE', ( #87847, #101443 ) ) ;
#88314=CARTESIAN_POINT ( 'NONE',  ( 46.00000000000000000, 487.9611973796579605, 0.4748239133083901331 ) ) ;
#88330=CARTESIAN_POINT ( 'NONE',  ( 3.412118697746299389, 304.8518027737318903, -10.00000000013250201 ) ) ;
#88347=DIRECTION ( 'NONE',  ( 0.3820442156512856013, 0.000000000000000000, -0.9241440457457885671 ) ) ;
#88350=CARTESIAN_POINT ( 'NONE',  ( 17.35892867067943257, 294.5707697310705839, -10.05973541782409164 ) ) ;
#88359=CARTESIAN_POINT ( 'NONE',  ( 31.66509552703032782, 329.0881724405557520, 16.35203811063302837 ) ) ;
#88363=ORIENTED_EDGE ( 'NONE', *, *, #77663, .F. ) ;
#88372=CARTESIAN_POINT ( 'NONE',  ( -32.90087558584281879, 300.4243346777823263, 3.191413055959525291 ) ) ;
#88380=ORIENTED_EDGE ( 'NONE', *, *, #64286, .T. ) ;
#88391=CARTESIAN_POINT ( 'NONE',  ( 0.000000000000000000, 304.8518027762758038, 9.936999415352289589 ) ) ;
#88392=CARTESIAN_POINT ( 'NONE',  ( 42.57401444030708149, 489.2306277911063717, 6.899166537239310060 ) ) ;
#88394=EDGE_CURVE ( 'NONE', #61408, #90700, #52658, .T. ) ;
#88396=CARTESIAN_POINT ( 'NONE',  ( 39.84233570596349949, 333.3323931548420660, 19.23895789620553032 ) ) ;
#88416=CARTESIAN_POINT ( 'NONE',  ( 0.000000000000000000, 0.000000000000000000, 0.000000000000000000 ) ) ;
#88453=ORIENTED_EDGE ( 'NONE', *, *, #44672, .F. ) ;
#88460=CARTESIAN_POINT ( 'NONE',  ( -43.00000000000001421, 485.2629658518202973, -2.796394914059383119 ) ) ;
#88466=CARTESIAN_POINT ( 'NONE',  ( -36.23446467943408322, 484.5294442009995350, -2.438443429317435740 ) ) ;
#88467=B_SPLINE_CURVE_WITH_KNOTS ( 'NONE', 3,
 ( #99727, #19400, #27485, #60361, #91649, #51159, #51699, #44159, #2078, #93236, #84077, #1541 ),
 .UNSPECIFIED., .F., .F.,
 ( 4, 2, 2, 2, 2, 4 ),
 ( 8.414750032627943091E-17, 0.001311657711814073106, 0.002623315423628062078, 0.003279144279535067298, 0.003934973135442072084, 0.005246630847256086860 ),
 .UNSPECIFIED. ) ;
#88471=CARTESIAN_POINT ( 'NONE',  ( 0.000000000000000000, 294.8518027762758038, -10.00000000000000178 ) ) ;
#88481=CARTESIAN_POINT ( 'NONE',  ( 13.63130828375568981, 294.5445729804733901, -10.06530370901874250 ) ) ;
#88486=CIRCLE ( 'NONE', #79843, 7.000000000000006217 ) ;
#88490=CARTESIAN_POINT ( 'NONE',  ( -33.47685715990249378, 300.6314875565626608, -0.6996443904386956403 ) ) ;
#88497=CARTESIAN_POINT ( 'NONE',  ( 23.67596972946360268, 306.0428419988428459, 9.198869806892925993 ) ) ;
#88498=CARTESIAN_POINT ( 'NONE',  ( -42.87058980226115068, 464.8475010141946768, 15.35427200435808892 ) ) ;
#88507=CARTESIAN_POINT ( 'NONE',  ( -34.01505262803539864, 439.9177708686792130, 24.30869736368872935 ) ) ;
#88525=CARTESIAN_POINT ( 'NONE',  ( 21.51569398614867623, 294.9107018935607698, -9.987480606144499617 ) ) ;
#88526=EDGE_CURVE ( 'NONE', #17301, #69972, #48506, .T. ) ;
#88532=CARTESIAN_POINT ( 'NONE',  ( -43.21901510197800889, 436.3299561109158162, 19.40633274081965709 ) ) ;
#88536=CARTESIAN_POINT ( 'NONE',  ( 43.86011134669068667, 435.5786695946740679, 9.518646890165630481 ) ) ;
#88537=CARTESIAN_POINT ( 'NONE',  ( -33.00496812084397646, 465.6658704666172639, 15.15901827095664522 ) ) ;
#88551=ORIENTED_EDGE ( 'NONE', *, *, #103018, .F. ) ;
#88564=EDGE_LOOP ( 'NONE', ( #105172, #47765, #2032, #53649 ) ) ;
#88577=CARTESIAN_POINT ( 'NONE',  ( 36.73867238004162061, 390.4005144646481540, 5.886277538419430577 ) ) ;
#88584=ADVANCED_FACE ( 'NONE', ( #69238 ), #41855, .F. ) ;
#88586=CARTESIAN_POINT ( 'NONE',  ( -40.00273928030988912, 314.7263521513793307, 2.786061341313883055 ) ) ;
#88587=CARTESIAN_POINT ( 'NONE',  ( 30.88056822677182112, 309.1697570866494971, -8.545327163282022909 ) ) ;
#88590=EDGE_LOOP ( 'NONE', ( #28628, #28632, #8548, #68887, #40160 ) ) ;
#88595=CARTESIAN_POINT ( 'NONE',  ( 33.95909125845500398, 464.3583096732872377, 17.59538848573625458 ) ) ;
#88597=ORIENTED_EDGE ( 'NONE', *, *, #100725, .F. ) ;
#88599=CARTESIAN_POINT ( 'NONE',  ( -29.01988888469873018, 321.8047804620298393, 14.12772110426748284 ) ) ;
#88601=CARTESIAN_POINT ( 'NONE',  ( -34.85398657184737914, 481.6352825967676381, 14.59780011294850866 ) ) ;
#88603=CARTESIAN_POINT ( 'NONE',  ( -38.69545490169445401, 437.5444261472158587, 4.829293893630138612 ) ) ;
#88605=CYLINDRICAL_SURFACE ( 'NONE', #36714, 5.000000000000000000 ) ;
#88607=CARTESIAN_POINT ( 'NONE',  ( -44.08840282922849241, 485.7747746244170912, 4.178803824085661311 ) ) ;
#88609=CARTESIAN_POINT ( 'NONE',  ( -34.47176506790572859, 489.5748983164075980, 11.69726377706254361 ) ) ;
#88625=VERTEX_POINT ( 'NONE', #97580 ) ;
#88635=CARTESIAN_POINT ( 'NONE',  ( 16.35737551353592067, 302.5695985197569939, 9.877143523090261112 ) ) ;
#88658=EDGE_CURVE ( 'NONE', #84046, #50361, #88467, .T. ) ;
#88664=DIRECTION ( 'NONE',  ( -0.9623543818480306822, -0.1986072300191265572, -0.1855511032627525092 ) ) ;
#88672=CARTESIAN_POINT ( 'NONE',  ( -43.74855578046756222, 328.6220886837048170, -1.765109843966993441 ) ) ;
#88678=CARTESIAN_POINT ( 'NONE',  ( 33.79394592499237859, 329.6538948152748389, -2.915499870108015035 ) ) ;
#88682=CARTESIAN_POINT ( 'NONE',  ( -20.37278541768183615, 303.8378246129572631, -10.00297115033342266 ) ) ;
#88683=CARTESIAN_POINT ( 'NONE',  ( 42.75104180402610154, 488.2556334690061703, 9.347379739029891610 ) ) ;
#88689=FACE_OUTER_BOUND ( 'NONE', #40583, .T. ) ;
#88701=CARTESIAN_POINT ( 'NONE',  ( 32.73025373822441253, 313.1192488950297843, -7.568336369384137008 ) ) ;
#88710=CARTESIAN_POINT ( 'NONE',  ( 43.56126634772264339, 484.2986656255879439, 0.7800160315374845554 ) ) ;
#88744=CARTESIAN_POINT ( 'NONE',  ( 33.16846355476446462, 397.4937985473089839, 25.83636734666645651 ) ) ;
#88745=CARTESIAN_POINT ( 'NONE',  ( -42.96462842659435211, 322.5525446679458810, -3.268891976929361398 ) ) ;
#88782=CARTESIAN_POINT ( 'NONE',  ( 13.25307200133307539, 303.5542396669459322, 9.873748816204125589 ) ) ;
#88787=EDGE_CURVE ( 'NONE', #46291, #17539, #33084, .T. ) ;
#88806=CARTESIAN_POINT ( 'NONE',  ( 40.56952547639649254, 460.8933045338673082, 2.221423359587424873 ) ) ;
#88815=CARTESIAN_POINT ( 'NONE',  ( 44.10120706205769636, 485.7576699374418467, 4.111328371165819284 ) ) ;
#88823=CARTESIAN_POINT ( 'NONE',  ( -29.72305811207850113, 326.8793782738446794, 14.35461530513359918 ) ) ;
#88834=CARTESIAN_POINT ( 'NONE',  ( 43.66147695926597549, 485.1157264602073838, -1.117513576741872683 ) ) ;
#88846=VERTEX_POINT ( 'NONE', #27910 ) ;
#88850=CARTESIAN_POINT ( 'NONE',  ( -43.81028729233671726, 434.3199584132789255, 12.84475684849438970 ) ) ;
#88855=CARTESIAN_POINT ( 'NONE',  ( 31.11679462788039530, 441.4271381875185511, 23.27438508043199406 ) ) ;
#88865=DIRECTION ( 'NONE',  ( 1.000000000000000000, 0.000000000000000000, 0.000000000000000000 ) ) ;
#88871=CARTESIAN_POINT ( 'NONE',  ( 44.17836536378470669, 435.2619773020559819, 14.65562696767914908 ) ) ;
#88872=CARTESIAN_POINT ( 'NONE',  ( -39.00566081833550669, 463.6621700551983167, 19.40488523433662493 ) ) ;
#88881=CARTESIAN_POINT ( 'NONE',  ( 41.33081450886904662, 330.4361996080641575, 10.57783742947384908 ) ) ;
#88885=CARTESIAN_POINT ( 'NONE',  ( 41.66665637657543186, 334.9189789097773655, 11.60746121313486334 ) ) ;
#88886=ORIENTED_EDGE ( 'NONE', *, *, #4616, .F. ) ;
#88888=CARTESIAN_POINT ( 'NONE',  ( -34.73554899884743463, 462.7241937368494860, 5.242808629193801195 ) ) ;
#88889=DIRECTION ( 'NONE',  ( 0.000000000000000000, 0.000000000000000000, -1.000000000000000000 ) ) ;
#88891=CARTESIAN_POINT ( 'NONE',  ( -35.46814660802463237, 430.5672163472734724, 5.860357238957815795 ) ) ;
#88892=CARTESIAN_POINT ( 'NONE',  ( -31.55816069737598184, 299.8186824367181202, 11.05464098791177463 ) ) ;
#88900=CARTESIAN_POINT ( 'NONE',  ( 0.000000000000000000, -18.92596047533412573, -20.36976895023282097 ) ) ;
#88919=CARTESIAN_POINT ( 'NONE',  ( 9.581329576345360977, 294.6545431190994009, -2.865389023834811422 ) ) ;
#88934=CARTESIAN_POINT ( 'NONE',  ( 21.04247164025375483, 37.86482112153537116, 10.52123582012687741 ) ) ;
#88953=CARTESIAN_POINT ( 'NONE',  ( 34.88900972249397370, 464.6206820655982028, 18.69027339340997784 ) ) ;
#88957=ADVANCED_FACE ( 'NONE', ( #55811 ), #74921, .T. ) ;
#88958=CARTESIAN_POINT ( 'NONE',  ( -31.84798727957934616, 480.8482684553740114, 11.59497121464450231 ) ) ;
#88963=CARTESIAN_POINT ( 'NONE',  ( -28.21644434148578640, 308.7733337496239301, -9.112255642778062992 ) ) ;
#88981=CARTESIAN_POINT ( 'NONE',  ( -4.024429837834814450, 294.8082127746760079, 1.927919365218930148 ) ) ;
#88985=CARTESIAN_POINT ( 'NONE',  ( 37.26845974722005650, 490.8898249940463074, 12.42613736167234961 ) ) ;
#88990=ORIENTED_EDGE ( 'NONE', *, *, #84105, .T. ) ;
#88991=ORIENTED_EDGE ( 'NONE', *, *, #18572, .T. ) ;
#89003=CARTESIAN_POINT ( 'NONE',  ( -1.128238012697766912, 300.0000000000000000, 9.936150108905552614 ) ) ;
#89009=CARTESIAN_POINT ( 'NONE',  ( -33.75641399212567961, 327.3064826613156129, -4.489452195648050647 ) ) ;
#89010=EDGE_CURVE ( 'NONE', #31406, #95757, #79265, .T. ) ;
#89016=CARTESIAN_POINT ( 'NONE',  ( -30.82234192912234860, 298.3178147627863268, -1.235162244126318365 ) ) ;
#89019=VERTEX_POINT ( 'NONE', #100943 ) ;
#89022=FACE_OUTER_BOUND ( 'NONE', #25746, .T. ) ;
#89023=CARTESIAN_POINT ( 'NONE',  ( 43.00000000000000000, 500.0000000000002274, -15.00000000000000711 ) ) ;
#89028=ORIENTED_EDGE ( 'NONE', *, *, #28994, .T. ) ;
#89053=VERTEX_POINT ( 'NONE', #13513 ) ;
#89076=FACE_OUTER_BOUND ( 'NONE', #53833, .T. ) ;
#89078=CARTESIAN_POINT ( 'NONE',  ( 36.14965894305566962, 491.8061723310889874, 12.56429772144723422 ) ) ;
#89080=ORIENTED_EDGE ( 'NONE', *, *, #53539, .T. ) ;
#89085=CARTESIAN_POINT ( 'NONE',  ( 32.93513049338668708, 465.6726574193326655, 10.66039033145099069 ) ) ;
#89089=DIRECTION ( 'NONE',  ( 0.1269898409407502204, 0.9919025243773941236, -0.001721171576547747550 ) ) ;
#89090=DIRECTION ( 'NONE',  ( -0.2259255479511525777, 0.3692254281732805232, 0.9014600545632787121 ) ) ;
#89097=CARTESIAN_POINT ( 'NONE',  ( -43.52996882529454581, 484.3120888848611685, 0.7833242031809297679 ) ) ;
#89112=CARTESIAN_POINT ( 'NONE',  ( 38.47428897412579119, 485.7788508071993760, -4.770630528148342542 ) ) ;
#89127=ORIENTED_EDGE ( 'NONE', *, *, #80262, .F. ) ;
#89130=CARTESIAN_POINT ( 'NONE',  ( -33.21102376836596903, 438.9613914113129454, 23.92328486949907074 ) ) ;
#89135=CIRCLE ( 'NONE', #46095, 0.9999999999999994449 ) ;
#89139=B_SPLINE_CURVE_WITH_KNOTS ( 'NONE', 3,
 ( #31455, #30927, #79960, #63807 ),
 .UNSPECIFIED., .F., .F.,
 ( 4, 4 ),
 ( 2.525795506525165703E-17, 0.0006696797651155423844 ),
 .UNSPECIFIED. ) ;
#89140=CARTESIAN_POINT ( 'NONE',  ( -43.49283539518359731, 484.8086609925252901, 4.190314177826777176 ) ) ;
#89142=CARTESIAN_POINT ( 'NONE',  ( -33.32781438306703592, 490.0012478078861022, 11.19551906514951156 ) ) ;
#89146=CARTESIAN_POINT ( 'NONE',  ( -30.00000000000000000, 450.0000000000002274, 1.202422573753698876 ) ) ;
#89155=TOROIDAL_SURFACE ( 'NONE', #71902, 5.999999999999994671, 1.000000000000000444 ) ;
#89168=CARTESIAN_POINT ( 'NONE',  ( 9.564994042045842804, 294.6554060604858591, 1.895260366468707103 ) ) ;
#89194=DIRECTION ( 'NONE',  ( -1.000000000000000000, 8.400342417351207405E-11, 8.400342417351195773E-11 ) ) ;
#89201=CARTESIAN_POINT ( 'NONE',  ( 36.20419914068524747, 464.0241112302276179, 19.56059989341736127 ) ) ;
#89205=CARTESIAN_POINT ( 'NONE',  ( -29.50756122520733271, 297.9063904818165724, 10.61050061783298126 ) ) ;
#89208=CARTESIAN_POINT ( 'NONE',  ( -40.75641113481592726, 360.0948485545300741, 24.37153223514695100 ) ) ;
#89212=CARTESIAN_POINT ( 'NONE',  ( 31.49034758424722114, 316.2669363177062110, -6.255441989756967303 ) ) ;
#89217=CARTESIAN_POINT ( 'NONE',  ( -42.38863085962758248, 465.0218298503912138, 14.26222171109765569 ) ) ;
#89223=CARTESIAN_POINT ( 'NONE',  ( -33.00000000000001421, 464.3970849722209095, 17.41240408234210335 ) ) ;
#89237=CARTESIAN_POINT ( 'NONE',  ( 38.74421784392040280, 310.1584125685482149, 1.633477494702207267 ) ) ;
#89246=CARTESIAN_POINT ( 'NONE',  ( 0.000000000000000000, 274.9999999999999432, 0.000000000000000000 ) ) ;
#89254=ORIENTED_EDGE ( 'NONE', *, *, #72986, .T. ) ;
#89256=CIRCLE ( 'NONE', #32447, 0.9999999999999976685 ) ;
#89261=CARTESIAN_POINT ( 'NONE',  ( -43.63213036653843346, 464.4895599185356900, 9.038982508269159055 ) ) ;
#89282=CARTESIAN_POINT ( 'NONE',  ( 28.58679432325043734, 310.5997541753422979, 11.78757380732785798 ) ) ;
#89283=CARTESIAN_POINT ( 'NONE',  ( -43.81524616929482363, 329.5241525934269475, -1.558685580567496176 ) ) ;
#89285=EDGE_CURVE ( 'NONE', #13768, #10730, #53119, .T. ) ;
#89292=CARTESIAN_POINT ( 'NONE',  ( 17.24303157407923237, 294.5700599009814482, 9.877113118490870036 ) ) ;
#89293=CARTESIAN_POINT ( 'NONE',  ( -40.17717846856324115, 485.8445156049142497, -4.962122411036295588 ) ) ;
#89300=CARTESIAN_POINT ( 'NONE',  ( 42.44442147538608623, 464.7190447730621941, 16.13393895236494657 ) ) ;
#89307=CARTESIAN_POINT ( 'NONE',  ( -36.65190467452315914, 491.8432146685187263, 12.58836626716444052 ) ) ;
#89311=CARTESIAN_POINT ( 'NONE',  ( -43.75010090113929806, 464.8337800386750018, 11.75004750934965791 ) ) ;
#89323=CARTESIAN_POINT ( 'NONE',  ( -39.04658448874435095, 485.1639453003155609, -4.285642725068625758 ) ) ;
#89327=CARTESIAN_POINT ( 'NONE',  ( -46.00000000000000000, 488.0336798547363628, -0.8984331811837280579 ) ) ;
#89331=CARTESIAN_POINT ( 'NONE',  ( -46.00000000000000000, 438.2055348968746102, 15.52909715636657495 ) ) ;
#89335=CARTESIAN_POINT ( 'NONE',  ( 35.07179216366485974, 463.5162043426228706, 19.70794395571530089 ) ) ;
#89343=B_SPLINE_SURFACE_WITH_KNOTS ( 'NONE', 1, 3, ( 
 ( #39274, #64084, #63009, #87818, #20999, #88350, #38737, #94856 ),
 ( #13895, #54344, #95906, #96442, #12837, #14424, #22030, #104510 ) ),
 .UNSPECIFIED., .F., .F., .F.,
 ( 2, 2 ),
 ( 4, 2, 2, 4 ),
 ( 0.000000000000000000, 1.000000000000000000 ),
 ( 0.000000000000000000, 0.04450745600790868145, 0.06676118401186306728, 0.08901491201581737678 ),
 .UNSPECIFIED. ) ;
#89355=CARTESIAN_POINT ( 'NONE',  ( -26.97491686565329161, 307.4599153070161606, -9.420584459367200125 ) ) ;
#89365=CARTESIAN_POINT ( 'NONE',  ( -26.22871651383309910, 309.5540286940661190, 10.04294722306419807 ) ) ;
#89378=CARTESIAN_POINT ( 'NONE',  ( 43.86560043478110060, 486.1043823555136214, 5.341761608528310390 ) ) ;
#89390=LINE ( 'NONE', #32763, #87025 ) ;
#89394=CARTESIAN_POINT ( 'NONE',  ( 35.76320840016588676, 388.4727839510825333, 5.610592865731860002 ) ) ;
#89408=CARTESIAN_POINT ( 'NONE',  ( -32.28552837373647577, 464.7648866755938002, 15.30384310834765671 ) ) ;
#89411=CARTESIAN_POINT ( 'NONE',  ( -42.00745990515054018, 464.8754194883779860, 15.22999261134830284 ) ) ;
#89414=EDGE_LOOP ( 'NONE', ( #20566, #88886, #31790, #70016 ) ) ;
#89421=CARTESIAN_POINT ( 'NONE',  ( 29.71096116145698218, 314.7497564551254641, 12.83474296151334748 ) ) ;
#89429=CARTESIAN_POINT ( 'NONE',  ( -35.51695525948886711, 413.2530085246343674, 6.941884492246507499 ) ) ;
#89431=CARTESIAN_POINT ( 'NONE',  ( -25.69622924537841868, 305.2338348851055230, 10.47102872775464100 ) ) ;
#89446=CARTESIAN_POINT ( 'NONE',  ( 35.41405072744154836, 437.5080630478382204, 4.889382217447025170 ) ) ;
#89456=CARTESIAN_POINT ( 'NONE',  ( 42.29361012145520249, 486.6953289214418419, 8.720858923656924944 ) ) ;
#89473=ORIENTED_EDGE ( 'NONE', *, *, #39210, .T. ) ;
#89475=AXIS2_PLACEMENT_3D ( 'NONE', #42241, #66529, #99400 ) ;
#89496=CARTESIAN_POINT ( 'NONE',  ( -9.789044728060147804, 294.6486233851416614, -2.043184600577789833 ) ) ;
#89506=ORIENTED_EDGE ( 'NONE', *, *, #31258, .F. ) ;
#89508=CARTESIAN_POINT ( 'NONE',  ( -1.487796992739244706, 297.5563421048641999, -10.00151720974388603 ) ) ;
#89519=CARTESIAN_POINT ( 'NONE',  ( 35.62683129835268403, 491.6879615318113110, 12.48649695628193257 ) ) ;
#89540=CARTESIAN_POINT ( 'NONE',  ( -32.11029369521102694, 318.6955982813968262, -5.641370532960698014 ) ) ;
#89549=ORIENTED_EDGE ( 'NONE', *, *, #87990, .F. ) ;
#89552=CARTESIAN_POINT ( 'NONE',  ( -42.69811214730272297, 434.9611672192513652, 18.34625614733208820 ) ) ;
#89562=CARTESIAN_POINT ( 'NONE',  ( -35.77486673446257726, 439.5646605908588072, 23.98731056691347874 ) ) ;
#89570=( BOUNDED_SURFACE ( )  B_SPLINE_SURFACE ( 3, 2, ( 
 ( #13828, #53252, #46740 ),
 ( #79630, #12240, #5747 ),
 ( #78568, #62411, #13292 ),
 ( #85626, #30053, #95305 ) ),
 .UNSPECIFIED., .F., .F., .F. ) 
 B_SPLINE_SURFACE_WITH_KNOTS ( ( 4, 4 ),
 ( 3, 3 ),
 ( 0.01539444365212560770, 0.01716277291647040973 ),
 ( 0.1628431039857609064, 1.000000000000000000 ),
 .UNSPECIFIED. ) 
 GEOMETRIC_REPRESENTATION_ITEM ( )  RATIONAL_B_SPLINE_SURFACE ( (
 ( 0.9201425306416459726, 0.7548024220745122026, 1.000000000000000000),
 ( 0.9252298807393682933, 0.7704228259270666790, 1.000000000000000000),
 ( 0.9301471562783281133, 0.7855210260307374792, 1.000000000000000000),
 ( 0.9349020401063605767, 0.8001206121097657054, 1.000000000000000000) ) ) 
 REPRESENTATION_ITEM ( '' )  SURFACE ( )  );
#89572=VERTEX_POINT ( 'NONE', #54907 ) ;
#89575=AXIS2_PLACEMENT_3D ( 'NONE', #21814, #72451, #54654 ) ;
#89586=ORIENTED_EDGE ( 'NONE', *, *, #17145, .F. ) ;
#89591=FACE_OUTER_BOUND ( 'NONE', #3010, .T. ) ;
#89597=CIRCLE ( 'NONE', #37986, 1.000000000000001332 ) ;
#89604=CARTESIAN_POINT ( 'NONE',  ( -17.35892867067943257, 294.5707697310705839, -10.05973541782409342 ) ) ;
#89609=CARTESIAN_POINT ( 'NONE',  ( 29.99999999999482014, 487.5694517063741955, 6.760539803216031984 ) ) ;
#89615=DIRECTION ( 'NONE',  ( 0.000000000000000000, 0.000000000000000000, 1.000000000000000000 ) ) ;
#89618=CARTESIAN_POINT ( 'NONE',  ( -6.657117369358112491, 304.7445948672375948, 8.914202651909654662 ) ) ;
#89622=CARTESIAN_POINT ( 'NONE',  ( -43.46689911038857446, 485.4921130118004271, 4.095024577345737882 ) ) ;
#89627=CARTESIAN_POINT ( 'NONE',  ( -43.65875038008589115, 484.6130917689293369, 3.255992392461536600 ) ) ;
#89634=CARTESIAN_POINT ( 'NONE',  ( 37.54559764570182523, 464.1143081516207189, 19.43664670202678835 ) ) ;
#89642=CARTESIAN_POINT ( 'NONE',  ( 33.11369981515476013, 485.0096198691156815, 0.6282636062398145871 ) ) ;
#89646=CARTESIAN_POINT ( 'NONE',  ( -43.66595852442649317, 384.2000512634306233, 15.34658628582926454 ) ) ;
#89658=EDGE_CURVE ( 'NONE', #90326, #45699, #27949, .T. ) ;
#89663=CARTESIAN_POINT ( 'NONE',  ( 45.17824257314219949, 354.4244853104167987, 3.762393652172960845 ) ) ;
#89689=VERTEX_POINT ( 'NONE', #48408 ) ;
#89701=CARTESIAN_POINT ( 'NONE',  ( -31.53898857890735030, 437.3650977026285886, 21.86279335866149509 ) ) ;
#89714=CARTESIAN_POINT ( 'NONE',  ( -38.97368692663644651, 491.1629893710622241, 12.12582181740389053 ) ) ;
#89717=CARTESIAN_POINT ( 'NONE',  ( 33.12944332324993013, 439.4248878830265994, 23.85028906779293933 ) ) ;
#89736=CARTESIAN_POINT ( 'NONE',  ( 37.54559764570471003, 464.1143081516196389, 19.43664670202597833 ) ) ;
#89740=CARTESIAN_POINT ( 'NONE',  ( -29.07128654445882887, 296.9339959557834163, -9.548856946221640385 ) ) ;
#89742=CARTESIAN_POINT ( 'NONE',  ( -45.48126212248870814, 413.7349014071057240, 8.309231847991947362 ) ) ;
#89745=CARTESIAN_POINT ( 'NONE',  ( 27.49382079585014793, 308.0021161605097291, -9.293432125849182768 ) ) ;
#89746=EDGE_LOOP ( 'NONE', ( #2921, #77050, #69619, #73310, #81220, #51368 ) ) ;
#89758=CARTESIAN_POINT ( 'NONE',  ( -35.52295374289839458, 436.6489517640831650, 4.915275271775389143 ) ) ;
#89770=PRESENTATION_STYLE_ASSIGNMENT (( #179 ) ) ;
#89773=CARTESIAN_POINT ( 'NONE',  ( 43.65809794933323218, 484.6141936383338020, 3.261896584721304393 ) ) ;
#89809=CARTESIAN_POINT ( 'NONE',  ( 33.10942959112523454, 427.0911879376557181, 25.12314773043819827 ) ) ;
#89810=CARTESIAN_POINT ( 'NONE',  ( -44.90174202792449165, 347.4042625033331433, 2.362512452797935758 ) ) ;
#89813=CARTESIAN_POINT ( 'NONE',  ( -44.19305039087728915, 485.5049587488591101, 3.133877349347021557 ) ) ;
#89815=ORIENTED_EDGE ( 'NONE', *, *, #47517, .F. ) ;
#89829=( NAMED_UNIT ( * ) SI_UNIT ( $, .STERADIAN. ) SOLID_ANGLE_UNIT ( ) );
#89832=CARTESIAN_POINT ( 'NONE',  ( -35.00143047691628340, 490.1822567707091594, 12.08765882792895852 ) ) ;
#89837=CARTESIAN_POINT ( 'NONE',  ( 33.00000000000002842, 489.5971041675261404, 10.80646835458719224 ) ) ;
#89847=EDGE_CURVE ( 'NONE', #87652, #66563, #63520, .T. ) ;
#89848=CARTESIAN_POINT ( 'NONE',  ( 0.000000000000000000, 0.000000000000000000, 0.000000000000000000 ) ) ;
#89872=CARTESIAN_POINT ( 'NONE',  ( 34.62348220644697960, 301.9590946549885189, -0.3855663969161592930 ) ) ;
#89877=CARTESIAN_POINT ( 'NONE',  ( -45.48003679188781234, 379.8448106960472614, 7.220331889307936457 ) ) ;
#89881=CARTESIAN_POINT ( 'NONE',  ( -34.67263685778915061, 485.1278622359849919, -2.016271555160150886 ) ) ;
#89885=CARTESIAN_POINT ( 'NONE',  ( -23.17107764268310888, 305.7664649652382423, 10.13667392129760536 ) ) ;
#89887=CARTESIAN_POINT ( 'NONE',  ( 33.94783393359897161, 484.1261039197349305, 1.321740980884978267 ) ) ;
#89894=CARTESIAN_POINT ( 'NONE',  ( 44.15102752603837644, 435.2229927719864122, 14.45803418847442146 ) ) ;
#89908=CARTESIAN_POINT ( 'NONE',  ( 29.45362385905110969, 325.9253963054578662, 15.14270878922920716 ) ) ;
#89911=CARTESIAN_POINT ( 'NONE',  ( 28.76346532419124458, 309.5219921958590135, -8.933260212751790164 ) ) ;
#89936=CARTESIAN_POINT ( 'NONE',  ( 29.55500230678722673, 314.0625905908086111, 12.66100350989708012 ) ) ;
#89939=B_SPLINE_CURVE_WITH_KNOTS ( 'NONE', 3,
 ( #44355, #95043, #86953, #100985, #77249, #35770, #85341, #102588, #60553, #3365, #60031, #35223, #36827, #21179, #11969, #10892 ),
 .UNSPECIFIED., .F., .F.,
 ( 4, 2, 2, 2, 2, 2, 2, 4 ),
 ( 4.525475972510097653E-17, 0.001025531879885757452, 0.001538297819828604628, 0.002051063759771452021, 0.002563829699714299196, 0.003076595639657146372, 0.003589361579599994415, 0.004102127519542841591 ),
 .UNSPECIFIED. ) ;
#89941=CARTESIAN_POINT ( 'NONE',  ( -40.90837589347040648, 460.4813280201778412, 2.460853848286399082 ) ) ;
#89948=CARTESIAN_POINT ( 'NONE',  ( -27.29693123059870885, 296.4603777880672055, 2.286005658668618601 ) ) ;
#89955=CARTESIAN_POINT ( 'NONE',  ( 3.267219863862204754, 300.0925129258962443, 9.454287392228017950 ) ) ;
#89961=CARTESIAN_POINT ( 'NONE',  ( 0.000000000000000000, -19.99999999999998934, 0.000000000000000000 ) ) ;
#89965=CARTESIAN_POINT ( 'NONE',  ( 34.47678062874017968, 437.1474145881098252, 5.468662283308795224 ) ) ;
#89971=AXIS2_PLACEMENT_3D ( 'NONE', #15761, #81527, #69117 ) ;
#89981=CIRCLE ( 'NONE', #76189, 1.000000000000016209 ) ;
#90009=ORIENTED_EDGE ( 'NONE', *, *, #17028, .F. ) ;
#90010=CARTESIAN_POINT ( 'NONE',  ( 29.42291439507181749, 324.0459798135065057, 13.67000796727436374 ) ) ;
#90038=CARTESIAN_POINT ( 'NONE',  ( 34.98071605569023745, 490.8360413343243067, 11.88490725385638669 ) ) ;
#90048=EDGE_CURVE ( 'NONE', #17301, #1547, #106528, .T. ) ;
#90050=( BOUNDED_SURFACE ( )  B_SPLINE_SURFACE ( 3, 2, ( 
 ( #99999, #26167, #91397 ),
 ( #24031, #106490, #42291 ),
 ( #83813, #105957, #34244 ),
 ( #83286, #50374, #15898 ) ),
 .UNSPECIFIED., .F., .F., .F. ) 
 B_SPLINE_SURFACE_WITH_KNOTS ( ( 4, 4 ),
 ( 3, 3 ),
 ( -2.023121253857951274E-15, 0.0002622513198896260392 ),
 ( 0.000000000000000000, 1.000000000000000000 ),
 .UNSPECIFIED. ) 
 GEOMETRIC_REPRESENTATION_ITEM ( )  RATIONAL_B_SPLINE_SURFACE ( (
 ( 1.000000000000000000, 0.7874655377939502321, 1.000000000000000000),
 ( 1.000000000000000000, 0.7887353030063457560, 1.000000000000000000),
 ( 1.000000000000000000, 0.7900011776560428300, 1.000000000000000000),
 ( 1.000000000000000000, 0.7912633096140608835, 1.000000000000000000) ) ) 
 REPRESENTATION_ITEM ( '' )  SURFACE ( )  );
#90061=CARTESIAN_POINT ( 'NONE',  ( -30.45624637448644023, 312.7340192834439563, -8.144926979512700171 ) ) ;
#90074=CARTESIAN_POINT ( 'NONE',  ( -40.84855644196625235, 369.2103136256716311, 25.49516658059198804 ) ) ;
#90075=CARTESIAN_POINT ( 'NONE',  ( 21.52280673074376338, 305.1198653818534581, 8.994423587666668496 ) ) ;
#90076=CARTESIAN_POINT ( 'NONE',  ( -40.44926925267034079, 464.0738508500458011, 18.39527504910404687 ) ) ;
#90079=EDGE_CURVE ( 'NONE', #39480, #89019, #103236, .T. ) ;
#90081=B_SPLINE_CURVE_WITH_KNOTS ( 'NONE', 3,
 ( #82363, #64082, #7933, #81282 ),
 .UNSPECIFIED., .F., .F.,
 ( 4, 4 ),
 ( 0.000000000000000000, 0.0001439741052586902467 ),
 .UNSPECIFIED. ) ;
#90086=CARTESIAN_POINT ( 'NONE',  ( 33.20902353462182788, 484.6199955813546580, 4.299886535038632829 ) ) ;
#90089=DIRECTION ( 'NONE',  ( 0.000000000000000000, -1.000000000000000000, -0.000000000000000000 ) ) ;
#90095=CARTESIAN_POINT ( 'NONE',  ( -44.21332904831282917, 435.2494715644501184, 14.45449769377396976 ) ) ;
#90107=AXIS2_PLACEMENT_3D ( 'NONE', #95808, #87717, #44069 ) ;
#90110=CIRCLE ( 'NONE', #69431, 12.00000000000001066 ) ;
#90119=ORIENTED_EDGE ( 'NONE', *, *, #28138, .F. ) ;
#90127=CARTESIAN_POINT ( 'NONE',  ( -6.624059643703564149, 294.7379298340728724, -10.02420444108935449 ) ) ;
#90131=CARTESIAN_POINT ( 'NONE',  ( 30.00000000000004619, 486.7222546968084771, 5.239171024090038209 ) ) ;
#90133=VERTEX_POINT ( 'NONE', #86140 ) ;
#90137=ORIENTED_EDGE ( 'NONE', *, *, #13817, .T. ) ;
#90140=CARTESIAN_POINT ( 'NONE',  ( 33.49627437231217186, 465.2401082455917845, 8.307162268779238801 ) ) ;
#90142=CARTESIAN_POINT ( 'NONE',  ( -3.318393640953817503, 303.8518027741603191, 9.936999414637822881 ) ) ;
#90145=DIRECTION ( 'NONE',  ( 0.000000000000000000, 0.000000000000000000, -1.000000000000000000 ) ) ;
#90171=FILL_AREA_STYLE_COLOUR ( '', #14090 ) ;
#90187=CARTESIAN_POINT ( 'NONE',  ( 45.50145573691759182, 405.2496736015978627, 8.430338687477670234 ) ) ;
#90191=CARTESIAN_POINT ( 'NONE',  ( 32.15166163075728178, 486.0589784586659903, 5.199393881400817818 ) ) ;
#90192=CARTESIAN_POINT ( 'NONE',  ( -37.62251730745837364, 437.3427388312646826, 4.535622330043170614 ) ) ;
#90193=CARTESIAN_POINT ( 'NONE',  ( -27.95570841088265368, 315.0023162612367287, 11.41332481783935826 ) ) ;
#90223=CARTESIAN_POINT ( 'NONE',  ( -33.09586041880449159, 373.7026161310072325, 24.17050744075106294 ) ) ;
#90227=B_SPLINE_CURVE_WITH_KNOTS ( 'NONE', 3,
 ( #63249, #69744, #96142, #20716, #70274, #62208, #5007, #21748, #94015, #54584, #21227, #22275, #70799, #53554, #87523, #95606 ),
 .UNSPECIFIED., .F., .F.,
 ( 4, 2, 2, 2, 2, 2, 2, 4 ),
 ( 0.000000000000000000, 0.0005175470994303207851, 0.001035094198860641570, 0.001552641298290962247, 0.002070188397721283140, 0.002587735497151604034, 0.003105282596581924494, 0.004140376795442568016 ),
 .UNSPECIFIED. ) ;
#90233=B_SPLINE_CURVE_WITH_KNOTS ( 'NONE', 3,
 ( #18479, #85321, #9814, #52402 ),
 .UNSPECIFIED., .F., .F.,
 ( 4, 4 ),
 ( 5.204170427930421283E-18, 0.001831984915194801279 ),
 .UNSPECIFIED. ) ;
#90236=CARTESIAN_POINT ( 'NONE',  ( -40.03783884386260894, 489.2292324564466526, 11.31445617789379554 ) ) ;
#90239=CARTESIAN_POINT ( 'NONE',  ( 36.41995684994217441, 439.0104540407872378, 23.96542090717511186 ) ) ;
#90243=ORIENTED_EDGE ( 'NONE', *, *, #50717, .F. ) ;
#90252=CARTESIAN_POINT ( 'NONE',  ( 32.10528697966009304, 486.1671898930079578, 5.449875171705039989 ) ) ;
#90255=CARTESIAN_POINT ( 'NONE',  ( 36.27064846733442494, 463.5381974806701919, 19.67843218035151054 ) ) ;
#90260=CARTESIAN_POINT ( 'NONE',  ( -40.61216075948964033, 351.1469683695276558, 22.89433108575548914 ) ) ;
#90261=CARTESIAN_POINT ( 'NONE',  ( -40.95420997525301487, 387.0967036739339164, 27.26945002580065136 ) ) ;
#90265=CARTESIAN_POINT ( 'NONE',  ( 27.36727613921635083, 306.5270185924862858, -9.405951803952929069 ) ) ;
#90279=CARTESIAN_POINT ( 'NONE',  ( 32.99999999999997158, 464.4386723251831768, 6.308603495333048983 ) ) ;
#90304=CARTESIAN_POINT ( 'NONE',  ( -32.62553167428460199, 485.9570050037687565, 7.214059741198010300 ) ) ;
#90320=CARTESIAN_POINT ( 'NONE',  ( 29.99999999999375078, 464.1513975948316784, 11.53706206233560394 ) ) ;
#90321=CARTESIAN_POINT ( 'NONE',  ( 46.00000000000000000, 461.7880546943557079, 10.79349299898485448 ) ) ;
#90323=ORIENTED_EDGE ( 'NONE', *, *, #95037, .F. ) ;
#90324=EDGE_CURVE ( 'NONE', #2640, #104315, #97218, .T. ) ;
#90326=VERTEX_POINT ( 'NONE', #52951 ) ;
#90331=CARTESIAN_POINT ( 'NONE',  ( 33.07276483573664905, 438.9325140356084489, 23.89537236861388081 ) ) ;
#90332=CARTESIAN_POINT ( 'NONE',  ( -35.77761637803537553, 327.7250599313179578, -3.907684277836948716 ) ) ;
#90346=CIRCLE ( 'NONE', #43831, 1.000000000000006439 ) ;
#90360=CARTESIAN_POINT ( 'NONE',  ( 33.13096700375007941, 488.4252353401654432, 9.689492805996717806 ) ) ;
#90371=AXIS2_PLACEMENT_3D ( 'NONE', #101637, #101100, #92465 ) ;
#90372=EDGE_CURVE ( 'NONE', #73090, #27223, #76573, .T. ) ;
#90383=CARTESIAN_POINT ( 'NONE',  ( -45.99999999999999289, 436.0213184034681717, 14.35141020368342879 ) ) ;
#90387=CARTESIAN_POINT ( 'NONE',  ( -32.22120753352784561, 464.6691781026584636, 10.60621122532581140 ) ) ;
#90391=VERTEX_POINT ( 'NONE', #2801 ) ;
#90396=EDGE_CURVE ( 'NONE', #7054, #6978, #38046, .T. ) ;
#90405=CARTESIAN_POINT ( 'NONE',  ( 29.43919633169317862, 307.1812765748473453, -9.021906422362246047 ) ) ;
#90415=CARTESIAN_POINT ( 'NONE',  ( -34.25540317603608997, 485.0620278916507573, -1.482526247037498246 ) ) ;
#90416=CARTESIAN_POINT ( 'NONE',  ( 43.56723210060331297, 370.0879074500739989, 13.88321950767064017 ) ) ;
#90417=CARTESIAN_POINT ( 'NONE',  ( 43.69871659247140627, 464.4396234996452790, 7.060974336473465840 ) ) ;
#90420=CARTESIAN_POINT ( 'NONE',  ( -22.09048636024830259, 305.2882331017710840, 9.030984930783928277 ) ) ;
#90422=CARTESIAN_POINT ( 'NONE',  ( 35.56870672589202087, 485.2859037185882016, -2.957003582718795709 ) ) ;
#90426=EDGE_LOOP ( 'NONE', ( #758, #52236 ) ) ;
#90430=CARTESIAN_POINT ( 'NONE',  ( 43.79026230967847511, 435.5799286522100147, 9.443751109679228151 ) ) ;
#90441=CARTESIAN_POINT ( 'NONE',  ( 19.70764564238371719, 304.7954121406193622, 9.925013215726785631 ) ) ;
#90444=CARTESIAN_POINT ( 'NONE',  ( -32.07049714173062682, 486.4381577779643635, 6.103659696309225779 ) ) ;
#90461=CARTESIAN_POINT ( 'NONE',  ( -42.20540931547580499, 464.9254549434357386, 14.73500713293301168 ) ) ;
#90463=CARTESIAN_POINT ( 'NONE',  ( 42.55949806392587931, 435.1558328882682645, 18.91815692826296313 ) ) ;
#90467=CARTESIAN_POINT ( 'NONE',  ( 32.39363610230712709, 435.1530561269337909, 14.92612657118719888 ) ) ;
#90469=CARTESIAN_POINT ( 'NONE',  ( 35.43884268025067286, 303.9034792765622797, 4.025496658314922094 ) ) ;
#90471=CARTESIAN_POINT ( 'NONE',  ( 44.45120377230470865, 484.8901964262618094, 4.471885531210140208 ) ) ;
#90479=CARTESIAN_POINT ( 'NONE',  ( 33.00540147335379260, 487.4196752801331627, 9.523982417622169905 ) ) ;
#90483=CARTESIAN_POINT ( 'NONE',  ( -28.52151309506147925, 297.0551483322281570, 2.417936164087576945 ) ) ;
#90489=CARTESIAN_POINT ( 'NONE',  ( 5.720759824257057424, 297.8120955430345589, 8.219233466110658526 ) ) ;
#90491=ORIENTED_EDGE ( 'NONE', *, *, #17687, .F. ) ;
#90505=CARTESIAN_POINT ( 'NONE',  ( -32.90756164719182664, 485.1133553471440791, 5.490574211026766349 ) ) ;
#90509=CARTESIAN_POINT ( 'NONE',  ( -34.47211195129267480, 489.5752767497882587, 11.69752549375507655 ) ) ;
#90511=CARTESIAN_POINT ( 'NONE',  ( 32.82691535583472842, 485.1045372766795367, 1.724905475515025266 ) ) ;
#90517=EDGE_CURVE ( 'NONE', #13955, #80654, #102388, .T. ) ;
#90534=CARTESIAN_POINT ( 'NONE',  ( -9.730604568514243269, 294.6502803634054999, -2.323175618299882395 ) ) ;
#90544=CARTESIAN_POINT ( 'NONE',  ( 32.13660303513785976, 374.7216330957919013, 24.09117032669768932 ) ) ;
#90548=CARTESIAN_POINT ( 'NONE',  ( -42.57704743493911081, 486.1612337113410263, 7.852296464539654686 ) ) ;
#90563=CARTESIAN_POINT ( 'NONE',  ( -1.798224084866679950, 298.0247695552619689, -10.00218504963178567 ) ) ;
#90575=CARTESIAN_POINT ( 'NONE',  ( 37.62595466100196262, 491.2446780561975856, 12.18850516984599786 ) ) ;
#90577=CARTESIAN_POINT ( 'NONE',  ( -32.12958771267418712, 464.7275665249413805, 11.12424126545828784 ) ) ;
#90579=CARTESIAN_POINT ( 'NONE',  ( -34.42195163688415960, 484.1350747783264410, 0.1342865971146420812 ) ) ;
#90583=CARTESIAN_POINT ( 'NONE',  ( -8.844479576175121593, 302.6213365498747407, -10.03676384835056723 ) ) ;
#90595=CARTESIAN_POINT ( 'NONE',  ( -35.11084318070448518, 353.0208097076877607, 2.079257881123132812 ) ) ;
#90604=CARTESIAN_POINT ( 'NONE',  ( -26.11633329837163942, 295.8773401828905207, -9.779540871743899189 ) ) ;
#90610=CARTESIAN_POINT ( 'NONE',  ( -33.15912019476756001, 406.2462808298095069, 25.90171796155655670 ) ) ;
#90620=AXIS2_PLACEMENT_3D ( 'NONE', #33127, #8285, #16377 ) ;
#90623=CARTESIAN_POINT ( 'NONE',  ( 43.46689911038831156, 485.4921130118007113, 4.095024577346795702 ) ) ;
#90624=CARTESIAN_POINT ( 'NONE',  ( -41.71452336584287934, 436.0710517509322131, 20.70662328852571576 ) ) ;
#90629=CARTESIAN_POINT ( 'NONE',  ( -32.91521444485699277, 465.6822365171608453, 10.74527606630527110 ) ) ;
#90639=PLANE ( 'NONE',  #44887 ) ;
#90645=CARTESIAN_POINT ( 'NONE',  ( 36.87655955837855970, 438.2068510013162950, 3.933030107424718924 ) ) ;
#90650=ORIENTED_EDGE ( 'NONE', *, *, #6744, .T. ) ;
#90653=ORIENTED_EDGE ( 'NONE', *, *, #59475, .T. ) ;
#90654=EDGE_CURVE ( 'NONE', #70575, #100942, #34221, .T. ) ;
#90666=B_SPLINE_CURVE_WITH_KNOTS ( 'NONE', 3,
 ( #28908, #61784, #14242, #47150 ),
 .UNSPECIFIED., .F., .F.,
 ( 4, 4 ),
 ( 0.000000000000000000, 0.0002045283294076029920 ),
 .UNSPECIFIED. ) ;
#90670=ORIENTED_EDGE ( 'NONE', *, *, #56144, .F. ) ;
#90674=AXIS2_PLACEMENT_3D ( 'NONE', #51498, #67168, #9426 ) ;
#90675=DIRECTION ( 'NONE',  ( 0.000000000000000000, 0.000000000000000000, -1.000000000000000000 ) ) ;
#90693=ORIENTED_EDGE ( 'NONE', *, *, #97789, .T. ) ;
#90697=TOROIDAL_SURFACE ( 'NONE', #57962, 12.00000000000001066, 3.000000000000000000 ) ;
#90698=ORIENTED_EDGE ( 'NONE', *, *, #3064, .F. ) ;
#90700=VERTEX_POINT ( 'NONE', #53232 ) ;
#90706=CARTESIAN_POINT ( 'NONE',  ( 36.41079454256790626, 485.4442866794557858, -3.629012552425965765 ) ) ;
#90723=CARTESIAN_POINT ( 'NONE',  ( 30.55228927099183522, 298.7536840786443690, 10.80461237140096209 ) ) ;
#90739=CARTESIAN_POINT ( 'NONE',  ( -43.00000000000000000, 450.0000000000002274, 13.20242257375370976 ) ) ;
#90742=CARTESIAN_POINT ( 'NONE',  ( 26.51901951938406654, 308.1855417876873844, 10.94630820763295453 ) ) ;
#90762=CARTESIAN_POINT ( 'NONE',  ( -24.52277916217002129, 304.2494540235151135, 10.24385320776191399 ) ) ;
#90779=CARTESIAN_POINT ( 'NONE',  ( 38.91686277342078171, 438.0826785806304997, 23.13445567070433384 ) ) ;
#90788=EDGE_CURVE ( 'NONE', #63262, #58013, #5829, .T. ) ;
#90794=CARTESIAN_POINT ( 'NONE',  ( 36.52561726181321689, 463.3029834606174973, 20.13286708880512776 ) ) ;
#90797=CARTESIAN_POINT ( 'NONE',  ( 1.227754105814699780E-15, 67.05096163904791240, 10.02537308446410691 ) ) ;
#90799=CARTESIAN_POINT ( 'NONE',  ( -30.55228927099183522, 298.7536840786443690, 10.80461237140096209 ) ) ;
#90804=CARTESIAN_POINT ( 'NONE',  ( 29.18041179959944387, 310.2186600874167084, -8.763845530462663902 ) ) ;
#90811=DIRECTION ( 'NONE',  ( 0.9605097441494802046, 0.000000000000000000, -0.2782463501897193825 ) ) ;
#90817=AXIS2_PLACEMENT_3D ( 'NONE', #60859, #53288, #93749 ) ;
#90825=ORIENTED_EDGE ( 'NONE', *, *, #61755, .T. ) ;
#90835=DIRECTION ( 'NONE',  ( -0.9995674975569972531, 0.02876390015618488644, 0.006120120541885859695 ) ) ;
#90843=CARTESIAN_POINT ( 'NONE',  ( 26.59373630444105885, 307.2488738721764889, -8.467865159397765851 ) ) ;
#90851=CARTESIAN_POINT ( 'NONE',  ( -15.38346597837744767, 302.5568188537556580, -10.06270105311703844 ) ) ;
#90854=CARTESIAN_POINT ( 'NONE',  ( -33.74977848768426725, 477.7786480585253344, 4.002244379145985853 ) ) ;
#90856=CARTESIAN_POINT ( 'NONE',  ( -35.72584807339683977, 463.6218724463183207, 19.50045127626819763 ) ) ;
#90860=CARTESIAN_POINT ( 'NONE',  ( 32.31726413982377011, 464.7724101315872076, 15.30491388830120236 ) ) ;
#90861=CARTESIAN_POINT ( 'NONE',  ( 18.69420657816679210, 304.6310092840336097, -10.04693110555011160 ) ) ;
#90872=CARTESIAN_POINT ( 'NONE',  ( 26.78666884061847853, 306.6412577338363690, 10.80680221502309912 ) ) ;
#90874=CARTESIAN_POINT ( 'NONE',  ( -45.37852524047085723, 369.5271474663848039, 5.963215168293914736 ) ) ;
#90883=CARTESIAN_POINT ( 'NONE',  ( 41.90617369998742703, 464.5440823313534793, 16.88098358180886294 ) ) ;
#90888=ORIENTED_EDGE ( 'NONE', *, *, #97029, .F. ) ;
#90897=CARTESIAN_POINT ( 'NONE',  ( -34.12349128637492157, 490.8027302422244134, 11.84948222508912430 ) ) ;
#90905=AXIS2_PLACEMENT_3D ( 'NONE', #47756, #103371, #55834 ) ;
#90910=EDGE_LOOP ( 'NONE', ( #91227, #90009 ) ) ;
#90911=CARTESIAN_POINT ( 'NONE',  ( 33.00000000000000000, 463.5362553048592531, 6.739467187734345721 ) ) ;
#90917=CIRCLE ( 'NONE', #4766, 12.00000000000000711 ) ;
#90940=EDGE_CURVE ( 'NONE', #7512, #23483, #104997, .T. ) ;
#90945=CARTESIAN_POINT ( 'NONE',  ( 34.02613438762318054, 301.2396209895970856, -0.5563051883781007234 ) ) ;
#90946=DIRECTION ( 'NONE',  ( -1.000000000000000000, -0.000000000000000000, -0.000000000000000000 ) ) ;
#90965=CARTESIAN_POINT ( 'NONE',  ( 34.88071508727530556, 485.0161356477989898, -0.9861291933420458511 ) ) ;
#90981=ORIENTED_EDGE ( 'NONE', *, *, #1542, .T. ) ;
#90984=CARTESIAN_POINT ( 'NONE',  ( 40.73878143178837519, 486.4834083601638213, 16.46716573231486436 ) ) ;
#90987=CARTESIAN_POINT ( 'NONE',  ( -32.01266203147167744, 486.7692091651749138, 6.765869859085228200 ) ) ;
#91000=ORIENTED_EDGE ( 'NONE', *, *, #99230, .F. ) ;
#91003=VERTEX_POINT ( 'NONE', #2937 ) ;
#91006=CARTESIAN_POINT ( 'NONE',  ( 43.40156817619795504, 435.0518544018561329, 15.31415127482170035 ) ) ;
#91010=CARTESIAN_POINT ( 'NONE',  ( -42.75106025684119260, 464.8151298349279728, 15.61142817803142790 ) ) ;
#91011=CARTESIAN_POINT ( 'NONE',  ( -31.60000081795433857, 345.3413446759684007, 19.62217261211241137 ) ) ;
#91022=CARTESIAN_POINT ( 'NONE',  ( 31.73931315321975433, 299.2822593833305405, 2.924664567257585723 ) ) ;
#91024=EDGE_CURVE ( 'NONE', #101821, #49452, #68909, .T. ) ;
#91028=ADVANCED_FACE ( 'NONE', ( #52550 ), #59844, .T. ) ;
#91029=CARTESIAN_POINT ( 'NONE',  ( -42.23079339798741927, 460.7352525929354101, 2.726051457480709761 ) ) ;
#91030=CARTESIAN_POINT ( 'NONE',  ( 42.69425402696286653, 372.2145364761282167, 18.00764261570441604 ) ) ;
#91033=ORIENTED_EDGE ( 'NONE', *, *, #69198, .T. ) ;
#91035=CARTESIAN_POINT ( 'NONE',  ( -27.69739594536710214, 296.8485875735327113, 10.37266411860409221 ) ) ;
#91036=DIRECTION ( 'NONE',  ( -1.000000000000000000, 0.000000000000000000, 0.000000000000000000 ) ) ;
#91037=CARTESIAN_POINT ( 'NONE',  ( -46.00000000000000000, 438.0652200859154846, 14.81161132415559223 ) ) ;
#91056=CARTESIAN_POINT ( 'NONE',  ( -46.00000000000000000, 500.0000000000002274, 0.000000000000000000 ) ) ;
#91057=CARTESIAN_POINT ( 'NONE',  ( -32.88333705524179607, 439.7317646416724415, 24.13381181826117583 ) ) ;
#91061=CARTESIAN_POINT ( 'NONE',  ( -31.56707703923818187, 439.0034412535504771, 23.33584616512316501 ) ) ;
#91085=CARTESIAN_POINT ( 'NONE',  ( -9.090810276835252779, 294.6686654934159151, -4.204479076929215076 ) ) ;
#91092=ORIENTED_EDGE ( 'NONE', *, *, #65003, .F. ) ;
#91093=ORIENTED_EDGE ( 'NONE', *, *, #54776, .T. ) ;
#91094=CARTESIAN_POINT ( 'NONE',  ( 29.58258320683665232, 319.4038838472506541, 13.76509249064623752 ) ) ;
#91097=CARTESIAN_POINT ( 'NONE',  ( -43.17378635869611259, 487.6240912981934343, 8.491167829017486568 ) ) ;
#91104=AXIS2_PLACEMENT_3D ( 'NONE', #56522, #31757, #72715 ) ;
#91106=CARTESIAN_POINT ( 'NONE',  ( 43.00000000000000000, 450.0000000000002274, 13.20242257375370976 ) ) ;
#91127=B_SPLINE_SURFACE_WITH_KNOTS ( 'NONE', 1, 3, ( 
 ( #63805, #105311, #15230, #64335, #31453, #31970, #7133, #40044, #47058, #40569, #32511, #22300, #98274, #15762, #72918, #105828, #56738, #89663, #24432, #57264, #55146, #90187, #46543, #79958, #79436, #38994, #38474, #71340 ),
 ( #104235, #30383, #63272, #49174, #91269, #597, #90723, #10319, #57799, #100927, #24946, #75042, #41108, #16837, #75593, #49719, #82627, #33562, #8729, #27088, #99867, #83673, #100397, #41637, #67517, #74520, #84224, #66438 ) ),
 .UNSPECIFIED., .F., .F., .F.,
 ( 2, 2 ),
 ( 4, 2, 2, 2, 2, 2, 2, 2, 2, 2, 2, 2, 2, 4 ),
 ( 0.000000000000000000, 1.000000000000000000 ),
 ( 0.08901491201581737678, 0.1032490540155679704, 0.1174831960153185778, 0.1317173380150691853, 0.1459514800148197788, 0.1744197640143299588, 0.2028880480138401388, 0.2598246160128514504, 0.3167611840118632616, 0.4306343200098861623, 0.5445074560079088410, 0.6583805920059359051, 0.7722537280039543095, 1.000000000000000000 ),
 .UNSPECIFIED. ) ;
#91128=CARTESIAN_POINT ( 'NONE',  ( 35.91982565306800979, 490.8454349930378271, 12.40602332252425377 ) ) ;
#91129=CARTESIAN_POINT ( 'NONE',  ( -34.84533357024655231, 490.9234226268542898, 11.68321824384988972 ) ) ;
#91134=CARTESIAN_POINT ( 'NONE',  ( -4.925922214360547891, 301.1861782522827866, -10.01402241915593372 ) ) ;
#91144=CARTESIAN_POINT ( 'NONE',  ( -31.03561048997209681, 439.3357289228141553, 22.68171793430912686 ) ) ;
#91147=CARTESIAN_POINT ( 'NONE',  ( -33.13240178283476212, 323.0802024858354002, -5.539852619051230498 ) ) ;
#91151=( BOUNDED_SURFACE ( )  B_SPLINE_SURFACE ( 3, 2, ( 
 ( #101474, #3306, #101994 ),
 ( #66989, #32847, #66247 ),
 ( #82436, #57604, #99129 ),
 ( #75400, #41970, #32314 ) ),
 .UNSPECIFIED., .F., .F., .F. ) 
 B_SPLINE_SURFACE_WITH_KNOTS ( ( 4, 4 ),
 ( 3, 3 ),
 ( 1.474514954580286030E-17, 0.001313222278771296152 ),
 ( 0.000000000000000000, 1.000000000000000000 ),
 .UNSPECIFIED. ) 
 GEOMETRIC_REPRESENTATION_ITEM ( )  RATIONAL_B_SPLINE_SURFACE ( (
 ( 1.000000000000000000, 0.8270258197359552366, 1.000000000000000000),
 ( 1.000000000000000000, 0.8180084242886545010, 1.000000000000000000),
 ( 1.000000000000000000, 0.8088315090908722027, 1.000000000000000000),
 ( 1.000000000000000000, 0.7996726260853299628, 1.000000000000000000) ) ) 
 REPRESENTATION_ITEM ( '' )  SURFACE ( )  );
#91153=EDGE_LOOP ( 'NONE', ( #84369, #92420, #8040, #46245, #50307, #73818, #66645 ) ) ;
#91156=CARTESIAN_POINT ( 'NONE',  ( -23.10650858598700452, 303.3356527799805917, -9.896241053147848632 ) ) ;
#91160=CARTESIAN_POINT ( 'NONE',  ( -38.81358894279936322, 485.1131561813189705, -4.191378885295510948 ) ) ;
#91161=EDGE_CURVE ( 'NONE', #22579, #54135, #37972, .T. ) ;
#91162=CARTESIAN_POINT ( 'NONE',  ( -40.95806866577292027, 396.9764538775766596, 27.65151128674859393 ) ) ;
#91178=CARTESIAN_POINT ( 'NONE',  ( -32.93513049338655918, 465.6726574193328929, 10.66039033145153425 ) ) ;
#91198=EDGE_CURVE ( 'NONE', #71461, #100372, #39654, .T. ) ;
#91205=VERTEX_POINT ( 'NONE', #36944 ) ;
#91212=CARTESIAN_POINT ( 'NONE',  ( -43.89279753500660064, 435.4168038201347599, 16.20034641759655258 ) ) ;
#91213=CARTESIAN_POINT ( 'NONE',  ( 35.44563196690202744, 355.0508310518326311, 1.542887188955126110 ) ) ;
#91214=CARTESIAN_POINT ( 'NONE',  ( 39.86761651079377344, 459.8416857619859570, 1.882458089123050904 ) ) ;
#91215=CARTESIAN_POINT ( 'NONE',  ( -35.45036406932369033, 436.3203772529674893, 5.179456583041581297 ) ) ;
#91221=CARTESIAN_POINT ( 'NONE',  ( -43.63899620156483650, 434.3182181978405652, 14.37213632273153330 ) ) ;
#91223=ORIENTED_EDGE ( 'NONE', *, *, #22137, .F. ) ;
#91227=ORIENTED_EDGE ( 'NONE', *, *, #61755, .F. ) ;
#91228=CARTESIAN_POINT ( 'NONE',  ( -19.83463548332443338, 303.8035096162418540, 9.926734387303303819 ) ) ;
#91231=CARTESIAN_POINT ( 'NONE',  ( 43.33854370778465182, 463.6229669622573510, 5.371557844377655933 ) ) ;
#91246=CARTESIAN_POINT ( 'NONE',  ( -20.17756551592432501, 302.8253764644770172, 1.931382329378721119 ) ) ;
#91263=EDGE_LOOP ( 'NONE', ( #52888, #49279, #31469, #99588 ) ) ;
#91264=CARTESIAN_POINT ( 'NONE',  ( 43.72886361455203996, 434.3043191536616519, 13.94145212282615631 ) ) ;
#91267=ORIENTED_EDGE ( 'NONE', *, *, #9971, .T. ) ;
#91269=CARTESIAN_POINT ( 'NONE',  ( 27.18908553330205180, 296.5274986157688772, 10.30015177545897842 ) ) ;
#91272=CARTESIAN_POINT ( 'NONE',  ( -43.03894652950290123, 464.9992092536287487, 11.55502599541316044 ) ) ;
#91275=CARTESIAN_POINT ( 'NONE',  ( -30.96044075740587331, 348.7637019778929357, 19.04753708084649233 ) ) ;
#91287=CARTESIAN_POINT ( 'NONE',  ( 28.53554096041415988, 313.9464476106043662, 12.39025823560460537 ) ) ;
#91304=CARTESIAN_POINT ( 'NONE',  ( -32.97750030479636507, 361.8904936952960725, 22.71549378251080853 ) ) ;
#91305=CARTESIAN_POINT ( 'NONE',  ( -32.81992448453860334, 465.7192846569213884, 11.17271167765305862 ) ) ;
#91314=CARTESIAN_POINT ( 'NONE',  ( 16.51330895492884210, 294.5655680487705013, -2.060813375747557075 ) ) ;
#91338=CARTESIAN_POINT ( 'NONE',  ( 19.70764564238371719, 304.7954121406193622, 9.925013215726785631 ) ) ;
#91339=CARTESIAN_POINT ( 'NONE',  ( -37.51854390953261742, 313.5286481325095451, 14.45587837336505999 ) ) ;
#91342=CARTESIAN_POINT ( 'NONE',  ( 25.61872641138599604, 306.5028686783192029, -9.638171963028243638 ) ) ;
#91354=EDGE_CURVE ( 'NONE', #23483, #90700, #14797, .T. ) ;
#91382=CARTESIAN_POINT ( 'NONE',  ( 26.02261751055236516, 306.8105359686700808, -8.568281061380174535 ) ) ;
#91383=ORIENTED_EDGE ( 'NONE', *, *, #59880, .F. ) ;
#91385=AXIS2_PLACEMENT_3D ( 'NONE', #105579, #32245, #80768 ) ;
#91390=CARTESIAN_POINT ( 'NONE',  ( -9.970195021759465703, 302.6460196488380348, -10.04373974541435466 ) ) ;
#91397=CARTESIAN_POINT ( 'NONE',  ( 32.22120753352737665, 464.6691781026588046, 10.60621122532779026 ) ) ;
#91399=CARTESIAN_POINT ( 'NONE',  ( 40.96815392870802697, 488.3809129049201374, 10.59964723858293745 ) ) ;
#91406=ORIENTED_EDGE ( 'NONE', *, *, #41679, .T. ) ;
#91408=FILL_AREA_STYLE ('',( #101076 ) ) ;
#91412=CARTESIAN_POINT ( 'NONE',  ( -32.43729139937729400, 312.3396530769931019, -7.763169779620859856 ) ) ;
#91425=B_SPLINE_CURVE_WITH_KNOTS ( 'NONE', 3,
 ( #85353, #2283, #77262, #35232 ),
 .UNSPECIFIED., .F., .F.,
 ( 4, 4 ),
 ( 0.000000000000000000, 0.0002604505668081740334 ),
 .UNSPECIFIED. ) ;
#91436=CARTESIAN_POINT ( 'NONE',  ( -34.79468063549888512, 490.6633164237441633, 11.75004032470205395 ) ) ;
#91470=( BOUNDED_SURFACE ( )  B_SPLINE_SURFACE ( 3, 2, ( 
 ( #102762, #69349, #45603 ),
 ( #2456, #28377, #61253 ),
 ( #44537, #27860, #85527 ),
 ( #60728, #61800, #53672 ) ),
 .UNSPECIFIED., .F., .F., .F. ) 
 B_SPLINE_SURFACE_WITH_KNOTS ( ( 4, 4 ),
 ( 3, 3 ),
 ( 0.05627786335318932243, 0.08234838753898729435 ),
 ( 0.000000000000000000, 0.6299190952401180210 ),
 .UNSPECIFIED. ) 
 GEOMETRIC_REPRESENTATION_ITEM ( )  RATIONAL_B_SPLINE_SURFACE ( (
 ( 1.000000000000000000, 0.8155006124047963212, 0.8634405994222458247),
 ( 1.000000000000000000, 0.8155002931124427645, 0.8634403630942395491),
 ( 1.000000000000000000, 0.8155003711612234252, 0.8634404208629662403),
 ( 1.000000000000000000, 0.8155006853121260502, 0.8634406533854668275) ) ) 
 REPRESENTATION_ITEM ( '' )  SURFACE ( )  );
#91478=CARTESIAN_POINT ( 'NONE',  ( 26.93224738266096097, 304.9750774871889689, -9.533213446127941637 ) ) ;
#91482=CARTESIAN_POINT ( 'NONE',  ( -43.27530345108696963, 461.7562057072040034, 3.870800370039641169 ) ) ;
#91490=CARTESIAN_POINT ( 'NONE',  ( 45.49126702261580135, 409.1826088023510124, 8.336894800179337039 ) ) ;
#91503=CARTESIAN_POINT ( 'NONE',  ( 43.65107446674234382, 435.6495114220916207, 9.088599805106140295 ) ) ;
#91512=CARTESIAN_POINT ( 'NONE',  ( 51.01037695545453232, 500.0000000000002274, -5.000000000000001776 ) ) ;
#91514=SURFACE_SIDE_STYLE ('',( #76366 ) ) ;
#91516=CARTESIAN_POINT ( 'NONE',  ( 26.54817876223620488, 310.6276912632132507, 11.31208242866018132 ) ) ;
#91519=CARTESIAN_POINT ( 'NONE',  ( -32.04667661469866147, 487.4982811826213833, 8.072210805887316099 ) ) ;
#91524=CARTESIAN_POINT ( 'NONE',  ( -43.00000000000000000, 438.3878896346931242, 16.22878885428556472 ) ) ;
#91527=DIRECTION ( 'NONE',  ( 0.000000000000000000, 0.000000000000000000, 1.000000000000000000 ) ) ;
#91529=CARTESIAN_POINT ( 'NONE',  ( -31.92839208162568454, 356.8913991353554138, 21.71261904506107143 ) ) ;
#91550=CARTESIAN_POINT ( 'NONE',  ( 26.71565930479108530, 306.5341601446122581, 10.78094868360216196 ) ) ;
#91553=CARTESIAN_POINT ( 'NONE',  ( -40.18832759596268289, 460.7626523741620872, 2.139563623142588966 ) ) ;
#91554=CARTESIAN_POINT ( 'NONE',  ( 30.33571977314562673, 298.1669207346403709, 2.668496471951124160 ) ) ;
#91560=CARTESIAN_POINT ( 'NONE',  ( -28.51914334966707543, 297.3191045173070393, 10.47832804806128060 ) ) ;
#91567=CARTESIAN_POINT ( 'NONE',  ( 8.730595983954971828, 295.2524660276815780, 4.886029594169265522 ) ) ;
#91587=CARTESIAN_POINT ( 'NONE',  ( -36.14965894305860417, 491.8061723310894990, 12.56429772144753443 ) ) ;
#91589=DIRECTION ( 'NONE',  ( -0.3845251595719093585, 0.02506431005095593675, 0.9227741771516296820 ) ) ;
#91598=CARTESIAN_POINT ( 'NONE',  ( 37.54559764570182523, 464.1143081516207189, 19.43664670202678835 ) ) ;
#91614=CARTESIAN_POINT ( 'NONE',  ( 0.000000000000000000, 294.8518027762758038, -10.00000000000000178 ) ) ;
#91617=EDGE_CURVE ( 'NONE', #45028, #23591, #89597, .T. ) ;
#91620=CARTESIAN_POINT ( 'NONE',  ( 30.19392226039637350, 332.6110142126161691, 15.69272685516405907 ) ) ;
#91629=CARTESIAN_POINT ( 'NONE',  ( -44.11327388758650159, 464.4313852428384735, 9.822198357558047377 ) ) ;
#91630=CARTESIAN_POINT ( 'NONE',  ( -31.02212611900126760, 360.5725590293961318, 22.12937154125974715 ) ) ;
#91638=CARTESIAN_POINT ( 'NONE',  ( -6.145867760194407836, 301.8770827788611086, -10.02048593162379042 ) ) ;
#91640=VERTEX_POINT ( 'NONE', #103637 ) ;
#91646=CARTESIAN_POINT ( 'NONE',  ( -19.22284019411856804, 302.7169880953082952, 9.908343670167209183 ) ) ;
#91649=CARTESIAN_POINT ( 'NONE',  ( 43.69697758767897966, 434.4335448986662982, 11.30914782516539674 ) ) ;
#91668=CARTESIAN_POINT ( 'NONE',  ( 34.87165355513719334, 435.0272833139666773, 7.833813470889964492 ) ) ;
#91671=CARTESIAN_POINT ( 'NONE',  ( -34.13897275411324017, 489.1603865320491309, 11.37941925714664926 ) ) ;
#91673=VERTEX_POINT ( 'NONE', #52422 ) ;
#91675=CARTESIAN_POINT ( 'NONE',  ( -27.31158286324798468, 296.2711421484885363, -9.693697505745531018 ) ) ;
#91677=AXIS2_PLACEMENT_3D ( 'NONE', #71574, #81254, #97984 ) ;
#91679=CARTESIAN_POINT ( 'NONE',  ( -36.02691569689581286, 484.4775272227933556, -2.201217060995769526 ) ) ;
#91680=CARTESIAN_POINT ( 'NONE',  ( -42.78195672996899646, 397.2058786343547467, 19.86382575910961990 ) ) ;
#91697=CARTESIAN_POINT ( 'NONE',  ( -32.93681933015854213, 464.9081438945292462, 10.83352224627681970 ) ) ;
#91707=CARTESIAN_POINT ( 'NONE',  ( 46.00000000000000000, 500.0000000000002274, 5.000000000000001776 ) ) ;
#91726=B_SPLINE_CURVE_WITH_KNOTS ( 'NONE', 3,
 ( #24919, #26013, #97706, #50740, #23871, #33538, #83646, #574 ),
 .UNSPECIFIED., .F., .F.,
 ( 4, 2, 2, 4 ),
 ( 0.000000000000000000, 0.002020203531082300028, 0.003030305296623449392, 0.004040407062164599189 ),
 .UNSPECIFIED. ) ;
#91731=CARTESIAN_POINT ( 'NONE',  ( -13.48662581987258946, 304.5494697335691967, -9.064266068579863500 ) ) ;
#91732=CARTESIAN_POINT ( 'NONE',  ( 22.18906107735381283, 305.1406206946286943, -9.938500898754245583 ) ) ;
#91735=CARTESIAN_POINT ( 'NONE',  ( 29.99999999996260058, 488.4118811724847546, 8.310946025480145494 ) ) ;
#91744=ORIENTED_EDGE ( 'NONE', *, *, #2015, .T. ) ;
#91750=CARTESIAN_POINT ( 'NONE',  ( 43.55305824496269906, 463.9995833982595741, 6.100617664814004470 ) ) ;
#91774=CARTESIAN_POINT ( 'NONE',  ( -21.25502769577498796, 305.0480251235313176, 9.978840188629131802 ) ) ;
#91775=CYLINDRICAL_SURFACE ( 'NONE', #105354, 5.000000000000000888 ) ;
#91785=CARTESIAN_POINT ( 'NONE',  ( 43.81062608880509401, 434.3289934330969686, 12.63519120572941823 ) ) ;
#91796=CARTESIAN_POINT ( 'NONE',  ( 42.99999999999999289, 464.8825480873695710, 15.07585856869433272 ) ) ;
#91807=CARTESIAN_POINT ( 'NONE',  ( 42.79891897446039906, 462.9518546951013604, 4.196605471998886117 ) ) ;
#91808=CARTESIAN_POINT ( 'NONE',  ( 23.38792459703088156, 304.7436589798348905, 10.13094752528676068 ) ) ;
#91820=FACE_BOUND ( 'NONE', #46355, .T. ) ;
#91822=CARTESIAN_POINT ( 'NONE',  ( -32.87491876135755575, 485.1684955303235824, 5.618973769089859793 ) ) ;
#91828=CARTESIAN_POINT ( 'NONE',  ( -22.86828579430564545, 303.4455862872093235, 10.06510526139748585 ) ) ;
#91834=CARTESIAN_POINT ( 'NONE',  ( -41.14856704871675674, 488.9704688040295650, 10.18682326004923056 ) ) ;
#91836=CARTESIAN_POINT ( 'NONE',  ( 40.91005831554789296, 436.7586844285373218, 21.64591360582873492 ) ) ;
#91849=CARTESIAN_POINT ( 'NONE',  ( 18.39953584734496062, 302.6496520256866916, 9.894388632544812268 ) ) ;
#91857=ORIENTED_EDGE ( 'NONE', *, *, #99905, .F. ) ;
#91868=CARTESIAN_POINT ( 'NONE',  ( 23.21947149027727875, 295.1914306511582708, 2.010027678589071165 ) ) ;
#91884=DIRECTION ( 'NONE',  ( -0.2908996821262230803, -0.5336441332596660869, -0.7941040951766978884 ) ) ;
#91900=CARTESIAN_POINT ( 'NONE',  ( 23.77225596033269284, 305.6233131784293846, -8.833847462781667659 ) ) ;
#91910=CARTESIAN_POINT ( 'NONE',  ( -36.69951191943324176, 463.3005535825507764, 20.13750663043760625 ) ) ;
#91914=CARTESIAN_POINT ( 'NONE',  ( 32.14710229350392012, 464.7836479068001267, 11.45504703818881609 ) ) ;
#91915=CARTESIAN_POINT ( 'NONE',  ( 41.58908019493944863, 487.6887286007225271, 9.912025820237996498 ) ) ;
#91919=ADVANCED_FACE ( 'NONE', ( #63732 ), #90639, .T. ) ;
#91921=VERTEX_POINT ( 'NONE', #25959 ) ;
#91924=PRESENTATION_STYLE_ASSIGNMENT (( #58503 ) ) ;
#91928=CARTESIAN_POINT ( 'NONE',  ( -37.17110534794960586, 304.2510796055892115, -7.844238214609251969 ) ) ;
#91929=CARTESIAN_POINT ( 'NONE',  ( -6.779925268006731898, 303.7378072031825127, -10.02423307061381230 ) ) ;
#91930=ORIENTED_EDGE ( 'NONE', *, *, #39752, .F. ) ;
#91931=CARTESIAN_POINT ( 'NONE',  ( -43.74985542820359541, 435.5770091380368854, 16.96136490515567985 ) ) ;
#91940=ORIENTED_EDGE ( 'NONE', *, *, #40871, .T. ) ;
#91984=CARTESIAN_POINT ( 'NONE',  ( 33.76105693399937024, 471.3091059247025782, 5.717665057388511940 ) ) ;
#91992=CARTESIAN_POINT ( 'NONE',  ( 34.45135090351298146, 300.8539718218502230, -8.652709364234928202 ) ) ;
#91995=CARTESIAN_POINT ( 'NONE',  ( 32.11957450231073352, 486.1307089099603331, 5.366351229209024076 ) ) ;
#92005=CARTESIAN_POINT ( 'NONE',  ( 37.63246688678780316, 374.2349153975987406, 4.690254487569156083 ) ) ;
#92008=CARTESIAN_POINT ( 'NONE',  ( -19.73463816634110302, 304.7971333121958537, 8.925379062039136002 ) ) ;
#92012=CARTESIAN_POINT ( 'NONE',  ( 32.62137895416793043, 486.7356100975906088, 7.182248123802368767 ) ) ;
#92016=CARTESIAN_POINT ( 'NONE',  ( 46.00000000005143619, 436.1645721954917576, 9.605727516982005554 ) ) ;
#92023=FACE_OUTER_BOUND ( 'NONE', #60328, .T. ) ;
#92029=FACE_OUTER_BOUND ( 'NONE', #53986, .T. ) ;
#92031=CARTESIAN_POINT ( 'NONE',  ( 31.00389226249483698, 502.9289871839745842, 8.047326149841639520 ) ) ;
#92034=CARTESIAN_POINT ( 'NONE',  ( -33.52002750074903759, 462.9426806248537218, 5.597136840648579970 ) ) ;
#92044=CARTESIAN_POINT ( 'NONE',  ( -29.60389654270521476, 319.5417381178118603, 13.79948592438576149 ) ) ;
#92057=CARTESIAN_POINT ( 'NONE',  ( 33.04853154822865235, 439.4047662902921729, 23.83380291423624797 ) ) ;
#92060=CARTESIAN_POINT ( 'NONE',  ( 32.73569771302867792, 300.2484905015194840, 3.150108463464334818 ) ) ;
#92070=CARTESIAN_POINT ( 'NONE',  ( -28.98553719038945431, 297.3123734288306537, 2.475459991885067712 ) ) ;
#92071=CARTESIAN_POINT ( 'NONE',  ( 30.00000000000000000, 450.0000000000002274, 13.20242257375370976 ) ) ;
#92088=( BOUNDED_SURFACE ( )  B_SPLINE_SURFACE ( 3, 2, ( 
 ( #583, #33548, #41091 ),
 ( #75029, #98777, #66419 ),
 ( #34100, #58883, #7637 ),
 ( #73973, #99304, #106331 ) ),
 .UNSPECIFIED., .F., .F., .F. ) 
 B_SPLINE_SURFACE_WITH_KNOTS ( ( 4, 4 ),
 ( 3, 3 ),
 ( 0.01401837328402458401, 0.01447126798403815945 ),
 ( 0.000000000000000000, 0.8297957905794470790 ),
 .UNSPECIFIED. ) 
 GEOMETRIC_REPRESENTATION_ITEM ( )  RATIONAL_B_SPLINE_SURFACE ( (
 ( 1.000000000000000000, 0.7688303398187896764, 0.9213079014936784716),
 ( 1.000000000000000000, 0.7649186838476292882, 0.9199763408694854316),
 ( 1.000000000000000000, 0.7609618042714275665, 0.9186293857494058912),
 ( 1.000000000000000000, 0.7569584399386413143, 0.9172666068268371387) ) ) 
 REPRESENTATION_ITEM ( '' )  SURFACE ( )  );
#92092=CARTESIAN_POINT ( 'NONE',  ( 34.99305553442271588, 490.1715275948229191, 12.08183789492280091 ) ) ;
#92096=CARTESIAN_POINT ( 'NONE',  ( 42.42823000592811411, 488.6172904996860211, 9.782215989753083818 ) ) ;
#92112=CARTESIAN_POINT ( 'NONE',  ( -36.64823341582351901, 437.5392299810053487, 4.281405873620232505 ) ) ;
#92116=CARTESIAN_POINT ( 'NONE',  ( 33.97359119245064818, 434.1099241184709285, 11.80501937577160732 ) ) ;
#92120=CARTESIAN_POINT ( 'NONE',  ( -0.5741732275940398811, 294.8518027760915743, -9.999999999999998224 ) ) ;
#92124=EDGE_LOOP ( 'NONE', ( #25062, #49239, #62708, #88070 ) ) ;
#92126=EDGE_LOOP ( 'NONE', ( #44728, #9399, #67134, #11113 ) ) ;
#92127=CARTESIAN_POINT ( 'NONE',  ( 32.14107381401169050, 425.0973432859777859, 24.99338633512491370 ) ) ;
#92137=CARTESIAN_POINT ( 'NONE',  ( -31.21759734847655210, 387.2566916973277671, 24.99345285570965913 ) ) ;
#92138=CARTESIAN_POINT ( 'NONE',  ( 38.83523057582821281, 469.0589752947456077, 0.4593318232150862546 ) ) ;
#92139=VECTOR ( 'NONE', #20884, 1000.000000000000000 ) ;
#92144=ORIENTED_EDGE ( 'NONE', *, *, #11892, .F. ) ;
#92165=CARTESIAN_POINT ( 'NONE',  ( -46.00000000000000711, 435.9790741282528188, 14.35705232862668623 ) ) ;
#92173=CARTESIAN_POINT ( 'NONE',  ( 32.70807617001185008, 465.7746982375700782, 13.85399747858312836 ) ) ;
#92174=CARTESIAN_POINT ( 'NONE',  ( -25.02938502635939244, 306.2014514788868382, -8.705669254435044024 ) ) ;
#92177=CIRCLE ( 'NONE', #81850, 1.000000000000000222 ) ;
#92185=CARTESIAN_POINT ( 'NONE',  ( -34.22920647855479359, 485.0586030974572509, -1.445294392290342733 ) ) ;
#92186=CARTESIAN_POINT ( 'NONE',  ( -33.08708714024299979, 372.5548079963469377, 24.04571688234041815 ) ) ;
#92198=CARTESIAN_POINT ( 'NONE',  ( 1.288479777019286136E-15, 37.86482112153537116, 10.52123582012687919 ) ) ;
#92200=CARTESIAN_POINT ( 'NONE',  ( 43.26971690803010517, 435.9072580013536822, 8.039630127099059109 ) ) ;
#92219=AXIS2_PLACEMENT_3D ( 'NONE', #99355, #76159, #59476 ) ;
#92220=CARTESIAN_POINT ( 'NONE',  ( -40.05599234025955013, 464.9362105862702492, 17.76115130056741265 ) ) ;
#92228=ADVANCED_FACE ( 'NONE', ( #102987 ), #70817, .T. ) ;
#92235=CARTESIAN_POINT ( 'NONE',  ( 31.21933008645656926, 405.2090764464551853, 25.56980379099173817 ) ) ;
#92236=CARTESIAN_POINT ( 'NONE',  ( 40.42601080768203303, 460.8348341399792503, 2.184598410783125111 ) ) ;
#92241=ORIENTED_EDGE ( 'NONE', *, *, #81449, .F. ) ;
#92245=ADVANCED_FACE ( 'NONE', ( #33850 ), #15701, .T. ) ;
#92278=CARTESIAN_POINT ( 'NONE',  ( -24.93816302196866275, 307.4233949143036284, 10.52291764336465008 ) ) ;
#92289=ORIENTED_EDGE ( 'NONE', *, *, #13613, .T. ) ;
#92294=FACE_OUTER_BOUND ( 'NONE', #106620, .T. ) ;
#92303=FACE_OUTER_BOUND ( 'NONE', #78850, .T. ) ;
#92311=CARTESIAN_POINT ( 'NONE',  ( 34.62919541716566840, 437.4394979580218319, 4.999019296794181777 ) ) ;
#92317=CARTESIAN_POINT ( 'NONE',  ( 28.84740160328638225, 315.3509136110029658, 12.74594617175954703 ) ) ;
#92321=CARTESIAN_POINT ( 'NONE',  ( 30.00000000000000000, 461.8802764867031669, 14.89328939272360053 ) ) ;
#92329=ADVANCED_FACE ( 'NONE', ( #36484 ), #48772, .F. ) ;
#92334=DIRECTION ( 'NONE',  ( 0.2271661929662003865, 0.3956501727921482581, 0.8898631701238041147 ) ) ;
#92339=CARTESIAN_POINT ( 'NONE',  ( -31.33955551928141503, 325.4742652106692731, 15.49549166411432921 ) ) ;
#92358=CARTESIAN_POINT ( 'NONE',  ( -32.02667885475513998, 464.8582969030198910, 12.88960884979827348 ) ) ;
#92359=CARTESIAN_POINT ( 'NONE',  ( -43.10371592039376054, 462.6168321841617512, 4.970041475410676313 ) ) ;
#92363=CARTESIAN_POINT ( 'NONE',  ( 31.73464696827581122, 436.7284713362857360, 21.10242107247917787 ) ) ;
#92377=( BOUNDED_SURFACE ( )  B_SPLINE_SURFACE ( 3, 2, ( 
 ( #93052, #92508, #18663 ),
 ( #52046, #47669, #88154 ),
 ( #71960, #102740, #70901 ),
 ( #70376, #22384, #28901 ),
 ( #39079, #38040, #69843 ),
 ( #36975, #55744, #96259 ),
 ( #6148, #63887, #54692 ),
 ( #104863, #20816, #87626 ),
 ( #29421, #103791, #47142 ),
 ( #104316, #103271, #61774 ),
 ( #21321, #5109, #53650 ),
 ( #31005, #86581, #4576 ),
 ( #45576, #13175, #12645 ),
 ( #30466, #55229, #96777 ),
 ( #22907, #29934, #14236 ),
 ( #80035, #37513, #88678 ),
 ( #14767, #80564, #94671 ),
 ( #78455, #62298, #63360 ),
 ( #95190, #13710, #62819 ),
 ( #54157, #95712, #87099 ),
 ( #21851, #46102, #78985 ),
 ( #46620, #79517, #5630 ),
 ( #38551, #71415, #89212 ),
 ( #15310, #48198, #98354 ),
 ( #97284, #33638, #23981 ),
 ( #40121, #7212, #64412 ),
 ( #81611, #48722, #49257 ),
 ( #73529, #72997, #8273 ),
 ( #57879, #90804, #25575 ),
 ( #7737, #105390, #24509 ),
 ( #81099, #98862, #105901 ),
 ( #49797, #89745, #72483 ),
 ( #41186, #106432, #152 ),
 ( #90265, #40647, #32590 ),
 ( #64931, #65462, #32052 ),
 ( #74597, #16921, #82701 ),
 ( #58433, #91342, #97816 ),
 ( #33119, #57344, #17457 ),
 ( #674, #8806, #41714 ),
 ( #50322, #66518, #16367 ),
 ( #6684, #99391, #39610 ),
 ( #56822, #31531, #82160 ),
 ( #15840, #74063, #23437 ),
 ( #56274, #65987, #25024 ) ),
 .UNSPECIFIED., .F., .F., .T. ) 
 B_SPLINE_SURFACE_WITH_KNOTS ( ( 4, 2, 2, 2, 2, 2, 2, 2, 2, 2, 2, 2, 2, 2, 2, 2, 2, 2, 2, 2, 2, 4 ),
 ( 3, 3 ),
 ( 0.05246299049208403426, 0.07033874506154716433, 0.08821449963101030134, 0.1060902542004734384, 0.1150281314852049930, 0.1239660087699365615, 0.1418417633393996846, 0.1597175179088628216, 0.1686553951935944040, 0.1731243338359601813, 0.1753588031571430839, 0.1775932724783259586, 0.1820622111206917360, 0.1831794457812832011, 0.1842966804418746385, 0.1865311497630575133, 0.1876483844236489507, 0.1887656190842404158, 0.1898828537448318809, 0.1910000884054233183, 0.1932345577266061931, 0.1954690270477890957 ),
 ( 0.000000000000000000, 1.000000000000000000 ),
 .UNSPECIFIED. ) 
 GEOMETRIC_REPRESENTATION_ITEM ( )  RATIONAL_B_SPLINE_SURFACE ( (
 ( 1.000000000000000000, 0.7071066982776790244, 1.000000000000000000),
 ( 1.000000000000000000, 0.7071066246860953086, 1.000000000000000000),
 ( 1.000000000000000000, 0.7071067817483319695, 1.000000000000000000),
 ( 1.000000000000000000, 0.7071067817483319695, 1.000000000000000000),
 ( 1.000000000000000000, 0.7071067820003403837, 1.000000000000000000),
 ( 1.000000000000000000, 0.7071067820003403837, 1.000000000000000000),
 ( 1.000000000000000000, 0.7071085911072407804, 1.000000000000000000),
 ( 1.000000000000000000, 0.7071090165955132845, 1.000000000000000000),
 ( 1.000000000000000000, 0.7071082982937503258, 1.000000000000000000),
 ( 1.000000000000000000, 0.7071068030320751818, 1.000000000000000000),
 ( 1.000000000000000000, 0.7071066538725350181, 1.000000000000000000),
 ( 1.000000000000000000, 0.7071092477002908216, 1.000000000000000000),
 ( 1.000000000000000000, 0.7071091921374882405, 1.000000000000000000),
 ( 1.000000000000000000, 0.7071056146855209112, 1.000000000000000000),
 ( 1.000000000000000000, 0.7070854685221523717, 1.000000000000000000),
 ( 1.000000000000000000, 0.7071229475123441688, 1.000000000000000000),
 ( 1.000000000000000000, 0.7071321772062534317, 1.000000000000000000),
 ( 1.000000000000000000, 0.7071076013889080469, 1.000000000000000000),
 ( 1.000000000000000000, 0.7071078047556201840, 1.000000000000000000),
 ( 1.000000000000000000, 0.7071116805962889273, 1.000000000000000000),
 ( 1.000000000000000000, 0.7071114737089826408, 1.000000000000000000),
 ( 1.000000000000000000, 0.7071088341742440830, 1.000000000000000000),
 ( 1.000000000000000000, 0.7071030604351956628, 1.000000000000000000),
 ( 1.000000000000000000, 0.7071149245157897223, 1.000000000000000000),
 ( 1.000000000000000000, 0.7072266118915774280, 1.000000000000000000),
 ( 1.000000000000000000, 0.7071506248185068788, 1.000000000000000000),
 ( 1.000000000000000000, 0.7071307950262011310, 1.000000000000000000),
 ( 1.000000000000000000, 0.7071052445289376376, 1.000000000000000000),
 ( 1.000000000000000000, 0.7071065825907152380, 1.000000000000000000),
 ( 1.000000000000000000, 0.7071121758606627727, 1.000000000000000000),
 ( 1.000000000000000000, 0.7071099217218235200, 1.000000000000000000),
 ( 1.000000000000000000, 0.7071058422322067383, 1.000000000000000000),
 ( 1.000000000000000000, 0.7071037979643884919, 1.000000000000000000),
 ( 1.000000000000000000, 0.7070993061526186230, 1.000000000000000000),
 ( 1.000000000000000000, 0.7070996420988305831, 1.000000000000000000),
 ( 1.000000000000000000, 0.7071045601661539726, 1.000000000000000000),
 ( 1.000000000000000000, 0.7071036778919828070, 1.000000000000000000),
 ( 1.000000000000000000, 0.7071145233811817477, 1.000000000000000000),
 ( 1.000000000000000000, 0.7071234056344251062, 1.000000000000000000),
 ( 1.000000000000000000, 0.7071224454176588958, 1.000000000000000000),
 ( 1.000000000000000000, 0.7071033992339055274, 1.000000000000000000),
 ( 1.000000000000000000, 0.7071405256055924848, 1.000000000000000000),
 ( 1.000000000000000000, 0.7071192080192385543, 1.000000000000000000),
 ( 1.000000000000000000, 0.7071067811865661135, 1.000000000000000000) ) ) 
 REPRESENTATION_ITEM ( '' )  SURFACE ( )  );
#92385=DIRECTION ( 'NONE',  ( 0.000000000000000000, 0.000000000000000000, -1.000000000000000000 ) ) ;
#92401=ORIENTED_EDGE ( 'NONE', *, *, #65298, .F. ) ;
#92420=ORIENTED_EDGE ( 'NONE', *, *, #17963, .T. ) ;
#92423=CARTESIAN_POINT ( 'NONE',  ( 16.12042885873492892, 302.5603998061997686, -10.06194182264846049 ) ) ;
#92424=CARTESIAN_POINT ( 'NONE',  ( -19.59509420870743668, 302.7300561768714147, -10.02587803886942197 ) ) ;
#92427=CARTESIAN_POINT ( 'NONE',  ( -37.31409640255164106, 464.0485063763171638, 19.52659819501306160 ) ) ;
#92434=ORIENTED_EDGE ( 'NONE', *, *, #3504, .T. ) ;
#92437=EDGE_LOOP ( 'NONE', ( #57138, #102494, #6109, #52846, #38256 ) ) ;
#92445=CARTESIAN_POINT ( 'NONE',  ( -39.80034396060564461, 313.8274241824321962, 2.558633328708789012 ) ) ;
#92465=DIRECTION ( 'NONE',  ( 0.000000000000000000, 0.000000000000000000, -1.000000000000000000 ) ) ;
#92482=CARTESIAN_POINT ( 'NONE',  ( -37.71459991402551282, 437.7716825518406836, 4.505118785440030749 ) ) ;
#92487=CARTESIAN_POINT ( 'NONE',  ( 32.94331731755185189, 463.6330061646623335, 6.942105804440950045 ) ) ;
#92491=B_SPLINE_CURVE_WITH_KNOTS ( 'NONE', 3,
 ( #41676, #74566, #639, #66479, #25538, #42203, #75086, #28196, #93430, #19583, #28722, #44886, #61065, #54520, #102032, #38392, #69162, #12480, #85330, #93959, #13008, #85884, #87464, #13543, #46461, #70205, #86938, #21170, #45934, #94501 ),
 .UNSPECIFIED., .F., .F.,
 ( 4, 2, 2, 2, 2, 2, 2, 2, 2, 2, 2, 2, 2, 2, 4 ),
 ( 0.000000000000000000, 0.0004909127471943187113, 0.0009818254943886374226, 0.001963650988777274845, 0.002945476483165912918, 0.003927301977554550558, 0.005890952966331935124, 0.007854603955109319691, 0.008836429449498011540, 0.009818254943886705124, 0.01178190593266408882, 0.01276373142705274771, 0.01374555692144140487, 0.01472738241583006549, 0.01570920791021872265 ),
 .UNSPECIFIED. ) ;
#92501=CARTESIAN_POINT ( 'NONE',  ( -44.03654441204246694, 435.3114017552750852, 15.42721916006553684 ) ) ;
#92508=CARTESIAN_POINT ( 'NONE',  ( 35.67188573693742626, 438.4052817328919787, 3.942852940163526831 ) ) ;
#92511=CARTESIAN_POINT ( 'NONE',  ( 32.42646496125431099, 485.5066083816492437, 3.829258843081624786 ) ) ;
#92512=CARTESIAN_POINT ( 'NONE',  ( -36.34772026823453928, 305.6056078828891032, 4.444403256936394264 ) ) ;
#92521=CARTESIAN_POINT ( 'NONE',  ( 45.49982102694234953, 388.3127959276886827, 7.886590035822850453 ) ) ;
#92529=AXIS2_PLACEMENT_3D ( 'NONE', #88108, #87579, #52140 ) ;
#92535=CARTESIAN_POINT ( 'NONE',  ( -42.61140200160144786, 465.9030374194822457, 13.21253569360411895 ) ) ;
#92537=CARTESIAN_POINT ( 'NONE',  ( 43.03357534759653902, 463.2291678140142608, 4.675918524165878054 ) ) ;
#92545=CARTESIAN_POINT ( 'NONE',  ( 32.68130198256140062, 486.6487900980583845, 8.407187415474162151 ) ) ;
#92548=B_SPLINE_CURVE_WITH_KNOTS ( 'NONE', 3,
 ( #93862, #94941, #12390, #21593, #5887, #45318, #54967, #87896, #69067, #78200, #103021, #29176 ),
 .UNSPECIFIED., .F., .F.,
 ( 4, 2, 2, 2, 2, 4 ),
 ( 5.851754814686364485E-16, 0.001874863313077309570, 0.003749726626154033671, 0.004687158282692394096, 0.005624589939230754954, 0.007499453252307401209 ),
 .UNSPECIFIED. ) ;
#92555=CARTESIAN_POINT ( 'NONE',  ( 37.61445974613948806, 372.0213524726607943, 4.443563355633848744 ) ) ;
#92558=DIRECTION ( 'NONE',  ( 0.000000000000000000, 0.000000000000000000, -1.000000000000000000 ) ) ;
#92562=CARTESIAN_POINT ( 'NONE',  ( -43.71999369285486381, 463.9422086738335338, 7.488562083380655210 ) ) ;
#92565=CARTESIAN_POINT ( 'NONE',  ( -30.00000000000000355, 489.0575207958488591, 4.971052219119334481 ) ) ;
#92575=CARTESIAN_POINT ( 'NONE',  ( -25.97927592289829946, 307.2264714490293613, 10.71202005274685298 ) ) ;
#92584=CARTESIAN_POINT ( 'NONE',  ( -31.39564607133891982, 425.0048870508487084, 23.79503637330282828 ) ) ;
#92592=CARTESIAN_POINT ( 'NONE',  ( 32.36394494278211198, 300.7469127741676971, 11.27404243930863714 ) ) ;
#92598=CARTESIAN_POINT ( 'NONE',  ( 26.55368054879998141, 296.1687614156957693, 2.221803138960261492 ) ) ;
#92631=CARTESIAN_POINT ( 'NONE',  ( 9.797174393178839462E-16, 80.00000000000000000, 8.000000000000010658 ) ) ;
#92637=EDGE_CURVE ( 'NONE', #93970, #103206, #66014, .T. ) ;
#92644=CARTESIAN_POINT ( 'NONE',  ( 43.75401118688382951, 486.3173572309547694, 5.908089951475070656 ) ) ;
#92645=DIRECTION ( 'NONE',  ( 1.000000000000000000, 0.000000000000000000, 0.000000000000000000 ) ) ;
#92654=ORIENTED_EDGE ( 'NONE', *, *, #70852, .T. ) ;
#92655=CARTESIAN_POINT ( 'NONE',  ( -5.855865337385174563, 294.7602933681740183, -8.111083302970204301 ) ) ;
#92665=CARTESIAN_POINT ( 'NONE',  ( 25.56551311124981751, 308.5030443763377548, 10.78605441908344531 ) ) ;
#92672=CARTESIAN_POINT ( 'NONE',  ( 31.43619199075894244, 438.9212978929645033, 23.14895173483415292 ) ) ;
#92676=CARTESIAN_POINT ( 'NONE',  ( -23.96375140441108442, 306.3052962357393199, 10.25885168886986243 ) ) ;
#92700=ORIENTED_EDGE ( 'NONE', *, *, #90048, .T. ) ;
#92702=CARTESIAN_POINT ( 'NONE',  ( -46.00000000000000000, 437.8919113138612147, 12.69150955565185335 ) ) ;
#92703=CARTESIAN_POINT ( 'NONE',  ( -43.00000000000000000, 485.2629658518202405, -2.796394914059407100 ) ) ;
#92707=ORIENTED_EDGE ( 'NONE', *, *, #65588, .F. ) ;
#92713=CARTESIAN_POINT ( 'NONE',  ( -23.13382475031087537, 305.4031188766097671, -9.881612764625065992 ) ) ;
#92717=CARTESIAN_POINT ( 'NONE',  ( -43.63899620156475834, 434.3182181978404515, 14.37213632273176600 ) ) ;
#92727=CARTESIAN_POINT ( 'NONE',  ( -31.09395556286335704, 323.2306627077637700, 14.95105751057811538 ) ) ;
#92742=EDGE_LOOP ( 'NONE', ( #11945, #99344, #104788, #69222 ) ) ;
#92744=CARTESIAN_POINT ( 'NONE',  ( -32.17646412119415800, 464.6980787822275261, 10.84896803612779514 ) ) ;
#92757=CARTESIAN_POINT ( 'NONE',  ( 0.1244054282680990831, 295.1039052012444586, -9.999999999994756195 ) ) ;
#92758=CARTESIAN_POINT ( 'NONE',  ( 34.95237279327285762, 304.8277712208536627, 12.26231981495593537 ) ) ;
#92770=CARTESIAN_POINT ( 'NONE',  ( -44.29577627588397348, 464.1408972797700585, 8.778647706801374184 ) ) ;
#92780=CARTESIAN_POINT ( 'NONE',  ( 38.55382211449396834, 464.3891087764564531, 18.94281067283265330 ) ) ;
#92782=CARTESIAN_POINT ( 'NONE',  ( 39.83854393463795418, 460.2189570659127753, 2.210463671043265244 ) ) ;
#92786=ORIENTED_EDGE ( 'NONE', *, *, #21429, .F. ) ;
#92787=CARTESIAN_POINT ( 'NONE',  ( -44.49963734947764493, 484.8409368627554272, 4.258617019824068706 ) ) ;
#92793=CARTESIAN_POINT ( 'NONE',  ( 33.74271564777244237, 484.1802673187708592, 2.058285076122321922 ) ) ;
#92802=CLOSED_SHELL ( 'NONE', ( #39739, #67399, #87719, #79664, #81102, #20850, #91919, #17828 ) ) ;
#92804=EDGE_CURVE ( 'NONE', #91205, #26711, #13449, .T. ) ;
#92820=EDGE_CURVE ( 'NONE', #5324, #41809, #67431, .T. ) ;
#92829=CARTESIAN_POINT ( 'NONE',  ( -31.96724538747962896, 486.9512181893487082, 7.078368790597582283 ) ) ;
#92862=ORIENTED_EDGE ( 'NONE', *, *, #96316, .F. ) ;
#92867=CARTESIAN_POINT ( 'NONE',  ( -32.86259851300448531, 485.9239370913668381, 5.440925357813682695 ) ) ;
#92868=CARTESIAN_POINT ( 'NONE',  ( -31.86888217434299264, 485.1577972469723363, 5.527887721100189999 ) ) ;
#92900=CARTESIAN_POINT ( 'NONE',  ( 32.37381880833165582, 435.2096513840866692, 18.54399430281184635 ) ) ;
#92907=CARTESIAN_POINT ( 'NONE',  ( -45.29905483860081716, 480.9466865490944656, -2.171671249451534003 ) ) ;
#92945=DIRECTION ( 'NONE',  ( 0.000000000000000000, 0.8299985787540355986, -0.5577655056260480970 ) ) ;
#92978=CARTESIAN_POINT ( 'NONE',  ( 37.50059943756144776, 490.7879993827856993, 12.38039871356534505 ) ) ;
#92990=CARTESIAN_POINT ( 'NONE',  ( -32.71417592245104800, 313.0749680721571622, -7.579415757426488653 ) ) ;
#93000=DIRECTION ( 'NONE',  ( 0.000000000000000000, -0.9584033143583334802, 0.2854173908978941965 ) ) ;
#93022=CARTESIAN_POINT ( 'NONE',  ( -36.74148664940358344, 437.9559008978174575, 4.252305828303493129 ) ) ;
#93025=CARTESIAN_POINT ( 'NONE',  ( 33.78656477175017869, 463.8460037827032352, 7.347243016399514381 ) ) ;
#93026=ORIENTED_EDGE ( 'NONE', *, *, #17401, .F. ) ;
#93027=CARTESIAN_POINT ( 'NONE',  ( 43.63899620156485781, 434.3182181978398830, 14.37213632273147290 ) ) ;
#93030=( BOUNDED_SURFACE ( )  B_SPLINE_SURFACE ( 3, 2, ( 
 ( #66774, #25834, #75382 ),
 ( #2553, #85084, #100196 ),
 ( #17699, #51639, #10122 ),
 ( #68916, #27958, #60821 ) ),
 .UNSPECIFIED., .F., .F., .F. ) 
 B_SPLINE_SURFACE_WITH_KNOTS ( ( 4, 4 ),
 ( 3, 3 ),
 ( 0.05672608053137292994, 0.08145892399347254287 ),
 ( 0.3700819440699701923, 1.000000000000000000 ),
 .UNSPECIFIED. ) 
 GEOMETRIC_REPRESENTATION_ITEM ( )  RATIONAL_B_SPLINE_SURFACE ( (
 ( 0.8634409826472493332, 0.8155016482958543644, 1.000000000000000000),
 ( 0.8634411984245984328, 0.8155019398223021243, 1.000000000000000000),
 ( 0.8634411456911572635, 0.8155018685766739495, 1.000000000000000000),
 ( 0.8634409290728097819, 0.8155015759139936371, 1.000000000000000000) ) ) 
 REPRESENTATION_ITEM ( '' )  SURFACE ( )  );
#93051=ORIENTED_EDGE ( 'NONE', *, *, #74780, .T. ) ;
#93052=CARTESIAN_POINT ( 'NONE',  ( 36.64546344323804306, 438.4369965796255997, 4.168996892756918093 ) ) ;
#93054=CARTESIAN_POINT ( 'NONE',  ( -41.57463013743633695, 490.5138136697628397, 10.95472345905721312 ) ) ;
#93055=CARTESIAN_POINT ( 'NONE',  ( -40.35833863900601415, 321.1205797084799656, 8.337674143375151559 ) ) ;
#93056=CARTESIAN_POINT ( 'NONE',  ( -46.00000000000000000, 500.0000000000002274, 0.000000000000000000 ) ) ;
#93057=EDGE_LOOP ( 'NONE', ( #35856, #99893, #22795, #19890, #11837, #86763, #106649, #82348, #60977, #7385 ) ) ;
#93059=CARTESIAN_POINT ( 'NONE',  ( 39.41037217365025214, 489.7138547546053928, 11.67903818732042431 ) ) ;
#93061=DIRECTION ( 'NONE',  ( -0.2230022920435996703, -0.09894799074349024115, 0.9697831060969909212 ) ) ;
#93064=CARTESIAN_POINT ( 'NONE',  ( 44.66387834505498944, 341.6072687625629101, 1.189588019127773677 ) ) ;
#93065=EDGE_CURVE ( 'NONE', #66369, #66199, #40196, .T. ) ;
#93074=CARTESIAN_POINT ( 'NONE',  ( 34.04963612134775985, 317.5215674871631109, -6.459372692351979417 ) ) ;
#93075=CARTESIAN_POINT ( 'NONE',  ( 44.22225178598134931, 464.2590902508150066, 9.202154635662399329 ) ) ;
#93077=CARTESIAN_POINT ( 'NONE',  ( -32.70432414512315233, 489.1110749878013735, 10.33859015772251055 ) ) ;
#93078=CARTESIAN_POINT ( 'NONE',  ( 31.83648269796258390, 439.0038992192014575, 23.56519623501327132 ) ) ;
#93113=CARTESIAN_POINT ( 'NONE',  ( -25.12075135752968436, 306.0640628473120159, 10.43383969269943279 ) ) ;
#93114=VERTEX_POINT ( 'NONE', #38845 ) ;
#93118=CARTESIAN_POINT ( 'NONE',  ( -32.75517716563597048, 465.7432004789473012, 11.49884209862459095 ) ) ;
#93128=ORIENTED_EDGE ( 'NONE', *, *, #83066, .F. ) ;
#93133=CARTESIAN_POINT ( 'NONE',  ( 24.17442261560467287, 295.4908974038082761, 10.07402396700452663 ) ) ;
#93139=CARTESIAN_POINT ( 'NONE',  ( 31.26787864934703265, 298.8785962927613014, 2.831404287848908297 ) ) ;
#93149=CARTESIAN_POINT ( 'NONE',  ( -32.87547266101557852, 465.6993878536674742, 10.91512469976539279 ) ) ;
#93152=CARTESIAN_POINT ( 'NONE',  ( 45.99999999998675548, 464.1057728262775868, 11.12967041734905393 ) ) ;
#93154=ADVANCED_FACE ( 'NONE', ( #86873 ), #5451, .T. ) ;
#93172=CARTESIAN_POINT ( 'NONE',  ( 42.74220749418567777, 488.2672406020900553, 9.363116084196963840 ) ) ;
#93203=CARTESIAN_POINT ( 'NONE',  ( 24.50496542748491891, 306.8888831740973160, 10.39605820579407158 ) ) ;
#93226=CARTESIAN_POINT ( 'NONE',  ( -9.738398295829064466, 294.6500605438453704, -2.277702036900738136 ) ) ;
#93236=CARTESIAN_POINT ( 'NONE',  ( 43.78304604341470707, 434.3019790015191575, 13.50139152689089883 ) ) ;
#93252=CARTESIAN_POINT ( 'NONE',  ( 32.70943946516541700, 465.7622690753372581, 11.83845320050794925 ) ) ;
#93253=CARTESIAN_POINT ( 'NONE',  ( -24.16082351539475326, 304.6853429583268280, -9.820488471465781188 ) ) ;
#93257=CARTESIAN_POINT ( 'NONE',  ( -44.34415387544927256, 435.2422591719043226, 12.20585227837768016 ) ) ;
#93269=CARTESIAN_POINT ( 'NONE',  ( -38.54376935657065673, 311.7842164531986100, 5.990876337056916690 ) ) ;
#93284=EDGE_LOOP ( 'NONE', ( #38039, #78403, #88363, #34567 ) ) ;
#93300=CARTESIAN_POINT ( 'NONE',  ( 3.396983858748188645, 299.9646488655011467, -10.00714413801396319 ) ) ;
#93301=CARTESIAN_POINT ( 'NONE',  ( 44.66387834505498944, 341.6072687625629101, 1.189588019127773677 ) ) ;
#93305=VERTEX_POINT ( 'NONE', #40955 ) ;
#93306=CARTESIAN_POINT ( 'NONE',  ( -3.364021409948656505, 294.8518027753228807, 9.936999415087239385 ) ) ;
#93330=CARTESIAN_POINT ( 'NONE',  ( -43.62590748909082805, 434.3202425174551422, 14.43486319446150645 ) ) ;
#93355=ORIENTED_EDGE ( 'NONE', *, *, #21549, .T. ) ;
#93371=CARTESIAN_POINT ( 'NONE',  ( 20.52350613252515643, 304.8999024697870937, 9.947223320822450532 ) ) ;
#93372=( BOUNDED_SURFACE ( )  B_SPLINE_SURFACE ( 3, 2, ( 
 ( #12128, #69851, #17188 ),
 ( #27310, #50061, #77941 ),
 ( #101683, #28907, #82970 ),
 ( #60192, #61781, #94676 ),
 ( #60713, #9064, #93059 ),
 ( #20823, #41971, #74854 ),
 ( #938, #52055, #47148 ),
 ( #31013, #88158, #62826 ),
 ( #71964, #71418, #56281 ),
 ( #30469, #63364, #96781 ),
 ( #88683, #47673, #70907 ),
 ( #31538, #104869, #14776 ) ),
 .UNSPECIFIED., .F., .F., .F. ) 
 B_SPLINE_SURFACE_WITH_KNOTS ( ( 4, 2, 2, 2, 2, 4 ),
 ( 3, 3 ),
 ( 1.348747502571967516E-16, 0.001914430196850316597, 0.002871645295275407350, 0.003828860393700498320, 0.005743290590550680259, 0.007657720787400862199 ),
 ( 0.000000000000000000, 1.000000000000000000 ),
 .UNSPECIFIED. ) 
 GEOMETRIC_REPRESENTATION_ITEM ( )  RATIONAL_B_SPLINE_SURFACE ( (
 ( 1.000000000000000000, 0.8904848454312670469, 1.000000000000000000),
 ( 1.000000000000000000, 0.8829463934862813446, 1.000000000000000000),
 ( 1.000000000000000000, 0.8737071328057678388, 1.000000000000000000),
 ( 1.000000000000000000, 0.8579777217483747220, 1.000000000000000000),
 ( 1.000000000000000000, 0.8524208109141675482, 1.000000000000000000),
 ( 1.000000000000000000, 0.8407737293550452407, 1.000000000000000000),
 ( 1.000000000000000000, 0.8346659945390565438, 1.000000000000000000),
 ( 1.000000000000000000, 0.8160698933129009180, 1.000000000000000000),
 ( 1.000000000000000000, 0.8031929192457759603, 1.000000000000000000),
 ( 1.000000000000000000, 0.7775868725374718293, 1.000000000000000000),
 ( 1.000000000000000000, 0.7647656555784809740, 1.000000000000000000),
 ( 1.000000000000000000, 0.7533433155455216967, 1.000000000000000000) ) ) 
 REPRESENTATION_ITEM ( '' )  SURFACE ( )  );
#93381=CARTESIAN_POINT ( 'NONE',  ( -31.96903519139038963, 486.7815514870781044, 6.755070114922749447 ) ) ;
#93384=B_SPLINE_CURVE_WITH_KNOTS ( 'NONE', 3,
 ( #10634, #52693, #102316, #85620, #2549, #19336, #11696, #3632, #84008, #1473, #83470, #42479, #68370, #28468, #92092, #60816 ),
 .UNSPECIFIED., .F., .F.,
 ( 4, 2, 2, 2, 2, 2, 2, 4 ),
 ( 1.398578778534940505E-17, 0.0003855832886952001220, 0.0007711665773903862578, 0.001156749866085572068, 0.001542333154780758421, 0.001927916443475944557, 0.002313499732171130259, 0.003084666309561404952 ),
 .UNSPECIFIED. ) ;
#93396=CARTESIAN_POINT ( 'NONE',  ( 32.82168481641626556, 434.5290828238659628, 16.70238291264138653 ) ) ;
#93403=ORIENTED_EDGE ( 'NONE', *, *, #27848, .T. ) ;
#93430=CARTESIAN_POINT ( 'NONE',  ( -2.587146340238325681, 300.7568995495286686, 9.662447471766515861 ) ) ;
#93448=B_SPLINE_CURVE_WITH_KNOTS ( 'NONE', 3,
 ( #98955, #75217, #49887, #83851 ),
 .UNSPECIFIED., .F., .F.,
 ( 4, 4 ),
 ( 0.0005341934512451263070, 0.02813855774923773589 ),
 .UNSPECIFIED. ) ;
#93450=VERTEX_POINT ( 'NONE', #26413 ) ;
#93455=CARTESIAN_POINT ( 'NONE',  ( 32.74193221581197832, 435.3845808012915768, 16.94201410894484994 ) ) ;
#93457=CARTESIAN_POINT ( 'NONE',  ( -33.85195725564127400, 465.2464970902067307, 17.18122764674263436 ) ) ;
#93492=ORIENTED_EDGE ( 'NONE', *, *, #37630, .F. ) ;
#93506=CARTESIAN_POINT ( 'NONE',  ( 37.62251730745840206, 437.3427388312646826, 4.535622330043183048 ) ) ;
#93516=CARTESIAN_POINT ( 'NONE',  ( 33.00000000000000000, 489.5971041675262541, 10.80646835458729349 ) ) ;
#93517=CARTESIAN_POINT ( 'NONE',  ( -28.76346532419124458, 309.5219921958590135, -8.933260212751790164 ) ) ;
#93519=CARTESIAN_POINT ( 'NONE',  ( -33.65518112486073221, 435.5968223796347161, 8.977797139137742022 ) ) ;
#93539=CARTESIAN_POINT ( 'NONE',  ( -36.05680654074119929, 304.0840038173946027, 0.1264612662495986917 ) ) ;
#93543=( BOUNDED_SURFACE ( )  B_SPLINE_SURFACE ( 3, 2, ( 
 ( #95549, #63191, #54526 ),
 ( #5474, #28729, #87470 ),
 ( #13551, #61616, #29267 ),
 ( #94509, #46469, #20661 ),
 ( #62149, #53500, #95039 ),
 ( #38399, #69169, #71264 ),
 ( #20117, #28203, #104158 ),
 ( #30303, #96084, #3359 ),
 ( #93966, #36303, #73908 ),
 ( #15677, #48566, #24861 ),
 ( #40489, #46983, #65300 ),
 ( #7052, #88525, #23815 ) ),
 .UNSPECIFIED., .F., .F., .F. ) 
 B_SPLINE_SURFACE_WITH_KNOTS ( ( 4, 2, 2, 2, 2, 4 ),
 ( 3, 3 ),
 ( 4.683753385137379155E-17, 0.005139846902489559645, 0.005782327765300748421, 0.006424808628111938064, 0.007709770353734315615, 0.01027969380497907245 ),
 ( 0.000000000000000000, 1.000000000000000000 ),
 .UNSPECIFIED. ) 
 GEOMETRIC_REPRESENTATION_ITEM ( )  RATIONAL_B_SPLINE_SURFACE ( (
 ( 1.000000000000000000, 0.7071066567438660799, 1.000000000000000000),
 ( 1.000000000000000000, 0.7071033644331966572, 1.000000000000000000),
 ( 1.000000000000000000, 0.7071056776559211388, 1.000000000000000000),
 ( 1.000000000000000000, 0.7071068248477218043, 1.000000000000000000),
 ( 1.000000000000000000, 0.7071068712035362136, 1.000000000000000000),
 ( 1.000000000000000000, 0.7071037121013128424, 1.000000000000000000),
 ( 1.000000000000000000, 0.7071011173528390925, 1.000000000000000000),
 ( 1.000000000000000000, 0.7070931233498599644, 1.000000000000000000),
 ( 1.000000000000000000, 0.7070878535667373121, 1.000000000000000000),
 ( 1.000000000000000000, 0.7070844239726482572, 1.000000000000000000),
 ( 1.000000000000000000, 0.7071028727339059294, 1.000000000000000000),
 ( 1.000000000000000000, 0.7071067811865477948, 1.000000000000000000) ) ) 
 REPRESENTATION_ITEM ( '' )  SURFACE ( )  );
#93547=DIRECTION ( 'NONE',  ( 4.547071256508659128E-15, -0.6177654251575146471, -0.7863624351912771315 ) ) ;
#93551=VERTEX_POINT ( 'NONE', #31058 ) ;
#93555=ADVANCED_FACE ( 'NONE', ( #52766 ), #96822, .F. ) ;
#93567=CARTESIAN_POINT ( 'NONE',  ( -43.50377727019363761, 435.9167426301696651, 18.24083946424746117 ) ) ;
#93580=CARTESIAN_POINT ( 'NONE',  ( 46.00000000000002132, 436.0213184034679443, 14.35141020368345366 ) ) ;
#93593=CARTESIAN_POINT ( 'NONE',  ( 33.74977848768428146, 477.7786480585253912, 4.002244379145972530 ) ) ;
#93602=CARTESIAN_POINT ( 'NONE',  ( 25.34756200978462815, 295.7221099550690155, -1.813076239403205836 ) ) ;
#93603=CARTESIAN_POINT ( 'NONE',  ( 35.44563196690202744, 355.0508310518326311, 1.542887188894044526 ) ) ;
#93615=CARTESIAN_POINT ( 'NONE',  ( 40.16383914097482943, 315.4761916235045192, 2.976046483704458900 ) ) ;
#93620=CARTESIAN_POINT ( 'NONE',  ( 31.31637074175829127, 438.7955421674503214, 22.44423981995848294 ) ) ;
#93630=DIRECTION ( 'NONE',  ( 0.9502668926229327351, 0.000000000000000000, 0.3114367235647647614 ) ) ;
#93643=CARTESIAN_POINT ( 'NONE',  ( 46.00000000000000000, 450.0000000000002274, 28.20242257375372219 ) ) ;
#93649=EDGE_LOOP ( 'NONE', ( #27998, #81916, #6931, #29876 ) ) ;
#93659=CARTESIAN_POINT ( 'NONE',  ( -32.03420920423447882, 464.8550977446592469, 13.91744750518814655 ) ) ;
#93671=CARTESIAN_POINT ( 'NONE',  ( 30.00000000000000000, 450.0000000000002274, 13.20242257375370976 ) ) ;
#93672=B_SPLINE_CURVE_WITH_KNOTS ( 'NONE', 3,
 ( #17434, #50303, #97794, #97267 ),
 .UNSPECIFIED., .F., .F.,
 ( 4, 4 ),
 ( 2.795030908892879291E-15, 0.0001439741052602189176 ),
 .UNSPECIFIED. ) ;
#93673=CARTESIAN_POINT ( 'NONE',  ( 25.11507076259356097, 295.6895725033105577, 2.116947622670480644 ) ) ;
#93689=CARTESIAN_POINT ( 'NONE',  ( 33.70225418941513595, 490.4053771885736523, 11.54106678936950381 ) ) ;
#93690=EDGE_CURVE ( 'NONE', #91640, #103206, #101903, .T. ) ;
#93695=ORIENTED_EDGE ( 'NONE', *, *, #22998, .F. ) ;
#93704=CARTESIAN_POINT ( 'NONE',  ( -32.14400760092462406, 464.7181002246661023, 11.03224828307551597 ) ) ;
#93720=CARTESIAN_POINT ( 'NONE',  ( 43.63933387927400531, 486.5321090506437258, 6.480556376458745937 ) ) ;
#93738=CARTESIAN_POINT ( 'NONE',  ( 24.47062261081072521, 306.7367191156716899, 9.359397442148701174 ) ) ;
#93747=CARTESIAN_POINT ( 'NONE',  ( 31.35227631363202150, 438.7809971775112672, 22.96771959711079703 ) ) ;
#93749=DIRECTION ( 'NONE',  ( 0.000000000000000000, 0.000000000000000000, 1.000000000000000000 ) ) ;
#93759=CARTESIAN_POINT ( 'NONE',  ( -4.926264938265286553, 301.1864079209049692, -10.01402411462996511 ) ) ;
#93774=ORIENTED_EDGE ( 'NONE', *, *, #88526, .T. ) ;
#93781=ORIENTED_EDGE ( 'NONE', *, *, #91198, .T. ) ;
#93788=CARTESIAN_POINT ( 'NONE',  ( 32.00754358908571362, 333.4989015379719035, 17.37153786538196343 ) ) ;
#93794=CARTESIAN_POINT ( 'NONE',  ( -44.21332904831276522, 435.2494715644500616, 14.45449769377424687 ) ) ;
#93801=CARTESIAN_POINT ( 'NONE',  ( -23.86237914550371642, 305.6547497236389290, -8.827011597931521791 ) ) ;
#93802=CARTESIAN_POINT ( 'NONE',  ( -38.99434193015822103, 323.4566427656836254, 16.92016985397825835 ) ) ;
#93813=CIRCLE ( 'NONE', #57589, 5.000000000000000888 ) ;
#93817=CARTESIAN_POINT ( 'NONE',  ( 6.582279166563815842, 304.7470068806263725, 8.914713973399436497 ) ) ;
#93820=EDGE_CURVE ( 'NONE', #35302, #85207, #42876, .T. ) ;
#93830=CARTESIAN_POINT ( 'NONE',  ( 1.853816988748078209, 295.4475851225615770, -10.00136337793448860 ) ) ;
#93831=CARTESIAN_POINT ( 'NONE',  ( 45.31383884518383098, 362.9196860876334085, 5.161789940898600548 ) ) ;
#93836=ORIENTED_EDGE ( 'NONE', *, *, #12100, .T. ) ;
#93838=CARTESIAN_POINT ( 'NONE',  ( 46.00000000000000000, 488.1802228726408543, 2.474914525454350755 ) ) ;
#93862=CARTESIAN_POINT ( 'NONE',  ( -43.00000000000000000, 487.9285348210879647, 8.903916466045071587 ) ) ;
#93873=CARTESIAN_POINT ( 'NONE',  ( 43.50250715914211952, 464.6389613228371900, 9.611700240006818774 ) ) ;
#93887=EDGE_LOOP ( 'NONE', ( #55447, #106360, #45221, #51671 ) ) ;
#93893=CARTESIAN_POINT ( 'NONE',  ( 20.97754405179121662, 294.8763868968453608, 9.942224931492262385 ) ) ;
#93894=CARTESIAN_POINT ( 'NONE',  ( -43.00000000000001421, 462.1685671383398244, 2.813679926073832327 ) ) ;
#93897=CARTESIAN_POINT ( 'NONE',  ( -31.11679462788039530, 441.4271381875185511, 23.27438508043199406 ) ) ;
#93903=FACE_BOUND ( 'NONE', #66789, .T. ) ;
#93916=CARTESIAN_POINT ( 'NONE',  ( -33.92709525147876093, 435.0559456452659219, 11.89085117398058955 ) ) ;
#93917=CARTESIAN_POINT ( 'NONE',  ( -26.77371412052617927, 310.9345145332244442, 10.38748261951031182 ) ) ;
#93940=AXIS2_PLACEMENT_3D ( 'NONE', #93056, #3519, #12650 ) ;
#93944=CARTESIAN_POINT ( 'NONE',  ( -41.96713667498163147, 484.5369099524149874, -2.773154793582960576 ) ) ;
#93948=CARTESIAN_POINT ( 'NONE',  ( -32.95646543402917672, 485.7809766657132400, 5.067016726494657064 ) ) ;
#93950=CARTESIAN_POINT ( 'NONE',  ( 46.00000000000000000, 500.0000000000002274, 0.000000000000000000 ) ) ;
#93959=CARTESIAN_POINT ( 'NONE',  ( -7.726607555805129479, 296.0525430558076323, 6.373197147326261636 ) ) ;
#93963=DIRECTION ( 'NONE',  ( 0.000000000000000000, 0.000000000000000000, -1.000000000000000000 ) ) ;
#93966=CARTESIAN_POINT ( 'NONE',  ( 17.36274101333847852, 302.5953464100861083, -10.05438841575618980 ) ) ;
#93970=VERTEX_POINT ( 'NONE', #95630 ) ;
#94009=CARTESIAN_POINT ( 'NONE',  ( 30.00000000000000000, 450.0000000000002274, 1.202422573753698876 ) ) ;
#94013=EDGE_LOOP ( 'NONE', ( #9499, #23559, #99815, #85218, #79183, #48131 ) ) ;
#94015=CARTESIAN_POINT ( 'NONE',  ( -40.33183555103232720, 485.8341092017944902, -4.932519190552891786 ) ) ;
#94022=ADVANCED_FACE ( 'NONE', ( #57263 ), #31969, .T. ) ;
#94024=CARTESIAN_POINT ( 'NONE',  ( 39.20264847829687938, 436.8475545326444944, 5.145470557644901355 ) ) ;
#94031=CARTESIAN_POINT ( 'NONE',  ( 38.23020704518827273, 485.0116943706019015, -3.938850139312762622 ) ) ;
#94035=CARTESIAN_POINT ( 'NONE',  ( -43.68669919770279364, 485.1453384654006982, 2.541696494117124061 ) ) ;
#94038=CARTESIAN_POINT ( 'NONE',  ( 32.66787492829552519, 465.0722615638334219, 12.52936269480703757 ) ) ;
#94039=CARTESIAN_POINT ( 'NONE',  ( -34.68490551324223503, 463.9993046474211269, 18.60480341025479234 ) ) ;
#94043=CARTESIAN_POINT ( 'NONE',  ( 33.21051451589296732, 465.5912171647664763, 15.87385029326350505 ) ) ;
#94045=CARTESIAN_POINT ( 'NONE',  ( -35.65409554988107033, 370.7248284907977904, 3.823559223723805189 ) ) ;
#94065=B_SPLINE_CURVE_WITH_KNOTS ( 'NONE', 3,
 ( #97298, #30476, #55241, #105914, #46632, #39093, #22920, #54705, #13188, #103805, #22398, #15324, #80578, #88166 ),
 .UNSPECIFIED., .F., .F.,
 ( 4, 2, 2, 2, 2, 2, 4 ),
 ( 1.430489624538199204E-17, 0.0003846054458897452057, 0.0007692108917794760999, 0.001153816337669206831, 0.001538421783558937888, 0.002307632675338383305, 0.003076843567117829373 ),
 .UNSPECIFIED. ) ;
#94108=( NAMED_UNIT ( * ) SI_UNIT ( $, .STERADIAN. ) SOLID_ANGLE_UNIT ( ) );
#94124=CARTESIAN_POINT ( 'NONE',  ( 27.97875226823191497, 296.5289436826013230, -9.637143995970028243 ) ) ;
#94127=DIRECTION ( 'NONE',  ( 0.000000000000000000, -0.8299985787546592109, 0.5577655056251200616 ) ) ;
#94132=CARTESIAN_POINT ( 'NONE',  ( 43.51595707245915889, 485.1238408984536363, -1.707557185930880905 ) ) ;
#94137=CARTESIAN_POINT ( 'NONE',  ( 40.61472136851750747, 317.8474547289473549, 3.573214933882146838 ) ) ;
#94139=ORIENTED_EDGE ( 'NONE', *, *, #720, .T. ) ;
#94142=CARTESIAN_POINT ( 'NONE',  ( 31.45629285601395608, 439.3226217137470258, 23.14484626223100960 ) ) ;
#94148=ADVANCED_FACE ( 'NONE', ( #74519 ), #48603, .T. ) ;
#94164=CARTESIAN_POINT ( 'NONE',  ( 34.06044893294480147, 463.4179081129763631, 6.463777546522439188 ) ) ;
#94191=CARTESIAN_POINT ( 'NONE',  ( -37.71419144549415137, 397.5045696453483401, 6.418798809479165257 ) ) ;
#94200=CARTESIAN_POINT ( 'NONE',  ( 29.13916688973899483, 297.4007265668975606, 2.495279913412661088 ) ) ;
#94210=ADVANCED_FACE ( 'NONE', ( #40043 ), #41779, .T. ) ;
#94219=CARTESIAN_POINT ( 'NONE',  ( -39.56197461363974099, -0.1944580884125578779, 19.78098730681987760 ) ) ;
#94230=CARTESIAN_POINT ( 'NONE',  ( 34.87160327596053833, 435.0271987811416921, 7.834040158382404861 ) ) ;
#94234=CARTESIAN_POINT ( 'NONE',  ( -37.52579488121514117, 438.0832148649091096, 4.091984033318601277 ) ) ;
#94238=CARTESIAN_POINT ( 'NONE',  ( 18.41162169223098033, 304.6294254666754568, 9.889731659030220001 ) ) ;
#94243=CARTESIAN_POINT ( 'NONE',  ( -43.63930228691581448, 486.5321682125791654, 6.480714085072397879 ) ) ;
#94249=DIRECTION ( 'NONE',  ( 0.000000000000000000, 0.000000000000000000, -1.000000000000000000 ) ) ;
#94252=CARTESIAN_POINT ( 'NONE',  ( 39.28947510688216482, 485.2043936288979467, -4.359233426732569860 ) ) ;
#94258=B_SPLINE_CURVE_WITH_KNOTS ( 'NONE', 3,
 ( #95588, #28232, #21724, #21204, #54566, #20152, #87502, #77812 ),
 .UNSPECIFIED., .F., .F.,
 ( 4, 2, 2, 4 ),
 ( 3.469446951953614189E-18, 0.002163004473986925285, 0.003244506710980385976, 0.004326008947973847100 ),
 .UNSPECIFIED. ) ;
#94263=B_SPLINE_CURVE_WITH_KNOTS ( 'NONE', 3,
 ( #63120, #22147, #79819, #87407 ),
 .UNSPECIFIED., .F., .F.,
 ( 4, 4 ),
 ( 8.270465868445859332E-17, 0.003416952886430538790 ),
 .UNSPECIFIED. ) ;
#94269=VERTEX_POINT ( 'NONE', #28677 ) ;
#94274=CARTESIAN_POINT ( 'NONE',  ( 26.27519682077350893, 310.0374129758119466, 11.16578451142825656 ) ) ;
#94304=EDGE_CURVE ( 'NONE', #62753, #1547, #19613, .T. ) ;
#94323=ORIENTED_EDGE ( 'NONE', *, *, #62426, .T. ) ;
#94327=AXIS2_PLACEMENT_3D ( 'NONE', #40460, #15119, #48005 ) ;
#94330=CARTESIAN_POINT ( 'NONE',  ( 32.95763196807708795, 360.4691531110863139, 22.50890827065293109 ) ) ;
#94332=CARTESIAN_POINT ( 'NONE',  ( -43.77664590664327449, 434.3717993398990984, 11.97532627841979469 ) ) ;
#94343=CARTESIAN_POINT ( 'NONE',  ( -39.14206789509485418, 314.2215094627067629, 6.606931266694046734 ) ) ;
#94369=EDGE_CURVE ( 'NONE', #49452, #26937, #3904, .T. ) ;
#94370=CARTESIAN_POINT ( 'NONE',  ( -1.435124379509183671E-09, 294.8518027762758038, -10.00000000000000178 ) ) ;
#94371=CARTESIAN_POINT ( 'NONE',  ( 45.33180403702434091, 464.4945808635454227, 2.178908857919817699 ) ) ;
#94372=CARTESIAN_POINT ( 'NONE',  ( 42.49652511093216134, 334.4904238026493886, 7.585808180445239302 ) ) ;
#94376=EDGE_CURVE ( 'NONE', #105760, #23483, #79904, .T. ) ;
#94385=ORIENTED_EDGE ( 'NONE', *, *, #17917, .T. ) ;
#94401=CARTESIAN_POINT ( 'NONE',  ( 44.13784562318636517, 464.3950638386343712, 9.689741638646596655 ) ) ;
#94406=ORIENTED_EDGE ( 'NONE', *, *, #105091, .F. ) ;
#94420=FACE_OUTER_BOUND ( 'NONE', #59551, .T. ) ;
#94426=ORIENTED_EDGE ( 'NONE', *, *, #27705, .F. ) ;
#94442=CARTESIAN_POINT ( 'NONE',  ( -40.73878142687892279, 503.7113041876743864, 10.19672445236252045 ) ) ;
#94443=CARTESIAN_POINT ( 'NONE',  ( 22.91885868373643831, 305.6172567281201964, 10.10309701371861912 ) ) ;
#94444=EDGE_CURVE ( 'NONE', #46291, #47279, #95229, .T. ) ;
#94461=CARTESIAN_POINT ( 'NONE',  ( -32.39696999578760028, 435.1504553356452334, 14.90852356088227459 ) ) ;
#94463=CIRCLE ( 'NONE', #42704, 0.9999999999999859002 ) ;
#94475=CARTESIAN_POINT ( 'NONE',  ( 40.03012460245055593, 436.4820657380745956, 5.641945619390446254 ) ) ;
#94481=EDGE_CURVE ( 'NONE', #64798, #48783, #34957, .T. ) ;
#94487=CARTESIAN_POINT ( 'NONE',  ( -44.09596412089000950, 463.0936910176846482, 6.209435503086969455 ) ) ;
#94501=CARTESIAN_POINT ( 'NONE',  ( -9.819056950928635175, 294.6481068335448299, 1.893705519456528652 ) ) ;
#94509=CARTESIAN_POINT ( 'NONE',  ( 15.38309070169586690, 302.5568164900287229, -10.06270155509156083 ) ) ;
#94511=EDGE_CURVE ( 'NONE', #18077, #13857, #76268, .T. ) ;
#94518=ADVANCED_FACE ( 'NONE', ( #56893 ), #102385, .F. ) ;
#94523=FACE_OUTER_BOUND ( 'NONE', #65936, .T. ) ;
#94545=CARTESIAN_POINT ( 'NONE',  ( 36.87655955837850286, 437.4206410680705517, 3.315070609669402035 ) ) ;
#94558=EDGE_LOOP ( 'NONE', ( #13496, #89080, #47395, #28287, #7698 ) ) ;
#94572=CARTESIAN_POINT ( 'NONE',  ( -32.74728942619589844, 438.8764684952981838, 23.82517967440724149 ) ) ;
#94576=CARTESIAN_POINT ( 'NONE',  ( -46.00000000000000711, 437.9213588505599546, 13.73447927187000595 ) ) ;
#94580=LINE ( 'NONE', #91512, #40193 ) ;
#94587=CARTESIAN_POINT ( 'NONE',  ( 34.56726037194530221, 484.1545686971866189, -0.1516737162341373901 ) ) ;
#94590=CARTESIAN_POINT ( 'NONE',  ( -26.27902093981875709, 306.9027577142574614, -9.548073367147230428 ) ) ;
#94591=DIRECTION ( 'NONE',  ( -0.000000000000000000, -1.000000000000000000, -0.000000000000000000 ) ) ;
#94592=CARTESIAN_POINT ( 'NONE',  ( -43.69219460922278842, 484.4832989965429419, 2.442496667980163405 ) ) ;
#94593=CARTESIAN_POINT ( 'NONE',  ( -41.92198544131502302, 435.4206365487660264, 7.395723383300994769 ) ) ;
#94600=FACE_OUTER_BOUND ( 'NONE', #85810, .T. ) ;
#94604=B_SPLINE_CURVE_WITH_KNOTS ( 'NONE', 3,
 ( #67698, #59076, #92487, #90911 ),
 .UNSPECIFIED., .F., .F.,
 ( 4, 4 ),
 ( 0.000000000000000000, 0.0006941752209892062099 ),
 .UNSPECIFIED. ) ;
#94613=DIRECTION ( 'NONE',  ( 0.000000000000000000, 0.000000000000000000, -1.000000000000000000 ) ) ;
#94618=DIRECTION ( 'NONE',  ( 0.000000000000000000, 0.7863624351912762434, -0.6177654251575154243 ) ) ;
#94621=ORIENTED_EDGE ( 'NONE', *, *, #43207, .F. ) ;
#94628=( BOUNDED_SURFACE ( )  B_SPLINE_SURFACE ( 3, 2, ( 
 ( #23710, #62563, #95449 ),
 ( #87373, #104593, #79263 ),
 ( #14504, #47416, #6419 ),
 ( #39357, #72234, #105137 ),
 ( #75416, #50076, #92127 ),
 ( #40926, #32863, #73819 ),
 ( #18275, #1509, #41983 ),
 ( #48997, #74865, #51130 ),
 ( #955, #74345, #99149 ),
 ( #8552, #32333, #33935 ),
 ( #57616, #98619, #90544 ),
 ( #66804, #24247, #16652 ),
 ( #17200, #84047, #100222 ),
 ( #25308, #67344, #10149 ),
 ( #82982, #99692, #26390 ),
 ( #422, #59252, #50587 ),
 ( #43064, #82448, #33388 ),
 ( #91620, #106171, #34474 ),
 ( #65739, #41454, #24769 ),
 ( #49542, #98096, #65201 ),
 ( #66262, #8017, #9079 ),
 ( #90010, #42517, #57094 ),
 ( #58719, #16113, #58166 ),
 ( #81899, #106712, #91094 ),
 ( #17729, #25864, #83503 ),
 ( #9604, #69991, #43587 ),
 ( #3130, #75950, #67863 ),
 ( #102893, #100748, #11729 ),
 ( #53797, #2051, #84588 ),
 ( #29056, #94274, #26914 ),
 ( #34997, #53279, #61926 ),
 ( #59789, #92665, #18824 ),
 ( #77553, #68408, #86725 ),
 ( #36604, #51666, #78079 ),
 ( #11195, #10669, #76471 ),
 ( #2583, #60851, #45203 ),
 ( #94816, #93203, #69468 ),
 ( #93738, #20963, #35533 ),
 ( #44130, #44668, #27450 ),
 ( #101301, #3670, #37127 ),
 ( #52735, #85110, #60330 ),
 ( #4193, #102352, #19368 ),
 ( #28499, #12798, #52199 ),
 ( #77013, #36074, #68945 ),
 ( #61385, #20439, #101818 ),
 ( #27983, #86199, #12272 ),
 ( #19894, #85659, #31676 ),
 ( #13858, #87777, #88307 ),
 ( #5777, #46249, #47289 ),
 ( #87248, #79136, #13326 ),
 ( #64558, #47812, #14384 ),
 ( #72632, #71047, #105534 ),
 ( #80188, #46771, #38699 ),
 ( #54848, #78597, #6293 ) ),
 .UNSPECIFIED., .F., .F., .T. ) 
 B_SPLINE_SURFACE_WITH_KNOTS ( ( 4, 2, 2, 2, 2, 2, 2, 2, 2, 2, 2, 2, 2, 2, 2, 2, 2, 2, 2, 2, 2, 2, 2, 2, 2, 2, 4 ),
 ( 3, 3 ),
 ( 0.04676915544590774798, 0.05566498745926091313, 0.06456081947261407827, 0.08235248349932039469, 0.1001441475260267250, 0.1179358115527330553, 0.1357274755794393717, 0.1446233075927925438, 0.1535191396061457159, 0.1579670556128223158, 0.1624149716194988879, 0.1668628876261754601, 0.1713108036328520600, 0.1757587196395286322, 0.1779826776428669044, 0.1802066356462052044, 0.1813186146478743543, 0.1824305936495435043, 0.1829865831503780793, 0.1835425726512126543, 0.1846545516528818043, 0.1852105411537163793, 0.1857665306545509543, 0.1863225201553855293, 0.1868785096562201042, 0.1879904886578892542, 0.1891024676595583764 ),
 ( 0.000000000000000000, 1.000000000000000000 ),
 .UNSPECIFIED. ) 
 GEOMETRIC_REPRESENTATION_ITEM ( )  RATIONAL_B_SPLINE_SURFACE ( (
 ( 1.000000000000000000, 0.7071068714016401913, 1.000000000000000000),
 ( 1.000000000000000000, 0.7071068931780433164, 1.000000000000000000),
 ( 1.000000000000000000, 0.7071068799845713349, 1.000000000000000000),
 ( 1.000000000000000000, 0.7071068180475085230, 1.000000000000000000),
 ( 1.000000000000000000, 0.7071067808201265681, 1.000000000000000000),
 ( 1.000000000000000000, 0.7071067808201265681, 1.000000000000000000),
 ( 1.000000000000000000, 0.7071067795786223353, 1.000000000000000000),
 ( 1.000000000000000000, 0.7071067795786223353, 1.000000000000000000),
 ( 1.000000000000000000, 0.7071059182714053426, 1.000000000000000000),
 ( 1.000000000000000000, 0.7071040218720007209, 1.000000000000000000),
 ( 1.000000000000000000, 0.7071071124652589246, 1.000000000000000000),
 ( 1.000000000000000000, 0.7071064137913863901, 1.000000000000000000),
 ( 1.000000000000000000, 0.7071032629227845812, 1.000000000000000000),
 ( 1.000000000000000000, 0.7071054820452861156, 1.000000000000000000),
 ( 1.000000000000000000, 0.7071073498263017454, 1.000000000000000000),
 ( 1.000000000000000000, 0.7071060860965120431, 1.000000000000000000),
 ( 1.000000000000000000, 0.7071042701190503044, 1.000000000000000000),
 ( 1.000000000000000000, 0.7071061861960223904, 1.000000000000000000),
 ( 1.000000000000000000, 0.7071092265142245870, 1.000000000000000000),
 ( 1.000000000000000000, 0.7071028837941631950, 1.000000000000000000),
 ( 1.000000000000000000, 0.7070914420358777042, 1.000000000000000000),
 ( 1.000000000000000000, 0.7070821610321850192, 1.000000000000000000),
 ( 1.000000000000000000, 0.7070849129775590436, 1.000000000000000000),
 ( 1.000000000000000000, 0.7071004802399988298, 1.000000000000000000),
 ( 1.000000000000000000, 0.7071085105257672865, 1.000000000000000000),
 ( 1.000000000000000000, 0.7071013087433613009, 1.000000000000000000),
 ( 1.000000000000000000, 0.7071049945832310613, 1.000000000000000000),
 ( 1.000000000000000000, 0.7071073724018395179, 1.000000000000000000),
 ( 1.000000000000000000, 0.7070679728041205925, 1.000000000000000000),
 ( 1.000000000000000000, 0.7070088173080720795, 1.000000000000000000),
 ( 1.000000000000000000, 0.7070194258748161431, 1.000000000000000000),
 ( 1.000000000000000000, 0.7070840790032983936, 1.000000000000000000),
 ( 1.000000000000000000, 0.7071075161209789961, 1.000000000000000000),
 ( 1.000000000000000000, 0.7071058500867670737, 1.000000000000000000),
 ( 1.000000000000000000, 0.7071008551465617353, 1.000000000000000000),
 ( 1.000000000000000000, 0.7071023055844545269, 1.000000000000000000),
 ( 1.000000000000000000, 0.7071042320260993996, 1.000000000000000000),
 ( 1.000000000000000000, 0.7071072094748438452, 1.000000000000000000),
 ( 1.000000000000000000, 0.7071072778665237202, 1.000000000000000000),
 ( 1.000000000000000000, 0.7071144736285724930, 1.000000000000000000),
 ( 1.000000000000000000, 0.7071122659468992433, 1.000000000000000000),
 ( 1.000000000000000000, 0.7071060123279735432, 1.000000000000000000),
 ( 1.000000000000000000, 0.7071046393532877117, 1.000000000000000000),
 ( 1.000000000000000000, 0.7070933101913624563, 1.000000000000000000),
 ( 1.000000000000000000, 0.7070896596052901328, 1.000000000000000000),
 ( 1.000000000000000000, 0.7070919439014947683, 1.000000000000000000),
 ( 1.000000000000000000, 0.7070971265612475687, 1.000000000000000000),
 ( 1.000000000000000000, 0.7071056421788293189, 1.000000000000000000),
 ( 1.000000000000000000, 0.7071090411609283199, 1.000000000000000000),
 ( 1.000000000000000000, 0.7070957058651622384, 1.000000000000000000),
 ( 1.000000000000000000, 0.7070787487242025104, 1.000000000000000000),
 ( 1.000000000000000000, 0.7070875582157836181, 1.000000000000000000),
 ( 1.000000000000000000, 0.7071060045247833381, 1.000000000000000000),
 ( 1.000000000000000000, 0.7071067811865683339, 1.000000000000000000) ) ) 
 REPRESENTATION_ITEM ( '' )  SURFACE ( )  );
#94641=CARTESIAN_POINT ( 'NONE',  ( -46.00000000000003553, 486.4340384878602208, 3.748479173867791392 ) ) ;
#94646=CARTESIAN_POINT ( 'NONE',  ( -46.00000000000000000, 500.0000000000002274, 0.000000000000000000 ) ) ;
#94658=FACE_OUTER_BOUND ( 'NONE', #65282, .T. ) ;
#94671=CARTESIAN_POINT ( 'NONE',  ( 33.48975799666246900, 326.8007346975397240, -3.612220824777813810 ) ) ;
#94674=FACE_BOUND ( 'NONE', #97702, .T. ) ;
#94676=CARTESIAN_POINT ( 'NONE',  ( 39.19091519714796590, 489.8676313716377990, 11.78787226601978944 ) ) ;
#94678=DIRECTION ( 'NONE',  ( 0.000000000000000000, 0.000000000000000000, -1.000000000000000000 ) ) ;
#94688=ORIENTED_EDGE ( 'NONE', *, *, #39752, .T. ) ;
#94689=CARTESIAN_POINT ( 'NONE',  ( 42.88788165728912105, 484.9809715184047150, -1.409177641729580932 ) ) ;
#94692=CARTESIAN_POINT ( 'NONE',  ( 37.60572600703760315, 371.3193617627527487, 4.346622703349591887 ) ) ;
#94696=CARTESIAN_POINT ( 'NONE',  ( -7.093721425956736049, 304.7303285792975771, 9.911179277710184365 ) ) ;
#94700=CARTESIAN_POINT ( 'NONE',  ( 44.24885999147007709, 485.2873706794222812, 1.656249348736088312 ) ) ;
#94733=ORIENTED_EDGE ( 'NONE', *, *, #105654, .T. ) ;
#94734=ORIENTED_EDGE ( 'NONE', *, *, #39252, .F. ) ;
#94738=CARTESIAN_POINT ( 'NONE',  ( -37.68817371937168303, 414.9405981843138989, 6.370433777595585489 ) ) ;
#94742=VERTEX_POINT ( 'NONE', #13514 ) ;
#94748=CARTESIAN_POINT ( 'NONE',  ( 24.36021057821819724, 304.1488456854494302, 10.22118185489211939 ) ) ;
#94750=CARTESIAN_POINT ( 'NONE',  ( 1.954498338103932698, 298.2604654188854170, -10.00252163445081521 ) ) ;
#94752=ORIENTED_EDGE ( 'NONE', *, *, #90517, .F. ) ;
#94758=EDGE_CURVE ( 'NONE', #5324, #76499, #25926, .T. ) ;
#94763=FACE_OUTER_BOUND ( 'NONE', #8723, .T. ) ;
#94777=CARTESIAN_POINT ( 'NONE',  ( 33.92709525147886751, 435.0559456452658651, 11.89085117398060021 ) ) ;
#94785=CARTESIAN_POINT ( 'NONE',  ( 0.000000000000000000, 304.8518027762758038, 9.936999415352289589 ) ) ;
#94788=CARTESIAN_POINT ( 'NONE',  ( -43.75401118688381530, 486.3173572309548831, 5.908089951475188784 ) ) ;
#94794=CARTESIAN_POINT ( 'NONE',  ( 39.65933660911757386, 485.2174287600339539, -4.382854859801245340 ) ) ;
#94805=CARTESIAN_POINT ( 'NONE',  ( -33.56345473223404241, 299.9083031499212666, -8.874823776836098688 ) ) ;
#94811=DIRECTION ( 'NONE',  ( 0.000000000000000000, -0.9746667163790283528, 0.2236622274388831710 ) ) ;
#94812=EDGE_LOOP ( 'NONE', ( #65112, #24523, #89549, #86996 ) ) ;
#94816=CARTESIAN_POINT ( 'NONE',  ( 24.68056467888841254, 306.9732456607671338, 9.415188885530078267 ) ) ;
#94832=ADVANCED_FACE ( 'NONE', ( #26969 ), #56330, .F. ) ;
#94856=CARTESIAN_POINT ( 'NONE',  ( 21.51569398614863715, 294.9107018935607130, -9.987480606144506723 ) ) ;
#94861=EDGE_LOOP ( 'NONE', ( #64367, #92707, #68320, #39910 ) ) ;
#94868=CARTESIAN_POINT ( 'NONE',  ( 41.72794603366077126, 484.6317694608904389, -3.103777363573142267 ) ) ;
#94871=CARTESIAN_POINT ( 'NONE',  ( -39.83854393464088162, 460.2189570659085120, 2.210463671045205913 ) ) ;
#94881=CARTESIAN_POINT ( 'NONE',  ( -38.37222421136043238, 311.1670517065257968, 5.835050788717471626 ) ) ;
#94886=CARTESIAN_POINT ( 'NONE',  ( 41.58031631500816871, 436.8046394031030673, 6.058257849348906987 ) ) ;
#94894=CARTESIAN_POINT ( 'NONE',  ( 33.00000000000000000, 461.8802764867031669, 14.89328939272360941 ) ) ;
#94904=EDGE_CURVE ( 'NONE', #29309, #103578, #84644, .T. ) ;
#94909=CARTESIAN_POINT ( 'NONE',  ( 8.392508714390126912, 295.8888084830643379, -10.03187903922701629 ) ) ;
#94912=CARTESIAN_POINT ( 'NONE',  ( 43.61687001562553689, 428.0553245671831064, 15.22863618831378218 ) ) ;
#94914=EDGE_CURVE ( 'NONE', #63799, #72871, #38496, .T. ) ;
#94920=CARTESIAN_POINT ( 'NONE',  ( 0.000000000000000000, -20.00000000000001776, -9.000000000000007105 ) ) ;
#94922=ORIENTED_EDGE ( 'NONE', *, *, #12027, .F. ) ;
#94936=CARTESIAN_POINT ( 'NONE',  ( 17.41226678943441897, 294.5863878355755787, 1.881106500063166598 ) ) ;
#94941=CARTESIAN_POINT ( 'NONE',  ( -42.74220749418430643, 488.2672406020914764, 9.363116084198825462 ) ) ;
#94953=CARTESIAN_POINT ( 'NONE',  ( -43.02661387979790675, 465.7449615347597387, 11.43319743843399827 ) ) ;
#94961=ORIENTED_EDGE ( 'NONE', *, *, #22623, .F. ) ;
#94964=CARTESIAN_POINT ( 'NONE',  ( 43.00000000000000000, 459.9277931459794218, 6.461582622334586468 ) ) ;
#94965=ORIENTED_EDGE ( 'NONE', *, *, #59770, .T. ) ;
#94978=CARTESIAN_POINT ( 'NONE',  ( -37.50031168351941346, 491.1141709719065034, 12.27711733876853906 ) ) ;
#94979=CARTESIAN_POINT ( 'NONE',  ( -33.00000000000000711, 485.0303364503728289, 0.9535057477320370012 ) ) ;
#94995=CARTESIAN_POINT ( 'NONE',  ( -31.61471011888779969, 437.7834120463330692, 21.48349580664253011 ) ) ;
#94996=CARTESIAN_POINT ( 'NONE',  ( -32.39498043692212548, 435.1520223549252364, 14.91902686226306152 ) ) ;
#95020=CARTESIAN_POINT ( 'NONE',  ( -44.08684117349997678, 464.4011528862877753, 9.618368244415259838 ) ) ;
#95023=CARTESIAN_POINT ( 'NONE',  ( -28.04142041209776437, 305.7898939697568608, -9.347126562776695735 ) ) ;
#95037=EDGE_CURVE ( 'NONE', #51548, #79974, #3991, .T. ) ;
#95039=CARTESIAN_POINT ( 'NONE',  ( 15.65616503042675767, 294.5586764198427545, -2.062307778642553213 ) ) ;
#95043=CARTESIAN_POINT ( 'NONE',  ( 41.96546066671465525, 485.5623541565433356, -4.077117913361723467 ) ) ;
#95045=CARTESIAN_POINT ( 'NONE',  ( 43.54152132068616510, 464.9591243096638777, 12.86066449444697035 ) ) ;
#95051=CARTESIAN_POINT ( 'NONE',  ( 35.96984634191181840, 491.2828258641249590, 12.80275614855168342 ) ) ;
#95055=CIRCLE ( 'NONE', #57137, 0.9999999999999980016 ) ;
#95060=CARTESIAN_POINT ( 'NONE',  ( -30.00000000000000000, 500.0000000000002274, 0.000000000000000000 ) ) ;
#95081=ORIENTED_EDGE ( 'NONE', *, *, #96164, .F. ) ;
#95086=CARTESIAN_POINT ( 'NONE',  ( -33.74362713068857289, 463.9326864247045137, 7.533159870298685057 ) ) ;
#95095=CARTESIAN_POINT ( 'NONE',  ( 32.80432905490892637, 485.2968070025902421, 5.900212245013106482 ) ) ;
#95101=CARTESIAN_POINT ( 'NONE',  ( 38.90208975916642942, 437.7929390081956740, 4.481369775529410404 ) ) ;
#95109=CARTESIAN_POINT ( 'NONE',  ( 38.81358894280276672, 485.1131561813238591, -4.191378885298274959 ) ) ;
#95111=CARTESIAN_POINT ( 'NONE',  ( -23.95564068939877345, 305.6666757346319514, -9.824255363917307804 ) ) ;
#95116=CARTESIAN_POINT ( 'NONE',  ( 0.000000000000000000, 0.000000000000000000, 0.000000000000000000 ) ) ;
#95118=CARTESIAN_POINT ( 'NONE',  ( -34.83844953172029335, 463.9146721063430618, 18.82558425661466828 ) ) ;
#95137=DIRECTION ( 'NONE',  ( -0.000000000000000000, -1.000000000000000000, -0.000000000000000000 ) ) ;
#95142=ORIENTED_EDGE ( 'NONE', *, *, #14359, .F. ) ;
#95149=ORIENTED_EDGE ( 'NONE', *, *, #29511, .F. ) ;
#95154=CIRCLE ( 'NONE', #81331, 12.00000000000000711 ) ;
#95190=CARTESIAN_POINT ( 'NONE',  ( 33.79349388191229053, 321.1166572771793426, -5.792392752899560904 ) ) ;
#95191=CARTESIAN_POINT ( 'NONE',  ( 43.55923498581227449, 484.2982027343990694, 0.7709916636031838300 ) ) ;
#95194=CARTESIAN_POINT ( 'NONE',  ( -25.49268852105929639, 305.2874338487552563, -9.687155370726696191 ) ) ;
#95198=CARTESIAN_POINT ( 'NONE',  ( -44.00534824917842514, 485.4287573672962708, 6.291782489092286212 ) ) ;
#95206=VERTEX_POINT ( 'NONE', #99624 ) ;
#95207=CARTESIAN_POINT ( 'NONE',  ( 43.03265099499984103, 484.2747968070553952, -0.8099405866656324005 ) ) ;
#95208=DIRECTION ( 'NONE',  ( 3.890967530689355418E-15, -0.2755684261031602356, 0.9612814585411637580 ) ) ;
#95212=CARTESIAN_POINT ( 'NONE',  ( 43.06571828467162533, 345.9933190868828774, 10.02031458026529265 ) ) ;
#95222=CARTESIAN_POINT ( 'NONE',  ( -44.21445409815639493, 435.3521084850503371, 10.81722560632401731 ) ) ;
#95223=EDGE_CURVE ( 'NONE', #50155, #10730, #60888, .T. ) ;
#95229=CIRCLE ( 'NONE', #28111, 0.9999999999999993339 ) ;
#95253=ORIENTED_EDGE ( 'NONE', *, *, #73620, .F. ) ;
#95257=CARTESIAN_POINT ( 'NONE',  ( -45.50297956008602540, 391.5886742618069434, 8.004120577752210863 ) ) ;
#95267=CARTESIAN_POINT ( 'NONE',  ( -40.08499133126677094, 485.6798096563409217, -4.492259481483594996 ) ) ;
#95304=CARTESIAN_POINT ( 'NONE',  ( 43.00000000000000000, 500.0000000000002274, 0.000000000000000000 ) ) ;
#95305=CARTESIAN_POINT ( 'NONE',  ( 46.00000000000000000, 488.3725375423282458, 3.127739281032916097 ) ) ;
#95308=CARTESIAN_POINT ( 'NONE',  ( 43.04469050570450150, 434.7734435962914290, 9.248231035223298591 ) ) ;
#95310=CARTESIAN_POINT ( 'NONE',  ( 41.46910480218708273, 484.7338956289814860, -3.418960549715457375 ) ) ;
#95325=CARTESIAN_POINT ( 'NONE',  ( -6.795502735115863224, 303.7372916219597414, -10.02434238300769032 ) ) ;
#95329=CARTESIAN_POINT ( 'NONE',  ( -28.84813086497338475, 319.7805192248010258, 12.61644190180718006 ) ) ;
#95362=AXIS2_PLACEMENT_3D ( 'NONE', #33710, #100010, #75737 ) ;
#95380=CARTESIAN_POINT ( 'NONE',  ( 32.46537690518270125, 342.4109961635215882, 19.27576733899797645 ) ) ;
#95387=CARTESIAN_POINT ( 'NONE',  ( -34.39884064632509819, 463.9244153862098301, 5.561476059303757324 ) ) ;
#95391=CARTESIAN_POINT ( 'NONE',  ( -32.76369084077356320, 322.0407035852106219, -4.798215932636743730 ) ) ;
#95392=CARTESIAN_POINT ( 'NONE',  ( -24.42128123963413344, 304.1868369482826324, 10.22974940677398692 ) ) ;
#95402=AXIS2_PLACEMENT_3D ( 'NONE', #64666, #71158, #71676 ) ;
#95413=ADVANCED_FACE ( 'NONE', ( #91820, #17407 ), #9812, .T. ) ;
#95414=CARTESIAN_POINT ( 'NONE',  ( -19.73463816634111012, 304.7971333121958537, 8.925379062039116462 ) ) ;
#95416=CARTESIAN_POINT ( 'NONE',  ( 42.08762648273145857, 487.0030674539048050, 9.106351919857864630 ) ) ;
#95418=CARTESIAN_POINT ( 'NONE',  ( 43.67632028636852937, 390.4705434914407078, 15.75357519261242167 ) ) ;
#95421=CARTESIAN_POINT ( 'NONE',  ( 46.00000000000000000, 450.0000000000002274, 13.20242257375370976 ) ) ;
#95427=CARTESIAN_POINT ( 'NONE',  ( 39.56197461363974099, -0.1944580884125578779, 19.78098730681987050 ) ) ;
#95439=CARTESIAN_POINT ( 'NONE',  ( -38.81358894280271699, 485.1131561813180042, -4.191378885296423995 ) ) ;
#95449=CARTESIAN_POINT ( 'NONE',  ( 32.09613187451483896, 439.8906214799515624, 23.54885978596032814 ) ) ;
#95480=CARTESIAN_POINT ( 'NONE',  ( -40.85254446136673323, 441.7500193615117610, 25.53625856138344474 ) ) ;
#95482=DIRECTION ( 'NONE',  ( 0.000000000000000000, -0.7605354461462394688, 0.6492964154799720777 ) ) ;
#95484=CARTESIAN_POINT ( 'NONE',  ( -38.81358894280271699, 485.1131561813180042, -4.191378885296423995 ) ) ;
#95502=CARTESIAN_POINT ( 'NONE',  ( -33.72112513506057496, 434.9249801536511768, 12.79203885703619292 ) ) ;
#95503=CARTESIAN_POINT ( 'NONE',  ( -33.00000000000002842, 489.5971041675260835, 10.80646835458717270 ) ) ;
#95511=CARTESIAN_POINT ( 'NONE',  ( -32.16602296798976823, 298.8760903595368177, -9.110068575937141588 ) ) ;
#95520=CARTESIAN_POINT ( 'NONE',  ( 43.51084452654469459, 465.2903130129626561, 9.421687747985401984 ) ) ;
#95529=CARTESIAN_POINT ( 'NONE',  ( -36.85885249723667556, 438.9055665639564268, 23.87932036944819814 ) ) ;
#95531=CARTESIAN_POINT ( 'NONE',  ( -34.46322806571021147, 319.4038054108495999, -5.983482695349220393 ) ) ;
#95534=CARTESIAN_POINT ( 'NONE',  ( 32.12566262182734533, 486.1613120233242853, 5.452106427430475577 ) ) ;
#95536=CARTESIAN_POINT ( 'NONE',  ( 0.000000000000000000, 37.86482112153536406, -10.52123582012688274 ) ) ;
#95549=CARTESIAN_POINT ( 'NONE',  ( 9.970195021754619802, 302.6460196488382053, -10.04373974541431380 ) ) ;
#95561=( BOUNDED_SURFACE ( )  B_SPLINE_SURFACE ( 3, 2, ( 
 ( #18716, #76372, #10580 ),
 ( #34373, #58618, #99584 ),
 ( #92565, #66160, #90444 ),
 ( #34901, #82347, #90987 ),
 ( #17098, #74772, #75854 ),
 ( #2483, #1948, #91519 ),
 ( #100124, #17635, #41355 ),
 ( #59151, #42962, #57523 ) ),
 .UNSPECIFIED., .F., .F., .T. ) 
 B_SPLINE_SURFACE_WITH_KNOTS ( ( 4, 2, 2, 4 ),
 ( 3, 3 ),
 ( 0.006812271038101275558, 0.007673844606673213380, 0.008535418175245151201, 0.01025856531238902858 ),
 ( 0.000000000000000000, 0.8457923845102014448 ),
 .UNSPECIFIED. ) 
 GEOMETRIC_REPRESENTATION_ITEM ( )  RATIONAL_B_SPLINE_SURFACE ( (
 ( 1.000000000000000000, 0.7678693572792288924, 0.9284073742078311486),
 ( 1.000000000000000000, 0.7757895751984035249, 0.9308500900467820971),
 ( 1.000000000000000000, 0.7815379911777921018, 0.9326229890888320107),
 ( 1.000000000000000000, 0.7881252992655237710, 0.9346546152342435354),
 ( 1.000000000000000000, 0.7889532766692782806, 0.9349099760764683076),
 ( 1.000000000000000000, 0.7842545691361754168, 0.9334608231073407980),
 ( 1.000000000000000000, 0.7715427182228143943, 0.9295402946717183923),
 ( 1.000000000000000000, 0.7522731460529035186, 0.9235972651200572425) ) ) 
 REPRESENTATION_ITEM ( '' )  SURFACE ( )  );
#95565=CARTESIAN_POINT ( 'NONE',  ( 43.98625509876906392, 435.4996938134206630, 9.950854633800886972 ) ) ;
#95566=DIRECTION ( 'NONE',  ( -1.000000000000000000, 0.000000000000000000, 0.000000000000000000 ) ) ;
#95569=CARTESIAN_POINT ( 'NONE',  ( -43.00000000000000000, 500.0000000000002274, -15.00000000000000711 ) ) ;
#95583=ORIENTED_EDGE ( 'NONE', *, *, #70960, .T. ) ;
#95588=CARTESIAN_POINT ( 'NONE',  ( -32.28930913497458022, 488.2717154064632723, 9.213726894912692700 ) ) ;
#95606=CARTESIAN_POINT ( 'NONE',  ( -42.19179521602280403, 485.4956273777414708, -3.824025998168937512 ) ) ;
#95608=CARTESIAN_POINT ( 'NONE',  ( 34.94142348598472125, 329.2055239765263650, -3.785525783732882399 ) ) ;
#95610=CARTESIAN_POINT ( 'NONE',  ( 32.82264240587376491, 485.2608142494332242, 5.823360857566779458 ) ) ;
#95616=EDGE_CURVE ( 'NONE', #2324, #103314, #15533, .T. ) ;
#95630=CARTESIAN_POINT ( 'NONE',  ( 0.000000000000000000, 80.00000000000000000, -10.00000000000000000 ) ) ;
#95631=CARTESIAN_POINT ( 'NONE',  ( -35.44563196690202744, 355.0508310518326311, 1.542887188955126110 ) ) ;
#95645=ADVANCED_FACE ( 'NONE', ( #31872 ), #67395, .F. ) ;
#95677=CARTESIAN_POINT ( 'NONE',  ( -46.00000000000004263, 486.8231468695061039, 5.689692765235337291 ) ) ;
#95679=CARTESIAN_POINT ( 'NONE',  ( -37.62251730745840916, 437.3427388312646258, 4.535622330043208805 ) ) ;
#95694=VECTOR ( 'NONE', #42960, 1000.000000000000000 ) ;
#95707=DIRECTION ( 'NONE',  ( -0.000000000000000000, -1.000000000000000000, -0.000000000000000000 ) ) ;
#95712=CARTESIAN_POINT ( 'NONE',  ( 32.40217524501196777, 319.2284543538688126, -6.509870530067201067 ) ) ;
#95713=CARTESIAN_POINT ( 'NONE',  ( -3.373226601126230406, 304.8518027749948374, -9.000000000275649725 ) ) ;
#95717=CARTESIAN_POINT ( 'NONE',  ( -30.57762908964539506, 310.6565871460678636, -8.419674958802174203 ) ) ;
#95733=CARTESIAN_POINT ( 'NONE',  ( 35.93223276062541061, 303.8771570922352225, 0.07619417529777239295 ) ) ;
#95737=CARTESIAN_POINT ( 'NONE',  ( 31.33625191410321875, 438.2398020556285019, 22.62030528329812995 ) ) ;
#95744=DIRECTION ( 'NONE',  ( -0.000000000000000000, -1.000000000000000000, -0.000000000000000000 ) ) ;
#95749=CARTESIAN_POINT ( 'NONE',  ( 43.86555507694461653, 486.1044689237371017, 5.341991804865976690 ) ) ;
#95755=B_SPLINE_CURVE_WITH_KNOTS ( 'NONE', 3,
 ( #8648, #26475, #49637, #74436, #43156, #34030, #76038, #515, #99787, #58817, #53373, #79231, #28070, #87341, #45289, #85203, #69038, #78167, #29662, #77650, #61479, #29146, #5357, #27544, #62532, #102985, #4818, #78686, #44220, #53885, #37755, #94372, #101912, #70618, #44761, #3227, #85758, #38277, #28596, #103509, #52292, #77112, #95418, #13417, #21558, #62016, #94912, #71137 ),
 .UNSPECIFIED., .F., .F.,
 ( 4, 2, 2, 2, 2, 2, 2, 2, 2, 2, 2, 2, 2, 2, 2, 2, 2, 2, 2, 2, 2, 2, 2, 4 ),
 ( -5.999999999093525979E-08, 0.002372776880890837756, 0.004745613761781666481, 0.009491287523563323933, 0.01067770596400873830, 0.01186412440445415092, 0.01423696128534487210, 0.01660979816623559674, 0.01898263504712631444, 0.02135547192801703908, 0.02372830880890775679, 0.02610114568979847449, 0.02847398257068919220, 0.03321965633247064148, 0.03796533009425209076, 0.04745667761781514199, 0.05694802514137819321, 0.06643937266494123750, 0.07593072018850428873, 0.08542206771206733995, 0.09491341523563037730, 0.1138961102827564797, 0.1328788053298826100, 0.1518615003770086846 ),
 .UNSPECIFIED. ) ;
#95757=VERTEX_POINT ( 'NONE', #17805 ) ;
#95781=CARTESIAN_POINT ( 'NONE',  ( 1.128077836147720614, 302.8478239976497548, 9.936168295454386623 ) ) ;
#95783=FACE_OUTER_BOUND ( 'NONE', #106230, .T. ) ;
#95788=ORIENTED_EDGE ( 'NONE', *, *, #24359, .F. ) ;
#95790=DIRECTION ( 'NONE',  ( 0.000000000000000000, -1.000000000000000000, 0.000000000000000000 ) ) ;
#95796=CARTESIAN_POINT ( 'NONE',  ( 2.289784721614370078, 298.7146547035764570, -10.00340817433579943 ) ) ;
#95799=EDGE_LOOP ( 'NONE', ( #24692, #68556, #45759 ) ) ;
#95808=CARTESIAN_POINT ( 'NONE',  ( -19.86162800728182276, 303.8052307878184024, 8.927100233615661296 ) ) ;
#95812=EDGE_CURVE ( 'NONE', #27254, #101726, #70366, .T. ) ;
#95825=ADVANCED_FACE ( 'NONE', ( #93903, #32941 ), #65811, .F. ) ;
#95832=CARTESIAN_POINT ( 'NONE',  ( -41.47644945075508360, 477.1143663313983438, -1.041634112212352692 ) ) ;
#95839=CARTESIAN_POINT ( 'NONE',  ( 39.99672247557288784, 437.4320613725466842, 22.45588292425958699 ) ) ;
#95846=CARTESIAN_POINT ( 'NONE',  ( -43.36787761363371629, 463.6242408504509172, 5.358769950476687249 ) ) ;
#95864=EDGE_LOOP ( 'NONE', ( #66050, #65151, #88551, #18859 ) ) ;
#95865=CARTESIAN_POINT ( 'NONE',  ( -27.85081853580795297, 315.3923268305527472, 12.51532622124604011 ) ) ;
#95867=ORIENTED_EDGE ( 'NONE', *, *, #16337, .F. ) ;
#95870=CARTESIAN_POINT ( 'NONE',  ( -40.56952547639716755, 460.8933045338675925, 2.221423359587606505 ) ) ;
#95877=AXIS2_PLACEMENT_3D ( 'NONE', #90739, #35185, #2777 ) ;
#95906=CARTESIAN_POINT ( 'NONE',  ( 6.763850406535977022, 294.7356673863635592, 9.912314076180619438 ) ) ;
#95916=CARTESIAN_POINT ( 'NONE',  ( 40.64097752467004909, 353.9523173779949161, 23.32106799875517567 ) ) ;
#95924=CARTESIAN_POINT ( 'NONE',  ( -34.03780482868043578, 462.4848023821838296, 4.882790418534471932 ) ) ;
#95926=ORIENTED_EDGE ( 'NONE', *, *, #40887, .F. ) ;
#95928=CARTESIAN_POINT ( 'NONE',  ( -25.65900546945094263, 305.1951251589714502, 10.46195101058732391 ) ) ;
#95948=CARTESIAN_POINT ( 'NONE',  ( 35.93056730070288296, 437.9188583894897420, 4.302256410569166967 ) ) ;
#95972=CARTESIAN_POINT ( 'NONE',  ( -44.14563638416869651, 463.1455159964050381, 6.337363416021459805 ) ) ;
#95976=CARTESIAN_POINT ( 'NONE',  ( -44.14911905790387436, 464.3766534541992996, 9.623404994945699897 ) ) ;
#95980=CARTESIAN_POINT ( 'NONE',  ( 33.00000000000000000, 463.5362553048592531, 6.739467187734345721 ) ) ;
#95987=ORIENTED_EDGE ( 'NONE', *, *, #89285, .T. ) ;
#96016=CARTESIAN_POINT ( 'NONE',  ( -42.19179521602280403, 485.4956273777414708, -3.824025998168937512 ) ) ;
#96021=CARTESIAN_POINT ( 'NONE',  ( -33.08751701378358945, 301.6823158026044780, 11.49690784967660662 ) ) ;
#96024=CARTESIAN_POINT ( 'NONE',  ( 43.00000000000000000, 462.1685671383398244, 2.813679926073844317 ) ) ;
#96036=VERTEX_POINT ( 'NONE', #104010 ) ;
#96041=CARTESIAN_POINT ( 'NONE',  ( -31.80699609565019514, 437.1986690746257409, 20.73198424672801465 ) ) ;
#96042=CARTESIAN_POINT ( 'NONE',  ( -35.74109609218656658, 414.8491554067354059, 5.919296220277036724 ) ) ;
#96043=CARTESIAN_POINT ( 'NONE',  ( -31.55401502570843419, 436.6824539894687973, 19.27688314274631054 ) ) ;
#96044=CARTESIAN_POINT ( 'NONE',  ( -30.00000000000000355, 488.6481008951263902, 3.890293910846380321 ) ) ;
#96049=ORIENTED_EDGE ( 'NONE', *, *, #87301, .T. ) ;
#96051=CARTESIAN_POINT ( 'NONE',  ( -28.50623484390343521, 306.2062397803906606, -9.250652555261318355 ) ) ;
#96067=CARTESIAN_POINT ( 'NONE',  ( -33.00000000000000711, 439.7597899781497404, 24.16317522621305258 ) ) ;
#96069=CARTESIAN_POINT ( 'NONE',  ( -30.48212520012076254, 308.5335761172966613, -8.699255827182120981 ) ) ;
#96081=CARTESIAN_POINT ( 'NONE',  ( 34.84618260875170392, 489.9833681528626812, 11.97975507378813731 ) ) ;
#96084=CARTESIAN_POINT ( 'NONE',  ( 17.14761585140983158, 294.5838192077795838, -10.05696245189486149 ) ) ;
#96095=AXIS2_PLACEMENT_3D ( 'NONE', #34036, #43682, #99793 ) ;
#96097=ORIENTED_EDGE ( 'NONE', *, *, #49060, .T. ) ;
#96119=CARTESIAN_POINT ( 'NONE',  ( -6.632175269158647524, 303.7449820775430567, 9.914291074352707511 ) ) ;
#96142=CARTESIAN_POINT ( 'NONE',  ( -38.79830821498207172, 485.8176106091539737, -4.884814968349580511 ) ) ;
#96147=CARTESIAN_POINT ( 'NONE',  ( -32.42271565838826319, 438.8719799267125268, 23.74906467565554991 ) ) ;
#96151=CARTESIAN_POINT ( 'NONE',  ( -37.15025629407706020, 306.0170503793525540, 0.5993149417967529313 ) ) ;
#96153=CARTESIAN_POINT ( 'NONE',  ( 28.86106494938684364, 306.5463937303920261, -9.171402789936776045 ) ) ;
#96155=EDGE_LOOP ( 'NONE', ( #3729, #53318, #76355, #106562, #22733, #43641, #33118, #95987, #3467 ) ) ;
#96159=COLOUR_RGB ( '', 0.09019608, 0.27058824, 0.51372549) ;
#96164=EDGE_CURVE ( 'NONE', #7054, #59047, #96167, .T. ) ;
#96166=DIRECTION ( 'NONE',  ( 0.000000000000000000, 0.000000000000000000, -1.000000000000000000 ) ) ;
#96167=B_SPLINE_CURVE_WITH_KNOTS ( 'NONE', 3,
 ( #9558, #98049, #33880, #16067, #82400, #99641 ),
 .UNSPECIFIED., .F., .F.,
 ( 4, 1, 1, 4 ),
 ( 0.000000000000000000, 0.4213833399777465738, 0.5213833399777465516, 0.9843640123765010630 ),
 .UNSPECIFIED. ) ;
#96170=CARTESIAN_POINT ( 'NONE',  ( -31.03867016165222026, 468.3124986733989772, 18.90871194958903345 ) ) ;
#96175=CARTESIAN_POINT ( 'NONE',  ( -40.79885302902677324, 436.7553892629194365, 6.138960499427065010 ) ) ;
#96181=CARTESIAN_POINT ( 'NONE',  ( -43.00000000000000000, 450.0000000000002274, 13.20242257375370976 ) ) ;
#96190=CARTESIAN_POINT ( 'NONE',  ( 32.11723263399798611, 433.0682605266380278, 24.32175648712328453 ) ) ;
#96197=ORIENTED_EDGE ( 'NONE', *, *, #86941, .T. ) ;
#96210=CARTESIAN_POINT ( 'NONE',  ( 12.03681039759596239, 294.5862353579262276, 9.880551326283205427 ) ) ;
#96221=B_SPLINE_CURVE_WITH_KNOTS ( 'NONE', 3,
 ( #2094, #25914, #93252, #33985, #58770, #92173, #51176, #99196 ),
 .UNSPECIFIED., .F., .F.,
 ( 4, 2, 2, 4 ),
 ( 0.000000000000000000, 0.001013125157727799708, 0.002026250315455599416, 0.004052500630911192760 ),
 .UNSPECIFIED. ) ;
#96233=CARTESIAN_POINT ( 'NONE',  ( -37.62251730745840916, 437.3427388312646258, 4.535622330043208805 ) ) ;
#96246=ADVANCED_FACE ( 'NONE', ( #67161 ), #67383, .F. ) ;
#96248=CARTESIAN_POINT ( 'NONE',  ( 37.67124221001551376, 463.6239404278543361, 19.49545380201367450 ) ) ;
#96259=CARTESIAN_POINT ( 'NONE',  ( 35.53901217317436334, 397.0550940254831289, 6.925270274446173602 ) ) ;
#96281=CARTESIAN_POINT ( 'NONE',  ( 40.07510820939334906, 310.1680218437383019, -6.385417175660951905 ) ) ;
#96316=EDGE_CURVE ( 'NONE', #11400, #696, #102657, .T. ) ;
#96327=CARTESIAN_POINT ( 'NONE',  ( -44.07637885077937057, 485.1585573880434481, 0.4493611555661314871 ) ) ;
#96333=CARTESIAN_POINT ( 'NONE',  ( 32.89533925684071392, 465.6911419323517975, 10.83014164272718638 ) ) ;
#96334=CARTESIAN_POINT ( 'NONE',  ( -40.98863139543954048, 485.5630605922909808, -4.100416933089532812 ) ) ;
#96335=AXIS2_PLACEMENT_3D ( 'NONE', #84686, #36183, #3778 ) ;
#96341=CARTESIAN_POINT ( 'NONE',  ( 37.54559764570580427, 464.1143081516195821, 19.43664670202559464 ) ) ;
#96342=FACE_OUTER_BOUND ( 'NONE', #28076, .T. ) ;
#96366=DIRECTION ( 'NONE',  ( -0.000000000000000000, -1.000000000000000000, -0.000000000000000000 ) ) ;
#96373=CARTESIAN_POINT ( 'NONE',  ( -41.31850805822637085, 460.1795573263363508, 2.184907985914082307 ) ) ;
#96383=ADVANCED_FACE ( 'NONE', ( #9698 ), #31561, .T. ) ;
#96402=CARTESIAN_POINT ( 'NONE',  ( -29.57905231772367216, 319.3810052452713535, 13.75938574405086179 ) ) ;
#96411=CARTESIAN_POINT ( 'NONE',  ( 46.00000000000568434, 486.1435775019263019, 2.115062948001753984 ) ) ;
#96412=VECTOR ( 'NONE', #67163, 1000.000000000000000 ) ;
#96427=CARTESIAN_POINT ( 'NONE',  ( 20.24579557674108088, 304.8297271373347144, -10.00469232190996749 ) ) ;
#96438=ORIENTED_EDGE ( 'NONE', *, *, #99267, .F. ) ;
#96442=CARTESIAN_POINT ( 'NONE',  ( 11.93255308427328565, 294.5886021379643580, 9.881054392645332030 ) ) ;
#96452=CARTESIAN_POINT ( 'NONE',  ( 28.40426897693866692, 310.0622289480394898, 11.65337055426186907 ) ) ;
#96455=CARTESIAN_POINT ( 'NONE',  ( -42.57704743493907529, 486.1612337113410831, 7.852296464539637810 ) ) ;
#96466=CARTESIAN_POINT ( 'NONE',  ( -25.39099590404848428, 304.9312849039644107, 10.40030929671710069 ) ) ;
#96476=VERTEX_POINT ( 'NONE', #91707 ) ;
#96478=CARTESIAN_POINT ( 'NONE',  ( 36.74148664940358344, 437.9559008978175143, 4.252305828303436286 ) ) ;
#96481=CIRCLE ( 'NONE', #3477, 12.00000000000001066 ) ;
#96484=CARTESIAN_POINT ( 'NONE',  ( 42.59877891056748922, 471.6664475130272081, 11.88903271301921727 ) ) ;
#96488=CARTESIAN_POINT ( 'NONE',  ( 40.77380256327629837, 468.8478597483947965, 21.13608272249925690 ) ) ;
#96499=( BOUNDED_SURFACE ( )  B_SPLINE_SURFACE ( 3, 2, ( 
 ( #82031, #48602, #98226 ),
 ( #24381, #38434, #90142 ),
 ( #89618, #16244, #96119 ),
 ( #14110, #96648, #6024 ),
 ( #38948, #71825, #22782 ),
 ( #80442, #6550, #105265 ),
 ( #99270, #83108, #24898 ),
 ( #25993, #58854, #25449 ),
 ( #57751, #26, #26516 ),
 ( #9205, #2175, #91228 ) ),
 .UNSPECIFIED., .F., .F., .F. ) 
 B_SPLINE_SURFACE_WITH_KNOTS ( ( 4, 2, 2, 2, 4 ),
 ( 3, 3 ),
 ( 0.009739192996185006695, 0.01968048317401947800, 0.02465112826293671539, 0.02713645080739533408, 0.02962177335185395277 ),
 ( 0.000000000000000000, 1.000000000000000000 ),
 .UNSPECIFIED. ) 
 GEOMETRIC_REPRESENTATION_ITEM ( )  RATIONAL_B_SPLINE_SURFACE ( (
 ( 1.000000000000000000, 0.7071067811865475727, 1.000000000000000000),
 ( 1.000000000000000000, 0.7071067811865475727, 1.000000000000000000),
 ( 1.000000000000000000, 0.7071032136392382261, 1.000000000000000000),
 ( 1.000000000000000000, 0.7071081508940738614, 1.000000000000000000),
 ( 1.000000000000000000, 0.7071048030622038016, 1.000000000000000000),
 ( 1.000000000000000000, 0.7071073475187125146, 1.000000000000000000),
 ( 1.000000000000000000, 0.7070920501327951913, 1.000000000000000000),
 ( 1.000000000000000000, 0.7070828652041093454, 1.000000000000000000),
 ( 1.000000000000000000, 0.7071010096815192325, 1.000000000000000000),
 ( 1.000000000000000000, 0.7071067811865493491, 1.000000000000000000) ) ) 
 REPRESENTATION_ITEM ( '' )  SURFACE ( )  );
#96501=ADVANCED_FACE ( 'NONE', ( #96748 ), #71460, .T. ) ;
#96502=CARTESIAN_POINT ( 'NONE',  ( 0.000000000000000000, -18.92596047533412573, -20.36976895023282097 ) ) ;
#96523=EDGE_LOOP ( 'NONE', ( #75520, #15573, #47049, #16780 ) ) ;
#96537=ADVANCED_FACE ( 'NONE', ( #97513 ), #85996, .F. ) ;
#96549=CARTESIAN_POINT ( 'NONE',  ( -6.379201817708943345, 294.7476909954166331, 1.915027666297735021 ) ) ;
#96571=CARTESIAN_POINT ( 'NONE',  ( -31.23453009850055651, 439.6107769536124579, 23.21210983230010783 ) ) ;
#96573=CARTESIAN_POINT ( 'NONE',  ( -31.03678703374875880, 438.6650838204938054, 21.86890379898545334 ) ) ;
#96576=EDGE_CURVE ( 'NONE', #89019, #103730, #81992, .T. ) ;
#96582=CARTESIAN_POINT ( 'NONE',  ( -29.09465867093638636, 306.7984205571843290, -9.112160268181819234 ) ) ;
#96589=CARTESIAN_POINT ( 'NONE',  ( 29.78761703785879433, 327.5675123215826261, 14.51873336366982059 ) ) ;
#96600=CARTESIAN_POINT ( 'NONE',  ( -37.85695620536581885, 439.1124626137719247, 23.53257295012781469 ) ) ;
#96611=CARTESIAN_POINT ( 'NONE',  ( 42.93430011342386621, 435.4574193743733872, 17.27214342660671065 ) ) ;
#96635=CARTESIAN_POINT ( 'NONE',  ( 20.52350613252515643, 304.8999024697870937, 9.947223320822450532 ) ) ;
#96648=CARTESIAN_POINT ( 'NONE',  ( -11.62661342925168384, 304.6006127265920327, 9.883607322378615834 ) ) ;
#96657=VERTEX_POINT ( 'NONE', #92631 ) ;
#96664=VERTEX_POINT ( 'NONE', #100719 ) ;
#96670=CARTESIAN_POINT ( 'NONE',  ( 36.69193770976632152, 378.6360570424787966, 4.935504223416926628 ) ) ;
#96672=CARTESIAN_POINT ( 'NONE',  ( 32.82325442954073225, 485.9854176254823983, 5.594246714727905356 ) ) ;
#96678=CARTESIAN_POINT ( 'NONE',  ( 20.59177611987304957, 302.8577050849145280, -9.998745446473192189 ) ) ;
#96687=CARTESIAN_POINT ( 'NONE',  ( 34.49820706013684912, 464.8461132933183535, 18.22442427699395395 ) ) ;
#96693=CARTESIAN_POINT ( 'NONE',  ( -22.42417502586373246, 305.3961751430792333, 10.05444931189341773 ) ) ;
#96694=DIRECTION ( 'NONE',  ( 0.000000000000000000, 0.000000000000000000, 1.000000000000000000 ) ) ;
#96707=B_SPLINE_CURVE_WITH_KNOTS ( 'NONE', 3,
 ( #47804, #46241, #87768, #54292, #105527, #79656, #104460, #71037 ),
 .UNSPECIFIED., .F., .F.,
 ( 4, 2, 2, 4 ),
 ( 8.156951321262543387E-15, 0.003573501338921054610, 0.005360252008377505532, 0.007147002677833957755 ),
 .UNSPECIFIED. ) ;
#96713=CARTESIAN_POINT ( 'NONE',  ( 32.19491124036529328, 391.9745737642126642, 25.40000947286657507 ) ) ;
#96728=EDGE_CURVE ( 'NONE', #18315, #44795, #90110, .T. ) ;
#96736=ORIENTED_EDGE ( 'NONE', *, *, #12792, .F. ) ;
#96737=B_SPLINE_CURVE_WITH_KNOTS ( 'NONE', 3,
 ( #75299, #74237, #82871, #9493, #41873, #58606, #841, #34360, #17087, #84473 ),
 .UNSPECIFIED., .F., .F.,
 ( 4, 2, 2, 2, 4 ),
 ( 4.768881061110644471E-15, 0.001938799274764216535, 0.003877598549523663882, 0.005816397824283111445, 0.007755197099042559009 ),
 .UNSPECIFIED. ) ;
#96746=CARTESIAN_POINT ( 'NONE',  ( -41.34887590656642686, 489.6219161921864043, 10.83929645669275565 ) ) ;
#96748=FACE_OUTER_BOUND ( 'NONE', #43183, .T. ) ;
#96766=EDGE_CURVE ( 'NONE', #103314, #44580, #22826, .T. ) ;
#96771=CARTESIAN_POINT ( 'NONE',  ( -37.04388863813380794, 311.3287000699716032, 13.89786840526617517 ) ) ;
#96777=CARTESIAN_POINT ( 'NONE',  ( 34.80740166408775593, 344.0579031421361833, 0.3694569702644521225 ) ) ;
#96778=VERTEX_POINT ( 'NONE', #25637 ) ;
#96780=CARTESIAN_POINT ( 'NONE',  ( -23.36542799780119495, 304.4283958914435857, -9.876218974521238536 ) ) ;
#96781=CARTESIAN_POINT ( 'NONE',  ( 41.59240229034593028, 487.6847433724397547, 9.907832703287217768 ) ) ;
#96784=CARTESIAN_POINT ( 'NONE',  ( -43.00000000000000000, 487.9285348210879647, 8.903916466045071587 ) ) ;
#96797=CARTESIAN_POINT ( 'NONE',  ( 39.12236032760809223, 311.3937239336017342, 1.944237020743172284 ) ) ;
#96802=CARTESIAN_POINT ( 'NONE',  ( 51.01037695545453232, 450.0000000000002274, 13.20242257375370976 ) ) ;
#96806=CARTESIAN_POINT ( 'NONE',  ( 43.39367449914676200, 484.9145775485792456, -0.08602995335240110064 ) ) ;
#96818=ORIENTED_EDGE ( 'NONE', *, *, #53495, .T. ) ;
#96822=CYLINDRICAL_SURFACE ( 'NONE', #103674, 5.000000000000000888 ) ;
#96842=CARTESIAN_POINT ( 'NONE',  ( -41.18714086166914967, 436.5287100296065432, 21.33940902914881477 ) ) ;
#96843=CARTESIAN_POINT ( 'NONE',  ( 33.09674748210675688, 373.8214981666397421, 24.18330061219716853 ) ) ;
#96845=CARTESIAN_POINT ( 'NONE',  ( -45.18761087313401958, 356.2647831403982650, 4.028119660265046420 ) ) ;
#96847=CARTESIAN_POINT ( 'NONE',  ( -45.99999999998584599, 486.3339417046910853, 3.364639354305617225 ) ) ;
#96873=CARTESIAN_POINT ( 'NONE',  ( -42.36162206505708383, 485.1874691988857080, -2.398526663485941235 ) ) ;
#96887=CARTESIAN_POINT ( 'NONE',  ( -30.00000000000004619, 464.1532935782769869, 11.21093587219735355 ) ) ;
#96911=ORIENTED_EDGE ( 'NONE', *, *, #61270, .F. ) ;
#96918=CARTESIAN_POINT ( 'NONE',  ( -29.85348551950092855, 328.3076999754412100, 14.69459570409856219 ) ) ;
#96919=ORIENTED_EDGE ( 'NONE', *, *, #92820, .F. ) ;
#96924=CARTESIAN_POINT ( 'NONE',  ( 46.00000000000000000, 488.0078051103527059, -0.5538049991179438969 ) ) ;
#96934=B_SPLINE_CURVE_WITH_KNOTS ( 'NONE', 3,
 ( #57405, #90321, #15900, #97878 ),
 .UNSPECIFIED., .F., .F.,
 ( 4, 4 ),
 ( 0.000000000000000000, 0.001874406674510234461 ),
 .UNSPECIFIED. ) ;
#96937=CARTESIAN_POINT ( 'NONE',  ( -43.72966438978023973, 434.3041953058478839, 13.93761445528323861 ) ) ;
#96942=CARTESIAN_POINT ( 'NONE',  ( 33.63427961064055438, 325.9154870834976236, -4.827994974213513757 ) ) ;
#96943=ORIENTED_EDGE ( 'NONE', *, *, #17873, .T. ) ;
#96947=CARTESIAN_POINT ( 'NONE',  ( 46.00000000000000000, 461.6622277975422435, 10.18145404766785589 ) ) ;
#96957=FACE_OUTER_BOUND ( 'NONE', #41027, .T. ) ;
#96958=CARTESIAN_POINT ( 'NONE',  ( 43.59756234217347526, 434.3244621007142996, 14.55946156040239003 ) ) ;
#96970=CARTESIAN_POINT ( 'NONE',  ( 38.19591848881191964, 317.3555448089408060, 15.41710542503021131 ) ) ;
#96971=CARTESIAN_POINT ( 'NONE',  ( 42.75230560876955366, 485.3312079086152266, -3.156031357493472189 ) ) ;
#96972=CARTESIAN_POINT ( 'NONE',  ( -42.45811724857414049, 486.4202366696187596, 8.302074271984052345 ) ) ;
#96975=CARTESIAN_POINT ( 'NONE',  ( 42.23213459610285980, 347.2701562730458704, 14.17138388578061381 ) ) ;
#96979=CARTESIAN_POINT ( 'NONE',  ( -38.11704196078224527, 460.5925777724487489, 2.566592005033819568 ) ) ;
#96984=CARTESIAN_POINT ( 'NONE',  ( -25.67144724221197905, 305.2079960181984006, 10.46496832936455412 ) ) ;
#96989=CARTESIAN_POINT ( 'NONE',  ( -44.45120377230485786, 484.8901964262616389, 4.471885531209228937 ) ) ;
#97002=CARTESIAN_POINT ( 'NONE',  ( 41.59976546006239317, 472.6866688315437841, 16.01926328807780564 ) ) ;
#97005=CARTESIAN_POINT ( 'NONE',  ( 42.45852508622710531, 486.4193484895208712, 8.300531886079083321 ) ) ;
#97008=CARTESIAN_POINT ( 'NONE',  ( 43.47770857297122404, 484.8227827122696567, 4.253339224811428565 ) ) ;
#97015=FACE_OUTER_BOUND ( 'NONE', #35014, .T. ) ;
#97018=AXIS2_PLACEMENT_3D ( 'NONE', #14436, #54898, #62490 ) ;
#97029=EDGE_CURVE ( 'NONE', #56041, #47515, #38118, .T. ) ;
#97035=CARTESIAN_POINT ( 'NONE',  ( 41.46910480218704009, 484.7338956289814860, -3.418960549715446717 ) ) ;
#97045=CARTESIAN_POINT ( 'NONE',  ( -26.97491686565329161, 307.4599153070161606, -9.420584459367196573 ) ) ;
#97054=CARTESIAN_POINT ( 'NONE',  ( -5.515535885668342964, 296.1986775320586958, -10.01281319186906948 ) ) ;
#97060=CARTESIAN_POINT ( 'NONE',  ( -8.647927412449892159, 302.6863289723537491, 9.901865204233580187 ) ) ;
#97064=B_SPLINE_SURFACE_WITH_KNOTS ( 'NONE', 1, 3, ( 
 ( #94785, #20930, #86693, #86167, #102317, #28469, #94238, #19860 ),
 ( #45685, #12235, #35493, #4163, #12762, #27417, #60297, #37094 ) ),
 .UNSPECIFIED., .F., .F., .F.,
 ( 2, 2 ),
 ( 4, 2, 2, 4 ),
 ( 0.000000000000000000, 1.000000000000000000 ),
 ( 0.000000000000000000, 0.04450745600790868145, 0.06676118401186306728, 0.08901491201581737678 ),
 .UNSPECIFIED. ) ;
#97068=CARTESIAN_POINT ( 'NONE',  ( -32.87537929228375333, 485.0716560791295819, 1.465306988351862572 ) ) ;
#97075=B_SPLINE_CURVE_WITH_KNOTS ( 'NONE', 3,
 ( #57428, #73076, #15929, #7292 ),
 .UNSPECIFIED., .F., .F.,
 ( 4, 4 ),
 ( 3.469446951953614189E-18, 0.0006941752209891988374 ),
 .UNSPECIFIED. ) ;
#97085=CARTESIAN_POINT ( 'NONE',  ( -35.51301801062162866, 414.8830440580413210, 6.892597979060226976 ) ) ;
#97095=CARTESIAN_POINT ( 'NONE',  ( -31.90403345410906155, 299.1470781681827020, -1.045240008406338017 ) ) ;
#97096=DIRECTION ( 'NONE',  ( 0.000000000000000000, -1.000000000000000000, 0.000000000000000000 ) ) ;
#97106=EDGE_CURVE ( 'NONE', #25883, #104525, #21325, .T. ) ;
#97109=CARTESIAN_POINT ( 'NONE',  ( -46.00000000000000000, 463.6727721072930422, 9.768113441060686242 ) ) ;
#97110=CARTESIAN_POINT ( 'NONE',  ( -34.80483904954093788, 439.1570050480630698, 24.08402132645205640 ) ) ;
#97112=FACE_OUTER_BOUND ( 'NONE', #55567, .T. ) ;
#97115=CARTESIAN_POINT ( 'NONE',  ( 38.81331445831525429, 485.4137471979039447, -4.286058349641296950 ) ) ;
#97118=( BOUNDED_SURFACE ( )  B_SPLINE_SURFACE ( 3, 2, ( 
 ( #71965, #97291, #64422 ),
 ( #80570, #89217, #22913 ),
 ( #16374, #106438, #32598 ),
 ( #74073, #39617, #82166 ) ),
 .UNSPECIFIED., .F., .F., .F. ) 
 B_SPLINE_SURFACE_WITH_KNOTS ( ( 4, 4 ),
 ( 3, 3 ),
 ( -4.336808689942017736E-19, 0.001861785345366374737 ),
 ( 0.000000000000000000, 1.000000000000000000 ),
 .UNSPECIFIED. ) 
 GEOMETRIC_REPRESENTATION_ITEM ( )  RATIONAL_B_SPLINE_SURFACE ( (
 ( 1.000000000000000000, 0.7560596356357087711, 1.000000000000000000),
 ( 1.000000000000000000, 0.7634190799318362197, 1.000000000000000000),
 ( 1.000000000000000000, 0.7696912645870082059, 1.000000000000000000),
 ( 1.000000000000000000, 0.7737149417968428589, 1.000000000000000000) ) ) 
 REPRESENTATION_ITEM ( '' )  SURFACE ( )  );
#97120=VERTEX_POINT ( 'NONE', #10989 ) ;
#97125=CARTESIAN_POINT ( 'NONE',  ( 34.88900972249397370, 464.6206820655982028, 18.69027339340997784 ) ) ;
#97163=CARTESIAN_POINT ( 'NONE',  ( -43.32920196732008122, 484.9664025106967529, 4.870547201827349681 ) ) ;
#97193=CARTESIAN_POINT ( 'NONE',  ( 32.48141916466479984, 312.4572366807472577, -7.733776394823530964 ) ) ;
#97197=CARTESIAN_POINT ( 'NONE',  ( -34.40527838988940346, 463.9171486810813008, 5.550078836969805529 ) ) ;
#97205=CARTESIAN_POINT ( 'NONE',  ( -31.21759734847655210, 387.2566916973277671, 24.99345285570965913 ) ) ;
#97213=CARTESIAN_POINT ( 'NONE',  ( -44.12472801210822837, 485.7238370326490440, 3.975897585127398770 ) ) ;
#97215=CARTESIAN_POINT ( 'NONE',  ( -33.84761347220297267, 488.7471039746335464, 11.01988148152531899 ) ) ;
#97218=B_SPLINE_CURVE_WITH_KNOTS ( 'NONE', 3,
 ( #74031, #82664, #43272, #99349, #58932, #25533, #8766, #24470, #67556, #42736, #75627, #90223, #58388, #91304, #24984, #16328, #1730, #41672, #33083, #66475, #65948, #100434, #92339, #17414, #98827, #74561, #50287, #59471, #33601, #50807, #83189, #18484, #42198, #75081, #1174, #51347, #34145, #8236, #84260, #67023, #57836, #90762, #99903, #35203, #26074, #91828, #17945, #57305, #16878, #4402, #12475, #45409 ),
 .UNSPECIFIED., .F., .F.,
 ( 4, 2, 2, 2, 2, 2, 2, 2, 2, 2, 2, 2, 2, 2, 2, 2, 2, 2, 2, 2, 2, 2, 2, 2, 2, 4 ),
 ( 0.0004915406311061616337, 0.01833906179314000878, 0.02726282237415693019, 0.03618658295517385159, 0.05403410411720769441, 0.06295786469822470255, 0.07188162527924170375, 0.08972914644127570616, 0.09865290702229272124, 0.1075766676033097224, 0.1120385478938182994, 0.1165004281843268902, 0.1209623084748354810, 0.1254241887653440579, 0.1298860690558526487, 0.1321170092011069441, 0.1343479493463612395, 0.1354634194189883734, 0.1365788894916155349, 0.1376943595642426688, 0.1382520946005562912, 0.1388098296368699136, 0.1399252997094971862, 0.1410407697821244311, 0.1421562398547517037, 0.1432717099273789485 ),
 .UNSPECIFIED. ) ;
#97224=DIRECTION ( 'NONE',  ( 0.000000000000000000, 1.000000000000000000, 0.000000000000000000 ) ) ;
#97247=CARTESIAN_POINT ( 'NONE',  ( 16.16318061117915050, 302.5659895892079021, 9.876333854622428632 ) ) ;
#97256=ORIENTED_EDGE ( 'NONE', *, *, #59770, .F. ) ;
#97259=CARTESIAN_POINT ( 'NONE',  ( -38.17429156479857255, 491.0342884836515509, 12.03746475763302293 ) ) ;
#97267=CARTESIAN_POINT ( 'NONE',  ( -33.21102376836597614, 438.9613914113129454, 23.92328486949907074 ) ) ;
#97275=CARTESIAN_POINT ( 'NONE',  ( 35.47699217159722451, 463.6829005663142311, 19.36631617874163780 ) ) ;
#97279=CARTESIAN_POINT ( 'NONE',  ( -32.16694665535142406, 298.7751107022914425, -9.134474995491629556 ) ) ;
#97281=CARTESIAN_POINT ( 'NONE',  ( -29.07128654445882887, 296.9339959557834163, -9.548856946221640385 ) ) ;
#97284=CARTESIAN_POINT ( 'NONE',  ( 31.53716978815729988, 312.6643757245456641, -7.923975285009635883 ) ) ;
#97291=CARTESIAN_POINT ( 'NONE',  ( -42.20540931547679264, 464.9254549434355681, 14.73500713293386966 ) ) ;
#97298=CARTESIAN_POINT ( 'NONE',  ( -37.54559764570181812, 464.1143081516144662, 19.43664670202813838 ) ) ;
#97307=CARTESIAN_POINT ( 'NONE',  ( 33.38428166833018196, 315.1392599553683453, -7.060717463013046924 ) ) ;
#97322=ORIENTED_EDGE ( 'NONE', *, *, #36927, .T. ) ;
#97329=( LENGTH_UNIT ( ) NAMED_UNIT ( * ) SI_UNIT ( .MILLI., .METRE. ) );
#97330=CARTESIAN_POINT ( 'NONE',  ( 37.24013875201491430, 460.4840697668730058, 2.466806968993466853 ) ) ;
#97331=DIRECTION ( 'NONE',  ( 1.000000000000000000, 0.000000000000000000, 0.000000000000000000 ) ) ;
#97332=CARTESIAN_POINT ( 'NONE',  ( -43.72580207737490809, 464.6834397206225731, 7.653156261463578858 ) ) ;
#97349=CARTESIAN_POINT ( 'NONE',  ( 26.97704838610725631, 306.9562238369655915, 10.88316440979279776 ) ) ;
#97350=CARTESIAN_POINT ( 'NONE',  ( -42.49116267755303511, 334.6731539865542686, 7.617589167841204656 ) ) ;
#97360=CARTESIAN_POINT ( 'NONE',  ( -41.97131279571158302, 485.5606288621841600, -4.070573943137918427 ) ) ;
#97414=CARTESIAN_POINT ( 'NONE',  ( -30.95643954367146833, 313.8918926584737505, -7.857037206977866006 ) ) ;
#97416=CARTESIAN_POINT ( 'NONE',  ( 44.12472801211155371, 485.7238370326410859, 3.975897585125152123 ) ) ;
#97425=CARTESIAN_POINT ( 'NONE',  ( -29.62245443890884644, 328.1031406420239023, 15.64580783456615976 ) ) ;
#97434=CARTESIAN_POINT ( 'NONE',  ( 43.90061006400386390, 485.1244223267523239, -0.3741013042735300553 ) ) ;
#97445=B_SPLINE_CURVE_WITH_KNOTS ( 'NONE', 3,
 ( #11640, #102258, #61281, #29475 ),
 .UNSPECIFIED., .F., .F.,
 ( 4, 4 ),
 ( 8.069727767687917553E-17, 0.001738772145482940555 ),
 .UNSPECIFIED. ) ;
#97455=CARTESIAN_POINT ( 'NONE',  ( 29.45362385905110969, 325.9253963054578662, 15.14270878922920716 ) ) ;
#97465=VERTEX_POINT ( 'NONE', #53069 ) ;
#97479=CARTESIAN_POINT ( 'NONE',  ( 37.64249068469757731, 314.2742867948412027, 14.64262686200194885 ) ) ;
#97489=CARTESIAN_POINT ( 'NONE',  ( -32.67001420327693495, 300.1801760985952683, 3.134090012117491497 ) ) ;
#97501=CARTESIAN_POINT ( 'NONE',  ( 36.87655955837854549, 438.2068510013161813, 3.933030107424686950 ) ) ;
#97505=B_SPLINE_CURVE_WITH_KNOTS ( 'NONE', 3,
 ( #85510, #12127, #45057, #18670, #35389, #68257, #60191, #52054, #43977, #75806, #44517, #36463, #77940, #76864, #83894, #11589, #2973, #34855, #4050, #69329, #10007, #42914, #105394, #20821, #29426, #4583, #47672, #39085, #12651, #95717, #38556, #46623, #71963, #63891, #79520, #6687, #62303, #46109, #103277, #95194, #6152, #78462, #96780, #80568, #22911, #55748, #62825, #70381, #21327, #78991, #14775, #47145, #88682 ),
 .UNSPECIFIED., .F., .F.,
 ( 4, 2, 2, 2, 2, 2, 2, 2, 2, 2, 2, 2, 2, 2, 2, 2, 2, 2, 2, 2, 2, 2, 2, 2, 1, 2, 4 ),
 ( 0.0004461995168100071582, 0.01816948080801145810, 0.03589276209921291039, 0.05361604339041435574, 0.06247768403601508536, 0.07133932468161581497, 0.08020096532721653071, 0.08906260597281724645, 0.1067858872640188722, 0.1156475279096197406, 0.1200783482324201817, 0.1245091685552206229, 0.1267245787166209614, 0.1278322837973212001, 0.1289399888780214110, 0.1311553990394218605, 0.1333708092008223101, 0.1344785142815225487, 0.1355862193622227319, 0.1366939244429229705, 0.1378016295236231814, 0.1400170396850236032, 0.1411247447657238419, 0.1416785973060739334, 0.1419555235762489931, 0.1420939867113365507, 0.1422324498464240805 ),
 .UNSPECIFIED. ) ;
#97511=CARTESIAN_POINT ( 'NONE',  ( -44.08840282922865583, 485.7747746244177165, 4.178803824087112595 ) ) ;
#97512=ORIENTED_EDGE ( 'NONE', *, *, #84348, .T. ) ;
#97513=FACE_OUTER_BOUND ( 'NONE', #47876, .T. ) ;
#97550=VERTEX_POINT ( 'NONE', #6893 ) ;
#97555=CARTESIAN_POINT ( 'NONE',  ( -42.45852508623016774, 486.4193484895183701, 8.300531886066563558 ) ) ;
#97559=CARTESIAN_POINT ( 'NONE',  ( -43.86560043478159088, 486.1043823555137919, 5.341761608528194039 ) ) ;
#97569=CARTESIAN_POINT ( 'NONE',  ( -2.524354896707237777E-26, 294.8518027762758038, -10.00000000000000178 ) ) ;
#97571=CARTESIAN_POINT ( 'NONE',  ( 42.61140200160144786, 465.9030374194822457, 13.21253569360410829 ) ) ;
#97576=CARTESIAN_POINT ( 'NONE',  ( -12.03689052648907420, 294.5862333106543929, 9.880550891260135415 ) ) ;
#97580=CARTESIAN_POINT ( 'NONE',  ( -33.85195725564127400, 465.2464970902067307, 17.18122764674263436 ) ) ;
#97581=CARTESIAN_POINT ( 'NONE',  ( -37.54639605868532470, 463.7795194819277640, 19.50795070292539179 ) ) ;
#97592=ORIENTED_EDGE ( 'NONE', *, *, #53495, .F. ) ;
#97598=CARTESIAN_POINT ( 'NONE',  ( 30.00000000000000355, 461.8887775513396150, 11.55279652844105520 ) ) ;
#97603=CARTESIAN_POINT ( 'NONE',  ( -34.72287390941859542, 327.1428504792561966, -4.289995664657297425 ) ) ;
#97612=CARTESIAN_POINT ( 'NONE',  ( -30.89844457542884015, 298.0228418896831499, -9.303756596353716546 ) ) ;
#97619=CARTESIAN_POINT ( 'NONE',  ( 31.35596682365711274, 438.0939828603570732, 22.55458131664589061 ) ) ;
#97623=EDGE_CURVE ( 'NONE', #62753, #95206, #86987, .T. ) ;
#97638=CARTESIAN_POINT ( 'NONE',  ( -44.19066549755412865, 435.2576907183107551, 14.58870676253298804 ) ) ;
#97639=ORIENTED_EDGE ( 'NONE', *, *, #51266, .T. ) ;
#97640=B_SPLINE_CURVE_WITH_KNOTS ( 'NONE', 3,
 ( #19999, #19465, #45824, #86825 ),
 .UNSPECIFIED., .F., .F.,
 ( 4, 4 ),
 ( 9.511364005193116742E-18, 0.001259908249732733529 ),
 .UNSPECIFIED. ) ;
#97665=DIRECTION ( 'NONE',  ( -0.000000000000000000, -1.000000000000000000, -0.000000000000000000 ) ) ;
#97668=CIRCLE ( 'NONE', #47711, 1.000000000000024203 ) ;
#97673=LINE ( 'NONE', #82015, #24335 ) ;
#97674=DIRECTION ( 'NONE',  ( 0.3968475291348042555, -0.1146398630990779210, 0.9106973923363488321 ) ) ;
#97696=CARTESIAN_POINT ( 'NONE',  ( -43.60327462000223875, 484.3404548884703900, 1.191632258386134069 ) ) ;
#97702=EDGE_LOOP ( 'NONE', ( #59561, #7764 ) ) ;
#97703=CIRCLE ( 'NONE', #30544, 0.9999999999999971134 ) ;
#97706=CARTESIAN_POINT ( 'NONE',  ( -46.00000000000000000, 487.9408407045908689, 0.4609445041378137931 ) ) ;
#97711=CARTESIAN_POINT ( 'NONE',  ( 33.24561022503103658, 485.0000549217729713, 0.3114934373725461447 ) ) ;
#97715=PRESENTATION_STYLE_ASSIGNMENT (( #17897 ) ) ;
#97727=DIRECTION ( 'NONE',  ( 0.000000000000000000, -0.000000000000000000, 1.000000000000000000 ) ) ;
#97728=CARTESIAN_POINT ( 'NONE',  ( -24.60488647473181345, 306.9835580411500473, 10.41807558718820914 ) ) ;
#97738=( BOUNDED_SURFACE ( )  B_SPLINE_SURFACE ( 3, 2, ( 
 ( #97215, #67396, #1006 ),
 ( #91671, #14166, #89142 ),
 ( #88609, #42041, #47069 ),
 ( #58774, #56203, #88086 ) ),
 .UNSPECIFIED., .F., .F., .F. ) 
 B_SPLINE_SURFACE_WITH_KNOTS ( ( 4, 4 ),
 ( 3, 3 ),
 ( -8.673617379884035472E-19, 0.002038086101534569098 ),
 ( 0.000000000000000000, 1.000000000000000000 ),
 .UNSPECIFIED. ) 
 GEOMETRIC_REPRESENTATION_ITEM ( )  RATIONAL_B_SPLINE_SURFACE ( (
 ( 1.000000000000000000, 0.7927020107002231697, 1.000000000000000000),
 ( 1.000000000000000000, 0.8068894940779135494, 1.000000000000000000),
 ( 1.000000000000000000, 0.8212065780166435403, 1.000000000000000000),
 ( 1.000000000000000000, 0.8350736500408031393, 1.000000000000000000) ) ) 
 REPRESENTATION_ITEM ( '' )  SURFACE ( )  );
#97742=ORIENTED_EDGE ( 'NONE', *, *, #13257, .F. ) ;
#97789=EDGE_CURVE ( 'NONE', #96664, #22950, #78020, .T. ) ;
#97794=CARTESIAN_POINT ( 'NONE',  ( -33.16501691561005316, 438.9509064377054415, 23.91453236866925636 ) ) ;
#97802=CIRCLE ( 'NONE', #47829, 2.999999999999999112 ) ;
#97809=CARTESIAN_POINT ( 'NONE',  ( -21.51569398614858031, 294.9107018935607130, -9.987480606144490736 ) ) ;
#97812=CARTESIAN_POINT ( 'NONE',  ( -40.07586470527510158, 337.7832441655235129, 20.21182470898328631 ) ) ;
#97813=AXIS2_PLACEMENT_3D ( 'NONE', #72575, #16464, #105477 ) ;
#97816=CARTESIAN_POINT ( 'NONE',  ( 25.50300299142718075, 306.4699755070969900, -8.645387582429501450 ) ) ;
#97820=EDGE_CURVE ( 'NONE', #234, #78207, #74161, .T. ) ;
#97827=ORIENTED_EDGE ( 'NONE', *, *, #21429, .T. ) ;
#97860=EDGE_LOOP ( 'NONE', ( #69504, #53282, #74141, #75524 ) ) ;
#97864=VERTEX_POINT ( 'NONE', #80124 ) ;
#97866=CARTESIAN_POINT ( 'NONE',  ( 38.51502786939605727, 460.0233756673479206, 2.043034587344084940 ) ) ;
#97877=CARTESIAN_POINT ( 'NONE',  ( 32.09753956878954284, 464.8111968410944996, 11.80755753166117650 ) ) ;
#97878=CARTESIAN_POINT ( 'NONE',  ( 46.00000000000000000, 461.9428920847514632, 12.03309428281642823 ) ) ;
#97886=CARTESIAN_POINT ( 'NONE',  ( -36.89235641323539028, 438.8966234958797941, 23.87184663332199364 ) ) ;
#97887=CARTESIAN_POINT ( 'NONE',  ( 32.29035655572196362, 338.5555644040533707, 18.47678205815309127 ) ) ;
#97888=CARTESIAN_POINT ( 'NONE',  ( -35.15293763552459438, 323.3451953424660701, -4.993677134961036046 ) ) ;
#97890=CARTESIAN_POINT ( 'NONE',  ( -44.23892967119426345, 485.3473288767967802, 2.237067153676693732 ) ) ;
#97895=ORIENTED_EDGE ( 'NONE', *, *, #15042, .F. ) ;
#97900=B_SPLINE_CURVE_WITH_KNOTS ( 'NONE', 3,
 ( #38996, #88601, #14156, #105313 ),
 .UNSPECIFIED., .F., .F.,
 ( 4, 4 ),
 ( 0.0007371174630664029549, 0.02698393829534635746 ),
 .UNSPECIFIED. ) ;
#97901=ORIENTED_EDGE ( 'NONE', *, *, #32315, .T. ) ;
#97912=CARTESIAN_POINT ( 'NONE',  ( -35.80547854524250084, 490.7930927354825030, 12.38248481219812902 ) ) ;
#97914=EDGE_CURVE ( 'NONE', #15190, #45269, #19722, .T. ) ;
#97922=CARTESIAN_POINT ( 'NONE',  ( 18.95008105897379025, 304.6966521252900293, 8.904021126966123134 ) ) ;
#97924=DIRECTION ( 'NONE',  ( 0.000000000000000000, -0.8784936690177046481, 0.4777539884666709424 ) ) ;
#97933=STYLED_ITEM ( 'NONE', ( #64592 ), #32808 ) ;
#97939=CARTESIAN_POINT ( 'NONE',  ( -44.03912857160338490, 435.2850055576093951, 15.29440791316631909 ) ) ;
#97942=AXIS2_PLACEMENT_3D ( 'NONE', #69389, #83961, #101740 ) ;
#97958=CARTESIAN_POINT ( 'NONE',  ( 29.07074031792576463, 306.7727993643221112, -9.118181477239474475 ) ) ;
#97975=CARTESIAN_POINT ( 'NONE',  ( 38.81358894280361937, 485.1131561813197095, -4.191378885297321055 ) ) ;
#97984=DIRECTION ( 'NONE',  ( 0.000000000000000000, 0.000000000000000000, -1.000000000000000000 ) ) ;
#97991=EDGE_CURVE ( 'NONE', #72492, #42175, #97075, .T. ) ;
#97993=ORIENTED_EDGE ( 'NONE', *, *, #104657, .F. ) ;
#97999=CARTESIAN_POINT ( 'NONE',  ( 34.72474116627837759, 338.3618661353910966, -1.881472242819908436 ) ) ;
#98006=( LENGTH_UNIT ( ) NAMED_UNIT ( * ) SI_UNIT ( .MILLI., .METRE. ) );
#98016=CARTESIAN_POINT ( 'NONE',  ( 43.21893375708788909, 435.1753267431913059, 16.08377476661154049 ) ) ;
#98017=CARTESIAN_POINT ( 'NONE',  ( -40.24406161231355128, 464.3083606258045393, 17.73326746338202398 ) ) ;
#98019=EDGE_LOOP ( 'NONE', ( #5525, #29709, #106188, #91093, #56038, #57197 ) ) ;
#98020=CARTESIAN_POINT ( 'NONE',  ( 43.50377727019363050, 435.9167426301696082, 18.24083946424738656 ) ) ;
#98026=CARTESIAN_POINT ( 'NONE',  ( 28.92518549787927284, 311.7025783839076780, 12.06490527370083576 ) ) ;
#98030=CARTESIAN_POINT ( 'NONE',  ( -41.35053930173865666, 461.4196900451802321, 2.572867796569714205 ) ) ;
#98038=CARTESIAN_POINT ( 'NONE',  ( -26.69297641637695406, 296.2154876107852601, 2.232032846593750897 ) ) ;
#98049=CARTESIAN_POINT ( 'NONE',  ( 1.102182119232618897E-15, -20.00000000000001776, 9.000000000000007105 ) ) ;
#98053=CARTESIAN_POINT ( 'NONE',  ( 36.14862957314556269, 438.2394791802972236, 3.891583768389438092 ) ) ;
#98082=AXIS2_PLACEMENT_3D ( 'NONE', #77777, #36300, #70738 ) ;
#98086=ORIENTED_EDGE ( 'NONE', *, *, #61923, .F. ) ;
#98096=CARTESIAN_POINT ( 'NONE',  ( 29.62325201385431228, 328.1122814157980088, 15.64796472796876792 ) ) ;
#98108=CARTESIAN_POINT ( 'NONE',  ( -26.27902093981875709, 306.9027577142574614, -9.548073367147230428 ) ) ;
#98109=DIRECTION ( 'NONE',  ( -0.2529971249647862130, 0.000000000000000000, -0.9674670303217327572 ) ) ;
#98118=CARTESIAN_POINT ( 'NONE',  ( -2.922700453530358899, 295.7443989526400401, -10.00347189219610122 ) ) ;
#98125=CARTESIAN_POINT ( 'NONE',  ( -15.88586298981787337, 294.5610647945437108, 1.875232895083775331 ) ) ;
#98131=B_SPLINE_CURVE_WITH_KNOTS ( 'NONE', 3,
 ( #103860, #4121, #87170, #5185 ),
 .UNSPECIFIED., .F., .F.,
 ( 4, 4 ),
 ( 0.000000000000000000, 0.002002928617504379401 ),
 .UNSPECIFIED. ) ;
#98145=CARTESIAN_POINT ( 'NONE',  ( -31.67837264767364402, 439.4052006294236890, 23.39994154329854226 ) ) ;
#98147=CARTESIAN_POINT ( 'NONE',  ( -33.28951410023742596, 318.6302480808201381, -6.419669330273621632 ) ) ;
#98153=CARTESIAN_POINT ( 'NONE',  ( -26.03744394287809882, 295.8532420388733044, -9.784778624385232604 ) ) ;
#98161=CARTESIAN_POINT ( 'NONE',  ( 23.52633860068766225, 305.9421485136137449, 9.176037288099113454 ) ) ;
#98162=CARTESIAN_POINT ( 'NONE',  ( -43.00000000000000000, 464.8825480873695710, 15.07585856869432206 ) ) ;
#98168=CARTESIAN_POINT ( 'NONE',  ( -33.21174982058442282, 465.5907685032092331, 15.87814633360742178 ) ) ;
#98172=CARTESIAN_POINT ( 'NONE',  ( -38.91012333415075375, 438.0862499651277631, 23.13793682581813371 ) ) ;
#98178=CARTESIAN_POINT ( 'NONE',  ( 0.000000000000000000, 274.9999999999999432, 0.000000000000000000 ) ) ;
#98192=CIRCLE ( 'NONE', #80944, 2.999999999999987121 ) ;
#98195=DIRECTION ( 'NONE',  ( -0.3845251595717362192, -0.02506431005118274144, -0.9227741771516956293 ) ) ;
#98208=CARTESIAN_POINT ( 'NONE',  ( 8.572527594031465301E-16, 0.000000000000000000, 6.999999999999993783 ) ) ;
#98212=CARTESIAN_POINT ( 'NONE',  ( 22.42417502586373246, 305.3961751430792333, 10.05444931189341773 ) ) ;
#98213=CARTESIAN_POINT ( 'NONE',  ( -32.87547266101637433, 465.6993878536673606, 10.91512469976170330 ) ) ;
#98215=CARTESIAN_POINT ( 'NONE',  ( 32.06550094448246568, 486.4396568316712433, 6.103009648082660554 ) ) ;
#98216=B_SPLINE_CURVE_WITH_KNOTS ( 'NONE', 3,
 ( #49133, #81489, #73407, #80444, #56145, #7090 ),
 .UNSPECIFIED., .F., .F.,
 ( 4, 2, 4 ),
 ( 0.000000000000000000, 0.001670251840623334597, 0.003340503681246669195 ),
 .UNSPECIFIED. ) ;
#98226=CARTESIAN_POINT ( 'NONE',  ( 2.019483917365790222E-25, 303.8518027762758038, 9.936999415352289589 ) ) ;
#98231=CARTESIAN_POINT ( 'NONE',  ( -43.75401118688380819, 486.3173572309548263, 5.908089951475190560 ) ) ;
#98233=AXIS2_PLACEMENT_3D ( 'NONE', #54147, #88664, #29406 ) ;
#98237=ORIENTED_EDGE ( 'NONE', *, *, #62637, .T. ) ;
#98238=CARTESIAN_POINT ( 'NONE',  ( -43.03265099499957813, 484.2747968070553384, -0.8099405866661226749 ) ) ;
#98249=DIRECTION ( 'NONE',  ( 0.000000000000000000, -0.9238632370064382426, 0.3827227708250269256 ) ) ;
#98261=CARTESIAN_POINT ( 'NONE',  ( -22.87160824404999815, 295.0982458469678136, -1.947616908246118106 ) ) ;
#98269=CARTESIAN_POINT ( 'NONE',  ( 43.77664590664291211, 434.3717993398995532, 11.97532627841538755 ) ) ;
#98274=CARTESIAN_POINT ( 'NONE',  ( 42.09210974227526947, 317.4093497706929270, -4.557617623460385126 ) ) ;
#98276=B_SPLINE_CURVE_WITH_KNOTS ( 'NONE', 3,
 ( #38709, #89378, #9354, #14930 ),
 .UNSPECIFIED., .F., .F.,
 ( 4, 4 ),
 ( 3.469446951953614189E-18, 0.001842998688485824764 ),
 .UNSPECIFIED. ) ;
#98277=CARTESIAN_POINT ( 'NONE',  ( -38.51502786940066869, 460.6916007118362018, 1.299075388248767116 ) ) ;
#98280=CARTESIAN_POINT ( 'NONE',  ( -40.32369798409565931, 437.3250542437391459, 5.179402639112346662 ) ) ;
#98281=CARTESIAN_POINT ( 'NONE',  ( -28.24509918527273555, 316.3792769537042773, 11.76181215083657250 ) ) ;
#98299=EDGE_CURVE ( 'NONE', #29166, #15460, #69647, .T. ) ;
#98317=CARTESIAN_POINT ( 'NONE',  ( -33.05273490460238861, 434.2935873781336795, 15.73821027039317855 ) ) ;
#98320=AXIS2_PLACEMENT_3D ( 'NONE', #4633, #38602, #87149 ) ;
#98329=CARTESIAN_POINT ( 'NONE',  ( 39.41877109955689917, 438.9233561163386526, 23.32050101277916454 ) ) ;
#98345=CARTESIAN_POINT ( 'NONE',  ( 34.83844953170066816, 463.9146721063449377, 18.82558425661361667 ) ) ;
#98350=CARTESIAN_POINT ( 'NONE',  ( -22.91651842568168362, 295.0901107613288445, -9.949346074078583513 ) ) ;
#98351=CARTESIAN_POINT ( 'NONE',  ( -32.35336999986095208, 300.6590557721156642, 11.25190399080426751 ) ) ;
#98354=CARTESIAN_POINT ( 'NONE',  ( 30.88074124778558271, 314.2284791753184550, -6.769356187408334335 ) ) ;
#98366=CARTESIAN_POINT ( 'NONE',  ( -34.62305774441605166, 437.4305192986070665, 5.012907847576948406 ) ) ;
#98384=( NAMED_UNIT ( * ) SI_UNIT ( $, .STERADIAN. ) SOLID_ANGLE_UNIT ( ) );
#98393=CARTESIAN_POINT ( 'NONE',  ( -32.78741055188834963, 485.3331003366709524, 5.977022408746728743 ) ) ;
#98399=FACE_OUTER_BOUND ( 'NONE', #16779, .T. ) ;
#98402=CARTESIAN_POINT ( 'NONE',  ( -36.00698207622544800, 463.3390700132996471, 20.06331035628171477 ) ) ;
#98406=AXIS2_PLACEMENT_3D ( 'NONE', #92071, #91036, #74810 ) ;
#98407=CARTESIAN_POINT ( 'NONE',  ( 30.00000000003604583, 464.1992935685874500, 14.61140485305311287 ) ) ;
#98419=CARTESIAN_POINT ( 'NONE',  ( -43.51548580532710986, 326.4597452001241891, -2.301069477277255082 ) ) ;
#98428=CARTESIAN_POINT ( 'NONE',  ( 13.82057366821712030, 304.5462546222179299, 9.872053150317878334 ) ) ;
#98429=CARTESIAN_POINT ( 'NONE',  ( 41.71962970575597041, 464.4826118731726865, 17.11510788665847471 ) ) ;
#98434=ADVANCED_FACE ( 'NONE', ( #7040 ), #81837, .T. ) ;
#98441=CARTESIAN_POINT ( 'NONE',  ( -37.50059943756435388, 490.7879993827817771, 12.38039871356567545 ) ) ;
#98454=FACE_OUTER_BOUND ( 'NONE', #98603, .T. ) ;
#98480=CARTESIAN_POINT ( 'NONE',  ( 31.90370271533504720, 298.6862772617328687, -9.153364518401147620 ) ) ;
#98486=ORIENTED_EDGE ( 'NONE', *, *, #28328, .T. ) ;
#98490=CARTESIAN_POINT ( 'NONE',  ( 45.42099917976970858, 373.9660313122255957, 6.497677916510750329 ) ) ;
#98492=CARTESIAN_POINT ( 'NONE',  ( 43.61182701071368939, 463.4400368046298127, 6.347502766232850924 ) ) ;
#98498=EDGE_CURVE ( 'NONE', #5193, #67017, #59333, .T. ) ;
#98501=VERTEX_POINT ( 'NONE', #22202 ) ;
#98521=CARTESIAN_POINT ( 'NONE',  ( 40.93292669599463096, 378.0706848361106722, 26.55786848468904537 ) ) ;
#98535=VERTEX_POINT ( 'NONE', #51205 ) ;
#98537=ORIENTED_EDGE ( 'NONE', *, *, #59285, .F. ) ;
#98540=CARTESIAN_POINT ( 'NONE',  ( -41.75466287779232033, 464.7989438035445460, 15.73053683052044960 ) ) ;
#98544=CARTESIAN_POINT ( 'NONE',  ( 32.96114378239634846, 439.7497662205600477, 24.15381041467298928 ) ) ;
#98547=CARTESIAN_POINT ( 'NONE',  ( 40.27367167681648397, 320.5181970100869648, 8.188281879750116232 ) ) ;
#98548=CARTESIAN_POINT ( 'NONE',  ( 41.66301127302160978, 485.3863426732067978, -3.409513628943111829 ) ) ;
#98554=CARTESIAN_POINT ( 'NONE',  ( 32.62553167428433198, 485.9570050037727356, 7.214059741204942533 ) ) ;
#98560=CARTESIAN_POINT ( 'NONE',  ( -29.13995660218273898, 297.4011841907129110, 2.495382766646905282 ) ) ;
#98568=CARTESIAN_POINT ( 'NONE',  ( 2.361169560329932526, 300.9835946509371070, 9.719902681333095984 ) ) ;
#98579=CARTESIAN_POINT ( 'NONE',  ( 21.29975379448946171, 294.8969325209483259, -1.990407376643353210 ) ) ;
#98582=ADVANCED_FACE ( 'NONE', ( #74425 ), #53514, .F. ) ;
#98603=EDGE_LOOP ( 'NONE', ( #68405, #49149, #47703, #3339 ) ) ;
#98615=ORIENTED_EDGE ( 'NONE', *, *, #15299, .T. ) ;
#98619=CARTESIAN_POINT ( 'NONE',  ( 31.16300488023808057, 374.7522420000291277, 23.86485433879470364 ) ) ;
#98620=EDGE_CURVE ( 'NONE', #51023, #58545, #100731, .T. ) ;
#98624=CARTESIAN_POINT ( 'NONE',  ( -43.31290673308605221, 487.3457497296792553, 8.045183856861967797 ) ) ;
#98634=CARTESIAN_POINT ( 'NONE',  ( -43.51084452654468748, 465.2903130129606666, 9.421687747985890482 ) ) ;
#98639=CARTESIAN_POINT ( 'NONE',  ( -2.569942033241107815, 295.6515237736050494, -10.00266688365466017 ) ) ;
#98650=CARTESIAN_POINT ( 'NONE',  ( 37.51493083963053721, 491.7337707781528024, 12.51683509955209672 ) ) ;
#98652=CARTESIAN_POINT ( 'NONE',  ( -34.16218064238212548, 484.1154536690855252, 0.7177099017928977309 ) ) ;
#98666=CARTESIAN_POINT ( 'NONE',  ( -31.38091039062430099, 439.2456886734215118, 22.99800500073227738 ) ) ;
#98667=CARTESIAN_POINT ( 'NONE',  ( -32.33884982129379182, 318.8862026410800468, -6.596051802676561771 ) ) ;
#98673=CARTESIAN_POINT ( 'NONE',  ( -25.12920025922564449, 295.5949704605591251, -9.840788051256282642 ) ) ;
#98679=CARTESIAN_POINT ( 'NONE',  ( -41.26652560176431450, 329.6458478461855179, 10.39356917096987054 ) ) ;
#98681=CARTESIAN_POINT ( 'NONE',  ( -40.67741014324408155, 464.1451327582763042, 18.19863275169177896 ) ) ;
#98688=CARTESIAN_POINT ( 'NONE',  ( 44.08840282922842846, 485.7747746244180576, 4.178803824088268115 ) ) ;
#98689=CARTESIAN_POINT ( 'NONE',  ( 46.00000000000000000, 500.0000000000002274, 0.000000000000000000 ) ) ;
#98730=CARTESIAN_POINT ( 'NONE',  ( -32.12958771267398816, 464.7275665249426311, 11.12424126545965386 ) ) ;
#98732=CARTESIAN_POINT ( 'NONE',  ( 32.15552878745101140, 487.8964323476858453, 8.685603495209447189 ) ) ;
#98739=CARTESIAN_POINT ( 'NONE',  ( 32.43176025740030610, 464.5282231481863846, 9.485014939590488581 ) ) ;
#98772=CARTESIAN_POINT ( 'NONE',  ( 44.16317469766475057, 463.2893454858578366, 6.606904447375195666 ) ) ;
#98777=CARTESIAN_POINT ( 'NONE',  ( -29.99999999999696243, 464.1078291054902252, 11.04693782968386628 ) ) ;
#98779=CARTESIAN_POINT ( 'NONE',  ( -31.75048384320466255, 299.0195043205505385, -1.074641621235506772 ) ) ;
#98784=VERTEX_POINT ( 'NONE', #11814 ) ;
#98785=CARTESIAN_POINT ( 'NONE',  ( 43.80679553849883945, 434.9371637098674910, 12.86766421698563967 ) ) ;
#98789=CARTESIAN_POINT ( 'NONE',  ( -42.20041562234357713, 435.2369744135580731, 7.788607701745519307 ) ) ;
#98801=B_SPLINE_CURVE_WITH_KNOTS ( 'NONE', 3,
 ( #42678, #35148, #66416, #82607 ),
 .UNSPECIFIED., .F., .F.,
 ( 4, 4 ),
 ( 4.718958039861916012E-17, 0.002256496660504680660 ),
 .UNSPECIFIED. ) ;
#98827=CARTESIAN_POINT ( 'NONE',  ( -30.83208909486066318, 321.1666868008755955, 14.44335677805165119 ) ) ;
#98837=CARTESIAN_POINT ( 'NONE',  ( -39.98667076425689260, 490.5869148090167187, 11.68052433275972746 ) ) ;
#98839=ADVANCED_FACE ( 'NONE', ( #23535 ), #56317, .F. ) ;
#98840=CARTESIAN_POINT ( 'NONE',  ( 36.61006234131809833, 439.8077055994807552, 24.20807427523271826 ) ) ;
#98842=SHAPE_DEFINITION_REPRESENTATION ( #59534, #19231 ) ;
#98849=ORIENTED_EDGE ( 'NONE', *, *, #53996, .F. ) ;
#98850=CARTESIAN_POINT ( 'NONE',  ( -42.19180677453720563, 462.2931784592651638, 3.389262873192010694 ) ) ;
#98852=CARTESIAN_POINT ( 'NONE',  ( 36.18016141387847284, 463.3220971514209054, 20.09605424492473702 ) ) ;
#98858=FACE_OUTER_BOUND ( 'NONE', #84366, .T. ) ;
#98862=CARTESIAN_POINT ( 'NONE',  ( 28.19925613136460640, 308.7765882544961755, -9.111076883841365159 ) ) ;
#98892=CARTESIAN_POINT ( 'NONE',  ( 30.00000000000000000, 500.0000000000002274, -5.000000000000001776 ) ) ;
#98896=CARTESIAN_POINT ( 'NONE',  ( 10.01915592506146879, 302.6453132215669939, -2.043889601136144485 ) ) ;
#98898=SURFACE_STYLE_FILL_AREA ( #24009 ) ;
#98905=CARTESIAN_POINT ( 'NONE',  ( 32.16569164323090035, 318.9480643375377440, -5.577539070780133557 ) ) ;
#98907=CARTESIAN_POINT ( 'NONE',  ( 33.94783393359906398, 484.1261039197348737, 1.321740980885009353 ) ) ;
#98919=FACE_OUTER_BOUND ( 'NONE', #21530, .T. ) ;
#98922=CARTESIAN_POINT ( 'NONE',  ( 12.08334041755991706, 304.5866437775407007, -10.05636128505472726 ) ) ;
#98931=CARTESIAN_POINT ( 'NONE',  ( 32.13832923886224080, 335.6472655370285452, 17.84808702340633602 ) ) ;
#98933=CARTESIAN_POINT ( 'NONE',  ( -36.51946503641791253, 336.4369612853828357, -1.859061548502462857 ) ) ;
#98947=ORIENTED_EDGE ( 'NONE', *, *, #100585, .F. ) ;
#98955=CARTESIAN_POINT ( 'NONE',  ( -37.54559764570181812, 464.1143081516144662, 19.43664670202813838 ) ) ;
#98956=CARTESIAN_POINT ( 'NONE',  ( -36.13333162057816139, 491.8038228668677903, 12.56276695383520092 ) ) ;
#98964=CARTESIAN_POINT ( 'NONE',  ( -17.24303157407923237, 294.5700599009814482, 9.877113118490870036 ) ) ;
#98980=B_SPLINE_CURVE_WITH_KNOTS ( 'NONE', 3,
 ( #1514, #50081, #51136, #34482 ),
 .UNSPECIFIED., .F., .F.,
 ( 4, 4 ),
 ( 1.734723475976807094E-17, 0.003262827847960974702 ),
 .UNSPECIFIED. ) ;
#98986=CARTESIAN_POINT ( 'NONE',  ( 36.02493936428268029, 463.3371199957072690, 20.06709031638022367 ) ) ;
#98999=CARTESIAN_POINT ( 'NONE',  ( 29.10832111663954791, 306.8131183972279814, -9.108704873592294859 ) ) ;
#99011=CARTESIAN_POINT ( 'NONE',  ( 43.65158569082660733, 382.1618310280565538, 15.13503673623559820 ) ) ;
#99012=CARTESIAN_POINT ( 'NONE',  ( 43.70836520789914914, 463.8610993545788119, 7.295416580059431055 ) ) ;
#99015=CARTESIAN_POINT ( 'NONE',  ( -21.93428938517136118, 305.2394520450566233, 9.020384747005401493 ) ) ;
#99018=CARTESIAN_POINT ( 'NONE',  ( 36.09356709110171124, 485.3869947698531178, -3.408842397901690635 ) ) ;
#99019=AXIS2_PLACEMENT_3D ( 'NONE', #94894, #101896, #37201 ) ;
#99027=CARTESIAN_POINT ( 'NONE',  ( 45.99999999999999289, 436.0322433031492437, 12.60696238181549234 ) ) ;
#99039=CARTESIAN_POINT ( 'NONE',  ( 22.42417502586373246, 305.3961751430792333, 10.05444931189341773 ) ) ;
#99042=CARTESIAN_POINT ( 'NONE',  ( 0.000000000000000000, 70.00000000000000000, 0.000000000000000000 ) ) ;
#99051=CARTESIAN_POINT ( 'NONE',  ( 51.01037695545453232, 500.0000000000002274, 0.000000000000000000 ) ) ;
#99059=CARTESIAN_POINT ( 'NONE',  ( 43.03357534759661718, 463.2291678140137492, 4.675918524166122303 ) ) ;
#99062=CARTESIAN_POINT ( 'NONE',  ( -31.14081447784786505, 433.9613651262616827, 24.00306230370002325 ) ) ;
#99065=CARTESIAN_POINT ( 'NONE',  ( 42.21835935851049726, 436.4384481632509392, 19.62208033733266888 ) ) ;
#99072=CARTESIAN_POINT ( 'NONE',  ( 33.31031872651021075, 302.0743058889032113, 11.59258997849307526 ) ) ;
#99077=CIRCLE ( 'NONE', #886, 6.999999999999982236 ) ;
#99079=CARTESIAN_POINT ( 'NONE',  ( 42.77045538396055946, 384.7557768097599364, 19.23094703895946012 ) ) ;
#99085=CARTESIAN_POINT ( 'NONE',  ( -24.84125933061083558, 295.6108665521396119, 2.099934395011584520 ) ) ;
#99090=CARTESIAN_POINT ( 'NONE',  ( 9.017160581220602822, 295.0459686547099523, 4.334444195353072793 ) ) ;
#99091=CARTESIAN_POINT ( 'NONE',  ( 46.00000000000000000, 464.2883104330365995, 11.80345442597034555 ) ) ;
#99096=ORIENTED_EDGE ( 'NONE', *, *, #100717, .F. ) ;
#99108=CARTESIAN_POINT ( 'NONE',  ( -32.96117425224259989, 439.7497740807306741, 24.15381775812842946 ) ) ;
#99109=DIRECTION ( 'NONE',  ( 0.000000000000000000, 0.000000000000000000, 1.000000000000000000 ) ) ;
#99113=CARTESIAN_POINT ( 'NONE',  ( 34.16642289233210050, 464.7650419733888043, 19.36631221618525345 ) ) ;
#99114=CARTESIAN_POINT ( 'NONE',  ( -43.75010090113929806, 464.8337800386750018, 11.75004750934965791 ) ) ;
#99118=ORIENTED_EDGE ( 'NONE', *, *, #15394, .F. ) ;
#99129=CARTESIAN_POINT ( 'NONE',  ( 41.98130293123185197, 462.0609698853055534, 3.143960326150163187 ) ) ;
#99132=B_SPLINE_CURVE_WITH_KNOTS ( 'NONE', 3,
 ( #39303, #65146, #106119, #81313, #22609, #80254, #57564, #32275, #7425, #81841 ),
 .UNSPECIFIED., .F., .F.,
 ( 4, 2, 2, 2, 4 ),
 ( -5.999999999154135157E-08, 0.002478699646394690818, 0.004957459292789372605, 0.009914978585578743120, 0.01983001717115747548 ),
 .UNSPECIFIED. ) ;
#99138=CARTESIAN_POINT ( 'NONE',  ( -43.99980723760477730, 434.6400489724846921, 17.20555692211243581 ) ) ;
#99144=ORIENTED_EDGE ( 'NONE', *, *, #35567, .F. ) ;
#99145=ORIENTED_EDGE ( 'NONE', *, *, #46604, .F. ) ;
#99149=CARTESIAN_POINT ( 'NONE',  ( 32.19533246082933431, 392.4695659865649304, 25.42398475254776358 ) ) ;
#99160=CARTESIAN_POINT ( 'NONE',  ( -31.03867016165222026, 468.3124986733989772, 18.90871194958903345 ) ) ;
#99169=CARTESIAN_POINT ( 'NONE',  ( -0.3768998506200362253, 294.9778291542829152, -9.999928804128023430 ) ) ;
#99172=CARTESIAN_POINT ( 'NONE',  ( 42.09158233638500235, 465.7816406625409513, 14.79318349170030089 ) ) ;
#99178=CARTESIAN_POINT ( 'NONE',  ( 36.65190467452017486, 491.8432146685188968, 12.58836626716453644 ) ) ;
#99184=CARTESIAN_POINT ( 'NONE',  ( -7.737907992291022552, 302.4298231441208031, -10.02991391761277207 ) ) ;
#99195=CARTESIAN_POINT ( 'NONE',  ( -31.31625665069342190, 438.7960044619113660, 22.44465281717054950 ) ) ;
#99196=CARTESIAN_POINT ( 'NONE',  ( 33.00496812083888898, 465.6658704666191966, 15.15901827093884258 ) ) ;
#99197=CARTESIAN_POINT ( 'NONE',  ( -29.13274776455849846, 308.3486360454327269, -8.978973805476414327 ) ) ;
#99201=AXIS2_PLACEMENT_3D ( 'NONE', #13018, #56115, #45946 ) ;
#99205=CARTESIAN_POINT ( 'NONE',  ( -25.82432753990636698, 295.8677741265493637, -1.781385710556211421 ) ) ;
#99206=ADVANCED_FACE ( 'NONE', ( #31502 ), #64544, .F. ) ;
#99211=CARTESIAN_POINT ( 'NONE',  ( -34.05377651491208013, 485.0003423799789743, 0.6720595971183709327 ) ) ;
#99212=CARTESIAN_POINT ( 'NONE',  ( -33.12749645818041699, 378.6598013907594691, 24.66483730404220154 ) ) ;
#99214=CARTESIAN_POINT ( 'NONE',  ( -39.73517528558786438, 463.8619862608260860, 18.93615324539412370 ) ) ;
#99226=CARTESIAN_POINT ( 'NONE',  ( -32.22120753352773193, 464.6691781026584636, 10.60621122532597305 ) ) ;
#99230=EDGE_CURVE ( 'NONE', #26488, #104525, #92177, .T. ) ;
#99240=AXIS2_PLACEMENT_3D ( 'NONE', #23748, #23211, #22688 ) ;
#99245=CARTESIAN_POINT ( 'NONE',  ( -41.97866624869027419, 465.7384095647168465, 15.05473019647155830 ) ) ;
#99257=CARTESIAN_POINT ( 'NONE',  ( 33.63427961064055438, 325.9154870834976236, -4.827994974213513757 ) ) ;
#99258=CARTESIAN_POINT ( 'NONE',  ( 40.18832759596136128, 460.7626523741619167, 2.139563623142427762 ) ) ;
#99263=CARTESIAN_POINT ( 'NONE',  ( -43.59756234217329762, 434.3244621007154365, 14.55946156040307926 ) ) ;
#99267=EDGE_CURVE ( 'NONE', #33881, #9120, #6106, .T. ) ;
#99270=CARTESIAN_POINT ( 'NONE',  ( -16.53877150159848242, 304.5679819412924871, 8.876634200354359905 ) ) ;
#99299=CARTESIAN_POINT ( 'NONE',  ( 45.99999999999412381, 462.6092035404159333, 6.975422689164243018 ) ) ;
#99301=( BOUNDED_SURFACE ( )  B_SPLINE_SURFACE ( 3, 2, ( 
 ( #53577, #91272, #66441 ),
 ( #58353, #1143, #17383 ),
 ( #24949, #50257, #73993 ),
 ( #16841, #33565, #7135 ) ),
 .UNSPECIFIED., .F., .F., .F. ) 
 B_SPLINE_SURFACE_WITH_KNOTS ( ( 4, 4 ),
 ( 3, 3 ),
 ( 5.642621786483559276E-15, 0.002106423517718437628 ),
 ( 0.000000000000000000, 1.000000000000000000 ),
 .UNSPECIFIED. ) 
 GEOMETRIC_REPRESENTATION_ITEM ( )  RATIONAL_B_SPLINE_SURFACE ( (
 ( 1.000000000000000000, 0.7977970988453120249, 1.000000000000000000),
 ( 1.000000000000000000, 0.8078744440618467193, 1.000000000000000000),
 ( 1.000000000000000000, 0.8177468419060218707, 1.000000000000000000),
 ( 1.000000000000000000, 0.8274831119534205026, 1.000000000000000000) ) ) 
 REPRESENTATION_ITEM ( '' )  SURFACE ( )  );
#99304=CARTESIAN_POINT ( 'NONE',  ( -30.00000000000005329, 464.1062179653383168, 10.70584622102857786 ) ) ;
#99314=CARTESIAN_POINT ( 'NONE',  ( 44.33427973454571713, 435.2106362794496590, 13.55537084937271430 ) ) ;
#99322=CARTESIAN_POINT ( 'NONE',  ( 33.22325481135199965, 463.2504524720463337, 6.140871053189498774 ) ) ;
#99324=CARTESIAN_POINT ( 'NONE',  ( -30.13306121044136177, 331.7621428518107223, 15.49882586424142694 ) ) ;
#99328=FACE_OUTER_BOUND ( 'NONE', #94013, .T. ) ;
#99334=DIRECTION ( 'NONE',  ( 0.000000000000000000, 0.000000000000000000, -1.000000000000000000 ) ) ;
#99335=CARTESIAN_POINT ( 'NONE',  ( 20.01715961282798872, 303.8268864493743422, 9.931703227614395502 ) ) ;
#99340=CARTESIAN_POINT ( 'NONE',  ( -40.35113922517010110, 477.0906381947924046, -2.238203954573617871 ) ) ;
#99344=ORIENTED_EDGE ( 'NONE', *, *, #42754, .T. ) ;
#99349=CARTESIAN_POINT ( 'NONE',  ( -33.13378764655153930, 418.1818430120953280, 25.61784589414144264 ) ) ;
#99355=CARTESIAN_POINT ( 'NONE',  ( -33.00000000000000000, 450.0000000000002274, 13.20242257375370976 ) ) ;
#99359=EDGE_CURVE ( 'NONE', #65357, #91640, #101520, .T. ) ;
#99364=CARTESIAN_POINT ( 'NONE',  ( 9.789044728060087408, 294.6486233851415477, -2.043184600578025201 ) ) ;
#99368=CARTESIAN_POINT ( 'NONE',  ( 36.96037796283875565, 439.3711962631035703, 23.79839446779178402 ) ) ;
#99384=PRODUCT ( '4. Handle', '4. Handle', '', ( #33096 ) ) ;
#99387=CARTESIAN_POINT ( 'NONE',  ( -25.93947128054312756, 296.0094280503604978, 10.18659011856751384 ) ) ;
#99390=EDGE_LOOP ( 'NONE', ( #60311, #34528, #309, #79112 ) ) ;
#99391=CARTESIAN_POINT ( 'NONE',  ( 23.06742787864941846, 305.3843356243662015, -9.885683119079418546 ) ) ;
#99395=EDGE_CURVE ( 'NONE', #44923, #64080, #104709, .T. ) ;
#99399=VERTEX_POINT ( 'NONE', #50816 ) ;
#99400=DIRECTION ( 'NONE',  ( 0.000000000000000000, 0.000000000000000000, 1.000000000000000000 ) ) ;
#99407=CARTESIAN_POINT ( 'NONE',  ( -35.75766626157646044, 437.8288023593529488, 4.424845182008526834 ) ) ;
#99410=ORIENTED_EDGE ( 'NONE', *, *, #54383, .F. ) ;
#99417=EDGE_CURVE ( 'NONE', #66822, #6722, #369, .T. ) ;
#99439=CARTESIAN_POINT ( 'NONE',  ( -32.80395775116956258, 487.0274233559226218, 8.980975396762143959 ) ) ;
#99441=EDGE_CURVE ( 'NONE', #100372, #31339, #1737, .T. ) ;
#99445=DIRECTION ( 'NONE',  ( 0.000000000000000000, 0.000000000000000000, 1.000000000000000000 ) ) ;
#99449=CARTESIAN_POINT ( 'NONE',  ( -13.31081044356851173, 294.5490281876303698, -2.064334394374285786 ) ) ;
#99455=ORIENTED_EDGE ( 'NONE', *, *, #88242, .T. ) ;
#99458=CARTESIAN_POINT ( 'NONE',  ( 30.00000000000000355, 462.0139486977120100, 13.78583326880718829 ) ) ;
#99459=CARTESIAN_POINT ( 'NONE',  ( 0.000000000000000000, 294.8518027762758038, -10.00000000000000355 ) ) ;
#99470=CARTESIAN_POINT ( 'NONE',  ( -39.70493663810997731, 309.1761292106233441, -6.633558359608890065 ) ) ;
#99474=CYLINDRICAL_SURFACE ( 'NONE', #66711, 4.999999999999999112 ) ;
#99495=CARTESIAN_POINT ( 'NONE',  ( -34.58748436418674288, 491.1940522429816838, 12.14470207312695393 ) ) ;
#99496=ADVANCED_FACE ( 'NONE', ( #78293 ), #93543, .T. ) ;
#99497=DIRECTION ( 'NONE',  ( 0.000000000000000000, 0.000000000000000000, 1.000000000000000000 ) ) ;
#99520=CARTESIAN_POINT ( 'NONE',  ( 32.17646412119353272, 464.6980787822281513, 10.84896803613063021 ) ) ;
#99538=CARTESIAN_POINT ( 'NONE',  ( -46.00000000000000000, 488.3725375423296668, 3.127739281037489771 ) ) ;
#99542=CARTESIAN_POINT ( 'NONE',  ( 35.41928903355742619, 301.9014398045767393, -8.406339170677471273 ) ) ;
#99554=CARTESIAN_POINT ( 'NONE',  ( 37.65605239364586510, 426.5628754408557484, 5.696003171475078730 ) ) ;
#99557=CARTESIAN_POINT ( 'NONE',  ( -21.87180833870418084, 305.2301849206776865, 10.01838919985740084 ) ) ;
#99561=CARTESIAN_POINT ( 'NONE',  ( 32.76481181382172281, 487.6128877199117255, 8.618969267250339072 ) ) ;
#99566=CARTESIAN_POINT ( 'NONE',  ( 44.21548463017017383, 435.3173990239856721, 11.13835373606124435 ) ) ;
#99571=PRODUCT_DEFINITION_CONTEXT ( 'detailed design', #5231, 'design' ) ;
#99572=DIRECTION ( 'NONE',  ( -1.000000000000000000, 0.000000000000000000, 0.000000000000000000 ) ) ;
#99584=CARTESIAN_POINT ( 'NONE',  ( -32.12115510384169426, 486.2840111611076281, 5.773919067741624112 ) ) ;
#99588=ORIENTED_EDGE ( 'NONE', *, *, #3666, .F. ) ;
#99594=CARTESIAN_POINT ( 'NONE',  ( -32.19491287036717608, 391.9754712875484870, 25.40006242682984094 ) ) ;
#99601=AXIS2_PLACEMENT_3D ( 'NONE', #96802, #49282, #56302 ) ;
#99605=CARTESIAN_POINT ( 'NONE',  ( -31.36033717110301566, 339.5230286683110421, 18.44560579463051297 ) ) ;
#99615=CARTESIAN_POINT ( 'NONE',  ( 35.30318952505669472, 303.6718279376253804, 3.969031666316281459 ) ) ;
#99624=CARTESIAN_POINT ( 'NONE',  ( 21.19348424345033521, 294.8901562694577478, 1.945151701991110205 ) ) ;
#99628=CARTESIAN_POINT ( 'NONE',  ( -23.98837369974533118, 303.9359044481634555, 10.17345894387965899 ) ) ;
#99637=AXIS2_PLACEMENT_3D ( 'NONE', #46921, #46409, #37823 ) ;
#99641=CARTESIAN_POINT ( 'NONE',  ( 1.227754105814699780E-15, 67.05096163904791240, 10.02537308446410691 ) ) ;
#99646=ADVANCED_FACE ( 'NONE', ( #10244 ), #66903, .T. ) ;
#99656=CARTESIAN_POINT ( 'NONE',  ( -32.84237740334621236, 485.2251842821281116, 5.746442123025396143 ) ) ;
#99657=B_SPLINE_CURVE_WITH_KNOTS ( 'NONE', 3,
 ( #3107, #26893, #93720, #92644 ),
 .UNSPECIFIED., .F., .F.,
 ( 4, 4 ),
 ( 0.000000000000000000, 0.001861443540404501048 ),
 .UNSPECIFIED. ) ;
#99672=CARTESIAN_POINT ( 'NONE',  ( 37.52420368444853693, 473.1130448734259630, 17.51438724206708741 ) ) ;
#99679=ADVANCED_FACE ( 'NONE', ( #18918, #75509 ), #10759, .T. ) ;
#99687=CARTESIAN_POINT ( 'NONE',  ( 8.242617580643319286, 294.6933141679140249, -5.691011467278013214 ) ) ;
#99692=CARTESIAN_POINT ( 'NONE',  ( 30.62720677515678602, 345.4155763350589154, 19.40254811826110526 ) ) ;
#99693=EDGE_CURVE ( 'NONE', #64080, #93305, #95755, .T. ) ;
#99700=CARTESIAN_POINT ( 'NONE',  ( -32.81882165182332756, 465.7334778289831547, 14.51165368403150957 ) ) ;
#99704=CARTESIAN_POINT ( 'NONE',  ( -35.74363442581862671, 380.1068966271811860, 4.951945592532029927 ) ) ;
#99713=CARTESIAN_POINT ( 'NONE',  ( 35.86580758070825681, 437.2863006609852050, 4.452567007867904714 ) ) ;
#99715=CARTESIAN_POINT ( 'NONE',  ( -9.789044728060268596, 294.6486233851412067, -2.043184600577135690 ) ) ;
#99723=CARTESIAN_POINT ( 'NONE',  ( -17.71457869773037785, 294.6047145785885846, 1.884974438337975844 ) ) ;
#99727=CARTESIAN_POINT ( 'NONE',  ( 43.04469050570450150, 434.7734435962914290, 9.248231035223298591 ) ) ;
#99728=CARTESIAN_POINT ( 'NONE',  ( -37.50813975974288184, 482.1285864697561010, 15.12809618359215946 ) ) ;
#99746=CARTESIAN_POINT ( 'NONE',  ( -35.75052666827532732, 338.6074967675372136, -1.573378144931428801 ) ) ;
#99753=CARTESIAN_POINT ( 'NONE',  ( -27.95499319877095701, 296.5192905871809330, -9.639268393704691462 ) ) ;
#99757=CARTESIAN_POINT ( 'NONE',  ( -33.06942034650614914, 440.0153633844964247, 23.76350862949321296 ) ) ;
#99771=CARTESIAN_POINT ( 'NONE',  ( -2.455508211629401138E-15, 67.05096163904791240, -10.02537308446411402 ) ) ;
#99787=CARTESIAN_POINT ( 'NONE',  ( 30.83282128361384977, 298.3240041198961308, -1.233783556676444793 ) ) ;
#99793=DIRECTION ( 'NONE',  ( 0.000000000000000000, 0.000000000000000000, 1.000000000000000000 ) ) ;
#99802=EDGE_CURVE ( 'NONE', #5652, #23052, #22631, .T. ) ;
#99807=CARTESIAN_POINT ( 'NONE',  ( 26.97491686565329161, 307.4599153070161606, -9.420584459367196573 ) ) ;
#99808=CARTESIAN_POINT ( 'NONE',  ( 40.26058501384567023, 460.2706387420194005, 2.258779328630807548 ) ) ;
#99815=ORIENTED_EDGE ( 'NONE', *, *, #85517, .T. ) ;
#99824=DIRECTION ( 'NONE',  ( 0.3009093847692427270, 0.4108943393899624485, 0.8605924610494111171 ) ) ;
#99838=DIRECTION ( 'NONE',  ( 0.3934424543276984210, -0.4342828891349996834, -0.8103094515906591466 ) ) ;
#99849=CARTESIAN_POINT ( 'NONE',  ( -23.43684916743750080, 295.2641918988800285, 10.02474406024658293 ) ) ;
#99850=CARTESIAN_POINT ( 'NONE',  ( 32.83708119314772489, 465.7129474592467773, 11.08629381895457477 ) ) ;
#99851=EDGE_CURVE ( 'NONE', #30344, #8292, #32008, .T. ) ;
#99867=CARTESIAN_POINT ( 'NONE',  ( 40.95420997525301487, 387.0967036739339164, 27.26945002580065136 ) ) ;
#99875=( GEOMETRIC_REPRESENTATION_CONTEXT ( 3 ) GLOBAL_UNCERTAINTY_ASSIGNED_CONTEXT ( ( #1942 ) ) GLOBAL_UNIT_ASSIGNED_CONTEXT ( ( #98006, #63001, #54877 ) ) REPRESENTATION_CONTEXT ( 'NONE', 'WORKASPACE' ) );
#99879=CARTESIAN_POINT ( 'NONE',  ( -38.88026246212550774, 468.9844136736957694, 0.4637902098120869065 ) ) ;
#99887=CARTESIAN_POINT ( 'NONE',  ( 30.83612787059712446, 330.9523264370013180, 16.54848976118583437 ) ) ;
#99888=CARTESIAN_POINT ( 'NONE',  ( -33.32951764101208880, 490.0033476588132544, 11.19754049617970182 ) ) ;
#99893=ORIENTED_EDGE ( 'NONE', *, *, #91354, .T. ) ;
#99903=CARTESIAN_POINT ( 'NONE',  ( -24.36717267311885138, 304.1505144958332494, 10.22149614222675140 ) ) ;
#99904=CARTESIAN_POINT ( 'NONE',  ( -32.37468555527969016, 435.2081350238080404, 18.54045473102533492 ) ) ;
#99905=EDGE_CURVE ( 'NONE', #17539, #34141, #106024, .T. ) ;
#99910=CARTESIAN_POINT ( 'NONE',  ( 43.00000000000000000, 461.4080316921935605, 3.462976341553817949 ) ) ;
#99918=CARTESIAN_POINT ( 'NONE',  ( -35.49824309011606260, 438.0806692989499993, 4.093885194488227519 ) ) ;
#99925=CARTESIAN_POINT ( 'NONE',  ( -42.36808196472508570, 461.6713445545159402, 3.771400599639992635 ) ) ;
#99935=CARTESIAN_POINT ( 'NONE',  ( -43.31389755119099050, 487.3431498771909105, 8.040475431002969131 ) ) ;
#99955=DIRECTION ( 'NONE',  ( 0.3009093847692517198, -0.4108943393901564600, -0.8605924610493154159 ) ) ;
#99984=CARTESIAN_POINT ( 'NONE',  ( 35.52983581801517943, 407.4223022866293604, 7.047109836617410750 ) ) ;
#99995=CARTESIAN_POINT ( 'NONE',  ( 32.81762910953230516, 465.7339109553614662, 14.50750636005276384 ) ) ;
#99999=CARTESIAN_POINT ( 'NONE',  ( 32.93513049338609733, 465.6726574193332908, 10.66039033145344384 ) ) ;
#100010=DIRECTION ( 'NONE',  ( -0.000000000000000000, 0.1742756985702848260, 0.9846968979781743903 ) ) ;
#100013=CARTESIAN_POINT ( 'NONE',  ( -40.64764563337315195, 311.8966148236026470, -5.951010960877825440 ) ) ;
#100033=DIRECTION ( 'NONE',  ( 1.000000000000000000, 0.000000000000000000, 0.000000000000000000 ) ) ;
#100049=CARTESIAN_POINT ( 'NONE',  ( 44.20232540310176006, 435.2535269811378384, 14.52161920496060077 ) ) ;
#100051=DIRECTION ( 'NONE',  ( -0.2276554125553486296, 0.04124382534092855407, 0.9728679047052077866 ) ) ;
#100055=EDGE_LOOP ( 'NONE', ( #84370, #30268 ) ) ;
#100066=CARTESIAN_POINT ( 'NONE',  ( 37.05595180434897173, 463.3109355731702976, 20.11755950910298196 ) ) ;
#100080=CARTESIAN_POINT ( 'NONE',  ( 28.49755062498792668, 296.9296401919173150, -1.547493658460767696 ) ) ;
#100090=CARTESIAN_POINT ( 'NONE',  ( 45.40857607514351457, 438.4254919824014678, 6.241822647824930570 ) ) ;
#100096=CARTESIAN_POINT ( 'NONE',  ( -21.45209470218146564, 305.1036098005744748, 8.990911056619731667 ) ) ;
#100098=CARTESIAN_POINT ( 'NONE',  ( 32.84237740334622657, 485.2251842821286800, 5.746442123025142124 ) ) ;
#100101=CARTESIAN_POINT ( 'NONE',  ( 32.78741055188848463, 485.3331003366708956, 5.977022408746977433 ) ) ;
#100121=CARTESIAN_POINT ( 'NONE',  ( 40.61216075948964033, 351.1469683695276558, 22.89433108575548914 ) ) ;
#100122=DIRECTION ( 'NONE',  ( -1.000000000000000000, 0.000000000000000000, 0.000000000000000000 ) ) ;
#100124=CARTESIAN_POINT ( 'NONE',  ( -30.00000000000000355, 490.2049413377403084, 6.956578743376784502 ) ) ;
#100134=CARTESIAN_POINT ( 'NONE',  ( -27.94791896389481778, 311.8549610008433319, 11.86231666168937693 ) ) ;
#100155=CARTESIAN_POINT ( 'NONE',  ( 31.51275525728127747, 299.7698742078038094, 11.04316810569213381 ) ) ;
#100159=CARTESIAN_POINT ( 'NONE',  ( 38.64013033672255659, 312.1321624020491186, 6.078733131242813670 ) ) ;
#100164=CARTESIAN_POINT ( 'NONE',  ( -22.33970404802145637, 303.2844704797087161, 10.02998793445647685 ) ) ;
#100166=UNCERTAINTY_MEASURE_WITH_UNIT (LENGTH_MEASURE( 1.000000000000000082E-05 ), #51119, 'distance_accuracy_value', 'NONE');
#100168=CARTESIAN_POINT ( 'NONE',  ( 0.9522842513689456778, 294.8487785400556618, 1.936375222902182225 ) ) ;
#100182=AXIS2_PLACEMENT_3D ( 'NONE', #96989, #367, #105086 ) ;
#100192=CARTESIAN_POINT ( 'NONE',  ( -31.81386177463738107, 439.0024176103436275, 23.54436022379337246 ) ) ;
#100193=CARTESIAN_POINT ( 'NONE',  ( 38.41498555331551756, 491.4234641122537823, 12.30872953874833442 ) ) ;
#100196=CARTESIAN_POINT ( 'NONE',  ( 43.49712683598065865, 471.1121331949958631, 8.167988778889762713 ) ) ;
#100215=CARTESIAN_POINT ( 'NONE',  ( -9.496182690454562092, 294.6569812313908869, -3.146984053371444379 ) ) ;
#100217=CARTESIAN_POINT ( 'NONE',  ( 9.403329628528986461, 294.6596496208666167, -3.414309514541682411 ) ) ;
#100220=EDGE_LOOP ( 'NONE', ( #106597, #24547, #3049, #104970 ) ) ;
#100222=CARTESIAN_POINT ( 'NONE',  ( 31.93152273642204619, 357.0352949535724747, 21.73667947981457971 ) ) ;
#100225=ORIENTED_EDGE ( 'NONE', *, *, #49768, .F. ) ;
#100227=CARTESIAN_POINT ( 'NONE',  ( -43.59756234217317683, 434.3244621007142996, 14.55946156040369921 ) ) ;
#100231=CARTESIAN_POINT ( 'NONE',  ( -43.75010090113929806, 464.8337800386750018, 11.75004750934965791 ) ) ;
#100242=CARTESIAN_POINT ( 'NONE',  ( -8.233767125222675176, 295.9462895465074439, -10.03054565981068258 ) ) ;
#100250=CARTESIAN_POINT ( 'NONE',  ( -16.35748688301842790, 302.5696007747827707, 9.877144026384431896 ) ) ;
#100279=( BOUNDED_SURFACE ( )  B_SPLINE_SURFACE ( 3, 2, ( 
 ( #78547, #4675, #86673 ),
 ( #37608, #70471, #62388 ),
 ( #18762, #52143, #43538 ),
 ( #2527, #85061, #11138 ) ),
 .UNSPECIFIED., .F., .F., .F. ) 
 B_SPLINE_SURFACE_WITH_KNOTS ( ( 4, 4 ),
 ( 3, 3 ),
 ( 1.416401718135062993E-15, 0.001833990318203171464 ),
 ( 0.000000000000000000, 1.000000000000000000 ),
 .UNSPECIFIED. ) 
 GEOMETRIC_REPRESENTATION_ITEM ( )  RATIONAL_B_SPLINE_SURFACE ( (
 ( 1.000000000000000000, 0.7977970988452940393, 1.000000000000000000),
 ( 1.000000000000000000, 0.7897979397240406652, 1.000000000000000000),
 ( 1.000000000000000000, 0.7817839364700247540, 1.000000000000000000),
 ( 1.000000000000000000, 0.7737149417968405274, 1.000000000000000000) ) ) 
 REPRESENTATION_ITEM ( '' )  SURFACE ( )  );
#100284=CARTESIAN_POINT ( 'NONE',  ( -33.51558356630641811, 484.9916844669999705, -0.2910019615253942593 ) ) ;
#100285=CARTESIAN_POINT ( 'NONE',  ( -33.14118366335542021, 381.7159081765646533, 24.92900331645760303 ) ) ;
#100296=CARTESIAN_POINT ( 'NONE',  ( -39.41119041386610888, 438.9267638094590893, 23.32421457530460529 ) ) ;
#100298=CARTESIAN_POINT ( 'NONE',  ( -40.73953790046564194, -18.92596047533412573, -20.36976895023281031 ) ) ;
#100312=CARTESIAN_POINT ( 'NONE',  ( 23.43684916743750080, 295.2641918988800285, 10.02474406024658293 ) ) ;
#100317=CARTESIAN_POINT ( 'NONE',  ( -11.93255308427328565, 294.5886021379643580, 9.881054392645332030 ) ) ;
#100322=CARTESIAN_POINT ( 'NONE',  ( -39.85421124144144045, 464.8562039746861387, 17.95120812561461321 ) ) ;
#100338=CARTESIAN_POINT ( 'NONE',  ( 31.11679462788039530, 441.4271381875185511, 23.27438508043199406 ) ) ;
#100341=CARTESIAN_POINT ( 'NONE',  ( -32.99999999999999289, 435.0774731480751143, 11.67986145722082902 ) ) ;
#100348=CARTESIAN_POINT ( 'NONE',  ( 19.96162532426522773, 302.8116070918645164, 9.928455558879880627 ) ) ;
#100351=CARTESIAN_POINT ( 'NONE',  ( 32.13672086716894682, 487.8704565892116420, 8.624753397812970235 ) ) ;
#100356=CARTESIAN_POINT ( 'NONE',  ( 43.73399259471502631, 464.6843803606428196, 7.646783569293355676 ) ) ;
#100358=CARTESIAN_POINT ( 'NONE',  ( -43.43869229197126458, 464.9661605157749591, 13.42065392471462637 ) ) ;
#100372=VERTEX_POINT ( 'NONE', #3414 ) ;
#100397=CARTESIAN_POINT ( 'NONE',  ( 40.93435977689158989, 414.3154843149413296, 27.72243992809649527 ) ) ;
#100404=CARTESIAN_POINT ( 'NONE',  ( -21.16803287062261774, 305.0380828635773582, 8.976778075698762294 ) ) ;
#100417=CARTESIAN_POINT ( 'NONE',  ( 19.83463548332445825, 303.8035096162420245, 9.926734387303332241 ) ) ;
#100428=CARTESIAN_POINT ( 'NONE',  ( -20.49977525862259142, 302.8459220885798686, -10.00124997875687427 ) ) ;
#100434=CARTESIAN_POINT ( 'NONE',  ( -31.47811980959860989, 326.9156455337226248, 15.84085572310068812 ) ) ;
#100442=CARTESIAN_POINT ( 'NONE',  ( -1.128130203588978198, 301.8985493317088071, 9.936162350048869385 ) ) ;
#100460=CARTESIAN_POINT ( 'NONE',  ( -30.00000000000000355, 461.8802764867011206, 14.89328939273810093 ) ) ;
#100462=CARTESIAN_POINT ( 'NONE',  ( 32.05117072706241999, 435.5678670110675057, 16.71961908548328424 ) ) ;
#100480=CIRCLE ( 'NONE', #19558, 0.9999999999999997780 ) ;
#100486=CARTESIAN_POINT ( 'NONE',  ( -34.88259098417105974, 437.7046102974885002, 4.606877878021536254 ) ) ;
#100517=ADVANCED_FACE ( 'NONE', ( #80990 ), #5006, .T. ) ;
#100518=ORIENTED_EDGE ( 'NONE', *, *, #73734, .T. ) ;
#100522=CARTESIAN_POINT ( 'NONE',  ( 18.31372175616277431, 302.6416072323730191, -10.04454203250753253 ) ) ;
#100523=CARTESIAN_POINT ( 'NONE',  ( -44.19630675229384309, 485.6206890027647205, 3.558858865138833316 ) ) ;
#100525=CARTESIAN_POINT ( 'NONE',  ( 32.75517716563783921, 465.7432004789072266, 11.49884209862490358 ) ) ;
#100526=CARTESIAN_POINT ( 'NONE',  ( -37.54237687662340051, 463.5961191364194178, 19.55587387183957304 ) ) ;
#100536=EDGE_LOOP ( 'NONE', ( #21153, #13158, #79956, #75415, #99455, #83768, #15163, #94752 ) ) ;
#100542=CARTESIAN_POINT ( 'NONE',  ( -33.37176405577542937, 315.0974072509098960, -7.071267840213817379 ) ) ;
#100579=ORIENTED_EDGE ( 'NONE', *, *, #10824, .F. ) ;
#100585=EDGE_CURVE ( 'NONE', #58214, #13401, #69761, .T. ) ;
#100594=FACE_OUTER_BOUND ( 'NONE', #100220, .T. ) ;
#100597=CARTESIAN_POINT ( 'NONE',  ( -33.00000000000000000, 461.8887775513397855, 11.55279652844097171 ) ) ;
#100604=CARTESIAN_POINT ( 'NONE',  ( -37.45944760690750286, 486.5144608516062590, 13.75040320519661918 ) ) ;
#100605=B_SPLINE_SURFACE_WITH_KNOTS ( 'NONE', 1, 3, ( 
 ( #65324, #96635, #105773, #98212, #22770, #24365, #105254, #71812, #49115, #73930, #57209, #16229, #32980, #72351, #63748, #14097, #47004, #31401, #59914, #27030, #83097, #92235, #50703, #26502, #100338, #540, #83616, #58287 ),
 ( #34053, #84697, #91732, #66377, #10264, #76059, #99807, #43178, #18389, #66927, #51242, #34589, #9190, #99257, #25978, #35114, #25433, #91213, #59373, #49659, #74460, #10781, #84169, #17851, #9720, #18941, #68529, #51784 ) ),
 .UNSPECIFIED., .F., .F., .F.,
 ( 2, 2 ),
 ( 4, 2, 2, 2, 2, 2, 2, 2, 2, 2, 2, 2, 2, 4 ),
 ( 0.000000000000000000, 1.000000000000000000 ),
 ( 0.08901491201581737678, 0.1032490540155679704, 0.1174831960153185778, 0.1317173380150691853, 0.1459514800148197788, 0.1744197640143299588, 0.2028880480138401388, 0.2598246160128514504, 0.3167611840118632616, 0.4306343200098861623, 0.5445074560079088410, 0.6583805920059359051, 0.7722537280039543095, 1.000000000000000000 ),
 .UNSPECIFIED. ) ;
#100606=CARTESIAN_POINT ( 'NONE',  ( 33.77559172535807619, 464.7834715296606305, 7.192701217093271815 ) ) ;
#100611=CARTESIAN_POINT ( 'NONE',  ( 0.000000000000000000, 0.000000000000000000, 0.000000000000000000 ) ) ;
#100612=CARTESIAN_POINT ( 'NONE',  ( 25.75971285069983807, 304.3014513131341801, -9.684463734016926395 ) ) ;
#100613=CARTESIAN_POINT ( 'NONE',  ( 35.66932529116966322, 438.9565575286536045, 4.011496722538590909 ) ) ;
#100619=ORIENTED_EDGE ( 'NONE', *, *, #74834, .F. ) ;
#100626=FACE_OUTER_BOUND ( 'NONE', #100848, .T. ) ;
#100629=CARTESIAN_POINT ( 'NONE',  ( 31.09389865030000522, 439.4630943131195977, 22.89591944113354316 ) ) ;
#100643=CARTESIAN_POINT ( 'NONE',  ( 37.67793878171265476, 380.9275077484064127, 5.379687045508362964 ) ) ;
#100649=CARTESIAN_POINT ( 'NONE',  ( -46.00000000000000000, 461.6622277975411635, 10.18145404766348783 ) ) ;
#100653=CARTESIAN_POINT ( 'NONE',  ( -37.87024700625071461, 460.2236392396199562, 2.222911568036097574 ) ) ;
#100659=AXIS2_PLACEMENT_3D ( 'NONE', #84664, #85190, #43663 ) ;
#100662=AXIS2_PLACEMENT_3D ( 'NONE', #93950, #54513, #20104 ) ;
#100670=CARTESIAN_POINT ( 'NONE',  ( -32.66167952489984572, 465.7843590037688273, 12.50185730157783048 ) ) ;
#100673=CARTESIAN_POINT ( 'NONE',  ( -32.09613050731442030, 439.8910643262784674, 23.54880513615299620 ) ) ;
#100680=CARTESIAN_POINT ( 'NONE',  ( 31.09148700014130640, 299.3363133847115591, 10.94160789497410313 ) ) ;
#100684=CARTESIAN_POINT ( 'NONE',  ( 37.28010227714514002, 307.7308894357594795, 4.972761938079513833 ) ) ;
#100691=CARTESIAN_POINT ( 'NONE',  ( 2.503172993490694775, 294.8391969675017208, 9.934319915356635278 ) ) ;
#100717=EDGE_CURVE ( 'NONE', #34395, #77744, #91726, .T. ) ;
#100719=CARTESIAN_POINT ( 'NONE',  ( 0.000000000000000000, 294.8518027762758038, -10.00000000000000178 ) ) ;
#100725=EDGE_CURVE ( 'NONE', #27254, #72783, #35638, .T. ) ;
#100731=CIRCLE ( 'NONE', #99019, 3.000000000000009326 ) ;
#100748=CARTESIAN_POINT ( 'NONE',  ( 26.96142313735197504, 312.0022853774228793, 11.65857948192350335 ) ) ;
#100749=CARTESIAN_POINT ( 'NONE',  ( -38.96902200852884590, 460.8405016383454722, 2.186950304199872352 ) ) ;
#100757=CARTESIAN_POINT ( 'NONE',  ( -35.66932529116966322, 438.9565575286536045, 4.011496722538590909 ) ) ;
#100771=CARTESIAN_POINT ( 'NONE',  ( -9.482342435886300436, 294.6573797848112690, -3.183473687071290303 ) ) ;
#100788=CARTESIAN_POINT ( 'NONE',  ( -46.00000000000000000, 437.9222508511568321, 13.74115800020528155 ) ) ;
#100799=CARTESIAN_POINT ( 'NONE',  ( -21.71806759225283656, 305.0526565939784973, -9.957254290847345146 ) ) ;
#100810=CARTESIAN_POINT ( 'NONE',  ( -34.14470975531866515, 484.1045092577827518, 0.7158976332298593315 ) ) ;
#100811=CARTESIAN_POINT ( 'NONE',  ( -40.95753704872183931, 390.7956291586450561, 27.40283599064078501 ) ) ;
#100812=CARTESIAN_POINT ( 'NONE',  ( -32.84239204141412216, 485.9541550691055249, 5.517081702403281440 ) ) ;
#100817=ORIENTED_EDGE ( 'NONE', *, *, #38258, .F. ) ;
#100839=CARTESIAN_POINT ( 'NONE',  ( 6.145867760142384562, 301.8770827788400766, -10.02048593162349555 ) ) ;
#100841=CARTESIAN_POINT ( 'NONE',  ( 32.35336999986095208, 300.6590557721156642, 11.25190399080426751 ) ) ;
#100847=EDGE_CURVE ( 'NONE', #104577, #10763, #6696, .T. ) ;
#100848=EDGE_LOOP ( 'NONE', ( #35736, #23707, #8631, #33512 ) ) ;
#100855=CARTESIAN_POINT ( 'NONE',  ( 37.39037644056565313, 437.8315769265258837, 4.421099621127080326 ) ) ;
#100861=VERTEX_POINT ( 'NONE', #24269 ) ;
#100862=PLANE ( 'NONE',  #28375 ) ;
#100868=CARTESIAN_POINT ( 'NONE',  ( 38.06554674067534449, 464.2394109421263693, 19.21791087872065162 ) ) ;
#100869=CARTESIAN_POINT ( 'NONE',  ( -34.99923118634553987, 435.2190035774330568, 7.261676763235612064 ) ) ;
#100877=CARTESIAN_POINT ( 'NONE',  ( -13.58955859254654364, 303.5476461695370745, -10.06465166092577590 ) ) ;
#100884=DIRECTION ( 'NONE',  ( 0.000000000000000000, -0.9024170203240217125, 0.4308636924011052804 ) ) ;
#100906=CARTESIAN_POINT ( 'NONE',  ( -31.19652432992544888, 378.3327707670021027, 24.28948218791313707 ) ) ;
#100908=( BOUNDED_SURFACE ( )  B_SPLINE_SURFACE ( 3, 2, ( 
 ( #81462, #65834, #90645 ),
 ( #75517, #101401, #10767 ),
 ( #74973, #100855, #8653 ),
 ( #1062, #66362, #84150 ) ),
 .UNSPECIFIED., .F., .F., .F. ) 
 B_SPLINE_SURFACE_WITH_KNOTS ( ( 4, 4 ),
 ( 3, 3 ),
 ( -4.163336342344337027E-17, 0.001025706331908650881 ),
 ( 0.000000000000000000, 1.000000000000000000 ),
 .UNSPECIFIED. ) 
 GEOMETRIC_REPRESENTATION_ITEM ( )  RATIONAL_B_SPLINE_SURFACE ( (
 ( 1.000000000000000000, 0.9193453746270781046, 1.000000000000000000),
 ( 1.000000000000000000, 0.9180307555289033417, 1.000000000000000000),
 ( 1.000000000000000000, 0.9167125567853835477, 1.000000000000000000),
 ( 1.000000000000000000, 0.9153908114178201938, 1.000000000000000000) ) ) 
 REPRESENTATION_ITEM ( '' )  SURFACE ( )  );
#100920=CARTESIAN_POINT ( 'NONE',  ( -32.04854177568304152, 486.3112398708803426, 5.779390795281895699 ) ) ;
#100925=VERTEX_POINT ( 'NONE', #43086 ) ;
#100927=CARTESIAN_POINT ( 'NONE',  ( 34.95237279327285762, 304.8277712208536627, 12.26231981495593537 ) ) ;
#100931=CIRCLE ( 'NONE', #50942, 0.9999999999999833467 ) ;
#100933=CARTESIAN_POINT ( 'NONE',  ( 34.25474529525818923, 462.3053719747810533, 4.620191449216225266 ) ) ;
#100935=CARTESIAN_POINT ( 'NONE',  ( 42.64966854229460580, 465.0854819100621853, 13.23715615004964086 ) ) ;
#100936=CARTESIAN_POINT ( 'NONE',  ( 33.97359119245064818, 434.1099241184709285, 11.80501937577160732 ) ) ;
#100942=VERTEX_POINT ( 'NONE', #50610 ) ;
#100943=CARTESIAN_POINT ( 'NONE',  ( -31.35596682365705945, 438.0939828603719093, 22.55458131664414267 ) ) ;
#100972=CARTESIAN_POINT ( 'NONE',  ( -1.128183577532071213, 300.9492746658231681, 9.936156289954721998 ) ) ;
#100982=CARTESIAN_POINT ( 'NONE',  ( 42.04659500829693997, 436.6121354927211087, 19.99047899505293913 ) ) ;
#100985=CARTESIAN_POINT ( 'NONE',  ( 41.28039629891261342, 485.7122505962505556, -4.568292046900871206 ) ) ;
#100991=ORIENTED_EDGE ( 'NONE', *, *, #102543, .F. ) ;
#101002=CARTESIAN_POINT ( 'NONE',  ( -45.33180403702434091, 464.4945808635454227, 2.178908857919817699 ) ) ;
#101012=CARTESIAN_POINT ( 'NONE',  ( 32.04737116497691574, 465.7264234052258871, 15.44069434686693221 ) ) ;
#101013=CARTESIAN_POINT ( 'NONE',  ( -35.76320840016588676, 388.4727839510825333, 5.610592865731860002 ) ) ;
#101032=ORIENTED_EDGE ( 'NONE', *, *, #28720, .T. ) ;
#101038=CARTESIAN_POINT ( 'NONE',  ( 29.25327276538528309, 308.5399522405340917, -8.932740553462334532 ) ) ;
#101043=CARTESIAN_POINT ( 'NONE',  ( 38.85446894546473828, 460.8903912184138676, 2.218456751109172398 ) ) ;
#101058=CARTESIAN_POINT ( 'NONE',  ( -34.25859903460757039, 436.5725446342189002, 6.424027449235138576 ) ) ;
#101067=CARTESIAN_POINT ( 'NONE',  ( 33.49978038599233798, 465.4670364598634364, 16.54746596774596057 ) ) ;
#101076=FILL_AREA_STYLE_COLOUR ( '', #40723 ) ;
#101082=CARTESIAN_POINT ( 'NONE',  ( -40.05504438264630096, 310.1124923933409718, -6.399326716180240737 ) ) ;
#101083=CARTESIAN_POINT ( 'NONE',  ( -3.412115861943773254, 304.8518027738260798, -10.00000000023261038 ) ) ;
#101088=CARTESIAN_POINT ( 'NONE',  ( -43.66727438528028671, 435.6676895479261020, 17.39383282232667227 ) ) ;
#101092=( BOUNDED_SURFACE ( )  B_SPLINE_SURFACE ( 3, 2, ( 
 ( #91215, #60452, #17853 ),
 ( #19481, #83618, #2161 ),
 ( #100869, #3253, #43180 ),
 ( #52318, #17321, #44246 ),
 ( #27032, #77138, #9722 ),
 ( #34591, #36194, #42638 ),
 ( #50196, #83098, #9192 ),
 ( #75535, #67462, #100341 ) ),
 .UNSPECIFIED., .F., .F., .F. ) 
 B_SPLINE_SURFACE_WITH_KNOTS ( ( 4, 2, 2, 4 ),
 ( 3, 3 ),
 ( -1.994931997373328159E-17, 0.003572974592251130545, 0.005359461888376705792, 0.007145949184502281039 ),
 ( 0.000000000000000000, 1.000000000000000000 ),
 .UNSPECIFIED. ) 
 GEOMETRIC_REPRESENTATION_ITEM ( )  RATIONAL_B_SPLINE_SURFACE ( (
 ( 1.000000000000000000, 0.7557288854865578109, 1.000000000000000000),
 ( 1.000000000000000000, 0.7511728107079237438, 1.000000000000000000),
 ( 1.000000000000000000, 0.7462898432665451276, 1.000000000000000000),
 ( 1.000000000000000000, 0.7384961912446853516, 1.000000000000000000),
 ( 1.000000000000000000, 0.7358197253153077044, 1.000000000000000000),
 ( 1.000000000000000000, 0.7303050827503990705, 1.000000000000000000),
 ( 1.000000000000000000, 0.7274799915864358368, 1.000000000000000000),
 ( 1.000000000000000000, 0.7246213771202483223, 1.000000000000000000) ) ) 
 REPRESENTATION_ITEM ( '' )  SURFACE ( )  );
#101100=DIRECTION ( 'NONE',  ( 1.000000000000000000, 0.000000000000000000, 0.000000000000000000 ) ) ;
#101112=DIRECTION ( 'NONE',  ( 0.9737456255366201407, 0.000000000000000000, 0.2276388735438140687 ) ) ;
#101113=CARTESIAN_POINT ( 'NONE',  ( -37.52575628270366792, 438.0832219636323543, 4.091974619433682570 ) ) ;
#101114=DIRECTION ( 'NONE',  ( 0.000000000000000000, 0.000000000000000000, -1.000000000000000000 ) ) ;
#101116=FACE_OUTER_BOUND ( 'NONE', #50713, .T. ) ;
#101118=CARTESIAN_POINT ( 'NONE',  ( 43.61505130863974955, 434.9783532604240008, 14.40542840455674423 ) ) ;
#101132=CARTESIAN_POINT ( 'NONE',  ( -43.00000000000000000, 435.1719937645106029, 7.191579780910007713 ) ) ;
#101135=TOROIDAL_SURFACE ( 'NONE', #101230, 12.00000000000000711, 3.000000000000000000 ) ;
#101140=ORIENTED_EDGE ( 'NONE', *, *, #104273, .F. ) ;
#101143=CARTESIAN_POINT ( 'NONE',  ( -41.58444704644840328, 481.6528781813217961, 13.64578380398117829 ) ) ;
#101144=CARTESIAN_POINT ( 'NONE',  ( -37.25380483576834934, 307.7259701645078280, 4.972132598451335816 ) ) ;
#101149=CARTESIAN_POINT ( 'NONE',  ( 31.86888217434322712, 485.1577972469718816, 5.527887721099247642 ) ) ;
#101152=CARTESIAN_POINT ( 'NONE',  ( 23.12331641935568527, 303.3400345184521143, -9.895296368007924670 ) ) ;
#101153=CARTESIAN_POINT ( 'NONE',  ( 35.96492786661492858, 302.4488314805894902, -8.278427239162008178 ) ) ;
#101167=CARTESIAN_POINT ( 'NONE',  ( 41.96862382816240711, 327.9039392355280711, 6.054989524861565720 ) ) ;
#101171=CARTESIAN_POINT ( 'NONE',  ( -12.19423397773156736, 304.5852035401753710, 9.880331998383338643 ) ) ;
#101172=CARTESIAN_POINT ( 'NONE',  ( 31.52580585160177051, 438.9871292739251771, 23.28495454672928489 ) ) ;
#101174=ORIENTED_EDGE ( 'NONE', *, *, #24121, .F. ) ;
#101193=DIRECTION ( 'NONE',  ( -1.000000000000000000, -0.000000000000000000, -0.000000000000000000 ) ) ;
#101198=AXIS2_PLACEMENT_3D ( 'NONE', #94964, #72254, #4874 ) ;
#101209=CARTESIAN_POINT ( 'NONE',  ( -28.84069063680069434, 315.3197465396486905, 12.73806496493308593 ) ) ;
#101211=ORIENTED_EDGE ( 'NONE', *, *, #6869, .T. ) ;
#101213=CARTESIAN_POINT ( 'NONE',  ( -32.65869381073711253, 465.0820644893343001, 12.85946116547015983 ) ) ;
#101214=EDGE_LOOP ( 'NONE', ( #41713, #36111, #71332, #3873 ) ) ;
#101216=CARTESIAN_POINT ( 'NONE',  ( -19.01441297883930304, 303.6984617652402676, 9.904405537397884984 ) ) ;
#101218=CARTESIAN_POINT ( 'NONE',  ( -31.42155219348691375, 380.7461170327588320, 23.45653096014077477 ) ) ;
#101223=EDGE_LOOP ( 'NONE', ( #43048, #83303, #52833, #5407, #31130, #9999 ) ) ;
#101229=CARTESIAN_POINT ( 'NONE',  ( 29.82401586680403938, 298.2086656657758681, 10.68039305417390139 ) ) ;
#101230=AXIS2_PLACEMENT_3D ( 'NONE', #95304, #39196, #104983 ) ;
#101247=CARTESIAN_POINT ( 'NONE',  ( 33.94429683799095443, 489.7044232353788971, 10.92862313927360596 ) ) ;
#101248=CARTESIAN_POINT ( 'NONE',  ( 42.61140200160144786, 465.9030374194822457, 13.21253569360410829 ) ) ;
#101286=CARTESIAN_POINT ( 'NONE',  ( -35.45036406932566564, 436.3203772529605544, 5.179456583033978490 ) ) ;
#101301=CARTESIAN_POINT ( 'NONE',  ( 24.02573244599213353, 306.3041407548990946, 9.258542674397354233 ) ) ;
#101310=CARTESIAN_POINT ( 'NONE',  ( 43.21667697146742881, 434.4554196591589630, 16.17972000939166222 ) ) ;
#101316=CARTESIAN_POINT ( 'NONE',  ( -43.51765957956997966, 464.6235667276147296, 9.550596550081237979 ) ) ;
#101323=CARTESIAN_POINT ( 'NONE',  ( -7.886225517035546417, 296.0473068317272123, -10.02775466922440195 ) ) ;
#101348=CARTESIAN_POINT ( 'NONE',  ( -26.46282106933370315, 307.1428501120792021, -8.492241753587084219 ) ) ;
#101351=ADVANCED_FACE ( 'NONE', ( #58642 ), #30861, .F. ) ;
#101360=CARTESIAN_POINT ( 'NONE',  ( -30.47697434215580259, 313.1714974985160325, -7.033864211245149711 ) ) ;
#101362=CARTESIAN_POINT ( 'NONE',  ( -35.82079281205172805, 304.5878133820737617, 4.193256625072890209 ) ) ;
#101378=CARTESIAN_POINT ( 'NONE',  ( 19.73463816634110657, 304.7971333121958537, 8.925379062039144884 ) ) ;
#101391=CARTESIAN_POINT ( 'NONE',  ( 2.569942032970752077, 295.6515237735611095, -10.00266688365501544 ) ) ;
#101392=CARTESIAN_POINT ( 'NONE',  ( 36.91281931599076671, 303.7809130842520631, -7.959270006439831846 ) ) ;
#101400=CARTESIAN_POINT ( 'NONE',  ( 46.00000000000000000, 488.0336798547363628, -0.8984331811833941028 ) ) ;
#101401=CARTESIAN_POINT ( 'NONE',  ( 37.06599482039754889, 437.8929527013448819, 4.336831230556377648 ) ) ;
#101405=CIRCLE ( 'NONE', #41120, 1.000000000000002442 ) ;
#101419=CARTESIAN_POINT ( 'NONE',  ( 41.59697046779439233, 465.5819587124576628, 15.80766635430880918 ) ) ;
#101425=CARTESIAN_POINT ( 'NONE',  ( -44.20228413058327277, 435.2535421915627012, 14.52187095974274911 ) ) ;
#101443=ORIENTED_EDGE ( 'NONE', *, *, #43951, .F. ) ;
#101457=CARTESIAN_POINT ( 'NONE',  ( -24.60488647473181345, 306.9835580411500473, 10.41807558718820914 ) ) ;
#101471=CARTESIAN_POINT ( 'NONE',  ( -43.00000000000000000, 436.0987441542287115, 7.567257455462746307 ) ) ;
#101474=CARTESIAN_POINT ( 'NONE',  ( 42.23079339798724163, 460.7352525929352964, 2.726051457480600515 ) ) ;
#101478=CARTESIAN_POINT ( 'NONE',  ( -23.05315642362847584, 305.6756567056184508, 9.116243019785128965 ) ) ;
#101479=CARTESIAN_POINT ( 'NONE',  ( 32.15496997666741663, 435.6577922786089516, 19.42935975044838415 ) ) ;
#101481=EDGE_CURVE ( 'NONE', #1725, #20836, #98131, .T. ) ;
#101486=CIRCLE ( 'NONE', #54951, 3.000000000000000000 ) ;
#101493=CARTESIAN_POINT ( 'NONE',  ( -33.70427618943709547, 490.4072845429053586, 11.54254722977865733 ) ) ;
#101504=DIRECTION ( 'NONE',  ( 0.000000000000000000, -0.9137523047315411207, 0.4062717386156671773 ) ) ;
#101509=ORIENTED_EDGE ( 'NONE', *, *, #19652, .T. ) ;
#101516=CARTESIAN_POINT ( 'NONE',  ( 42.69811214730273718, 434.9611672192513652, 18.34625614733207399 ) ) ;
#101520=LINE ( 'NONE', #60548, #69800 ) ;
#101521=DIRECTION ( 'NONE',  ( -0.3893994694819514213, 0.000000000000000000, 0.9210689730781157492 ) ) ;
#101526=CARTESIAN_POINT ( 'NONE',  ( -34.84618260875176787, 489.9833681528637044, 11.97975507378787619 ) ) ;
#101531=ORIENTED_EDGE ( 'NONE', *, *, #106081, .T. ) ;
#101535=ADVANCED_FACE ( 'NONE', ( #74665 ), #99474, .T. ) ;
#101536=CARTESIAN_POINT ( 'NONE',  ( 32.21158651034458131, 436.2407106940943322, 19.11433863909860875 ) ) ;
#101538=CARTESIAN_POINT ( 'NONE',  ( -34.49859336299155643, 464.8458904554828450, 18.22488476268509316 ) ) ;
#101545=DIRECTION ( 'NONE',  ( 0.3934424543256375140, 0.4342828891348778364, 0.8103094515917250718 ) ) ;
#101549=( BOUNDED_SURFACE ( )  B_SPLINE_SURFACE ( 3, 2, ( 
 ( #12576, #68171, #102127 ),
 ( #94043, #3444, #53060 ),
 ( #101067, #52509, #60112 ),
 ( #44437, #36387, #45512 ) ),
 .UNSPECIFIED., .F., .F., .F. ) 
 B_SPLINE_SURFACE_WITH_KNOTS ( ( 4, 4 ),
 ( 3, 3 ),
 ( -8.673617379884035472E-19, 0.002473307515803177190 ),
 ( 0.000000000000000000, 1.000000000000000000 ),
 .UNSPECIFIED. ) 
 GEOMETRIC_REPRESENTATION_ITEM ( )  RATIONAL_B_SPLINE_SURFACE ( (
 ( 1.000000000000000000, 0.8138888783289754958, 1.000000000000000000),
 ( 1.000000000000000000, 0.8083744009271378594, 1.000000000000000000),
 ( 1.000000000000000000, 0.7997328579908555835, 1.000000000000000000),
 ( 1.000000000000000000, 0.7904469216848438728, 1.000000000000000000) ) ) 
 REPRESENTATION_ITEM ( '' )  SURFACE ( )  );
#101555=CARTESIAN_POINT ( 'NONE',  ( 19.96162532426522773, 302.8116070918645164, 9.928455558879877074 ) ) ;
#101602=CARTESIAN_POINT ( 'NONE',  ( -43.56126634772117967, 484.2986656255091589, 0.7800160315439713665 ) ) ;
#101603=CARTESIAN_POINT ( 'NONE',  ( 32.12958771267400948, 464.7275665249413237, 11.12424126545885628 ) ) ;
#101606=AXIS2_PLACEMENT_3D ( 'NONE', #105397, #7745, #64423 ) ;
#101609=ADVANCED_FACE ( 'NONE', ( #2908 ), #8773, .F. ) ;
#101610=CARTESIAN_POINT ( 'NONE',  ( -36.64547244151101069, 438.4340776271736217, 4.169367496923826799 ) ) ;
#101622=CARTESIAN_POINT ( 'NONE',  ( -30.96957840895870362, 309.3457195621996334, -8.501950603266685391 ) ) ;
#101623=CARTESIAN_POINT ( 'NONE',  ( -18.61215960593760244, 304.6205012219655828, -10.04916466315146906 ) ) ;
#101637=CARTESIAN_POINT ( 'NONE',  ( -30.00000000000000000, 500.0000000000002274, 0.000000000000000000 ) ) ;
#101659=VECTOR ( 'NONE', #62235, 1000.000000000000000 ) ;
#101668=DIRECTION ( 'NONE',  ( 0.000000000000000000, 0.000000000000000000, -1.000000000000000000 ) ) ;
#101676=FACE_OUTER_BOUND ( 'NONE', #33719, .T. ) ;
#101678=CARTESIAN_POINT ( 'NONE',  ( -37.46539295237194978, 482.0432618190212111, 15.05095727675832684 ) ) ;
#101679=CARTESIAN_POINT ( 'NONE',  ( -31.26587727109280479, 298.8769331254652570, 2.831021014789372625 ) ) ;
#101682=B_SPLINE_CURVE_WITH_KNOTS ( 'NONE', 3,
 ( #194, #82742, #16413, #50360, #83795, #67100, #99984, #34764, #26671, #33158, #42815, #41218, #75711, #42276, #1806, #66027, #59550, #25065, #74638, #66558, #83273, #98905, #26155, #15885, #48761, #9362, #7779, #59011, #40684, #18025, #58477, #73571, #90843, #91382, #33686, #106473, #32631, #91900, #41750, #25616, #16960, #49837 ),
 .UNSPECIFIED., .F., .F.,
 ( 4, 2, 2, 2, 2, 2, 2, 2, 2, 2, 2, 2, 2, 2, 2, 2, 2, 2, 2, 2, 4 ),
 ( 0.001097384766869235941, 0.009808348211478244358, 0.01851931165608725061, 0.03594123854530526657, 0.05336316543452327560, 0.06207412887913228011, 0.07078509232374130544, 0.08820701921295932835, 0.1056289461021773235, 0.1143399095467863419, 0.1186953912690908441, 0.1230508729913953325, 0.1274063547136998487, 0.1295840955748520373, 0.1317618364360041983, 0.1328507068665802926, 0.1339395772971563869, 0.1350284477277324813, 0.1361173181583085756, 0.1382950590194607643, 0.1404727998806129252 ),
 .UNSPECIFIED. ) ;
#101683=CARTESIAN_POINT ( 'NONE',  ( 38.97459859895755585, 491.1625636263767092, 12.12552269506736913 ) ) ;
#101687=CARTESIAN_POINT ( 'NONE',  ( 25.85345068545198544, 295.8771030381062133, -1.779349931180276512 ) ) ;
#101688=CARTESIAN_POINT ( 'NONE',  ( 45.50145573691759182, 405.2496736015978627, 8.430338687477670234 ) ) ;
#101695=CARTESIAN_POINT ( 'NONE',  ( 42.79914298582033894, 484.2777690190574162, -1.375851118309875387 ) ) ;
#101699=CARTESIAN_POINT ( 'NONE',  ( 40.75098415788840356, 318.6269542384334841, 3.769023074406288476 ) ) ;
#101700=CARTESIAN_POINT ( 'NONE',  ( 43.72375837489602191, 464.7599263999839536, 7.850687543234091237 ) ) ;
#101703=CARTESIAN_POINT ( 'NONE',  ( 32.02768009620982070, 439.4026772796270848, 23.60435309139906579 ) ) ;
#101726=VERTEX_POINT ( 'NONE', #26710 ) ;
#101740=DIRECTION ( 'NONE',  ( 0.000000000000000000, 0.000000000000000000, 1.000000000000000000 ) ) ;
#101750=CARTESIAN_POINT ( 'NONE',  ( 23.16176619586232732, 303.5563662793418871, 10.08948326321344524 ) ) ;
#101765=CARTESIAN_POINT ( 'NONE',  ( 4.238124563102311448, 302.8058401784392117, 9.927349086999059935 ) ) ;
#101795=CARTESIAN_POINT ( 'NONE',  ( 38.79307744977586481, 485.8212363931093591, -4.896981067619740280 ) ) ;
#101798=ADVANCED_FACE ( 'NONE', ( #62765 ), #26776, .T. ) ;
#101800=CARTESIAN_POINT ( 'NONE',  ( -43.00000000000000000, 436.5989882784185170, 19.94133085611150591 ) ) ;
#101801=ORIENTED_EDGE ( 'NONE', *, *, #80811, .T. ) ;
#101818=CARTESIAN_POINT ( 'NONE',  ( 23.16208212304022851, 304.6450008528781837, 10.10914924364463907 ) ) ;
#101821=VERTEX_POINT ( 'NONE', #5054 ) ;
#101840=CARTESIAN_POINT ( 'NONE',  ( -4.691302026902953948, 301.0269659577480752, -10.01286862727976867 ) ) ;
#101842=VERTEX_POINT ( 'NONE', #102148 ) ;
#101851=( BOUNDED_SURFACE ( )  B_SPLINE_SURFACE ( 3, 2, ( 
 ( #16971, #82752, #8854 ),
 ( #34239, #67110, #99995 ),
 ( #7258, #1816, #102663 ),
 ( #51969, #102122, #19667 ),
 ( #51443, #94038, #75722 ),
 ( #28822, #50899, #59559 ),
 ( #52504, #68721, #100525 ),
 ( #101603, #76781, #69249 ) ),
 .UNSPECIFIED., .F., .F., .F. ) 
 B_SPLINE_SURFACE_WITH_KNOTS ( ( 4, 2, 2, 4 ),
 ( 3, 3 ),
 ( 1.821459649775647449E-17, 0.002244734355330710134, 0.003367101532996056093, 0.004489468710661402052 ),
 ( 0.000000000000000000, 1.000000000000000000 ),
 .UNSPECIFIED. ) 
 GEOMETRIC_REPRESENTATION_ITEM ( )  RATIONAL_B_SPLINE_SURFACE ( (
 ( 1.000000000000000000, 0.8138888783289954798, 1.000000000000000000),
 ( 1.000000000000000000, 0.8201127045485649969, 1.000000000000000000),
 ( 1.000000000000000000, 0.8211215022261788565, 1.000000000000000000),
 ( 1.000000000000000000, 0.8168533336260839217, 1.000000000000000000),
 ( 1.000000000000000000, 0.8144062529165223552, 1.000000000000000000),
 ( 1.000000000000000000, 0.8072737967807479542, 1.000000000000000000),
 ( 1.000000000000000000, 0.8026171117809203226, 1.000000000000000000),
 ( 1.000000000000000000, 0.7964893136846624699, 1.000000000000000000) ) ) 
 REPRESENTATION_ITEM ( '' )  SURFACE ( )  );
#101864=ORIENTED_EDGE ( 'NONE', *, *, #5532, .F. ) ;
#101869=CARTESIAN_POINT ( 'NONE',  ( 41.79722565532031098, 337.2140685331145278, 12.11318237481769877 ) ) ;
#101874=CARTESIAN_POINT ( 'NONE',  ( -44.26374899283617026, 435.3115877954970188, 11.30001004034635770 ) ) ;
#101879=CARTESIAN_POINT ( 'NONE',  ( -32.39662675564067484, 439.6664204692525573, 24.00562780833886123 ) ) ;
#101883=CARTESIAN_POINT ( 'NONE',  ( -31.25520399608259936, 324.6763390771653235, 15.30305406351194186 ) ) ;
#101890=CARTESIAN_POINT ( 'NONE',  ( 38.38188837495465577, 437.9257690784075407, 4.300778830038875178 ) ) ;
#101896=DIRECTION ( 'NONE',  ( 0.000000000000000000, 0.1409055682474881777, -0.9900230405585784821 ) ) ;
#101903=CIRCLE ( 'NONE', #64130, 10.00000000000000178 ) ;
#101910=CARTESIAN_POINT ( 'NONE',  ( 4.598202642359287218, 296.0917469168782077, -10.00877229851196404 ) ) ;
#101912=CARTESIAN_POINT ( 'NONE',  ( 42.68131856673817026, 337.5603479645903917, 8.268498401259357422 ) ) ;
#101914=ORIENTED_EDGE ( 'NONE', *, *, #36499, .F. ) ;
#101915=CARTESIAN_POINT ( 'NONE',  ( -19.07845090537422550, 294.6331628770684574, 9.890526070132905190 ) ) ;
#101926=EDGE_CURVE ( 'NONE', #59443, #11535, #42677, .T. ) ;
#101947=CARTESIAN_POINT ( 'NONE',  ( 33.86879232827773478, 484.1347737343853623, 1.564974661443952364 ) ) ;
#101974=FACE_OUTER_BOUND ( 'NONE', #25651, .T. ) ;
#101994=CARTESIAN_POINT ( 'NONE',  ( 41.50820411079195793, 461.5963371455320612, 2.703439750996331270 ) ) ;
#101998=CARTESIAN_POINT ( 'NONE',  ( -9.970195021759442611, 302.6460196488377505, -10.04373974541436887 ) ) ;
#102014=CARTESIAN_POINT ( 'NONE',  ( -33.21587117934102196, 465.5376285004398937, 9.463823683521015440 ) ) ;
#102031=AXIS2_PLACEMENT_3D ( 'NONE', #99042, #83942, #25210 ) ;
#102032=CARTESIAN_POINT ( 'NONE',  ( -5.715859758579841632, 297.8165492175919553, 8.222449063051152862 ) ) ;
#102036=FACE_OUTER_BOUND ( 'NONE', #24327, .T. ) ;
#102043=CARTESIAN_POINT ( 'NONE',  ( -37.38583316527437717, 490.8443774175583485, 12.40598127368437531 ) ) ;
#102047=ADVANCED_FACE ( 'NONE', ( #58371 ), #45957, .F. ) ;
#102051=CARTESIAN_POINT ( 'NONE',  ( 34.89131925218347874, 463.6463204812255867, 18.89898487466263077 ) ) ;
#102056=CARTESIAN_POINT ( 'NONE',  ( 31.80017143950496106, 436.0492156885775330, 18.01770255577284630 ) ) ;
#102063=CIRCLE ( 'NONE', #55547, 3.000000000000000000 ) ;
#102105=CARTESIAN_POINT ( 'NONE',  ( 38.55706197333972085, 437.0914394628474611, 4.833655886047981909 ) ) ;
#102107=ORIENTED_EDGE ( 'NONE', *, *, #8530, .F. ) ;
#102114=EDGE_CURVE ( 'NONE', #75855, #4655, #9290, .T. ) ;
#102115=CARTESIAN_POINT ( 'NONE',  ( 35.04348997865178461, 484.2371297655228091, -0.9829126381495068010 ) ) ;
#102117=CARTESIAN_POINT ( 'NONE',  ( -32.11411341898570981, 317.7919323371296514, -6.873671351699469412 ) ) ;
#102122=CARTESIAN_POINT ( 'NONE',  ( 32.65869381073299138, 465.0820644893343569, 12.85946116546466200 ) ) ;
#102123=DIRECTION ( 'NONE',  ( 0.02699252395738975518, -0.001721171576548164101, 0.9996341536876447442 ) ) ;
#102127=CARTESIAN_POINT ( 'NONE',  ( 32.28552837373270279, 464.7648866755952213, 15.30384310833110462 ) ) ;
#102128=CARTESIAN_POINT ( 'NONE',  ( -35.68994829237247757, 432.5459415766960092, 4.686749143785717386 ) ) ;
#102148=CARTESIAN_POINT ( 'NONE',  ( -33.74271564777242816, 484.1802673187708592, 2.058285076122308155 ) ) ;
#102155=ORIENTED_EDGE ( 'NONE', *, *, #103458, .F. ) ;
#102162=ORIENTED_EDGE ( 'NONE', *, *, #16463, .T. ) ;
#102171=CIRCLE ( 'NONE', #17801, 12.00000000000000711 ) ;
#102174=AXIS2_PLACEMENT_3D ( 'NONE', #26739, #43944, #36948 ) ;
#102176=CARTESIAN_POINT ( 'NONE',  ( 33.88461414431416330, 464.6055380068779073, 6.798187872881690019 ) ) ;
#102196=ADVANCED_FACE ( 'NONE', ( #12147 ), #10179, .F. ) ;
#102200=CARTESIAN_POINT ( 'NONE',  ( -42.36808196472509280, 461.6713445545159971, 3.771400599640011286 ) ) ;
#102205=CARTESIAN_POINT ( 'NONE',  ( 37.18119764941855721, 491.8021068614486921, 12.56169729800603463 ) ) ;
#102210=CARTESIAN_POINT ( 'NONE',  ( 33.00000000000000000, 450.0000000000002274, 13.20242257375370976 ) ) ;
#102211=CARTESIAN_POINT ( 'NONE',  ( -30.00000000000000000, 500.0000000000002274, 0.000000000000000000 ) ) ;
#102216=CARTESIAN_POINT ( 'NONE',  ( 21.23684446602553777, 304.9566545053270943, -9.977713076987676288 ) ) ;
#102226=CARTESIAN_POINT ( 'NONE',  ( 41.04411817078318592, 313.2288094300998296, -5.615143661017929055 ) ) ;
#102227=CARTESIAN_POINT ( 'NONE',  ( 43.54570344706467466, 464.5919001250003362, 9.427857144828974967 ) ) ;
#102254=CARTESIAN_POINT ( 'NONE',  ( 0.3760805802986251778, 300.0000000000000000, 9.936999415321508877 ) ) ;
#102258=CARTESIAN_POINT ( 'NONE',  ( 43.51330286016530380, 435.7669547662781042, 8.554287073368662675 ) ) ;
#102273=CARTESIAN_POINT ( 'NONE',  ( -31.34146884395068966, 438.6798339901752115, 22.89183309451972548 ) ) ;
#102282=CARTESIAN_POINT ( 'NONE',  ( 26.04978609391949718, 296.0924368275842653, 10.20507325036795443 ) ) ;
#102302=CARTESIAN_POINT ( 'NONE',  ( -4.844944557854277199E-15, -0.1944580884125578779, -19.78098730681987405 ) ) ;
#102316=CARTESIAN_POINT ( 'NONE',  ( 37.26719918006427434, 490.8904285930220226, 12.42640642751123714 ) ) ;
#102317=CARTESIAN_POINT ( 'NONE',  ( 13.82057366821712030, 304.5462546222179299, 9.872053150317878334 ) ) ;
#102329=CARTESIAN_POINT ( 'NONE',  ( 40.34962789288341867, 485.8327705809480221, -4.928685277743327653 ) ) ;
#102335=CARTESIAN_POINT ( 'NONE',  ( 39.42064391485031649, 485.2093941173905023, -4.368290657543239419 ) ) ;
#102352=CARTESIAN_POINT ( 'NONE',  ( 23.28067972821365217, 305.8297143474431437, 10.15087365266885122 ) ) ;
#102385=B_SPLINE_SURFACE_WITH_KNOTS ( 'NONE', 1, 3, ( 
 ( #80117, #80643, #57421, #33193, #16447, #89292, #15921, #6765 ),
 ( #40719, #39686, #66063, #105465, #98428, #63967, #7285, #39157 ) ),
 .UNSPECIFIED., .F., .F., .F.,
 ( 2, 2 ),
 ( 4, 2, 2, 4 ),
 ( 0.000000000000000000, 1.000000000000000000 ),
 ( 0.000000000000000000, 0.04450745600790868145, 0.06676118401186306728, 0.08901491201581737678 ),
 .UNSPECIFIED. ) ;
#102388=B_SPLINE_CURVE_WITH_KNOTS ( 'NONE', 3,
 ( #32279, #105605, #62655, #49493 ),
 .UNSPECIFIED., .F., .F.,
 ( 4, 4 ),
 ( 0.000000000000000000, 0.002847824002212423055 ),
 .UNSPECIFIED. ) ;
#102405=FACE_OUTER_BOUND ( 'NONE', #101223, .T. ) ;
#102413=CARTESIAN_POINT ( 'NONE',  ( -43.79395675348489192, 434.3550296691299195, 12.19643612485312190 ) ) ;
#102423=CARTESIAN_POINT ( 'NONE',  ( -40.03675158195893147, 318.9422692625357740, 7.795136733933277995 ) ) ;
#102448=CARTESIAN_POINT ( 'NONE',  ( 6.549255471752022828, 294.7416366638802856, -7.570647764325297402 ) ) ;
#102466=ORIENTED_EDGE ( 'NONE', *, *, #75972, .F. ) ;
#102478=DIRECTION ( 'NONE',  ( -1.000000000000000000, 0.000000000000000000, 0.000000000000000000 ) ) ;
#102494=ORIENTED_EDGE ( 'NONE', *, *, #987, .T. ) ;
#102510=ADVANCED_FACE ( 'NONE', ( #98919 ), #90050, .F. ) ;
#102516=CARTESIAN_POINT ( 'NONE',  ( 30.55228927099183522, 298.7536840786443690, 10.80461237140096209 ) ) ;
#102537=CARTESIAN_POINT ( 'NONE',  ( -31.88369140427094806, 435.8716523888044208, 17.58732034368808073 ) ) ;
#102543=EDGE_CURVE ( 'NONE', #41735, #59443, #8858, .T. ) ;
#102554=CARTESIAN_POINT ( 'NONE',  ( -43.61212006920826667, 434.3223099624050292, 14.49719201759458898 ) ) ;
#102557=AXIS2_PLACEMENT_3D ( 'NONE', #16242, #72875, #90675 ) ;
#102567=CARTESIAN_POINT ( 'NONE',  ( -32.17606763901869016, 486.0066785907575877, 5.076925403390320390 ) ) ;
#102575=ORIENTED_EDGE ( 'NONE', *, *, #10243, .T. ) ;
#102588=CARTESIAN_POINT ( 'NONE',  ( 40.33183555103128271, 485.8341092017946039, -4.932519190553093402 ) ) ;
#102593=B_SPLINE_CURVE_WITH_KNOTS ( 'NONE', 3,
 ( #91614, #68401, #9598, #41976, #10664, #26384, #50069, #66799, #17721, #1504, #51660, #85103, #99687, #60324, #18268, #100217, #27444, #51122, #25857, #83498 ),
 .UNSPECIFIED., .F., .F.,
 ( 4, 2, 2, 2, 2, 2, 2, 2, 2, 4 ),
 ( 0.000000000000000000, 0.001698246576620752709, 0.003396493153241505417, 0.005094739729862258343, 0.006792986306483010835, 0.008491232883103763326, 0.01018947945972451322, 0.01188772603634526658, 0.01273684932465564239, 0.01358597261296601820 ),
 .UNSPECIFIED. ) ;
#102595=FACE_OUTER_BOUND ( 'NONE', #5062, .T. ) ;
#102646=CARTESIAN_POINT ( 'NONE',  ( -45.99999999999999289, 438.0740625310870087, 11.26011362676991467 ) ) ;
#102656=CARTESIAN_POINT ( 'NONE',  ( -42.51086551946191605, 484.3281707585954337, -1.915972276551850095 ) ) ;
#102657=B_SPLINE_CURVE_WITH_KNOTS ( 'NONE', 3,
 ( #95679, #39050, #20252, #103766 ),
 .UNSPECIFIED., .F., .F.,
 ( 4, 4 ),
 ( 5.028454403087268254E-17, 0.001025896622541378790 ),
 .UNSPECIFIED. ) ;
#102661=CARTESIAN_POINT ( 'NONE',  ( -43.51067860848499436, 485.4417974898086641, 3.909400899866716461 ) ) ;
#102663=CARTESIAN_POINT ( 'NONE',  ( 32.70701262248892505, 465.7750753107771970, 13.84670167513632144 ) ) ;
#102669=CARTESIAN_POINT ( 'NONE',  ( -35.45332598873516616, 373.5548271054980773, 5.144531785461577300 ) ) ;
#102675=EDGE_LOOP ( 'NONE', ( #75724, #87645, #69016, #105136 ) ) ;
#102683=CARTESIAN_POINT ( 'NONE',  ( 0.000000000000000000, 0.000000000000000000, 0.000000000000000000 ) ) ;
#102687=EDGE_LOOP ( 'NONE', ( #464, #98237, #47311, #89815, #82007, #58170 ) ) ;
#102698=CIRCLE ( 'NONE', #33804, 2.999999999999999112 ) ;
#102729=CARTESIAN_POINT ( 'NONE',  ( 44.03912857151497917, 435.2850055576267323, 15.29440791315701098 ) ) ;
#102740=CARTESIAN_POINT ( 'NONE',  ( 35.70858988364064146, 426.6102125256102227, 5.236736094956324195 ) ) ;
#102761=CARTESIAN_POINT ( 'NONE',  ( 45.18811156849615429, 356.2875363396749435, 4.031983282298342353 ) ) ;
#102762=CARTESIAN_POINT ( 'NONE',  ( 33.78214696664169736, 461.9283422808849764, 7.821959642284836534 ) ) ;
#102765=CARTESIAN_POINT ( 'NONE',  ( -32.46316046841231184, 488.6793347432158043, 9.801212136597996505 ) ) ;
#102766=CARTESIAN_POINT ( 'NONE',  ( 31.13400694707459238, 439.5192420142489027, 23.00466474004402073 ) ) ;
#102823=CARTESIAN_POINT ( 'NONE',  ( 24.62001147270324353, 295.5497811818883065, 2.086785639818852456 ) ) ;
#102832=CARTESIAN_POINT ( 'NONE',  ( -41.58031631500816871, 436.8046394031031809, 6.058257849348906987 ) ) ;
#102838=CARTESIAN_POINT ( 'NONE',  ( 2.494577234427376227E-15, -18.92596047533412573, 20.36976895023282097 ) ) ;
#102850=CARTESIAN_POINT ( 'NONE',  ( 35.22753116013103636, 435.7360350475310042, 6.213956812072554570 ) ) ;
#102867=FACE_OUTER_BOUND ( 'NONE', #39267, .T. ) ;
#102893=CARTESIAN_POINT ( 'NONE',  ( 27.18528066925738429, 312.1751590076182765, 10.69940225286546642 ) ) ;
#102911=CARTESIAN_POINT ( 'NONE',  ( 39.16821133293519352, 459.8632445465572118, 1.901232704179921518 ) ) ;
#102925=ORIENTED_EDGE ( 'NONE', *, *, #28994, .F. ) ;
#102929=CARTESIAN_POINT ( 'NONE',  ( 43.02621584241283870, 434.6128289108256695, 16.97888786058994270 ) ) ;
#102931=CARTESIAN_POINT ( 'NONE',  ( -46.00000000000000000, 459.9277931459707247, 6.461582622321701663 ) ) ;
#102944=CARTESIAN_POINT ( 'NONE',  ( 33.08830340003491699, 433.8978689942874212, 24.52079292137695177 ) ) ;
#102946=CARTESIAN_POINT ( 'NONE',  ( -42.61140200160144786, 465.9030374194823594, 13.21253569360413849 ) ) ;
#102949=CARTESIAN_POINT ( 'NONE',  ( -38.83326880618827204, 459.9245326792292303, 1.954253696922295447 ) ) ;
#102950=AXIS2_PLACEMENT_3D ( 'NONE', #67241, #101193, #3020 ) ;
#102956=CARTESIAN_POINT ( 'NONE',  ( -20.21880305278369150, 304.8280059657581660, -9.005058168222323189 ) ) ;
#102957=CARTESIAN_POINT ( 'NONE',  ( -28.92282554148816587, 311.6946508351041984, 12.06290651036217909 ) ) ;
#102984=CARTESIAN_POINT ( 'NONE',  ( 7.653149673922322371, 294.7103690673997107, -6.445128602839910847 ) ) ;
#102985=CARTESIAN_POINT ( 'NONE',  ( 40.00882285048881926, 314.7542622495009823, 2.793119429658786235 ) ) ;
#102987=FACE_OUTER_BOUND ( 'NONE', #47935, .T. ) ;
#103000=FACE_OUTER_BOUND ( 'NONE', #59851, .T. ) ;
#103003=ORIENTED_EDGE ( 'NONE', *, *, #76985, .F. ) ;
#103004=AXIS2_PLACEMENT_3D ( 'NONE', #59115, #32730, #50987 ) ;
#103018=EDGE_CURVE ( 'NONE', #57174, #100925, #84535, .T. ) ;
#103021=CARTESIAN_POINT ( 'NONE',  ( -38.41498555331915554, 491.4234641122523612, 12.30872953874726328 ) ) ;
#103023=VERTEX_POINT ( 'NONE', #28549 ) ;
#103041=CARTESIAN_POINT ( 'NONE',  ( 42.45811724857436076, 486.4202366696182480, 8.302074271983164166 ) ) ;
#103052=CARTESIAN_POINT ( 'NONE',  ( 29.50756122520733271, 297.9063904818165724, 10.61050061783298126 ) ) ;
#103058=CARTESIAN_POINT ( 'NONE',  ( -32.93320410569342016, 485.0465637715133198, 1.208268278909949478 ) ) ;
#103074=CARTESIAN_POINT ( 'NONE',  ( -32.82875765654047484, 434.9824960647666217, 12.61072594640184441 ) ) ;
#103075=CARTESIAN_POINT ( 'NONE',  ( -30.00000000000000355, 488.8442721620237421, 4.433647275927526721 ) ) ;
#103082=EDGE_CURVE ( 'NONE', #70272, #72766, #5307, .T. ) ;
#103088=CARTESIAN_POINT ( 'NONE',  ( 46.00000000000000711, 437.9187945550052063, 12.32659313045543747 ) ) ;
#103098=ORIENTED_EDGE ( 'NONE', *, *, #9585, .F. ) ;
#103103=CARTESIAN_POINT ( 'NONE',  ( -35.42077910799415008, 325.1303593571471424, -4.549127494966866969 ) ) ;
#103111=CARTESIAN_POINT ( 'NONE',  ( 7.347880794884112834E-16, 69.00000000000000000, 5.999999999999994671 ) ) ;
#103121=CARTESIAN_POINT ( 'NONE',  ( -36.63177234734323662, 490.9974527155399642, 12.47316876380962292 ) ) ;
#103124=( BOUNDED_SURFACE ( )  B_SPLINE_SURFACE ( 3, 2, ( 
 ( #87165, #4116, #38622 ),
 ( #86120, #69912, #4651 ),
 ( #62891, #45642, #28421 ),
 ( #94738, #103343, #13776 ),
 ( #46688, #5695, #61297 ),
 ( #94191, #12191, #29490 ),
 ( #62367, #95257, #21389 ),
 ( #81682, #82772, #65532 ),
 ( #40183, #57950, #105456 ),
 ( #25093, #57414, #6756 ),
 ( #48789, #15911, #33185 ),
 ( #39676, #105969, #72550 ),
 ( #220, #90874, #23504 ),
 ( #7804, #7275, #31596 ),
 ( #40712, #96845, #32113 ),
 ( #56348, #89810, #81164 ),
 ( #74136, #14838, #16988 ),
 ( #73600, #106504, #64481 ),
 ( #24571, #80633, #66056 ),
 ( #72030, #73061, #97350 ),
 ( #98933, #47734, #49866 ),
 ( #8343, #31079, #104937 ),
 ( #63958, #32660, #64995 ),
 ( #82230, #89283, #8875 ),
 ( #90332, #98419, #22973 ),
 ( #55809, #88745, #48264 ),
 ( #97888, #24043, #15377 ),
 ( #56884, #16440, #49323 ),
 ( #41247, #2375, #50917 ),
 ( #43385, #42307, #26706 ),
 ( #58507, #2903, #92445 ),
 ( #35862, #83829, #74662 ),
 ( #18601, #51989, #59579 ),
 ( #41780, #10467, #747 ),
 ( #68185, #75740, #9938 ),
 ( #100542, #50388, #84907 ),
 ( #66589, #83300, #18059 ),
 ( #51461, #100013, #19684 ),
 ( #1291, #42845, #84376 ),
 ( #92990, #101082, #60127 ),
 ( #91412, #99470, #10992 ),
 ( #43909, #76797, #76269 ),
 ( #35321, #52523, #27240 ),
 ( #1836, #27778, #75195 ),
 ( #101622, #19153, #9389 ),
 ( #68738, #60651, #93539 ),
 ( #34257, #34793, #67128 ),
 ( #85439, #33713, #26182 ),
 ( #25644, #67662, #59042 ),
 ( #17525, #91928, #46946 ),
 ( #104120, #30808, #22179 ),
 ( #38363, #4915, #29751 ),
 ( #46432, #6484, #37846 ),
 ( #55554, #63693, #71747 ),
 ( #72806, #105195, #54489 ),
 ( #96582, #22715, #80905 ),
 ( #13512, #63154, #88490 ),
 ( #47474, #104656, #39933 ),
 ( #78782, #14566, #80370 ),
 ( #5953, #56624, #71227 ),
 ( #30265, #39414, #55029 ),
 ( #96051, #70709, #62624 ),
 ( #79321, #72289, #103600 ),
 ( #31342, #64223, #97095 ),
 ( #11522, #14041, #5441 ),
 ( #15111, #95511, #105713 ),
 ( #87961, #23236, #89016 ),
 ( #56073, #79847, #38878 ),
 ( #7016, #47999, #31855 ),
 ( #64735, #97612, #23777 ),
 ( #45905, #21652, #87434 ),
 ( #40987, #40453, #74928 ),
 ( #66322, #1012, #480 ),
 ( #49061, #99753, #81423 ),
 ( #81956, #91675, #82510 ),
 ( #74400, #33449, #49603 ),
 ( #106232, #9134, #99205 ),
 ( #65264, #90604, #8083 ),
 ( #73877, #98153, #42046 ),
 ( #33996, #8612, #41515 ),
 ( #25371, #66866, #58227 ),
 ( #57680, #73334, #7537 ),
 ( #91156, #98673, #17262 ),
 ( #32392, #16714, #106772 ),
 ( #24309, #15639, #50134 ),
 ( #83042, #32921, #57155 ) ),
 .UNSPECIFIED., .F., .F., .F. ) 
 B_SPLINE_SURFACE_WITH_KNOTS ( ( 4, 2, 2, 2, 2, 2, 2, 2, 2, 2, 2, 2, 2, 2, 2, 2, 2, 2, 2, 2, 2, 2, 2, 2, 2, 2, 2, 2, 2, 2, 2, 2, 2, 2, 2, 2, 2, 2, 2, 2, 2, 2, 4 ),
 ( 3, 3 ),
 ( 0.06724859676077497850, 0.08531197731406328644, 0.1033753578673516083, 0.1214387384206399162, 0.1304704286972840632, 0.1349862738356061298, 0.1395021189739282241, 0.1575654995272165459, 0.1665971898038606791, 0.1711130349421827734, 0.1733709575113437928, 0.1756288800805048400, 0.1846605703571490009, 0.1869184929263100203, 0.1891764154954710675, 0.1936922606337931341, 0.1942567412760833889, 0.1945389815972285164, 0.1948212219183736438, 0.1959501832029541812, 0.1982081057721152284, 0.2004660283412762478, 0.2006071485018487977, 0.2007482686624213752, 0.2010305089835665027, 0.2015949896258567575, 0.2027239509104372950, 0.2032884315527275776, 0.2034295517133001274, 0.2035706718738727050, 0.2038529121950178324, 0.2044173928373080873, 0.2049818734795983421, 0.2055463541218885970, 0.2058285944430337244, 0.2061108347641788519, 0.2072397960487593616, 0.2083687573333398713, 0.2086509976544849987, 0.2087921178150575763, 0.2089332379756301261, 0.2094977186179204087, 0.2117556411870814559 ),
 ( 0.000000000000000000, 1.000000000000000000 ),
 .UNSPECIFIED. ) 
 GEOMETRIC_REPRESENTATION_ITEM ( )  RATIONAL_B_SPLINE_SURFACE ( (
 ( 1.000000000000000000, 0.7071068666375163181, 1.000000000000000000),
 ( 1.000000000000000000, 0.7071069333971968796, 1.000000000000000000),
 ( 1.000000000000000000, 0.7071067806372003384, 1.000000000000000000),
 ( 1.000000000000000000, 0.7071067806372003384, 1.000000000000000000),
 ( 1.000000000000000000, 0.7071067802067261265, 1.000000000000000000),
 ( 1.000000000000000000, 0.7071067802067261265, 1.000000000000000000),
 ( 1.000000000000000000, 0.7071051933422836111, 1.000000000000000000),
 ( 1.000000000000000000, 0.7071044938463821872, 1.000000000000000000),
 ( 1.000000000000000000, 0.7071050750596493684, 1.000000000000000000),
 ( 1.000000000000000000, 0.7071061969560579197, 1.000000000000000000),
 ( 1.000000000000000000, 0.7071065824458093729, 1.000000000000000000),
 ( 1.000000000000000000, 0.7071068690440487359, 1.000000000000000000),
 ( 1.000000000000000000, 0.7071066644500461074, 1.000000000000000000),
 ( 1.000000000000000000, 0.7071047487608218551, 1.000000000000000000),
 ( 1.000000000000000000, 0.7071039044805524920, 1.000000000000000000),
 ( 1.000000000000000000, 0.7071067951707197263, 1.000000000000000000),
 ( 1.000000000000000000, 0.7071060022142037216, 1.000000000000000000),
 ( 1.000000000000000000, 0.7071045490108263110, 1.000000000000000000),
 ( 1.000000000000000000, 0.7071047837343714670, 1.000000000000000000),
 ( 1.000000000000000000, 0.7071057220880505589, 1.000000000000000000),
 ( 1.000000000000000000, 0.7071061026645381054, 1.000000000000000000),
 ( 1.000000000000000000, 0.7071066713307564422, 1.000000000000000000),
 ( 1.000000000000000000, 0.7071075855488917483, 1.000000000000000000),
 ( 1.000000000000000000, 0.7071018469519960714, 1.000000000000000000),
 ( 1.000000000000000000, 0.7070769257863378510, 1.000000000000000000),
 ( 1.000000000000000000, 0.7070959128786372672, 1.000000000000000000),
 ( 1.000000000000000000, 0.7071006937020449801, 1.000000000000000000),
 ( 1.000000000000000000, 0.7071069821649591525, 1.000000000000000000),
 ( 1.000000000000000000, 0.7071070273698751851, 1.000000000000000000),
 ( 1.000000000000000000, 0.7071019450278684948, 1.000000000000000000),
 ( 1.000000000000000000, 0.7071033604888681268, 1.000000000000000000),
 ( 1.000000000000000000, 0.7071062872278021105, 1.000000000000000000),
 ( 1.000000000000000000, 0.7071065490437030698, 1.000000000000000000),
 ( 1.000000000000000000, 0.7071067506450113838, 1.000000000000000000),
 ( 1.000000000000000000, 0.7071068759948633264, 1.000000000000000000),
 ( 1.000000000000000000, 0.7071066670383303610, 1.000000000000000000),
 ( 1.000000000000000000, 0.7071057208227836677, 1.000000000000000000),
 ( 1.000000000000000000, 0.7070977502787308966, 1.000000000000000000),
 ( 1.000000000000000000, 0.7070812549423161064, 1.000000000000000000),
 ( 1.000000000000000000, 0.7070331502134156176, 1.000000000000000000),
 ( 1.000000000000000000, 0.7070087972399150544, 1.000000000000000000),
 ( 1.000000000000000000, 0.7070383350363120822, 1.000000000000000000),
 ( 1.000000000000000000, 0.7070972093601404218, 1.000000000000000000),
 ( 1.000000000000000000, 0.7071064900542932685, 1.000000000000000000),
 ( 1.000000000000000000, 0.7071067816304712483, 1.000000000000000000),
 ( 1.000000000000000000, 0.7071067807484303636, 1.000000000000000000),
 ( 1.000000000000000000, 0.7071067188699946549, 1.000000000000000000),
 ( 1.000000000000000000, 0.7071063936914395720, 1.000000000000000000),
 ( 1.000000000000000000, 0.7071059926591559686, 1.000000000000000000),
 ( 1.000000000000000000, 0.7071045708296856969, 1.000000000000000000),
 ( 1.000000000000000000, 0.7071033560782118421, 1.000000000000000000),
 ( 1.000000000000000000, 0.7071008937454664744, 1.000000000000000000),
 ( 1.000000000000000000, 0.7071014222377458580, 1.000000000000000000),
 ( 1.000000000000000000, 0.7071047036589576118, 1.000000000000000000),
 ( 1.000000000000000000, 0.7071060773287295431, 1.000000000000000000),
 ( 1.000000000000000000, 0.7071067222128313290, 1.000000000000000000),
 ( 1.000000000000000000, 0.7071067639124569704, 1.000000000000000000),
 ( 1.000000000000000000, 0.7071068043621556720, 1.000000000000000000),
 ( 1.000000000000000000, 0.7071069265355697242, 1.000000000000000000),
 ( 1.000000000000000000, 0.7071075016079259035, 1.000000000000000000),
 ( 1.000000000000000000, 0.7071081591294727797, 1.000000000000000000),
 ( 1.000000000000000000, 0.7071103244092352691, 1.000000000000000000),
 ( 1.000000000000000000, 0.7071119687239084683, 1.000000000000000000),
 ( 1.000000000000000000, 0.7071137400171658705, 1.000000000000000000),
 ( 1.000000000000000000, 0.7071138641451193418, 1.000000000000000000),
 ( 1.000000000000000000, 0.7071124901834935361, 1.000000000000000000),
 ( 1.000000000000000000, 0.7071110053402942519, 1.000000000000000000),
 ( 1.000000000000000000, 0.7071088051577407718, 1.000000000000000000),
 ( 1.000000000000000000, 0.7071080886590817016, 1.000000000000000000),
 ( 1.000000000000000000, 0.7071070405652588597, 1.000000000000000000),
 ( 1.000000000000000000, 0.7071069706112402820, 1.000000000000000000),
 ( 1.000000000000000000, 0.7071058445581541729, 1.000000000000000000),
 ( 1.000000000000000000, 0.7070928369275982783, 1.000000000000000000),
 ( 1.000000000000000000, 0.7070888553714566038, 1.000000000000000000),
 ( 1.000000000000000000, 0.7070962487307334010, 1.000000000000000000),
 ( 1.000000000000000000, 0.7071039365152042011, 1.000000000000000000),
 ( 1.000000000000000000, 0.7071052774665896878, 1.000000000000000000),
 ( 1.000000000000000000, 0.7071064534178541638, 1.000000000000000000),
 ( 1.000000000000000000, 0.7071067052480206616, 1.000000000000000000),
 ( 1.000000000000000000, 0.7071068279545691393, 1.000000000000000000),
 ( 1.000000000000000000, 0.7071066124722539259, 1.000000000000000000),
 ( 1.000000000000000000, 0.7071040194681652569, 1.000000000000000000),
 ( 1.000000000000000000, 0.7070980359047702724, 1.000000000000000000),
 ( 1.000000000000000000, 0.7070730461235169573, 1.000000000000000000),
 ( 1.000000000000000000, 0.7070935438803431783, 1.000000000000000000),
 ( 1.000000000000000000, 0.7071067811865452413, 1.000000000000000000) ) ) 
 REPRESENTATION_ITEM ( '' )  SURFACE ( )  );
#103130=CARTESIAN_POINT ( 'NONE',  ( -34.16642289233715246, 463.8422268500497125, 18.98106911353877280 ) ) ;
#103139=DIRECTION ( 'NONE',  ( 0.000000000000000000, 0.000000000000000000, -1.000000000000000000 ) ) ;
#103140=CARTESIAN_POINT ( 'NONE',  ( -46.00000000000000000, 450.0000000000002274, 13.20242257375370976 ) ) ;
#103142=ADVANCED_FACE ( 'NONE', ( #104514 ), #98, .T. ) ;
#103166=ORIENTED_EDGE ( 'NONE', *, *, #94481, .F. ) ;
#103181=CARTESIAN_POINT ( 'NONE',  ( -46.00000000000000711, 437.8930939855516158, 12.65921861419373151 ) ) ;
#103183=CARTESIAN_POINT ( 'NONE',  ( 37.71162862628988677, 389.8339943296927004, 6.083486274822005768 ) ) ;
#103198=CARTESIAN_POINT ( 'NONE',  ( -40.95645226494054469, 436.0015890305718358, 6.362679593778101328 ) ) ;
#103205=DIRECTION ( 'NONE',  ( 1.000000000000000000, 0.000000000000000000, 0.000000000000000000 ) ) ;
#103206=VERTEX_POINT ( 'NONE', #22583 ) ;
#103209=ORIENTED_EDGE ( 'NONE', *, *, #87990, .T. ) ;
#103236=CIRCLE ( 'NONE', #77366, 0.9999999999999947820 ) ;
#103260=CIRCLE ( 'NONE', #98082, 1.000000000000000666 ) ;
#103271=CARTESIAN_POINT ( 'NONE',  ( 35.68024356520923135, 373.5070696322856065, 4.158998345878070602 ) ) ;
#103274=CARTESIAN_POINT ( 'NONE',  ( 37.00811329507128988, 491.8246567885115610, 12.57632236122393010 ) ) ;
#103277=CARTESIAN_POINT ( 'NONE',  ( -26.15559236925495412, 305.6589228050500537, -9.603828203464059854 ) ) ;
#103290=DIRECTION ( 'NONE',  ( -0.9915366780650392009, -0.1269898409407490270, -0.02699252395738697963 ) ) ;
#103299=CARTESIAN_POINT ( 'NONE',  ( 36.79086635616850742, 340.8131496176287101, -0.8880945147259954320 ) ) ;
#103301=CARTESIAN_POINT ( 'NONE',  ( 44.14911905790289381, 464.3766534542007207, 9.623404994951323843 ) ) ;
#103303=CARTESIAN_POINT ( 'NONE',  ( 0.000000000000000000, 304.8518027762758038, 9.936999415352289589 ) ) ;
#103309=DIRECTION ( 'NONE',  ( 8.034710196240791752E-11, 0.000000000000000000, -1.000000000000000000 ) ) ;
#103313=CARTESIAN_POINT ( 'NONE',  ( -34.64581139903613405, 463.6418748650343105, 19.44242283797569470 ) ) ;
#103314=VERTEX_POINT ( 'NONE', #47338 ) ;
#103328=EDGE_LOOP ( 'NONE', ( #93355, #101140, #50488, #106051 ) ) ;
#103343=CARTESIAN_POINT ( 'NONE',  ( -45.47728949670318599, 415.0252377317643209, 8.193707597952228028 ) ) ;
#103355=CARTESIAN_POINT ( 'NONE',  ( 23.45015351654351932, 303.6741448883345242, 10.11546188763766452 ) ) ;
#103371=DIRECTION ( 'NONE',  ( -0.000000000000000000, -1.000000000000000000, -0.000000000000000000 ) ) ;
#103372=CARTESIAN_POINT ( 'NONE',  ( 1.227754105814700766E-15, 67.05096163904791240, 10.02537308446411402 ) ) ;
#103389=CARTESIAN_POINT ( 'NONE',  ( -46.00000000000000000, 461.6622277975411635, 10.18145404766348783 ) ) ;
#103394=CARTESIAN_POINT ( 'NONE',  ( 41.29724588151264442, 485.7091420655442562, -4.558554568103089899 ) ) ;
#103397=CARTESIAN_POINT ( 'NONE',  ( -42.51570042820637951, 437.0229838707177237, 20.73732745754740847 ) ) ;
#103422=ORIENTED_EDGE ( 'NONE', *, *, #17445, .F. ) ;
#103437=ORIENTED_EDGE ( 'NONE', *, *, #13090, .F. ) ;
#103440=DIRECTION ( 'NONE',  ( -0.000000000000000000, -1.000000000000000000, -0.000000000000000000 ) ) ;
#103441=ORIENTED_EDGE ( 'NONE', *, *, #88526, .F. ) ;
#103457=FACE_OUTER_BOUND ( 'NONE', #7683, .T. ) ;
#103458=EDGE_CURVE ( 'NONE', #52196, #23615, #877, .T. ) ;
#103468=CARTESIAN_POINT ( 'NONE',  ( 33.08796297677666587, 372.6636829999529823, 24.05784598877716363 ) ) ;
#103474=ADVANCED_FACE ( 'NONE', ( #51594 ), #105177, .F. ) ;
#103475=CARTESIAN_POINT ( 'NONE',  ( -34.14329934198877226, 464.2299144111568125, 6.063562457997684341 ) ) ;
#103476=AXIS2_PLACEMENT_3D ( 'NONE', #48505, #65239, #988 ) ;
#103479=CARTESIAN_POINT ( 'NONE',  ( -22.06692060364423824, 305.1441668778134044, -8.937571418765491771 ) ) ;
#103481=CARTESIAN_POINT ( 'NONE',  ( -36.03738032064502050, 307.9717951417662789, 13.05167544916968403 ) ) ;
#103504=CARTESIAN_POINT ( 'NONE',  ( 41.61991837719464371, 463.6613259647958785, 18.05819200971493288 ) ) ;
#103507=CARTESIAN_POINT ( 'NONE',  ( 43.17378635866474212, 487.6240912981842826, 8.491167829005039636 ) ) ;
#103509=CARTESIAN_POINT ( 'NONE',  ( 43.58459202512976560, 371.6927194222791968, 14.08847290620314752 ) ) ;
#103539=ORIENTED_EDGE ( 'NONE', *, *, #64576, .T. ) ;
#103542=VERTEX_POINT ( 'NONE', #88231 ) ;
#103561=ORIENTED_EDGE ( 'NONE', *, *, #62385, .F. ) ;
#103572=CARTESIAN_POINT ( 'NONE',  ( -40.75641113481592726, 360.0948485545300741, 24.37153223514695100 ) ) ;
#103575=CARTESIAN_POINT ( 'NONE',  ( 30.38238271166915538, 438.0643985705939372, 22.32817737082370257 ) ) ;
#103576=CARTESIAN_POINT ( 'NONE',  ( -33.94783393359910662, 484.1261039197349305, 1.321740980884783978 ) ) ;
#103578=VERTEX_POINT ( 'NONE', #73068 ) ;
#103592=CARTESIAN_POINT ( 'NONE',  ( -31.17407356531878193, 437.9983974556887460, 21.19255796710519846 ) ) ;
#103593=CARTESIAN_POINT ( 'NONE',  ( -32.13417934727930714, 435.4422780298330622, 16.28732618035900614 ) ) ;
#103599=ORIENTED_EDGE ( 'NONE', *, *, #70560, .T. ) ;
#103600=CARTESIAN_POINT ( 'NONE',  ( -32.41288963471964735, 299.5866157103865248, -0.9436238929854601221 ) ) ;
#103603=ORIENTED_EDGE ( 'NONE', *, *, #15299, .F. ) ;
#103621=CARTESIAN_POINT ( 'NONE',  ( -37.58421307733613048, 369.0431394919717718, 4.069084478531508786 ) ) ;
#103624=DIRECTION ( 'NONE',  ( 1.000000000000000000, -0.000000000000000000, -0.000000000000000000 ) ) ;
#103632=CARTESIAN_POINT ( 'NONE',  ( 43.74985542820356699, 435.5770091380370559, 16.96136490515564788 ) ) ;
#103636=CARTESIAN_POINT ( 'NONE',  ( -30.00000000000000000, 488.7105273189911259, 4.072454560254398892 ) ) ;
#103637=CARTESIAN_POINT ( 'NONE',  ( 1.224646799147353454E-15, 70.00000000000000000, 10.00000000000000178 ) ) ;
#103639=ORIENTED_EDGE ( 'NONE', *, *, #21752, .F. ) ;
#103651=ORIENTED_EDGE ( 'NONE', *, *, #93820, .F. ) ;
#103658=CARTESIAN_POINT ( 'NONE',  ( -43.03357534758885095, 463.2291678140052227, 4.675918524150252331 ) ) ;
#103673=B_SPLINE_CURVE_WITH_KNOTS ( 'NONE', 3,
 ( #18307, #36636, #2618, #26421 ),
 .UNSPECIFIED., .F., .F.,
 ( 4, 4 ),
 ( 3.766727042548887005E-15, 0.0002629889189324963639 ),
 .UNSPECIFIED. ) ;
#103674=AXIS2_PLACEMENT_3D ( 'NONE', #38597, #104362, #99445 ) ;
#103702=CARTESIAN_POINT ( 'NONE',  ( 33.00000000000000000, 450.0000000000002274, 13.20242257375370976 ) ) ;
#103703=CARTESIAN_POINT ( 'NONE',  ( -43.58447375880955121, 371.6794660751320976, 14.08692068712289469 ) ) ;
#103704=CARTESIAN_POINT ( 'NONE',  ( 24.51545473835047417, 303.7716308844144351, -9.801422722447242109 ) ) ;
#103725=DIRECTION ( 'NONE',  ( 0.000000000000000000, -0.6935263888315827963, 0.7204312236391647861 ) ) ;
#103730=VERTEX_POINT ( 'NONE', #63439 ) ;
#103740=LINE ( 'NONE', #87048, #22620 ) ;
#103756=CARTESIAN_POINT ( 'NONE',  ( 8.647875585311235014, 302.6863304874600544, 9.901865528037117059 ) ) ;
#103765=CARTESIAN_POINT ( 'NONE',  ( -45.99999999995679900, 486.6678415250283933, 5.056251502196789538 ) ) ;
#103766=CARTESIAN_POINT ( 'NONE',  ( -36.64823341582351901, 437.5392299810053487, 4.281405873620232505 ) ) ;
#103791=CARTESIAN_POINT ( 'NONE',  ( 35.72263983187427527, 379.3987609744327187, 4.779922119910973599 ) ) ;
#103794=CARTESIAN_POINT ( 'NONE',  ( 34.12349128637390550, 490.8027302422246407, 11.84948222508928062 ) ) ;
#103805=CARTESIAN_POINT ( 'NONE',  ( -35.81121297974355144, 464.1169797044130974, 19.43538228465078177 ) ) ;
#103815=CARTESIAN_POINT ( 'NONE',  ( 37.63019879891060526, 304.9912133630514859, -7.664751180836238298 ) ) ;
#103860=CARTESIAN_POINT ( 'NONE',  ( 43.03185303983483578, 485.3613526602390493, 6.073233449168488285 ) ) ;
#103864=CARTESIAN_POINT ( 'NONE',  ( -40.67924138885464913, 485.8013567632088439, -4.837443355060405459 ) ) ;
#103865=AXIS2_PLACEMENT_3D ( 'NONE', #42003, #33952, #50604 ) ;
#103878=B_SPLINE_CURVE_WITH_KNOTS ( 'NONE', 3,
 ( #55880, #80706, #106038, #48338 ),
 .UNSPECIFIED., .F., .F.,
 ( 4, 4 ),
 ( 0.000000000000000000, 0.001748759895725735458 ),
 .UNSPECIFIED. ) ;
#103893=CARTESIAN_POINT ( 'NONE',  ( -2.019483917365790222E-25, 304.8518027762758038, 8.936999415352287812 ) ) ;
#103904=CARTESIAN_POINT ( 'NONE',  ( -38.82095410878641673, 477.1411610313862752, -1.685344478752615727 ) ) ;
#103912=CARTESIAN_POINT ( 'NONE',  ( 40.86966971611426658, 485.5857298029578146, -4.179518346805715545 ) ) ;
#103916=CARTESIAN_POINT ( 'NONE',  ( 39.45725925859274952, 460.7192990590706927, 2.112476274834731882 ) ) ;
#103925=CARTESIAN_POINT ( 'NONE',  ( -44.66387834505498944, 341.6072687625629101, 1.189588019127773677 ) ) ;
#103927=CARTESIAN_POINT ( 'NONE',  ( 32.17889379758945267, 439.3695696554025858, 23.63219374846805465 ) ) ;
#103937=CARTESIAN_POINT ( 'NONE',  ( -27.53978464381656366, 314.0199944737697137, 12.16771398945173566 ) ) ;
#103939=ORIENTED_EDGE ( 'NONE', *, *, #27784, .F. ) ;
#103941=ORIENTED_EDGE ( 'NONE', *, *, #41028, .F. ) ;
#103946=CARTESIAN_POINT ( 'NONE',  ( 46.00000000000000711, 485.7857398469772647, -0.3390537564248662927 ) ) ;
#103948=DIRECTION ( 'NONE',  ( 0.2776092459786534405, 0.06763270420356301549, -0.9583104527601048472 ) ) ;
#103957=CARTESIAN_POINT ( 'NONE',  ( 36.64823341582350480, 437.5392299810053487, 4.281405873620231617 ) ) ;
#103973=CIRCLE ( 'NONE', #57453, 3.000000000000020872 ) ;
#103978=CARTESIAN_POINT ( 'NONE',  ( -46.00000000000000000, 438.3644743595980344, 10.24495404218449757 ) ) ;
#103988=CARTESIAN_POINT ( 'NONE',  ( 33.16871688984772959, 397.1242636821970677, 25.83017931078799734 ) ) ;
#103990=CARTESIAN_POINT ( 'NONE',  ( -39.08187240373793969, 460.7913535929719728, 2.155912156267088875 ) ) ;
#103994=EDGE_CURVE ( 'NONE', #35302, #337, #15758, .T. ) ;
#103999=CARTESIAN_POINT ( 'NONE',  ( -31.19627331860082720, 299.4406361361442350, 10.96598005625576100 ) ) ;
#104010=CARTESIAN_POINT ( 'NONE',  ( 30.00000000000000000, 500.0000000000002274, 5.000000000000001776 ) ) ;
#104011=EDGE_LOOP ( 'NONE', ( #92289, #105337, #68093, #42300 ) ) ;
#104015=CARTESIAN_POINT ( 'NONE',  ( 35.73700087854440000, 437.1201388800395193, 4.567739269147286230 ) ) ;
#104018=AXIS2_PLACEMENT_3D ( 'NONE', #4871, #71186, #62584 ) ;
#104026=CARTESIAN_POINT ( 'NONE',  ( 42.19618372163381537, 487.7264399052799035, 8.629926728122860879 ) ) ;
#104037=( BOUNDED_SURFACE ( )  B_SPLINE_SURFACE ( 3, 2, ( 
 ( #26426, #92165, #10186 ),
 ( #100788, #26950, #18312 ),
 ( #43099, #75987, #59827 ),
 ( #92702, #18861, #51704 ),
 ( #84623, #5302, #47332 ),
 ( #79176, #30659, #55414 ),
 ( #29606, #4232, #86238 ),
 ( #6330, #63008, #61963 ),
 ( #103978, #62478, #13363 ),
 ( #30118, #78631, #39272 ) ),
 .UNSPECIFIED., .F., .F., .F. ) 
 B_SPLINE_SURFACE_WITH_KNOTS ( ( 4, 2, 2, 2, 4 ),
 ( 3, 3 ),
 ( 0.007286154432480420814, 0.008335500519278869064, 0.009384846606077319048, 0.01043419269287576730, 0.01148353877967421555 ),
 ( 0.000000000000000000, 0.8533017117288693720 ),
 .UNSPECIFIED. ) 
 GEOMETRIC_REPRESENTATION_ITEM ( )  RATIONAL_B_SPLINE_SURFACE ( (
 ( 1.000000000000000000, 0.8072324461154417596, 0.9434426596218448147),
 ( 1.000000000000000000, 0.8170226563706388667, 0.9463150737943484270),
 ( 1.000000000000000000, 0.8232679997191755250, 0.9481474361521402550),
 ( 1.000000000000000000, 0.8276101782779371474, 0.9494214164760159669),
 ( 1.000000000000000000, 0.8256847820051311793, 0.9488565118010874322),
 ( 1.000000000000000000, 0.8144349657408164189, 0.9455558542224080654),
 ( 1.000000000000000000, 0.8051540590290614530, 0.9428328679659709888),
 ( 1.000000000000000000, 0.7811619758966467097, 0.9357936729108033980),
 ( 1.000000000000000000, 0.7664691029299778302, 0.9314828342828123109),
 ( 1.000000000000000000, 0.7500737150327089209, 0.9266724836026711820) ) ) 
 REPRESENTATION_ITEM ( '' )  SURFACE ( )  );
#104038=CARTESIAN_POINT ( 'NONE',  ( 0.000000000000000000, -19.99999999999998934, 0.000000000000000000 ) ) ;
#104049=DIRECTION ( 'NONE',  ( 0.000000000000000000, 0.000000000000000000, -1.000000000000000000 ) ) ;
#104062=CARTESIAN_POINT ( 'NONE',  ( 42.18756898894580587, 484.4522853017719513, -2.425645685620450909 ) ) ;
#104065=ADVANCED_FACE ( 'NONE', ( #105373 ), #83117, .T. ) ;
#104070=CARTESIAN_POINT ( 'NONE',  ( -43.97709758272682734, 485.9234630640621617, 4.765357662999615052 ) ) ;
#104081=ORIENTED_EDGE ( 'NONE', *, *, #54906, .F. ) ;
#104093=CARTESIAN_POINT ( 'NONE',  ( -25.93947128054312756, 296.0094280503604978, 10.18659011856751384 ) ) ;
#104096=FACE_OUTER_BOUND ( 'NONE', #3110, .T. ) ;
#104099=VERTEX_POINT ( 'NONE', #35092 ) ;
#104100=ORIENTED_EDGE ( 'NONE', *, *, #10839, .T. ) ;
#104108=CARTESIAN_POINT ( 'NONE',  ( 32.18412820475327862, 464.7176420235827550, 10.95006602420748010 ) ) ;
#104110=CARTESIAN_POINT ( 'NONE',  ( -31.43278154310612393, 439.6985105754050664, 23.49139273982680010 ) ) ;
#104112=CARTESIAN_POINT ( 'NONE',  ( -33.50185725303997231, 488.2566613463952194, 10.59321780392846613 ) ) ;
#104113=CARTESIAN_POINT ( 'NONE',  ( -30.00000000000000355, 488.7105343895983083, 4.072475191987426690 ) ) ;
#104120=CARTESIAN_POINT ( 'NONE',  ( -30.46600437442538123, 308.5397930899359267, -8.697262802616858579 ) ) ;
#104122=ADVANCED_FACE ( 'NONE', ( #4291 ), #19744, .F. ) ;
#104129=FACE_OUTER_BOUND ( 'NONE', #74171, .T. ) ;
#104140=CARTESIAN_POINT ( 'NONE',  ( -46.00000000000000000, 461.6622277975413340, 10.18145404766431206 ) ) ;
#104141=CARTESIAN_POINT ( 'NONE',  ( -35.53357291648787708, 439.5860488598422080, 24.00787122424867093 ) ) ;
#104143=CARTESIAN_POINT ( 'NONE',  ( -37.71426560610335343, 395.7663590576279944, 6.364238202227666896 ) ) ;
#104146=DIRECTION ( 'NONE',  ( 0.000000000000000000, 0.000000000000000000, -1.000000000000000000 ) ) ;
#104151=CARTESIAN_POINT ( 'NONE',  ( 43.00000000000000000, 450.0000000000002274, 13.20242257375370976 ) ) ;
#104158=CARTESIAN_POINT ( 'NONE',  ( 16.36917923056512691, 294.5678716157545978, -2.060237494721419260 ) ) ;
#104181=CARTESIAN_POINT ( 'NONE',  ( 30.00000000000000000, 450.0000000000002274, 13.20242257375370976 ) ) ;
#104205=B_SPLINE_CURVE_WITH_KNOTS ( 'NONE', 3,
 ( #58078, #31713, #868, #72672 ),
 .UNSPECIFIED., .F., .F.,
 ( 4, 4 ),
 ( 0.000000000000000000, 0.0007664883490339958897 ),
 .UNSPECIFIED. ) ;
#104208=CARTESIAN_POINT ( 'NONE',  ( -30.00000000000000000, 500.0000000000002274, -5.000000000000001776 ) ) ;
#104217=FACE_OUTER_BOUND ( 'NONE', #81271, .T. ) ;
#104218=CARTESIAN_POINT ( 'NONE',  ( -32.09911992168218831, 438.9232547152092252, 23.66653216045979491 ) ) ;
#104222=CARTESIAN_POINT ( 'NONE',  ( -38.55369376853367669, 309.5668124549920321, 1.485156153254792999 ) ) ;
#104224=VERTEX_POINT ( 'NONE', #53377 ) ;
#104228=CIRCLE ( 'NONE', #43956, 1.000000000000002442 ) ;
#104235=CARTESIAN_POINT ( 'NONE',  ( 20.97754405179121662, 294.8763868968453608, 9.942224931492262385 ) ) ;
#104236=CARTESIAN_POINT ( 'NONE',  ( -32.96114378239634846, 439.7497662205610709, 24.15381041467389167 ) ) ;
#104241=CARTESIAN_POINT ( 'NONE',  ( -42.68684796707171358, 436.2654864220197055, 7.155924890008083850 ) ) ;
#104262=CARTESIAN_POINT ( 'NONE',  ( 34.92245183780732276, 464.4742769089222065, 18.75702545252121922 ) ) ;
#104263=ADVANCED_FACE ( 'NONE', ( #39328 ), #46864, .T. ) ;
#104271=ORIENTED_EDGE ( 'NONE', *, *, #101481, .F. ) ;
#104273=EDGE_CURVE ( 'NONE', #60854, #46619, #11566, .T. ) ;
#104278=CARTESIAN_POINT ( 'NONE',  ( 15.88575968060462706, 294.5610636378226559, 1.875232630976614967 ) ) ;
#104279=ORIENTED_EDGE ( 'NONE', *, *, #100585, .T. ) ;
#104287=DIRECTION ( 'NONE',  ( 0.2472079847635963445, 0.000000000000000000, 0.9689624411034318818 ) ) ;
#104307=CARTESIAN_POINT ( 'NONE',  ( 34.84618260875170392, 489.9833681528626812, 11.97975507378813731 ) ) ;
#104309=AXIS2_PLACEMENT_3D ( 'NONE', #5031, #94591, #37963 ) ;
#104315=VERTEX_POINT ( 'NONE', #23150 ) ;
#104316=CARTESIAN_POINT ( 'NONE',  ( 36.65380293431815062, 373.4724601506463841, 4.384826873228177213 ) ) ;
#104336=CARTESIAN_POINT ( 'NONE',  ( 36.73469237171850921, 305.2482013543003632, 0.4103627608394692095 ) ) ;
#104337=ADVANCED_FACE ( 'NONE', ( #16625 ), #72091, .F. ) ;
#104349=CARTESIAN_POINT ( 'NONE',  ( -44.33510700167990137, 435.2103804628540047, 13.54837514018881706 ) ) ;
#104353=CARTESIAN_POINT ( 'NONE',  ( -36.71005241817288578, 463.3006260613076961, 20.13736821485169415 ) ) ;
#104362=DIRECTION ( 'NONE',  ( -1.000000000000000000, -0.000000000000000000, -0.000000000000000000 ) ) ;
#104364=CARTESIAN_POINT ( 'NONE',  ( -43.55333112596418488, 465.2342844084849958, 9.238213423004522085 ) ) ;
#104375=( BOUNDED_SURFACE ( )  B_SPLINE_SURFACE ( 3, 2, ( 
 ( #106110, #40331, #47877 ),
 ( #14446, #63572, #31735 ),
 ( #80784, #32260, #13390 ),
 ( #65139, #6897, #80247 ) ),
 .UNSPECIFIED., .F., .F., .F. ) 
 B_SPLINE_SURFACE_WITH_KNOTS ( ( 4, 4 ),
 ( 3, 3 ),
 ( 6.505213034913026604E-18, 0.002066227528073411295 ),
 ( 0.000000000000000000, 1.000000000000000000 ),
 .UNSPECIFIED. ) 
 GEOMETRIC_REPRESENTATION_ITEM ( )  RATIONAL_B_SPLINE_SURFACE ( (
 ( 1.000000000000000000, 0.7788880963805245861, 1.000000000000000000),
 ( 1.000000000000000000, 0.7743040464398175393, 1.000000000000000000),
 ( 1.000000000000000000, 0.7669333544817443782, 1.000000000000000000),
 ( 1.000000000000000000, 0.7583909709669810484, 1.000000000000000000) ) ) 
 REPRESENTATION_ITEM ( '' )  SURFACE ( )  );
#104386=CARTESIAN_POINT ( 'NONE',  ( -46.00000000000000711, 485.6346359681443232, -1.078553770025317826 ) ) ;
#104399=CARTESIAN_POINT ( 'NONE',  ( 42.74607419124097163, 464.8137795011914477, 15.62215520944410052 ) ) ;
#104420=CARTESIAN_POINT ( 'NONE',  ( -2.019483917365790222E-25, 303.8518027762758038, 9.936999415352289589 ) ) ;
#104427=CARTESIAN_POINT ( 'NONE',  ( -40.75255125189226391, 485.0466573014779215, -4.066699219997739867 ) ) ;
#104440=ORIENTED_EDGE ( 'NONE', *, *, #6989, .F. ) ;
#104442=CARTESIAN_POINT ( 'NONE',  ( 40.91184305475058380, 436.7571283257985328, 21.64376470813695263 ) ) ;
#104445=CARTESIAN_POINT ( 'NONE',  ( 39.83997765698279636, 460.7086825730507371, 2.106271324414728419 ) ) ;
#104460=CARTESIAN_POINT ( 'NONE',  ( -34.10831268713208431, 434.1698048432537576, 11.21913565533539447 ) ) ;
#104468=EDGE_LOOP ( 'NONE', ( #18812, #66885, #3997, #35873 ) ) ;
#104469=CARTESIAN_POINT ( 'NONE',  ( -24.52418941431424315, 305.4846864080880664, 10.29874865197013101 ) ) ;
#104492=CARTESIAN_POINT ( 'NONE',  ( -1.262177448353618889E-25, 304.8518027762758038, -9.000000000000005329 ) ) ;
#104502=SURFACE_STYLE_FILL_AREA ( #31704 ) ;
#104510=CARTESIAN_POINT ( 'NONE',  ( 20.97754405179127346, 294.8763868968453608, 9.942224931492237516 ) ) ;
#104511=ORIENTED_EDGE ( 'NONE', *, *, #17445, .T. ) ;
#104514=FACE_OUTER_BOUND ( 'NONE', #102687, .T. ) ;
#104519=CARTESIAN_POINT ( 'NONE',  ( 36.03903953312295272, 307.9766817680012991, 13.05290268685154231 ) ) ;
#104525=VERTEX_POINT ( 'NONE', #90387 ) ;
#104528=CARTESIAN_POINT ( 'NONE',  ( -33.89250494191506391, 463.6575930728432127, 6.993601543838152246 ) ) ;
#104529=CARTESIAN_POINT ( 'NONE',  ( -31.83945028356544782, 465.6738295161418364, 10.98138951113073780 ) ) ;
#104531=CARTESIAN_POINT ( 'NONE',  ( 32.12958771267400948, 464.7275665249413237, 11.12424126545837133 ) ) ;
#104532=CARTESIAN_POINT ( 'NONE',  ( -25.70845616436730197, 305.2466841868522351, 10.47404382804886147 ) ) ;
#104554=DIRECTION ( 'NONE',  ( 1.000000000000000000, 0.000000000000000000, 0.000000000000000000 ) ) ;
#104577=VERTEX_POINT ( 'NONE', #796 ) ;
#104593=CARTESIAN_POINT ( 'NONE',  ( 31.13164466794002649, 436.9146031748717860, 23.68605626514782969 ) ) ;
#104601=CARTESIAN_POINT ( 'NONE',  ( -43.75401118688380819, 486.3173572309548263, 5.908089951475163915 ) ) ;
#104604=CIRCLE ( 'NONE', #1256, 1.000000000000000888 ) ;
#104625=CARTESIAN_POINT ( 'NONE',  ( -2.503177626522498755, 294.8391969429503092, 9.934319910064267845 ) ) ;
#104627=CARTESIAN_POINT ( 'NONE',  ( -40.93292669599463096, 378.0706848361106722, 26.55786848468904537 ) ) ;
#104645=CARTESIAN_POINT ( 'NONE',  ( -31.50544488634473339, 439.3527810931634576, 23.21716044688400515 ) ) ;
#104647=CARTESIAN_POINT ( 'NONE',  ( -35.75515486453239333, 408.9583410871374554, 6.060592194821802892 ) ) ;
#104649=CARTESIAN_POINT ( 'NONE',  ( -32.16914446836677399, 486.0693400665468289, 5.247150504720089259 ) ) ;
#104656=CARTESIAN_POINT ( 'NONE',  ( -34.68392891983880588, 301.0938521591136805, -8.596509045476626198 ) ) ;
#104657=EDGE_CURVE ( 'NONE', #36986, #39480, #20625, .T. ) ;
#104664=CARTESIAN_POINT ( 'NONE',  ( 19.73463816634110657, 304.7971333121958537, 8.925379062039144884 ) ) ;
#104665=CARTESIAN_POINT ( 'NONE',  ( 37.62251730745840916, 437.3427388312647395, 4.535622330043188377 ) ) ;
#104674=CARTESIAN_POINT ( 'NONE',  ( -45.99999999996713740, 463.5261361515072167, 9.383844849049905790 ) ) ;
#104676=CARTESIAN_POINT ( 'NONE',  ( -34.11324467909268776, 439.1267449652036134, 24.05939132677088921 ) ) ;
#104709=B_SPLINE_CURVE_WITH_KNOTS ( 'NONE', 3,
 ( #99364, #58402, #1740, #91314, #83722, #17423, #42209, #75091 ),
 .UNSPECIFIED., .F., .F.,
 ( 4, 2, 2, 4 ),
 ( 6.938893903907228378E-18, 0.005764214328876836498, 0.008646321493315253445, 0.01152842865775367126 ),
 .UNSPECIFIED. ) ;
#104718=B_SPLINE_CURVE_WITH_KNOTS ( 'NONE', 3,
 ( #6212, #86650, #30004, #70968 ),
 .UNSPECIFIED., .F., .F.,
 ( 4, 4 ),
 ( 1.022751534364685075E-16, 0.001950293525757256386 ),
 .UNSPECIFIED. ) ;
#104724=EDGE_CURVE ( 'NONE', #79974, #24620, #72652, .T. ) ;
#104761=CARTESIAN_POINT ( 'NONE',  ( 27.16282903641085866, 305.1222582335363995, -9.499934379274456830 ) ) ;
#104776=CARTESIAN_POINT ( 'NONE',  ( -21.25502769577498796, 305.0480251235313176, 9.978840188629131802 ) ) ;
#104777=CARTESIAN_POINT ( 'NONE',  ( -32.92225573320412479, 439.7404251386054739, 24.14402493977262765 ) ) ;
#104788=ORIENTED_EDGE ( 'NONE', *, *, #14168, .T. ) ;
#104793=DIRECTION ( 'NONE',  ( 0.000000000000000000, 0.000000000000000000, 1.000000000000000000 ) ) ;
#104817=CARTESIAN_POINT ( 'NONE',  ( 16.55832830662598454, 294.5717066613688075, 1.877661829258160164 ) ) ;
#104823=AXIS2_PLACEMENT_3D ( 'NONE', #20205, #85425, #59565 ) ;
#104830=CARTESIAN_POINT ( 'NONE',  ( -40.61984019992077322, 488.7256223871871725, 10.90533736068143433 ) ) ;
#104834=ADVANCED_FACE ( 'NONE', ( #32584 ), #61955, .F. ) ;
#104835=CIRCLE ( 'NONE', #23951, 3.000000000000000000 ) ;
#104844=CARTESIAN_POINT ( 'NONE',  ( -46.00000000000000000, 461.8824355611604915, 11.41562375508724081 ) ) ;
#104847=EDGE_LOOP ( 'NONE', ( #31745, #5154, #92401, #95867 ) ) ;
#104853=CARTESIAN_POINT ( 'NONE',  ( 33.77559172535807619, 464.7834715296606305, 7.192701217093271815 ) ) ;
#104858=CARTESIAN_POINT ( 'NONE',  ( -35.96492786661492858, 302.4488314805894902, -8.278427239160079054 ) ) ;
#104863=CARTESIAN_POINT ( 'NONE',  ( 36.71071896821285208, 382.3218912538050063, 5.272091887305267122 ) ) ;
#104869=CARTESIAN_POINT ( 'NONE',  ( 42.19618372163381537, 487.7264399052799604, 8.629926728122889301 ) ) ;
#104881=CARTESIAN_POINT ( 'NONE',  ( -33.20892452561020036, 484.6201576160080435, 4.300277591919697606 ) ) ;
#104890=CARTESIAN_POINT ( 'NONE',  ( 40.82495241567565358, 312.4806794415787294, -5.803827984348647107 ) ) ;
#104908=EDGE_LOOP ( 'NONE', ( #90693, #33482, #76678, #34992, #63090 ) ) ;
#104933=ORIENTED_EDGE ( 'NONE', *, *, #24389, .T. ) ;
#104934=CARTESIAN_POINT ( 'NONE',  ( 44.26831907014823742, 485.5169161718123974, 3.139294003717259418 ) ) ;
#104936=CARTESIAN_POINT ( 'NONE',  ( 29.22860602677112851, 312.6791165392893390, 12.31020644618178572 ) ) ;
#104937=CARTESIAN_POINT ( 'NONE',  ( -42.33059488474484766, 332.4056956521847610, 7.101971215149171179 ) ) ;
#104938=CARTESIAN_POINT ( 'NONE',  ( -31.90195216159215263, 465.6468698803304846, 10.69263942007498969 ) ) ;
#104943=EDGE_CURVE ( 'NONE', #29420, #4192, #31194, .T. ) ;
#104947=CARTESIAN_POINT ( 'NONE',  ( -38.81358894280032956, 485.1131561813190274, -4.191378885295818257 ) ) ;
#104950=CARTESIAN_POINT ( 'NONE',  ( 0.5047266530460114975, 295.8573157252483270, -10.00013740465520762 ) ) ;
#104952=VERTEX_POINT ( 'NONE', #83746 ) ;
#104953=CARTESIAN_POINT ( 'NONE',  ( 41.92560882005241041, 464.5504518700566905, 16.85555372449807265 ) ) ;
#104969=CARTESIAN_POINT ( 'NONE',  ( 19.83463548332442983, 303.8035096162418540, 9.926734387303303819 ) ) ;
#104970=ORIENTED_EDGE ( 'NONE', *, *, #26652, .F. ) ;
#104982=CARTESIAN_POINT ( 'NONE',  ( -32.09335762069173370, 464.8098810386746322, 11.80769741171398302 ) ) ;
#104983=DIRECTION ( 'NONE',  ( 0.000000000000000000, 0.000000000000000000, 1.000000000000000000 ) ) ;
#104992=CARTESIAN_POINT ( 'NONE',  ( 39.08699041849416034, 460.7998460666120764, 2.161775044689363767 ) ) ;
#104996=CARTESIAN_POINT ( 'NONE',  ( 43.52560348121181732, 486.7876442849059231, 7.034435017225325382 ) ) ;
#104997=CIRCLE ( 'NONE', #46416, 1.000000000000000444 ) ;
#105004=CARTESIAN_POINT ( 'NONE',  ( 44.08840282922849241, 485.7747746244180007, 4.178803824087734320 ) ) ;
#105010=ORIENTED_EDGE ( 'NONE', *, *, #90940, .F. ) ;
#105011=CARTESIAN_POINT ( 'NONE',  ( -25.27112035471596130, 306.2417877789772547, 10.47586605097270329 ) ) ;
#105040=CARTESIAN_POINT ( 'NONE',  ( 6.818946241788777840, 304.7371849810256208, -9.024366745380079990 ) ) ;
#105041=CARTESIAN_POINT ( 'NONE',  ( 31.14694070047868735, 432.3293837220155069, 24.29762062537629319 ) ) ;
#105044=ORIENTED_EDGE ( 'NONE', *, *, #89010, .T. ) ;
#105046=CARTESIAN_POINT ( 'NONE',  ( 45.99999999999999289, 460.6999119684549555, 7.611097089574335506 ) ) ;
#105059=ORIENTED_EDGE ( 'NONE', *, *, #81241, .F. ) ;
#105069=CARTESIAN_POINT ( 'NONE',  ( 31.25856554251603470, 324.7076297242331293, 15.31063495038612565 ) ) ;
#105070=CARTESIAN_POINT ( 'NONE',  ( -43.75010090113919148, 464.8337800386752292, 11.75004750935041109 ) ) ;
#105073=CARTESIAN_POINT ( 'NONE',  ( -39.32386068306119142, 460.7288320239698578, 2.118193558184112923 ) ) ;
#105078=CARTESIAN_POINT ( 'NONE',  ( -34.89951189943284504, 462.5771273340574226, 5.012025534192016352 ) ) ;
#105082=CARTESIAN_POINT ( 'NONE',  ( -32.84478897102435724, 300.3640702886290796, 3.177245060986884972 ) ) ;
#105086=DIRECTION ( 'NONE',  ( 0.9722532735310974727, 0.000000000000000000, -0.2339306993707007676 ) ) ;
#105091=EDGE_CURVE ( 'NONE', #11535, #63343, #95154, .T. ) ;
#105099=EDGE_CURVE ( 'NONE', #12476, #52196, #30705, .T. ) ;
#105104=CARTESIAN_POINT ( 'NONE',  ( 37.46539396549699319, 482.0424347141847647, 15.05118261291089254 ) ) ;
#105127=EDGE_LOOP ( 'NONE', ( #55228, #84200, #38081, #14045, #18880 ) ) ;
#105135=VERTEX_POINT ( 'NONE', #45441 ) ;
#105136=ORIENTED_EDGE ( 'NONE', *, *, #10839, .F. ) ;
#105137=CARTESIAN_POINT ( 'NONE',  ( 32.13232479388067730, 428.0674789085878729, 24.77008313062577827 ) ) ;
#105143=CARTESIAN_POINT ( 'NONE',  ( -16.51294481928371383, 294.5655612426596690, -2.060814981937608259 ) ) ;
#105154=ORIENTED_EDGE ( 'NONE', *, *, #68759, .F. ) ;
#105163=CARTESIAN_POINT ( 'NONE',  ( 43.53995238963187120, 465.2530981678414719, 9.299505628815621705 ) ) ;
#105166=CARTESIAN_POINT ( 'NONE',  ( 43.00000000000000000, 436.5989882784185738, 19.94133085611158407 ) ) ;
#105172=ORIENTED_EDGE ( 'NONE', *, *, #45255, .F. ) ;
#105177=( BOUNDED_SURFACE ( )  B_SPLINE_SURFACE ( 3, 2, ( 
 ( #24695, #59178, #66188 ),
 ( #348, #83433, #98544 ),
 ( #57545, #92057, #16578 ),
 ( #83968, #42988, #26841 ) ),
 .UNSPECIFIED., .F., .F., .F. ) 
 B_SPLINE_SURFACE_WITH_KNOTS ( ( 4, 4 ),
 ( 3, 3 ),
 ( 2.726768463801043652E-17, 0.0001614739849793452150 ),
 ( 0.000000000000000000, 1.000000000000000000 ),
 .UNSPECIFIED. ) 
 GEOMETRIC_REPRESENTATION_ITEM ( )  RATIONAL_B_SPLINE_SURFACE ( (
 ( 1.000000000000000000, 0.9028401456532979541, 1.000000000000000000),
 ( 1.000000000000000000, 0.9031964952773774424, 1.000000000000000000),
 ( 1.000000000000000000, 0.9035643897147043191, 1.000000000000000000),
 ( 1.000000000000000000, 0.9039444415359939589, 1.000000000000000000) ) ) 
 REPRESENTATION_ITEM ( '' )  SURFACE ( )  );
#105185=B_SPLINE_CURVE_WITH_KNOTS ( 'NONE', 3,
 ( #67070, #38693, #37879, #52416 ),
 .UNSPECIFIED., .F., .F.,
 ( 4, 4 ),
 ( 3.198672041575564518E-17, 0.0001993833013610890766 ),
 .UNSPECIFIED. ) ;
#105188=CARTESIAN_POINT ( 'NONE',  ( 33.46689243939714231, 485.1693579416230477, 2.982310567427692405 ) ) ;
#105195=CARTESIAN_POINT ( 'NONE',  ( -35.16787835860036893, 301.6138128548261648, -8.474289318537694626 ) ) ;
#105197=EDGE_CURVE ( 'NONE', #73295, #104315, #97673, .T. ) ;
#105204=CARTESIAN_POINT ( 'NONE',  ( 31.39110793407987643, 426.5490676794047999, 23.68232819820003598 ) ) ;
#105210=DIRECTION ( 'NONE',  ( 2.312964634635754888E-15, -0.9612814585413570478, -0.2755684261024861081 ) ) ;
#105214=B_SPLINE_CURVE_WITH_KNOTS ( 'NONE', 3,
 ( #53733, #4663, #37596, #54236, #53212, #22463, #87179, #20899, #69927, #5191, #72041, #13259, #54777, #95796, #94750, #46700, #13787, #104950, #12731, #80119 ),
 .UNSPECIFIED., .F., .F.,
 ( 4, 2, 2, 2, 2, 2, 2, 2, 2, 4 ),
 ( 0.000000000000000000, 0.001681824184508711427, 0.003363648369017425456, 0.005045472553526139485, 0.005886384645780496500, 0.006727296738034854381, 0.008409120922543570145, 0.01009094510705228591, 0.01177276929156100167, 0.01345459347606971744 ),
 .UNSPECIFIED. ) ;
#105216=ORIENTED_EDGE ( 'NONE', *, *, #32315, .F. ) ;
#105254=CARTESIAN_POINT ( 'NONE',  ( 23.96375140441108442, 306.3052962357393199, 10.25885168886986243 ) ) ;
#105255=CARTESIAN_POINT ( 'NONE',  ( 38.85446894546219454, 460.8903912184133560, 2.218456751110199132 ) ) ;
#105258=ORIENTED_EDGE ( 'NONE', *, *, #29291, .T. ) ;
#105264=ADVANCED_FACE ( 'NONE', ( #81476 ), #34892, .F. ) ;
#105265=CARTESIAN_POINT ( 'NONE',  ( -15.73175472929735541, 303.5560492990851458, 9.874135533399703846 ) ) ;
#105267=CARTESIAN_POINT ( 'NONE',  ( -33.00000000000000000, 450.0000000000002274, 13.20242257375370976 ) ) ;
#105272=CIRCLE ( 'NONE', #12259, 7.025805963803935406 ) ;
#105281=DIRECTION ( 'NONE',  ( 0.000000000000000000, -1.000000000000000000, 0.000000000000000000 ) ) ;
#105283=DIRECTION ( 'NONE',  ( 0.000000000000000000, 0.000000000000000000, -1.000000000000000000 ) ) ;
#105285=DIRECTION ( 'NONE',  ( 1.000000000000000000, 0.000000000000000000, 0.000000000000000000 ) ) ;
#105290=CARTESIAN_POINT ( 'NONE',  ( 36.14207491791087534, 485.3942915881601152, -3.424055767584778920 ) ) ;
#105295=CARTESIAN_POINT ( 'NONE',  ( -43.51678756415928007, 365.4275696025253524, 13.28716395725119348 ) ) ;
#105296=ADVANCED_FACE ( 'NONE', ( #88018 ), #100605, .F. ) ;
#105297=CARTESIAN_POINT ( 'NONE',  ( 20.68638090159294762, 302.8702952610971693, -9.996063631021495866 ) ) ;
#105311=CARTESIAN_POINT ( 'NONE',  ( 22.91651842568168362, 295.0901107613288445, -9.949346074078583513 ) ) ;
#105313=CARTESIAN_POINT ( 'NONE',  ( -34.88900972249400212, 464.6206820655984870, 18.69027339340994232 ) ) ;
#105320=( BOUNDED_SURFACE ( )  B_SPLINE_SURFACE ( 3, 2, ( 
 ( #55339, #7317, #21959 ),
 ( #13286, #6798, #39718 ),
 ( #80154, #79625, #62406 ),
 ( #23550, #30048, #55851 ) ),
 .UNSPECIFIED., .F., .F., .F. ) 
 B_SPLINE_SURFACE_WITH_KNOTS ( ( 4, 4 ),
 ( 3, 3 ),
 ( 2.769486029396972526E-15, 0.002106423517722433563 ),
 ( 0.000000000000000000, 1.000000000000000000 ),
 .UNSPECIFIED. ) 
 GEOMETRIC_REPRESENTATION_ITEM ( )  RATIONAL_B_SPLINE_SURFACE ( (
 ( 1.000000000000000000, 0.7977970988452620649, 1.000000000000000000),
 ( 1.000000000000000000, 0.8078744440618430556, 1.000000000000000000),
 ( 1.000000000000000000, 0.8177468419059694682, 1.000000000000000000),
 ( 1.000000000000000000, 0.8274831119535078772, 1.000000000000000000) ) ) 
 REPRESENTATION_ITEM ( '' )  SURFACE ( )  );
#105322=CARTESIAN_POINT ( 'NONE',  ( 41.46910480218704009, 484.7338956289814860, -3.418960549715446717 ) ) ;
#105337=ORIENTED_EDGE ( 'NONE', *, *, #25478, .T. ) ;
#105354=AXIS2_PLACEMENT_3D ( 'NONE', #82065, #57251, #24412 ) ;
#105365=CARTESIAN_POINT ( 'NONE',  ( 40.62117264245587478, 438.3092160654453551, 22.60618477163586348 ) ) ;
#105370=EDGE_CURVE ( 'NONE', #47279, #104577, #77099, .T. ) ;
#105373=FACE_OUTER_BOUND ( 'NONE', #59633, .T. ) ;
#105377=EDGE_LOOP ( 'NONE', ( #90981, #102162, #33372, #77557, #62705, #6402, #94323 ) ) ;
#105380=CARTESIAN_POINT ( 'NONE',  ( 36.98821436528865547, 463.5274861635172101, 19.70078135305745803 ) ) ;
#105385=CARTESIAN_POINT ( 'NONE',  ( -37.51854390953261742, 313.5286481325095451, 14.45587837336505999 ) ) ;
#105387=CARTESIAN_POINT ( 'NONE',  ( -44.66387834505498944, 341.6072687625629101, 1.189588019127773677 ) ) ;
#105390=CARTESIAN_POINT ( 'NONE',  ( 28.61526283629831724, 309.3341729851595119, -8.977869265197252702 ) ) ;
#105394=CARTESIAN_POINT ( 'NONE',  ( -32.86055893256200733, 316.8313229355889575, -6.875028717072126483 ) ) ;
#105397=CARTESIAN_POINT ( 'NONE',  ( 33.00000000000000000, 500.0000000000002274, 0.000000000000000000 ) ) ;
#105398=ORIENTED_EDGE ( 'NONE', *, *, #58298, .T. ) ;
#105411=CARTESIAN_POINT ( 'NONE',  ( 39.03119707554853335, 311.0870578039430825, 1.866927532141321677 ) ) ;
#105416=CYLINDRICAL_SURFACE ( 'NONE', #99601, 5.000000000000000888 ) ;
#105420=CARTESIAN_POINT ( 'NONE',  ( 43.67509741642236065, 485.0313177283746882, 1.734658347999106676 ) ) ;
#105446=CARTESIAN_POINT ( 'NONE',  ( 0.000000000000000000, 70.00000000000000000, 5.000000000000000000 ) ) ;
#105451=VERTEX_POINT ( 'NONE', #69061 ) ;
#105453=CARTESIAN_POINT ( 'NONE',  ( -35.75984758101135697, 439.1067915602654352, 24.04383837159262782 ) ) ;
#105454=CARTESIAN_POINT ( 'NONE',  ( 21.43353486660526031, 303.0521706313907089, 9.980247409275479598 ) ) ;
#105456=CARTESIAN_POINT ( 'NONE',  ( -43.63759230290430224, 379.1247326692748061, 14.86908692522124831 ) ) ;
#105465=CARTESIAN_POINT ( 'NONE',  ( 12.19423397773156736, 304.5852035401753710, 9.880331998383338643 ) ) ;
#105466=CARTESIAN_POINT ( 'NONE',  ( -40.34962789288057650, 485.8327705809454642, -4.928685277735865178 ) ) ;
#105477=DIRECTION ( 'NONE',  ( 0.000000000000000000, 0.000000000000000000, -1.000000000000000000 ) ) ;
#105486=ADVANCED_FACE ( 'NONE', ( #36192 ), #3677, .T. ) ;
#105488=CARTESIAN_POINT ( 'NONE',  ( -43.27459526351814389, 485.1620945307481634, -2.264801863400593529 ) ) ;
#105495=LINE ( 'NONE', #106009, #43457 ) ;
#105499=FACE_OUTER_BOUND ( 'NONE', #95864, .T. ) ;
#105501=CARTESIAN_POINT ( 'NONE',  ( -30.00000000000000355, 462.0097303356245106, 12.67201001741399047 ) ) ;
#105502=FACE_OUTER_BOUND ( 'NONE', #76774, .T. ) ;
#105527=CARTESIAN_POINT ( 'NONE',  ( -34.50218234403093476, 434.5102366699516097, 9.485624649973072309 ) ) ;
#105529=CARTESIAN_POINT ( 'NONE',  ( -37.83758010121304238, 485.6941950553117522, -4.518273513594293078 ) ) ;
#105532=CARTESIAN_POINT ( 'NONE',  ( -29.85808249604284370, 330.9700016804235361, 16.31510691329269847 ) ) ;
#105534=CARTESIAN_POINT ( 'NONE',  ( 20.55501430260233420, 303.9056691006283586, 9.948455458498445481 ) ) ;
#105543=CARTESIAN_POINT ( 'NONE',  ( 43.02621584241283870, 434.6128289108255558, 16.97888786058996402 ) ) ;
#105558=CARTESIAN_POINT ( 'NONE',  ( 26.27902093981875709, 306.9027577142574614, -9.548073367147230428 ) ) ;
#105562=CARTESIAN_POINT ( 'NONE',  ( 46.00000000000001421, 460.3170374101630955, 7.034854880083544870 ) ) ;
#105579=CARTESIAN_POINT ( 'NONE',  ( 43.00000000000000000, 450.0000000000002274, 13.20242257375370976 ) ) ;
#105584=CARTESIAN_POINT ( 'NONE',  ( 31.09748479556632006, 323.2603612422993251, 14.95832153367667772 ) ) ;
#105587=CARTESIAN_POINT ( 'NONE',  ( -41.18500240987163608, 460.1236783698128647, 2.133705300515147840 ) ) ;
#105593=CARTESIAN_POINT ( 'NONE',  ( -33.82446905678677496, 302.9270370839546445, 11.79982883588897913 ) ) ;
#105605=CARTESIAN_POINT ( 'NONE',  ( 1.128183577527849701, 300.9492746658232818, 9.936156289954276133 ) ) ;
#105607=ORIENTED_EDGE ( 'NONE', *, *, #78316, .F. ) ;
#105621=CARTESIAN_POINT ( 'NONE',  ( 9.740083726526258090, 294.6493269980091441, -10.04303756037257322 ) ) ;
#105624=CARTESIAN_POINT ( 'NONE',  ( 6.123233995736766282E-16, 0.000000000000000000, -5.000000000000000000 ) ) ;
#105629=FACE_OUTER_BOUND ( 'NONE', #72629, .T. ) ;
#105634=ORIENTED_EDGE ( 'NONE', *, *, #8817, .T. ) ;
#105652=CARTESIAN_POINT ( 'NONE',  ( 33.85195725564128821, 465.2464970902066739, 17.18122764674265568 ) ) ;
#105654=EDGE_CURVE ( 'NONE', #96476, #96036, #66660, .T. ) ;
#105661=DIRECTION ( 'NONE',  ( -0.6297424739189366738, -0.1980345732161221117, 0.7511369544587498392 ) ) ;
#105674=CARTESIAN_POINT ( 'NONE',  ( -3.396983858844193183, 299.9646488656019869, -10.00714413801434333 ) ) ;
#105676=EDGE_LOOP ( 'NONE', ( #38616, #34812, #66366, #47151 ) ) ;
#105681=CARTESIAN_POINT ( 'NONE',  ( -15.57846540788180434, 302.5584973853110569, 9.874655226133899788 ) ) ;
#105685=CARTESIAN_POINT ( 'NONE',  ( 6.795673391948847453, 303.7372862655386143, -10.02434351962803838 ) ) ;
#105686=CARTESIAN_POINT ( 'NONE',  ( 36.65199127662912559, 490.9971735395452583, 12.47305305857692304 ) ) ;
#105687=FACE_OUTER_BOUND ( 'NONE', #71722, .T. ) ;
#105704=CARTESIAN_POINT ( 'NONE',  ( -36.51065643851772080, 361.8862209142205870, 2.816516898780279998 ) ) ;
#105713=CARTESIAN_POINT ( 'NONE',  ( -31.09938947669733267, 298.5175562217006586, -1.189641983160760308 ) ) ;
#105714=DIRECTION ( 'NONE',  ( 0.000000000000000000, 0.000000000000000000, -1.000000000000000000 ) ) ;
#105720=CARTESIAN_POINT ( 'NONE',  ( 30.23373458370678790, 333.1884278479437285, 15.82348625706909573 ) ) ;
#105736=ADVANCED_FACE ( 'NONE', ( #43982 ), #84261, .F. ) ;
#105744=B_SPLINE_CURVE_WITH_KNOTS ( 'NONE', 3,
 ( #49183, #57807, #72923, #40049, #64853, #81020, #105834, #24952, #49726, #56196, #603, #82633, #33568, #91275, #7138, #31977, #73457, #8735, #99324, #25498, #50260, #83162, #23901, #106355, #56743, #98281, #90193, #16295, #1698, #93917, #68039, #58905, #51849, #51308, #42703, #52378, #75600, #34654, #84761, #36255, #50769, #67523, #101478, #59980, #17916, #68593, #100404, #10844, #69124, #19005 ),
 .UNSPECIFIED., .F., .F.,
 ( 4, 2, 2, 2, 2, 2, 2, 2, 2, 2, 2, 2, 2, 2, 2, 2, 2, 2, 2, 2, 2, 2, 2, 2, 4 ),
 ( 0.0001642028872464954957, 0.008867656351590888150, 0.01757110981593528257, 0.03497801674462389793, 0.05238492367331251676, 0.06979183060200115640, 0.08719873753068978217, 0.09590219099503416444, 0.1046056444593785467, 0.1089573711915507448, 0.1133090979237229429, 0.1176608246558951409, 0.1220125513880673390, 0.1263642781202395371, 0.1285401414863256431, 0.1307160048524117213, 0.1328918682184978273, 0.1339797999015408803, 0.1345237657430624068, 0.1350677315845839332, 0.1356116974261054597, 0.1361556632676269862, 0.1372435949506700947, 0.1383315266337132032, 0.1394194583167563117 ),
 .UNSPECIFIED. ) ;
#105754=CARTESIAN_POINT ( 'NONE',  ( 30.00000000000000000, 450.0000000000002274, 13.20242257375370976 ) ) ;
#105760=VERTEX_POINT ( 'NONE', #87111 ) ;
#105773=CARTESIAN_POINT ( 'NONE',  ( 21.25502769577498796, 305.0480251235313176, 9.978840188629131802 ) ) ;
#105801=CARTESIAN_POINT ( 'NONE',  ( -43.94716957228371967, 463.1429429498322747, 4.278538522888820417 ) ) ;
#105803=CARTESIAN_POINT ( 'NONE',  ( 35.03615891056482923, 464.5070978657896035, 18.87180892930519605 ) ) ;
#105811=CARTESIAN_POINT ( 'NONE',  ( 46.00000000000000000, 462.1625373399974137, 5.827014411081228751 ) ) ;
#105817=CARTESIAN_POINT ( 'NONE',  ( -42.68011869748734455, 337.5389550235125284, 8.263828678100116676 ) ) ;
#105828=CARTESIAN_POINT ( 'NONE',  ( 44.43774958859658142, 337.2802145563449017, 0.2445019049555710311 ) ) ;
#105829=CARTESIAN_POINT ( 'NONE',  ( -33.08902662346056900, 439.4144565034866901, 23.84226355454047663 ) ) ;
#105834=CARTESIAN_POINT ( 'NONE',  ( -31.43654312788580896, 409.1921748638893064, 24.49080981961512293 ) ) ;
#105839=CARTESIAN_POINT ( 'NONE',  ( -46.00000000000000000, 500.0000000000002274, 12.00000000000000711 ) ) ;
#105847=CARTESIAN_POINT ( 'NONE',  ( -33.47652930794097870, 484.3276552595484077, 3.198545968219471458 ) ) ;
#105882=ORIENTED_EDGE ( 'NONE', *, *, #15856, .F. ) ;
#105892=CARTESIAN_POINT ( 'NONE',  ( 37.04971407824480423, 463.3105192861256114, 20.11836016812624806 ) ) ;
#105897=CARTESIAN_POINT ( 'NONE',  ( -40.95420997525301487, 387.0967036739339164, 27.26945002580065136 ) ) ;
#105898=CARTESIAN_POINT ( 'NONE',  ( -29.50756122520733271, 297.9063904818165724, 10.61050061783298126 ) ) ;
#105901=CARTESIAN_POINT ( 'NONE',  ( 28.01912030120706021, 308.6873964030780257, -8.131358077288096453 ) ) ;
#105908=CARTESIAN_POINT ( 'NONE',  ( -44.57115381837943602, 434.3516557708484243, 14.78613344168394583 ) ) ;
#105914=CARTESIAN_POINT ( 'NONE',  ( -37.06716861312675348, 464.0035714960436621, 19.58716087303068676 ) ) ;
#105930=FACE_OUTER_BOUND ( 'NONE', #11241, .T. ) ;
#105957=CARTESIAN_POINT ( 'NONE',  ( 32.91772945487191038, 464.9199415683442567, 10.91424143556163351 ) ) ;
#105963=VERTEX_POINT ( 'NONE', #41065 ) ;
#105968=CARTESIAN_POINT ( 'NONE',  ( 31.48211130897418641, 326.9585451694341600, 15.85107797452106659 ) ) ;
#105969=CARTESIAN_POINT ( 'NONE',  ( -45.39376174025734656, 370.9991130468319511, 6.147894588093572921 ) ) ;
#105986=ADVANCED_FACE ( 'NONE', ( #80975 ), #12236, .F. ) ;
#105992=CARTESIAN_POINT ( 'NONE',  ( -36.50840931122232291, 491.4427145161785120, 12.32866606332187942 ) ) ;
#106001=CARTESIAN_POINT ( 'NONE',  ( -42.63514723966559927, 485.0526260718492040, -1.920325882447441179 ) ) ;
#106009=CARTESIAN_POINT ( 'NONE',  ( -46.00000000000000000, 500.0000000000002274, -15.00000000000000711 ) ) ;
#106024=CIRCLE ( 'NONE', #23390, 1.000000000000002665 ) ;
#106028=VERTEX_POINT ( 'NONE', #7092 ) ;
#106032=CARTESIAN_POINT ( 'NONE',  ( 32.44539866313899523, 299.6034349815453766, -0.9399606259422752519 ) ) ;
#106036=CARTESIAN_POINT ( 'NONE',  ( -34.72474116627837759, 338.3618661353910966, -1.881472242819908436 ) ) ;
#106038=CARTESIAN_POINT ( 'NONE',  ( -42.51801476543344194, 435.0274750839319609, 8.236762145195060114 ) ) ;
#106041=CARTESIAN_POINT ( 'NONE',  ( -33.11369981515483119, 485.0096198691158520, 0.6282636062397999321 ) ) ;
#106046=CARTESIAN_POINT ( 'NONE',  ( -25.03733421107493129, 305.9738044749904589, 10.41262473261235044 ) ) ;
#106048=CARTESIAN_POINT ( 'NONE',  ( 37.21746376929104372, 485.5895280773364675, -4.183112156774711821 ) ) ;
#106049=CARTESIAN_POINT ( 'NONE',  ( 31.03678703375144821, 438.6650838204807314, 21.86890379897223013 ) ) ;
#106050=CARTESIAN_POINT ( 'NONE',  ( -33.00000000000000000, 435.0774731480752848, 11.67986145722080948 ) ) ;
#106051=ORIENTED_EDGE ( 'NONE', *, *, #45419, .F. ) ;
#106052=EDGE_CURVE ( 'NONE', #96657, #29420, #57158, .T. ) ;
#106081=EDGE_CURVE ( 'NONE', #85790, #1493, #2033, .T. ) ;
#106094=CARTESIAN_POINT ( 'NONE',  ( 42.99999999999998579, 436.5989882784185738, 19.94133085611157341 ) ) ;
#106101=CARTESIAN_POINT ( 'NONE',  ( 29.07017008048624618, 312.2030387978562089, 12.19116356018488823 ) ) ;
#106109=ORIENTED_EDGE ( 'NONE', *, *, #91161, .T. ) ;
#106110=CARTESIAN_POINT ( 'NONE',  ( -43.50377727019363761, 435.9167426301696651, 18.24083946424744340 ) ) ;
#106111=CARTESIAN_POINT ( 'NONE',  ( -24.36065331428383374, 304.1491164910331122, 10.22124288038939710 ) ) ;
#106119=CARTESIAN_POINT ( 'NONE',  ( 18.18910696884454126, 303.6388988518723977, 9.891725748637984594 ) ) ;
#106127=CARTESIAN_POINT ( 'NONE',  ( 36.50546997061839249, 437.5879066196142162, 4.249723241246290861 ) ) ;
#106146=CARTESIAN_POINT ( 'NONE',  ( 33.86867596911348954, 484.1347864990123639, 1.565332731468491945 ) ) ;
#106147=EDGE_LOOP ( 'NONE', ( #16956, #49453, #68685, #54108 ) ) ;
#106157=CARTESIAN_POINT ( 'NONE',  ( 33.84761347220318584, 488.7471039746334895, 11.01988148152525504 ) ) ;
#106171=CARTESIAN_POINT ( 'NONE',  ( 29.96324721583764727, 332.4108250884644349, 16.64494553332287907 ) ) ;
#106181=DIRECTION ( 'NONE',  ( 0.9488877907218276064, 0.1950364375161156294, -0.2481385674579254796 ) ) ;
#106188=ORIENTED_EDGE ( 'NONE', *, *, #14725, .T. ) ;
#106191=CARTESIAN_POINT ( 'NONE',  ( -0.5082004254278419397, 295.8543628274115918, -10.00017741440582242 ) ) ;
#106197=CARTESIAN_POINT ( 'NONE',  ( -10.24592498679531261, 302.6397288294038503, 9.891918830032325971 ) ) ;
#106208=CARTESIAN_POINT ( 'NONE',  ( -3.010552705096329440, 299.5657579542672693, -10.00571845265126214 ) ) ;
#106218=TOROIDAL_SURFACE ( 'NONE', #56242, 12.00000000000001066, 3.000000000000000000 ) ;
#106221=CARTESIAN_POINT ( 'NONE',  ( -31.84138247899937468, 438.9968886095898029, 23.56020719208648373 ) ) ;
#106223=CARTESIAN_POINT ( 'NONE',  ( -32.66601306147397565, 321.4771002738425523, -4.939848896245494281 ) ) ;
#106230=EDGE_LOOP ( 'NONE', ( #26012, #72521, #15919, #68535, #22908, #77968, #29495 ) ) ;
#106232=CARTESIAN_POINT ( 'NONE',  ( -23.92380886547979557, 303.5731447498800435, -9.844749896117946264 ) ) ;
#106239=CARTESIAN_POINT ( 'NONE',  ( 22.56511519009970002, 305.4508729011461128, 9.066418547683744222 ) ) ;
#106250=CARTESIAN_POINT ( 'NONE',  ( 33.47652930794067316, 484.3276552595487487, 3.198545968220822378 ) ) ;
#106268=EDGE_CURVE ( 'NONE', #63495, #63262, #58951, .T. ) ;
#106274=CARTESIAN_POINT ( 'NONE',  ( -43.00000000000000000, 488.0336798547363628, -0.8984331811837273918 ) ) ;
#106288=CARTESIAN_POINT ( 'NONE',  ( 43.69218681961980622, 484.4816931224910945, 2.431261704629519294 ) ) ;
#106297=ORIENTED_EDGE ( 'NONE', *, *, #64968, .T. ) ;
#106298=ORIENTED_EDGE ( 'NONE', *, *, #24718, .F. ) ;
#106314=EDGE_LOOP ( 'NONE', ( #62437, #74100, #33757, #106702 ) ) ;
#106325=CARTESIAN_POINT ( 'NONE',  ( 44.16394502333565697, 464.2849401354476413, 9.200602954361984942 ) ) ;
#106331=CARTESIAN_POINT ( 'NONE',  ( -32.25199865210507255, 464.6771562214397022, 10.60479922511891893 ) ) ;
#106332=EDGE_CURVE ( 'NONE', #69972, #19762, #80695, .T. ) ;
#106349=CARTESIAN_POINT ( 'NONE',  ( -31.19652432992544888, 378.3327707670021027, 24.28948218791313707 ) ) ;
#106354=CARTESIAN_POINT ( 'NONE',  ( -37.85084083633361729, 438.0234350436313093, 4.171260309356204843 ) ) ;
#106355=CARTESIAN_POINT ( 'NONE',  ( -28.96386208545641594, 320.5436640882624033, 12.80660157965214729 ) ) ;
#106356=AXIS2_PLACEMENT_3D ( 'NONE', #101132, #20271, #34839 ) ;
#106360=ORIENTED_EDGE ( 'NONE', *, *, #35133, .T. ) ;
#106374=EDGE_CURVE ( 'NONE', #79406, #75687, #70961, .T. ) ;
#106377=ORIENTED_EDGE ( 'NONE', *, *, #97029, .T. ) ;
#106388=DIRECTION ( 'NONE',  ( -0.9915366780650377576, 0.1269898409407599904, 0.02699252395738913415 ) ) ;
#106400=CARTESIAN_POINT ( 'NONE',  ( -40.01928047903233931, 489.9206396166244417, 11.12040978472883879 ) ) ;
#106404=CARTESIAN_POINT ( 'NONE',  ( 36.86311888821725091, 438.9044241143811860, 23.87836450218838635 ) ) ;
#106419=CARTESIAN_POINT ( 'NONE',  ( 36.69951191943477653, 463.3005535825504353, 20.13750663043823863 ) ) ;
#106429=EDGE_CURVE ( 'NONE', #89689, #696, #51921, .T. ) ;
#106432=CARTESIAN_POINT ( 'NONE',  ( 27.24829532723339653, 307.7585719329687208, -9.350284670461302738 ) ) ;
#106438=CARTESIAN_POINT ( 'NONE',  ( -42.54181027564564488, 465.0722614357791258, 13.76085909083398739 ) ) ;
#106463=CARTESIAN_POINT ( 'NONE',  ( 43.69141235712699967, 485.1129823701804185, 2.341835213797379467 ) ) ;
#106465=( NAMED_UNIT ( * ) PLANE_ANGLE_UNIT ( ) SI_UNIT ( $, .RADIAN. ) );
#106473=CARTESIAN_POINT ( 'NONE',  ( 25.09730810927034739, 306.2366149690730595, -8.697816624931766327 ) ) ;
#106481=CARTESIAN_POINT ( 'NONE',  ( -17.14862568216160099, 294.5838465266265302, -10.05695664460883521 ) ) ;
#106486=CARTESIAN_POINT ( 'NONE',  ( -36.18016141387858653, 463.3220971514191433, 20.09605424492809433 ) ) ;
#106490=CARTESIAN_POINT ( 'NONE',  ( 32.93681933017204955, 464.9081438944968454, 10.83352224628442251 ) ) ;
#106491=CARTESIAN_POINT ( 'NONE',  ( 32.03075683730855161, 464.8596926554154152, 12.88957819155500850 ) ) ;
#106504=CARTESIAN_POINT ( 'NONE',  ( -44.56312866057822930, 339.9956215472535632, 0.8225827590551298973 ) ) ;
#106519=ORIENTED_EDGE ( 'NONE', *, *, #41026, .F. ) ;
#106524=ORIENTED_EDGE ( 'NONE', *, *, #46273, .T. ) ;
#106528=CIRCLE ( 'NONE', #67050, 0.9999999999999977796 ) ;
#106529=CARTESIAN_POINT ( 'NONE',  ( -35.80932576323957761, 491.2997492151604888, 12.22805875982552948 ) ) ;
#106536=CARTESIAN_POINT ( 'NONE',  ( 0.000000000000000000, 304.8518027762758038, 9.936999415352289589 ) ) ;
#106544=EDGE_CURVE ( 'NONE', #7582, #37996, #70413, .T. ) ;
#106546=CIRCLE ( 'NONE', #91104, 5.000000000000001776 ) ;
#106552=AXIS2_PLACEMENT_3D ( 'NONE', #79817, #56047, #39903 ) ;
#106562=ORIENTED_EDGE ( 'NONE', *, *, #29212, .T. ) ;
#106574=CARTESIAN_POINT ( 'NONE',  ( 29.99261461565485476, 297.7707857721058531, -1.359080099825844989 ) ) ;
#106580=CARTESIAN_POINT ( 'NONE',  ( -35.66932529116966322, 438.9565575286536045, 4.011496722538590909 ) ) ;
#106585=CARTESIAN_POINT ( 'NONE',  ( -33.00000000000000000, 485.0303364503728289, 0.9535057477320436625 ) ) ;
#106591=CARTESIAN_POINT ( 'NONE',  ( -22.40060265138178153, 305.3960761985100021, 9.054534321561812149 ) ) ;
#106593=CARTESIAN_POINT ( 'NONE',  ( 38.69275568812178534, 485.6230355318868988, -4.306148472021496865 ) ) ;
#106594=CARTESIAN_POINT ( 'NONE',  ( 31.00201403163103819, 438.8339473355226801, 22.04021393888145042 ) ) ;
#106597=ORIENTED_EDGE ( 'NONE', *, *, #84767, .T. ) ;
#106616=CARTESIAN_POINT ( 'NONE',  ( 13.58423288633485804, 304.5480220053966605, -10.06457059527332376 ) ) ;
#106617=CARTESIAN_POINT ( 'NONE',  ( 24.80105969489321893, 306.0237540681346218, -9.745911707960095427 ) ) ;
#106620=EDGE_LOOP ( 'NONE', ( #24527, #51956, #18369, #35608 ) ) ;
#106635=CARTESIAN_POINT ( 'NONE',  ( -39.39457526263961995, 464.0483451943321143, 18.48383133219108032 ) ) ;
#106641=CARTESIAN_POINT ( 'NONE',  ( 30.13260911416876908, 316.8380131115717404, 13.36150501092329534 ) ) ;
#106645=CARTESIAN_POINT ( 'NONE',  ( -41.02721008360138910, 460.5398098099256572, 2.518281297462771295 ) ) ;
#106649=ORIENTED_EDGE ( 'NONE', *, *, #58884, .T. ) ;
#106652=CARTESIAN_POINT ( 'NONE',  ( -26.60267441690067258, 296.3168466367462202, 10.25441967244310071 ) ) ;
#106673=ADVANCED_FACE ( 'NONE', ( #67355 ), #64128, .T. ) ;
#106702=ORIENTED_EDGE ( 'NONE', *, *, #33654, .F. ) ;
#106704=CARTESIAN_POINT ( 'NONE',  ( -9.789044728060147804, 294.6486233851416614, -2.043184600577789833 ) ) ;
#106710=EDGE_LOOP ( 'NONE', ( #10660, #45193 ) ) ;
#106712=CARTESIAN_POINT ( 'NONE',  ( 28.62099872728884264, 319.6015458412052794, 13.57403514487685392 ) ) ;
#106724=CARTESIAN_POINT ( 'NONE',  ( -24.80105969489321893, 306.0237540681346218, -9.745911707960095427 ) ) ;
#106728=CARTESIAN_POINT ( 'NONE',  ( -43.55333112596419909, 465.2342844084849389, 9.238213423004411951 ) ) ;
#106734=CARTESIAN_POINT ( 'NONE',  ( -0.1244055672601159790, 295.1039051330173493, -10.00000000000143530 ) ) ;
#106743=FACE_OUTER_BOUND ( 'NONE', #101214, .T. ) ;
#106745=CARTESIAN_POINT ( 'NONE',  ( 36.94051212421975805, 491.4300504572173054, 12.31983948577891397 ) ) ;
#106765=CARTESIAN_POINT ( 'NONE',  ( -32.90191502941880231, 322.8794145886470233, -4.587724655176066868 ) ) ;
#106769=CARTESIAN_POINT ( 'NONE',  ( -43.28401190482631478, 435.3393147692558500, 9.722488360058175516 ) ) ;
#106772=CARTESIAN_POINT ( 'NONE',  ( -23.31543317473521526, 295.1959631832629043, -1.926156989552331167 ) ) ;
#106777=CARTESIAN_POINT ( 'NONE',  ( -32.17878052566634750, 336.4077344679339490, 18.01554293220755909 ) ) ;
#106779=CARTESIAN_POINT ( 'NONE',  ( -42.25157195694011136, 464.6564439579760801, 16.40419412090410134 ) ) ;
#106783=B_SPLINE_CURVE_WITH_KNOTS ( 'NONE', 3,
 ( #21426, #54807, #94234, #87739 ),
 .UNSPECIFIED., .F., .F.,
 ( 4, 4 ),
 ( 0.000000000000000000, 0.001019617110105292294 ),
 .UNSPECIFIED. ) ;
ENDSEC;
END-ISO-10303-21;
